ISO-10303-21;
HEADER;
FILE_DESCRIPTION (('STEP AP214'),
    '1' );
FILE_NAME ('Injection Molded Chain Links 4.step',
    '2026-10-08T22:59:04',
    ( '' ),
    ( '' ),
    'SwSTEP 2.0',
    'SolidWorks 2020',
    '' );
FILE_SCHEMA (( 'AUTOMOTIVE_DESIGN' ));
ENDSEC;

DATA;
#21=CARTESIAN_POINT ( 'NONE',  ( 20.97462148592267539, 8.874737576461731337, -112.7546443317310434 ) ) ;
#44=EDGE_CURVE ( 'NONE', #241330, #245837, #16247, .T. ) ;
#45=AXIS2_PLACEMENT_3D ( 'NONE', #144433, #222696, #243559 ) ;
#68=ORIENTED_EDGE ( 'NONE', *, *, #6404, .T. ) ;
#70=VECTOR ( 'NONE', #89864, 1000.000000000000000 ) ;
#82=VECTOR ( 'NONE', #56443, 999.9999999999998863 ) ;
#194=ORIENTED_EDGE ( 'NONE', *, *, #188174, .T. ) ;
#205=VERTEX_POINT ( 'NONE', #188945 ) ;
#232=AXIS2_PLACEMENT_3D ( 'NONE', #173463, #54731, #134253 ) ;
#234=CIRCLE ( 'NONE', #162756, 0.09999999999998898659 ) ;
#235=DIRECTION ( 'NONE',  ( 1.000000000000000000, 0.000000000000000000, 0.000000000000000000 ) ) ;
#238=CARTESIAN_POINT ( 'NONE',  ( 21.97500000000000497, 9.750000000011153745, -112.7500000000000284 ) ) ;
#254=CARTESIAN_POINT ( 'NONE',  ( -23.15000000000000213, 2.000000000011154189, -113.7246219227621395 ) ) ;
#261=CARTESIAN_POINT ( 'NONE',  ( -22.39999999999999858, 11.65000000001115588, -100.5000000000000284 ) ) ;
#270=CARTESIAN_POINT ( 'NONE',  ( -21.59142135623730852, 7.850000000011158718, -112.7500000000000284 ) ) ;
#280=DIRECTION ( 'NONE',  ( 1.000000000000000000, 0.000000000000000000, -0.000000000000000000 ) ) ;
#285=EDGE_CURVE ( 'NONE', #102466, #142934, #55807, .T. ) ;
#287=CARTESIAN_POINT ( 'NONE',  ( -18.50000000000000000, -1.637172712959223952, -112.0821533654720383 ) ) ;
#319=VERTEX_POINT ( 'NONE', #153722 ) ;
#320=CARTESIAN_POINT ( 'NONE',  ( 20.94999999999999929, 1.115600667400684642E-11, -134.0000000000000284 ) ) ;
#344=DIRECTION ( 'NONE',  ( 1.000000000000000000, 0.000000000000000000, 0.000000000000000000 ) ) ;
#370=DIRECTION ( 'NONE',  ( 1.836970198721029934E-16, -1.000000000000000000, -0.000000000000000000 ) ) ;
#410=CIRCLE ( 'NONE', #104453, 0.09999999999999939493 ) ;
#415=CARTESIAN_POINT ( 'NONE',  ( -20.94999999999999929, -11.48912529306489994, -130.9000000000000341 ) ) ;
#417=CARTESIAN_POINT ( 'NONE',  ( -23.15000000000000213, 11.65000000001115588, -88.75000000000004263 ) ) ;
#460=CARTESIAN_POINT ( 'NONE',  ( 21.09813707148777340, 6.385062105747659977, -100.4686485004705219 ) ) ;
#522=EDGE_LOOP ( 'NONE', ( #79861, #184621, #166928, #70389 ) ) ;
#529=EDGE_LOOP ( 'NONE', ( #16011, #85095, #85187, #255666 ) ) ;
#554=FACE_OUTER_BOUND ( 'NONE', #175787, .T. ) ;
#569=ORIENTED_EDGE ( 'NONE', *, *, #82426, .T. ) ;
#578=ORIENTED_EDGE ( 'NONE', *, *, #68615, .F. ) ;
#612=CARTESIAN_POINT ( 'NONE',  ( 22.48660254037843842, 11.75000000001115730, -100.4500000000000313 ) ) ;
#616=VECTOR ( 'NONE', #164742, 1000.000000000000000 ) ;
#661=DIRECTION ( 'NONE',  ( 0.000000000000000000, 0.000000000000000000, 1.000000000000000000 ) ) ;
#666=ORIENTED_EDGE ( 'NONE', *, *, #40911, .T. ) ;
#676=( BOUNDED_SURFACE ( )  B_SPLINE_SURFACE ( 3, 2, ( 
 ( #42500, #144156, #123339 ),
 ( #141606, #122052, #161182 ),
 ( #201576, #238130, #24253 ),
 ( #39977, #239438, #103734 ),
 ( #45076, #120792, #243261 ),
 ( #223694, #59464, #119492 ) ),
 .UNSPECIFIED., .F., .F., .F. ) 
 B_SPLINE_SURFACE_WITH_KNOTS ( ( 4, 2, 4 ),
 ( 3, 3 ),
 ( 4.712388980384689674, 5.497787143782137953, 6.283185307179586232 ),
 ( 0.000000000000000000, 1.000000000000000000 ),
 .UNSPECIFIED. ) 
 GEOMETRIC_REPRESENTATION_ITEM ( )  RATIONAL_B_SPLINE_SURFACE ( (
 ( 1.000000000000000000, 0.7071067811865536790, 1.000000000000000000),
 ( 1.000000000000000000, 0.7727932973495903468, 1.000000000000000000),
 ( 1.000000000000000000, 0.8282379607643433062, 1.000000000000000000),
 ( 1.000000000000000000, 0.9038128468045532049, 1.000000000000000000),
 ( 1.000000000000000000, 0.9240297172239071433, 1.000000000000000000),
 ( 1.000000000000000000, 0.9238795325112914014, 1.000000000000000000) ) ) 
 REPRESENTATION_ITEM ( '' )  SURFACE ( )  );
#682=ADVANCED_FACE ( 'NONE', ( #93369 ), #256227, .F. ) ;
#740=ORIENTED_EDGE ( 'NONE', *, *, #146274, .F. ) ;
#753=AXIS2_PLACEMENT_3D ( 'NONE', #237667, #179014, #176429 ) ;
#758=DIRECTION ( 'NONE',  ( 0.000000000000000000, 0.000000000000000000, -1.000000000000000000 ) ) ;
#759=ORIENTED_EDGE ( 'NONE', *, *, #133909, .T. ) ;
#766=EDGE_CURVE ( 'NONE', #120723, #201736, #30504, .T. ) ;
#780=ORIENTED_EDGE ( 'NONE', *, *, #246088, .F. ) ;
#811=AXIS2_PLACEMENT_3D ( 'NONE', #209395, #174172, #150714 ) ;
#882=AXIS2_PLACEMENT_3D ( 'NONE', #20233, #158478, #21524 ) ;
#903=CARTESIAN_POINT ( 'NONE',  ( 20.94999999999999929, 1.115600667400684642E-11, -134.0000000000000284 ) ) ;
#917=ORIENTED_EDGE ( 'NONE', *, *, #4878, .T. ) ;
#945=CARTESIAN_POINT ( 'NONE',  ( 20.94999999999999574, 1.115600667400684642E-11, -100.5000000000000284 ) ) ;
#961=FACE_OUTER_BOUND ( 'NONE', #150516, .T. ) ;
#1000=CARTESIAN_POINT ( 'NONE',  ( -23.15000000000000213, 1.115651490242849210E-11, -96.35000000000003695 ) ) ;
#1002=CARTESIAN_POINT ( 'NONE',  ( -20.85000000000000142, 7.120270961708750512, -137.6595630418393625 ) ) ;
#1022=ORIENTED_EDGE ( 'NONE', *, *, #256802, .T. ) ;
#1077=DIRECTION ( 'NONE',  ( -0.000000000000000000, -0.1350103645451876666, 0.9908441862701600211 ) ) ;
#1089=CARTESIAN_POINT ( 'NONE',  ( -20.54999999999999716, 1.115625160336667635E-11, -136.0000000000000284 ) ) ;
#1118=ORIENTED_EDGE ( 'NONE', *, *, #258057, .F. ) ;
#1145=DIRECTION ( 'NONE',  ( -1.000000000000000000, -3.265361837132813093E-16, 0.000000000000000000 ) ) ;
#1167=DIRECTION ( 'NONE',  ( -0.000000000000000000, 0.000000000000000000, 1.000000000000000000 ) ) ;
#1180=DIRECTION ( 'NONE',  ( 0.000000000000000000, 0.000000000000000000, 1.000000000000000000 ) ) ;
#1181=VECTOR ( 'NONE', #107103, 1000.000000000000000 ) ;
#1198=ADVANCED_FACE ( 'NONE', ( #80877 ), #126440, .F. ) ;
#1201=FACE_OUTER_BOUND ( 'NONE', #201757, .T. ) ;
#1244=AXIS2_PLACEMENT_3D ( 'NONE', #170789, #254105, #134165 ) ;
#1265=VECTOR ( 'NONE', #67470, 1000.000000000000000 ) ;
#1278=PLANE ( 'NONE',  #112418 ) ;
#1355=DIRECTION ( 'NONE',  ( 1.000000000000000000, -3.965082230804126670E-15, 0.000000000000000000 ) ) ;
#1356=DIRECTION ( 'NONE',  ( 1.000000000000000000, 3.265361837132813093E-16, -0.000000000000000000 ) ) ;
#1360=CIRCLE ( 'NONE', #163695, 0.1000000000000028644 ) ;
#1368=DIRECTION ( 'NONE',  ( 0.000000000000000000, 0.000000000000000000, -1.000000000000000000 ) ) ;
#1393=CARTESIAN_POINT ( 'NONE',  ( 19.97071067811864609, 11.72071067812981404, -125.1500000000000341 ) ) ;
#1415=ORIENTED_EDGE ( 'NONE', *, *, #119535, .T. ) ;
#1430=CIRCLE ( 'NONE', #180516, 11.74999999999999645 ) ;
#1497=EDGE_CURVE ( 'NONE', #177351, #201736, #196861, .T. ) ;
#1513=DIRECTION ( 'NONE',  ( 0.000000000000000000, 0.000000000000000000, -1.000000000000000000 ) ) ;
#1523=DIRECTION ( 'NONE',  ( 0.000000000000000000, 0.8700118002898321601, -0.4930308989875230585 ) ) ;
#1574=CIRCLE ( 'NONE', #63947, 11.89999999999999325 ) ;
#1587=EDGE_CURVE ( 'NONE', #218579, #256518, #102684, .T. ) ;
#1656=ORIENTED_EDGE ( 'NONE', *, *, #16266, .F. ) ;
#1658=EDGE_CURVE ( 'NONE', #80403, #225274, #159467, .T. ) ;
#1680=FACE_OUTER_BOUND ( 'NONE', #211007, .T. ) ;
#1701=CARTESIAN_POINT ( 'NONE',  ( 23.14999999999999858, 1.115600667400684642E-11, -138.0000000000000284 ) ) ;
#1747=AXIS2_PLACEMENT_3D ( 'NONE', #232911, #148207, #227739 ) ;
#1796=DIRECTION ( 'NONE',  ( 0.000000000000000000, 0.000000000000000000, -1.000000000000000000 ) ) ;
#1830=CARTESIAN_POINT ( 'NONE',  ( 20.94999999999999929, 1.115600667400684642E-11, -135.9000000000000625 ) ) ;
#1835=DIRECTION ( 'NONE',  ( 2.952720810173289112E-16, -1.000000000000000000, -0.000000000000000000 ) ) ;
#1852=SPHERICAL_SURFACE ( 'NONE', #180446, 0.1000000000000000056 ) ;
#1855=CYLINDRICAL_SURFACE ( 'NONE', #177529, 0.1000000000000001443 ) ;
#1886=CARTESIAN_POINT ( 'NONE',  ( 20.95556889135987788, 10.62194358774625336, -108.1423942218575434 ) ) ;
#1898=CARTESIAN_POINT ( 'NONE',  ( -21.04999999999999716, 6.300179817925787518, -100.4485171181182039 ) ) ;
#1904=DIRECTION ( 'NONE',  ( 0.000000000000000000, 0.000000000000000000, -1.000000000000000000 ) ) ;
#1909=ORIENTED_EDGE ( 'NONE', *, *, #95376, .F. ) ;
#1915=CARTESIAN_POINT ( 'NONE',  ( -22.39999999999999858, 11.75000000001115552, -100.6000000000000369 ) ) ;
#1936=CARTESIAN_POINT ( 'NONE',  ( 21.05315837450969596, 11.75000000001116085, -127.1583560044167029 ) ) ;
#1954=CARTESIAN_POINT ( 'NONE',  ( -18.59999999999999787, 11.75000000001115197, -121.8500000000000369 ) ) ;
#2029=AXIS2_PLACEMENT_3D ( 'NONE', #26764, #47564, #67147 ) ;
#2033=EDGE_LOOP ( 'NONE', ( #233919, #3187, #70039, #165221 ) ) ;
#2051=DIRECTION ( 'NONE',  ( 0.000000000000000000, 0.000000000000000000, -1.000000000000000000 ) ) ;
#2056=ORIENTED_EDGE ( 'NONE', *, *, #230473, .T. ) ;
#2082=ORIENTED_EDGE ( 'NONE', *, *, #111279, .F. ) ;
#2137=ORIENTED_EDGE ( 'NONE', *, *, #120516, .T. ) ;
#2142=ORIENTED_EDGE ( 'NONE', *, *, #212820, .F. ) ;
#2145=DIRECTION ( 'NONE',  ( 0.000000000000000000, 0.000000000000000000, 1.000000000000000000 ) ) ;
#2174=EDGE_CURVE ( 'NONE', #28041, #167915, #76409, .T. ) ;
#2195=DIRECTION ( 'NONE',  ( -1.000000000000000000, -2.952720810173289112E-16, 0.000000000000000000 ) ) ;
#2204=DIRECTION ( 'NONE',  ( 0.000000000000000000, 0.000000000000000000, -1.000000000000000000 ) ) ;
#2233=ORIENTED_EDGE ( 'NONE', *, *, #117676, .T. ) ;
#2237=EDGE_LOOP ( 'NONE', ( #95473, #164357, #65139, #155619 ) ) ;
#2242=FACE_OUTER_BOUND ( 'NONE', #130637, .T. ) ;
#2257=CARTESIAN_POINT ( 'NONE',  ( 20.95224633520496127, 8.900522166568386240, -108.9932764479213034 ) ) ;
#2283=ORIENTED_EDGE ( 'NONE', *, *, #158672, .T. ) ;
#2286=AXIS2_PLACEMENT_3D ( 'NONE', #49761, #73209, #129304 ) ;
#2291=DIRECTION ( 'NONE',  ( 0.000000000000000000, -0.4791956752371546169, -0.8777080977375152360 ) ) ;
#2302=ORIENTED_EDGE ( 'NONE', *, *, #37868, .T. ) ;
#2405=DIRECTION ( 'NONE',  ( 0.000000000000000000, -0.1455152366551721865, -0.9893560106964475187 ) ) ;
#2425=AXIS2_PLACEMENT_3D ( 'NONE', #153513, #135160, #16531 ) ;
#2427=ORIENTED_EDGE ( 'NONE', *, *, #164308, .F. ) ;
#2430=VERTEX_POINT ( 'NONE', #45974 ) ;
#2565=CARTESIAN_POINT ( 'NONE',  ( 18.59999999999999076, 1.115600667400684642E-11, -134.0000000000000284 ) ) ;
#2570=ORIENTED_EDGE ( 'NONE', *, *, #217766, .T. ) ;
#2593=ORIENTED_EDGE ( 'NONE', *, *, #35173, .F. ) ;
#2603=DIRECTION ( 'NONE',  ( 0.000000000000000000, -1.000000000000000000, 0.000000000000000000 ) ) ;
#2633=EDGE_CURVE ( 'NONE', #164361, #241144, #126198, .T. ) ;
#2662=EDGE_LOOP ( 'NONE', ( #255372, #111312, #30213, #95104, #189538, #13881, #156912, #145096 ) ) ;
#2679=CARTESIAN_POINT ( 'NONE',  ( 20.95512820512820440, 10.62384868372303615, -108.1649135690876449 ) ) ;
#2684=CIRCLE ( 'NONE', #215083, 0.1000000000000028644 ) ;
#2717=ORIENTED_EDGE ( 'NONE', *, *, #109385, .T. ) ;
#2735=ADVANCED_FACE ( 'NONE', ( #94776 ), #154785, .F. ) ;
#2758=CARTESIAN_POINT ( 'NONE',  ( -21.11833042828134310, 0.007100509070570094547, -94.05435530614481365 ) ) ;
#2762=CARTESIAN_POINT ( 'NONE',  ( -18.59999999999999787, 9.350000000011156942, -112.7500000000000284 ) ) ;
#2763=FACE_OUTER_BOUND ( 'NONE', #129096, .T. ) ;
#2795=VECTOR ( 'NONE', #83860, 1000.000000000000000 ) ;
#2807=AXIS2_PLACEMENT_3D ( 'NONE', #76164, #209263, #13640 ) ;
#2822=VERTEX_POINT ( 'NONE', #38663 ) ;
#2826=DIRECTION ( 'NONE',  ( 1.000000000000000000, 0.000000000000000000, 0.000000000000000000 ) ) ;
#2879=DIRECTION ( 'NONE',  ( -1.000000000000000000, -0.000000000000000000, -0.000000000000000000 ) ) ;
#2891=ADVANCED_FACE ( 'NONE', ( #236850 ), #77763, .F. ) ;
#2892=ORIENTED_EDGE ( 'NONE', *, *, #191215, .F. ) ;
#2930=DIRECTION ( 'NONE',  ( -1.000000000000000000, 0.000000000000000000, 0.000000000000000000 ) ) ;
#2941=ORIENTED_EDGE ( 'NONE', *, *, #60875, .T. ) ;
#2946=AXIS2_PLACEMENT_3D ( 'NONE', #28210, #169012, #208117 ) ;
#2971=FACE_OUTER_BOUND ( 'NONE', #130807, .T. ) ;
#2993=DIRECTION ( 'NONE',  ( 0.000000000000000000, 0.000000000000000000, -1.000000000000000000 ) ) ;
#3019=CARTESIAN_POINT ( 'NONE',  ( -21.05000000000000071, 11.75000000001115197, -126.9851942293460922 ) ) ;
#3027=CARTESIAN_POINT ( 'NONE',  ( 21.08198257630413508, 6.336596734026219480, -100.4273566762154246 ) ) ;
#3090=CYLINDRICAL_SURFACE ( 'NONE', #242187, 0.1000000000000000472 ) ;
#3096=CYLINDRICAL_SURFACE ( 'NONE', #111320, 0.09999999999999939493 ) ;
#3123=CIRCLE ( 'NONE', #11545, 0.09999999999998898659 ) ;
#3149=EDGE_LOOP ( 'NONE', ( #96305, #247720, #133107, #55062 ) ) ;
#3154=VECTOR ( 'NONE', #203310, 1000.000000000000000 ) ;
#3159=ORIENTED_EDGE ( 'NONE', *, *, #39886, .F. ) ;
#3165=DIRECTION ( 'NONE',  ( -1.000000000000000000, -0.000000000000000000, -0.000000000000000000 ) ) ;
#3177=ORIENTED_EDGE ( 'NONE', *, *, #218307, .T. ) ;
#3187=ORIENTED_EDGE ( 'NONE', *, *, #39610, .F. ) ;
#3196=EDGE_CURVE ( 'NONE', #319, #15812, #176975, .T. ) ;
#3203=CARTESIAN_POINT ( 'NONE',  ( -20.64999999999999858, 7.150000000011155876, -112.7500000000000284 ) ) ;
#3214=VECTOR ( 'NONE', #210563, 1000.000000000000000 ) ;
#3215=EDGE_CURVE ( 'NONE', #62956, #234572, #251947, .T. ) ;
#3223=CARTESIAN_POINT ( 'NONE',  ( 20.99780126800918723, 11.60538868788781031, -127.0873525717055657 ) ) ;
#3234=CYLINDRICAL_SURFACE ( 'NONE', #24908, 12.87499999999999822 ) ;
#3262=ORIENTED_EDGE ( 'NONE', *, *, #256802, .F. ) ;
#3266=AXIS2_PLACEMENT_3D ( 'NONE', #28334, #204352, #226470 ) ;
#3282=FACE_OUTER_BOUND ( 'NONE', #75299, .T. ) ;
#3295=VECTOR ( 'NONE', #57949, 1000.000000000000000 ) ;
#3315=AXIS2_PLACEMENT_3D ( 'NONE', #86205, #206185, #121545 ) ;
#3316=DIRECTION ( 'NONE',  ( 0.000000000000000000, -0.000000000000000000, 1.000000000000000000 ) ) ;
#3333=ORIENTED_EDGE ( 'NONE', *, *, #85396, .T. ) ;
#3339=DIRECTION ( 'NONE',  ( 1.000000000000000000, 0.000000000000000000, 0.000000000000000000 ) ) ;
#3340=ORIENTED_EDGE ( 'NONE', *, *, #155397, .F. ) ;
#3349=AXIS2_PLACEMENT_3D ( 'NONE', #125486, #167213, #82469 ) ;
#3353=FACE_OUTER_BOUND ( 'NONE', #18056, .T. ) ;
#3375=CARTESIAN_POINT ( 'NONE',  ( 20.74625933824090396, 8.882913521095439080, -109.0551710241217620 ) ) ;
#3407=CARTESIAN_POINT ( 'NONE',  ( 18.49999999999999645, 1.728086936805617757, -87.38443500516778784 ) ) ;
#3472=CARTESIAN_POINT ( 'NONE',  ( -18.59999999999999787, 1.115600667400684642E-11, -100.5000000000000284 ) ) ;
#3473=AXIS2_PLACEMENT_3D ( 'NONE', #183624, #201899, #126197 ) ;
#3475=ORIENTED_EDGE ( 'NONE', *, *, #196797, .F. ) ;
#3484=DIRECTION ( 'NONE',  ( 2.952720810173289112E-16, -1.000000000000000000, 0.000000000000000000 ) ) ;
#3520=AXIS2_PLACEMENT_3D ( 'NONE', #45822, #6691, #234733 ) ;
#3528=AXIS2_PLACEMENT_3D ( 'NONE', #68817, #111787, #191348 ) ;
#3586=AXIS2_PLACEMENT_3D ( 'NONE', #179881, #40396, #42924 ) ;
#3595=DIRECTION ( 'NONE',  ( 0.000000000000000000, 0.000000000000000000, -1.000000000000000000 ) ) ;
#3614=EDGE_LOOP ( 'NONE', ( #51488, #246574, #212234, #72556 ) ) ;
#3651=DIRECTION ( 'NONE',  ( 0.000000000000000000, 0.000000000000000000, -1.000000000000000000 ) ) ;
#3676=ORIENTED_EDGE ( 'NONE', *, *, #72005, .T. ) ;
#3682=EDGE_CURVE ( 'NONE', #245768, #11304, #135849, .T. ) ;
#3726=AXIS2_PLACEMENT_3D ( 'NONE', #190397, #149995, #26180 ) ;
#3752=EDGE_CURVE ( 'NONE', #211300, #23430, #77158, .T. ) ;
#3811=FACE_OUTER_BOUND ( 'NONE', #174490, .T. ) ;
#3822=CARTESIAN_POINT ( 'NONE',  ( 18.59999999999999076, 10.49142135624846617, -125.2500000000000568 ) ) ;
#3833=CIRCLE ( 'NONE', #158000, 0.09999999999999939493 ) ;
#3838=FACE_OUTER_BOUND ( 'NONE', #154431, .T. ) ;
#3845=DIRECTION ( 'NONE',  ( 1.734723475976817507E-14, -1.000000000000000000, 0.000000000000000000 ) ) ;
#3888=ADVANCED_FACE ( 'NONE', ( #216046 ), #176967, .T. ) ;
#3893=CARTESIAN_POINT ( 'NONE',  ( 20.94999999999999574, 6.350000000011161383, -110.3438220896831581 ) ) ;
#3901=CARTESIAN_POINT ( 'NONE',  ( -23.15000000000000213, -11.74999999998884448, -88.75000000000004263 ) ) ;
#3929=CIRCLE ( 'NONE', #149694, 11.74999999999999645 ) ;
#3993=ADVANCED_FACE ( 'NONE', ( #192658 ), #256336, .T. ) ;
#4009=AXIS2_PLACEMENT_3D ( 'NONE', #139379, #58560, #59837 ) ;
#4027=CARTESIAN_POINT ( 'NONE',  ( -18.59999999999999787, 11.65000000001115232, -107.5148057706540357 ) ) ;
#4043=VERTEX_POINT ( 'NONE', #141655 ) ;
#4054=CARTESIAN_POINT ( 'NONE',  ( -21.05000000000000071, 0.03175835306658782164, -94.24115287691907383 ) ) ;
#4091=CIRCLE ( 'NONE', #187454, 0.2000000000000057288 ) ;
#4105=DIRECTION ( 'NONE',  ( 1.000000000000000000, 0.000000000000000000, 0.000000000000000000 ) ) ;
#4115=ORIENTED_EDGE ( 'NONE', *, *, #127897, .F. ) ;
#4150=VERTEX_POINT ( 'NONE', #46390 ) ;
#4203=DIRECTION ( 'NONE',  ( 1.000000000000000000, -0.000000000000000000, -0.000000000000000000 ) ) ;
#4225=ORIENTED_EDGE ( 'NONE', *, *, #100171, .F. ) ;
#4233=AXIS2_PLACEMENT_3D ( 'NONE', #118675, #177380, #41702 ) ;
#4241=VECTOR ( 'NONE', #33020, 1000.000000000000000 ) ;
#4249=EDGE_CURVE ( 'NONE', #242555, #177524, #149919, .T. ) ;
#4252=CARTESIAN_POINT ( 'NONE',  ( 22.40000000000020819, -0.1008583690885111045, -88.75043287651033097 ) ) ;
#4253=ORIENTED_EDGE ( 'NONE', *, *, #193929, .F. ) ;
#4294=CARTESIAN_POINT ( 'NONE',  ( 22.39999999999999503, 1.115600667400684642E-11, -92.70922040162665212 ) ) ;
#4308=CARTESIAN_POINT ( 'NONE',  ( -21.05315837450971372, 11.75000000001115019, -127.1583560044167456 ) ) ;
#4321=ORIENTED_EDGE ( 'NONE', *, *, #46739, .T. ) ;
#4352=EDGE_LOOP ( 'NONE', ( #172143, #231080, #89656, #195062 ) ) ;
#4362=VECTOR ( 'NONE', #88073, 1000.000000000000000 ) ;
#4375=DIRECTION ( 'NONE',  ( 1.000000000000000000, -0.000000000000000000, -0.000000000000000000 ) ) ;
#4399=EDGE_CURVE ( 'NONE', #31301, #67239, #34070, .T. ) ;
#4403=ORIENTED_EDGE ( 'NONE', *, *, #207992, .F. ) ;
#4433=DIRECTION ( 'NONE',  ( -0.000000000000000000, -0.9876197685951252359, -0.1568667991644863424 ) ) ;
#4450=AXIS2_PLACEMENT_3D ( 'NONE', #178287, #240806, #197811 ) ;
#4468=LINE ( 'NONE', #124440, #236351 ) ;
#4487=FACE_OUTER_BOUND ( 'NONE', #73704, .T. ) ;
#4498=CARTESIAN_POINT ( 'NONE',  ( -21.14999999999999858, 6.540656951712397138, -100.5000000000000284 ) ) ;
#4512=PLANE ( 'NONE',  #154316 ) ;
#4518=FACE_OUTER_BOUND ( 'NONE', #201056, .T. ) ;
#4524=ORIENTED_EDGE ( 'NONE', *, *, #235188, .T. ) ;
#4529=CARTESIAN_POINT ( 'NONE',  ( 23.24999999999999289, 6.650000000011155876, -112.8500000000000369 ) ) ;
#4534=DIRECTION ( 'NONE',  ( 0.000000000000000000, 1.000000000000000000, 0.000000000000000000 ) ) ;
#4539=AXIS2_PLACEMENT_3D ( 'NONE', #62462, #83268, #199418 ) ;
#4543=ORIENTED_EDGE ( 'NONE', *, *, #151028, .F. ) ;
#4569=DIRECTION ( 'NONE',  ( 1.000000000000000000, -0.000000000000000000, -0.000000000000000000 ) ) ;
#4576=LINE ( 'NONE', #205343, #7262 ) ;
#4610=AXIS2_PLACEMENT_3D ( 'NONE', #249161, #168372, #208749 ) ;
#4624=VECTOR ( 'NONE', #241905, 1000.000000000000000 ) ;
#4649=ORIENTED_EDGE ( 'NONE', *, *, #16713, .T. ) ;
#4731=CARTESIAN_POINT ( 'NONE',  ( 20.94999999999999574, 14.00000000001115730, -105.9270925303825663 ) ) ;
#4751=LINE ( 'NONE', #103856, #208949 ) ;
#4757=CIRCLE ( 'NONE', #133781, 12.77500000000000036 ) ;
#4764=CARTESIAN_POINT ( 'NONE',  ( -20.54999999999999361, 11.65000000001115232, -121.8500000000000369 ) ) ;
#4791=AXIS2_PLACEMENT_3D ( 'NONE', #168113, #123809, #202059 ) ;
#4807=LINE ( 'NONE', #59639, #118306 ) ;
#4812=ORIENTED_EDGE ( 'NONE', *, *, #226171, .F. ) ;
#4816=ORIENTED_EDGE ( 'NONE', *, *, #249441, .T. ) ;
#4826=EDGE_CURVE ( 'NONE', #84341, #60618, #165768, .T. ) ;
#4853=CIRCLE ( 'NONE', #63136, 0.3999999999999975797 ) ;
#4867=CIRCLE ( 'NONE', #238115, 0.1000000000000028644 ) ;
#4877=ADVANCED_FACE ( 'NONE', ( #114762 ), #130049, .F. ) ;
#4878=EDGE_CURVE ( 'NONE', #143179, #227912, #188325, .T. ) ;
#4910=CARTESIAN_POINT ( 'NONE',  ( 22.45301702632625762, 0.01521087972134078925, -88.85020777573963358 ) ) ;
#4925=EDGE_LOOP ( 'NONE', ( #85855, #225126, #183330, #204374 ) ) ;
#4937=DIRECTION ( 'NONE',  ( 0.000000000000000000, 1.000000000000000000, 0.000000000000000000 ) ) ;
#4953=EDGE_CURVE ( 'NONE', #197578, #6436, #33985, .T. ) ;
#4974=DIRECTION ( 'NONE',  ( 0.000000000000000000, 0.000000000000000000, -1.000000000000000000 ) ) ;
#4980=AXIS2_PLACEMENT_3D ( 'NONE', #38781, #37505, #72799 ) ;
#4991=FACE_OUTER_BOUND ( 'NONE', #10154, .T. ) ;
#4993=DIRECTION ( 'NONE',  ( 0.000000000000000000, 0.000000000000000000, -1.000000000000000000 ) ) ;
#4996=CARTESIAN_POINT ( 'NONE',  ( -23.25000000000000000, 1.115600667400684642E-11, -141.9000000000000341 ) ) ;
#5010=DIRECTION ( 'NONE',  ( -3.265361837132813093E-16, 1.000000000000000000, 0.000000000000000000 ) ) ;
#5011=ORIENTED_EDGE ( 'NONE', *, *, #117671, .T. ) ;
#5014=CARTESIAN_POINT ( 'NONE',  ( -21.05000000000000071, 11.75000000001115552, -126.9851942293460922 ) ) ;
#5044=CARTESIAN_POINT ( 'NONE',  ( 18.59999999999999787, -1.835341550213255957, -112.0551512925630107 ) ) ;
#5045=AXIS2_PLACEMENT_3D ( 'NONE', #113863, #55136, #212965 ) ;
#5057=CIRCLE ( 'NONE', #175795, 0.09999999999999939493 ) ;
#5059=AXIS2_PLACEMENT_3D ( 'NONE', #146006, #202143, #125179 ) ;
#5081=VERTEX_POINT ( 'NONE', #59894 ) ;
#5082=DIRECTION ( 'NONE',  ( 0.000000000000000000, -0.8700118002898321601, 0.4930308989875230030 ) ) ;
#5113=DIRECTION ( 'NONE',  ( -0.000000000000000000, 1.000000000000000000, -0.000000000000000000 ) ) ;
#5131=CARTESIAN_POINT ( 'NONE',  ( 20.95512828230152280, 8.876151312336450161, -112.7024302655031391 ) ) ;
#5133=DIRECTION ( 'NONE',  ( -0.000000000000000000, -1.000000000000000000, 0.000000000000000000 ) ) ;
#5143=VECTOR ( 'NONE', #108671, 1000.000000000000000 ) ;
#5145=LINE ( 'NONE', #84673, #125891 ) ;
#5148=AXIS2_PLACEMENT_3D ( 'NONE', #92777, #212749, #174953 ) ;
#5149=AXIS2_PLACEMENT_3D ( 'NONE', #98365, #136225, #198792 ) ;
#5199=ORIENTED_EDGE ( 'NONE', *, *, #5853, .T. ) ;
#5206=ORIENTED_EDGE ( 'NONE', *, *, #78423, .T. ) ;
#5224=CARTESIAN_POINT ( 'NONE',  ( -21.52071067811865746, 7.779289321892505882, -121.7500000000000426 ) ) ;
#5256=CARTESIAN_POINT ( 'NONE',  ( 18.40000000000000568, -9.499999999988851584, -107.4993620971801533 ) ) ;
#5263=CARTESIAN_POINT ( 'NONE',  ( 20.85000000000000142, 7.120270961708750512, -137.6595630418393625 ) ) ;
#5272=EDGE_CURVE ( 'NONE', #182849, #86438, #106732, .T. ) ;
#5307=ORIENTED_EDGE ( 'NONE', *, *, #83225, .T. ) ;
#5310=AXIS2_PLACEMENT_3D ( 'NONE', #90810, #33465, #214612 ) ;
#5391=ORIENTED_EDGE ( 'NONE', *, *, #159553, .T. ) ;
#5429=VECTOR ( 'NONE', #9922, 1000.000000000000000 ) ;
#5450=VERTEX_POINT ( 'NONE', #138779 ) ;
#5489=DIRECTION ( 'NONE',  ( 1.000000000000000000, 0.000000000000000000, 0.000000000000000000 ) ) ;
#5493=CIRCLE ( 'NONE', #226231, 11.79999999999999893 ) ;
#5506=VERTEX_POINT ( 'NONE', #198789 ) ;
#5517=AXIS2_PLACEMENT_3D ( 'NONE', #72795, #245307, #253946 ) ;
#5529=ADVANCED_FACE ( 'NONE', ( #98362 ), #1855, .F. ) ;
#5532=ORIENTED_EDGE ( 'NONE', *, *, #10692, .F. ) ;
#5580=CARTESIAN_POINT ( 'NONE',  ( -20.85000000000000142, 11.75000000001115197, -127.2161343370219413 ) ) ;
#5657=CARTESIAN_POINT ( 'NONE',  ( 18.59999999999999076, 11.65000000001115943, -125.3500000000000512 ) ) ;
#5660=DIRECTION ( 'NONE',  ( -0.000000000000000000, 1.000000000000000000, 1.626303258728266709E-15 ) ) ;
#5682=AXIS2_PLACEMENT_3D ( 'NONE', #237276, #58610, #218978 ) ;
#5685=DIRECTION ( 'NONE',  ( -1.000000000000000000, -1.836970198721029934E-16, -0.000000000000000000 ) ) ;
#5710=EDGE_CURVE ( 'NONE', #101017, #15694, #148464, .T. ) ;
#5745=CARTESIAN_POINT ( 'NONE',  ( -21.05000000000000071, 6.257814610492678398, -100.4022097086908047 ) ) ;
#5764=DIRECTION ( 'NONE',  ( 1.000000000000000000, 0.000000000000000000, 0.000000000000000000 ) ) ;
#5778=CARTESIAN_POINT ( 'NONE',  ( -18.50000000000000000, 1.115600667400684642E-11, -134.0000000000000284 ) ) ;
#5791=VECTOR ( 'NONE', #160905, 1000.000000000000000 ) ;
#5792=EDGE_CURVE ( 'NONE', #223717, #120532, #19467, .T. ) ;
#5853=EDGE_CURVE ( 'NONE', #130606, #231975, #161109, .T. ) ;
#5861=AXIS2_PLACEMENT_3D ( 'NONE', #33591, #251289, #72697 ) ;
#5870=ORIENTED_EDGE ( 'NONE', *, *, #192865, .T. ) ;
#5875=VERTEX_POINT ( 'NONE', #149959 ) ;
#5879=ADVANCED_FACE ( 'NONE', ( #69140 ), #48670, .F. ) ;
#5920=DIRECTION ( 'NONE',  ( -1.000000000000000000, -7.304098846218133681E-16, 4.217023435051677994E-16 ) ) ;
#5946=ORIENTED_EDGE ( 'NONE', *, *, #48496, .F. ) ;
#5953=CARTESIAN_POINT ( 'NONE',  ( -21.00023020733437562, 6.390869245278860689, -100.5000000000000426 ) ) ;
#5961=CIRCLE ( 'NONE', #151763, 0.09999999999999939493 ) ;
#5970=CARTESIAN_POINT ( 'NONE',  ( 18.59999999999999787, -1.835859311432481045, -145.5044391687985694 ) ) ;
#5979=CARTESIAN_POINT ( 'NONE',  ( -20.88420186297724612, 10.33025634372637391, -139.5870929282639281 ) ) ;
#5984=CARTESIAN_POINT ( 'NONE',  ( -20.85000000000000142, 10.33248238083634440, -139.5948465439131780 ) ) ;
#6047=FACE_OUTER_BOUND ( 'NONE', #104293, .T. ) ;
#6052=AXIS2_PLACEMENT_3D ( 'NONE', #128601, #209409, #126016 ) ;
#6070=FACE_OUTER_BOUND ( 'NONE', #190652, .T. ) ;
#6084=DIRECTION ( 'NONE',  ( 0.000000000000000000, 1.000000000000000000, 0.000000000000000000 ) ) ;
#6109=DIRECTION ( 'NONE',  ( -2.952720810173289112E-16, 1.000000000000000000, 0.000000000000000000 ) ) ;
#6112=ADVANCED_FACE ( 'NONE', ( #23290 ), #40295, .T. ) ;
#6135=EDGE_CURVE ( 'NONE', #21483, #189415, #86245, .T. ) ;
#6171=CIRCLE ( 'NONE', #151966, 0.3999999999999975797 ) ;
#6190=TOROIDAL_SURFACE ( 'NONE', #235162, 11.90000000000000391, 0.1000000000000000056 ) ;
#6197=ORIENTED_EDGE ( 'NONE', *, *, #80907, .T. ) ;
#6219=VERTEX_POINT ( 'NONE', #91273 ) ;
#6261=EDGE_LOOP ( 'NONE', ( #199812, #149038, #46766, #85249 ) ) ;
#6268=CARTESIAN_POINT ( 'NONE',  ( 22.39999999999999503, 11.65000000001116298, -100.4000000000000483 ) ) ;
#6285=VECTOR ( 'NONE', #183755, 1000.000000000000000 ) ;
#6294=CARTESIAN_POINT ( 'NONE',  ( -22.48970261584618058, 11.65000000001115588, -100.4446305117826199 ) ) ;
#6314=DIRECTION ( 'NONE',  ( 0.000000000000000000, 0.000000000000000000, -1.000000000000000000 ) ) ;
#6326=DIRECTION ( 'NONE',  ( 2.557131231893037478E-16, -0.8660254037844385966, 0.5000000000000003331 ) ) ;
#6327=VECTOR ( 'NONE', #192543, 1000.000000000000000 ) ;
#6349=AXIS2_PLACEMENT_3D ( 'NONE', #141744, #42651, #117064 ) ;
#6357=LINE ( 'NONE', #23399, #111952 ) ;
#6359=ADVANCED_FACE ( 'NONE', ( #173425 ), #223612, .T. ) ;
#6379=CIRCLE ( 'NONE', #131280, 0.09999999999999939493 ) ;
#6396=PLANE ( 'NONE',  #106716 ) ;
#6404=EDGE_CURVE ( 'NONE', #120532, #144062, #15613, .T. ) ;
#6436=VERTEX_POINT ( 'NONE', #95115 ) ;
#6437=CARTESIAN_POINT ( 'NONE',  ( -20.54999999999999716, -9.499999999988846255, -124.1060308773475924 ) ) ;
#6462=CYLINDRICAL_SURFACE ( 'NONE', #24828, 0.1000000000000028644 ) ;
#6475=EDGE_LOOP ( 'NONE', ( #86672, #149683, #69792, #79971, #80467 ) ) ;
#6484=CARTESIAN_POINT ( 'NONE',  ( -21.14999999999999858, -0.09999999998884338825, -88.85042919245522341 ) ) ;
#6500=FACE_OUTER_BOUND ( 'NONE', #91520, .T. ) ;
#6557=CARTESIAN_POINT ( 'NONE',  ( -21.05000000000000071, 11.65000000001115588, -100.6000000000000369 ) ) ;
#6575=ORIENTED_EDGE ( 'NONE', *, *, #103185, .F. ) ;
#6583=CARTESIAN_POINT ( 'NONE',  ( -21.03571358705782401, 11.75000000001115197, -107.3251068220583733 ) ) ;
#6604=EDGE_CURVE ( 'NONE', #21528, #91963, #145776, .T. ) ;
#6621=EDGE_CURVE ( 'NONE', #245711, #241330, #148364, .T. ) ;
#6653=DIRECTION ( 'NONE',  ( 0.000000000000000000, 0.000000000000000000, -1.000000000000000000 ) ) ;
#6691=DIRECTION ( 'NONE',  ( -1.000000000000000000, 0.000000000000000000, 0.000000000000000000 ) ) ;
#6755=DIRECTION ( 'NONE',  ( 1.000000000000000000, 0.000000000000000000, 0.000000000000000000 ) ) ;
#6763=AXIS2_PLACEMENT_3D ( 'NONE', #150871, #128755, #30962 ) ;
#6779=VECTOR ( 'NONE', #68842, 1000.000000000000114 ) ;
#6803=AXIS2_PLACEMENT_3D ( 'NONE', #143629, #84911, #144901 ) ;
#6804=EDGE_CURVE ( 'NONE', #235011, #71456, #248215, .T. ) ;
#6812=CARTESIAN_POINT ( 'NONE',  ( 23.14999999999999858, 1.115600667400684642E-11, -113.3750000000000284 ) ) ;
#6831=DIRECTION ( 'NONE',  ( -7.304098846218134667E-16, -1.000000000000000000, 0.000000000000000000 ) ) ;
#6847=VECTOR ( 'NONE', #33101, 1000.000000000000000 ) ;
#6849=DIRECTION ( 'NONE',  ( 6.938893903907222067E-15, -1.000000000000000000, -0.000000000000000000 ) ) ;
#6864=ORIENTED_EDGE ( 'NONE', *, *, #84048, .F. ) ;
#6887=CARTESIAN_POINT ( 'NONE',  ( -23.15000000000000213, -8.999999999988846255, -110.3939691226524786 ) ) ;
#6901=ORIENTED_EDGE ( 'NONE', *, *, #21879, .T. ) ;
#6916=ORIENTED_EDGE ( 'NONE', *, *, #195915, .F. ) ;
#6930=DIRECTION ( 'NONE',  ( 0.000000000000000000, 0.000000000000000000, -1.000000000000000000 ) ) ;
#6934=DIRECTION ( 'NONE',  ( 0.000000000000000000, 6.308085367182471812E-16, 1.000000000000000000 ) ) ;
#6964=CARTESIAN_POINT ( 'NONE',  ( -18.59999999999999787, -1.263275465206102233, -141.9018646667464338 ) ) ;
#6971=DIRECTION ( 'NONE',  ( 0.000000000000000000, 0.000000000000000000, -1.000000000000000000 ) ) ;
#7045=ORIENTED_EDGE ( 'NONE', *, *, #161271, .T. ) ;
#7054=DIRECTION ( 'NONE',  ( 1.000000000000000000, -0.000000000000000000, -0.000000000000000000 ) ) ;
#7059=DIRECTION ( 'NONE',  ( 0.000000000000000000, 0.000000000000000000, 1.000000000000000000 ) ) ;
#7066=VERTEX_POINT ( 'NONE', #52459 ) ;
#7084=DIRECTION ( 'NONE',  ( 0.000000000000000000, 0.000000000000000000, -1.000000000000000000 ) ) ;
#7085=FACE_OUTER_BOUND ( 'NONE', #89310, .T. ) ;
#7096=CARTESIAN_POINT ( 'NONE',  ( -18.51555513499605254, -9.352657054493127120, -107.6951698956974752 ) ) ;
#7148=CARTESIAN_POINT ( 'NONE',  ( 23.14999999999999858, 5.600000000011153389, -121.5947339810869465 ) ) ;
#7167=CARTESIAN_POINT ( 'NONE',  ( 18.59999999999999787, -1.736705739456431807, -145.5174225876237699 ) ) ;
#7174=ADVANCED_FACE ( 'NONE', ( #12098 ), #152902, .F. ) ;
#7197=EDGE_CURVE ( 'NONE', #144708, #110957, #216687, .T. ) ;
#7251=( LENGTH_UNIT ( ) NAMED_UNIT ( * ) SI_UNIT ( .MILLI., .METRE. ) );
#7262=VECTOR ( 'NONE', #228795, 1000.000000000000000 ) ;
#7270=CARTESIAN_POINT ( 'NONE',  ( -20.89878130938411616, 10.32747123227773045, -139.5774032850249569 ) ) ;
#7278=DIRECTION ( 'NONE',  ( 1.000000000000000000, 0.000000000000000000, 0.000000000000000000 ) ) ;
#7281=VERTEX_POINT ( 'NONE', #135851 ) ;
#7328=CIRCLE ( 'NONE', #90515, 0.09999999999999939493 ) ;
#7388=PLANE ( 'NONE',  #183294 ) ;
#7392=DIRECTION ( 'NONE',  ( 1.000000000000000000, 0.000000000000000000, 0.000000000000000000 ) ) ;
#7396=ORIENTED_EDGE ( 'NONE', *, *, #161251, .T. ) ;
#7398=FACE_BOUND ( 'NONE', #133633, .T. ) ;
#7431=APPLICATION_CONTEXT ( 'automotive_design' ) ;
#7451=DIRECTION ( 'NONE',  ( 1.000000000000000000, -0.000000000000000000, -0.000000000000000000 ) ) ;
#7473=CLOSED_SHELL ( 'NONE', ( #248885, #156414, #244097, #97757, #22956, #208919, #163552, #115611, #128513, #20482, #79103, #161161, #95090, #167472, #89690, #82642, #179085, #74440, #186703, #168736, #203307, #66624, #54874, #228346, #36670, #238368, #255410, #211723, #115822, #193030, #212788, #213699, #83286, #184157, #48220, #53750, #167890, #150883, #171546, #169532, #209817, #5879, #217750, #153821, #216971, #158966, #51866, #239319, #127587, #11398, #165897, #2735, #96949, #64419, #44432, #227744, #213742, #56756, #152634, #167641, #152498, #161909, #170310, #41104, #196591, #104612, #37233, #123844, #88546, #113577, #36664, #47110, #189584, #134233, #97413, #84253, #22281, #70956, #107079, #50697, #1198, #122288, #58992, #245621, #104360, #248476, #178154, #231636, #26161, #226587, #253427, #88233, #148447, #119349, #163257, #163642, #180957, #249779, #51597, #173773, #82026, #40640, #153162, #253389, #79996, #221027, #117648, #61388, #20198, #205341, #221074, #91165, #27798, #98125, #169736, #21901, #21705, #131556, #210470, #139399, #169780, #125076, #27325, #213547, #54693, #10276, #82346, #58343, #41440, #169140, #90464, #7174, #157496, #68792, #70942, #157947, #195589, #20870, #107861, #81487, #108059, #181989, #229986, #10007, #13095, #26343, #256694, #126533, #91082, #163700, #87103, #50801, #193783, #111873, #101780, #202442, #205758, #123410, #254584, #232703, #240505, #77480, #247807, #131998, #87378, #76048, #231024, #255054, #178590, #206666, #249933, #167217, #62603, #113456, #187102, #218937, #31649, #120373, #130451, #8486, #230779, #247881, #170108, #98914, #124471, #83346, #143041, #6112, #54258, #116219, #196245, #57068, #180015, #246284, #52886, #240024, #33277, #257168, #96125, #39393, #152065, #121553, #177485, #214379, #37050, #30316, #151286, #241006, #42079, #5529, #244444, #202400, #15305, #218634, #162274, #95022, #250578, #190909, #122773, #197635, #105707, #66491, #220114, #177762, #116179, #139393, #49792, #130294, #156854, #85360, #45781, #144378, #224790, #10393, #130395, #231648, #144928, #164652, #78712, #134803, #186395, #86637, #101620, #227166, #122713, #130755, #234876, #106111, #110559, #60449, #175163, #36009, #113315, #109525, #247787, #18263, #113891, #249920, #165752, #19661, #236594, #103885, #63105, #171669, #68743, #54862, #161817, #154221, #33155, #220445, #64429, #119918, #13742, #682, #6359, #152609, #23891, #74932, #32022, #14388, #115443, #53493, #211302, #35276, #237872, #22056, #33483, #39033, #84230, #108368, #235239, #183872, #165561, #197201, #150429, #48363, #145125, #64595, #46240, #57683, #197619, #194427, #130631, #80502, #218108, #108964, #102539, #67372, #47246, #255718, #216859, #97465, #126175, #208849, #63711, #235441, #237090, #3888, #114191, #75100, #245632, #228479, #100017, #158358, #48746, #111914, #251843, #190650, #98160, #69593, #216033, #55884, #64324, #44369, #201520, #115973, #77974, #108557, #83498, #168209, #118074, #156551, #66160, #45105, #121021, #201283, #64923, #45927, #183542, #56022, #213659, #122521, #227628, #141409, #78823, #7860, #60080, #207292, #228038, #252030, #105160, #82536, #161324, #252203, #196560, #252154, #55212, #253736, #65462, #225786, #224788, #207254, #71994, #143714, #232264, #42780, #24963, #13677, #194319, #257383, #94688, #180730, #38967, #74800, #248150, #208873, #49819, #151052, #248092, #224140, #145369, #241968, #243107, #184472, #26617, #196780, #217830, #248179, #145882, #242479, #143879, #251826, #224097, #211204, #169847, #157538, #49580, #180380, #147974, #4877, #193041, #126973, #161778, #232706, #55479, #254707, #80554, #33975, #188953, #192402, #137724, #239598, #58131, #155965, #101770, #87213, #175398, #95852, #3993, #75598, #21310, #28114, #128200, #20624, #46907, #40933, #65630, #2891, #71870, #196097, #81096, #59018, #21188, #64038, #158882, #84548, #51079, #189593, #202061, #63530, #167732, #7708, #169382, #254526, #127782, #78449, #176835, #218620, #228760, #121459, #233256, #184993, #156399, #49495, #72358, #23124, #226657, #95892, #45473, #173413, #63574, #26788, #23456, #65135, #230694, #78561, #123011, #82016 ) ) ;
#7480=LINE ( 'NONE', #186123, #235874 ) ;
#7489=ORIENTED_EDGE ( 'NONE', *, *, #159553, .F. ) ;
#7495=AXIS2_PLACEMENT_3D ( 'NONE', #191302, #89583, #248672 ) ;
#7546=ORIENTED_EDGE ( 'NONE', *, *, #256226, .F. ) ;
#7564=CARTESIAN_POINT ( 'NONE',  ( -23.15000000000000213, -11.48912529306489994, -130.9000000000000341 ) ) ;
#7597=ORIENTED_EDGE ( 'NONE', *, *, #72224, .F. ) ;
#7610=DIRECTION ( 'NONE',  ( -1.000000000000000000, 7.304098846218135653E-16, -4.607487905232624742E-31 ) ) ;
#7708=ADVANCED_FACE ( 'NONE', ( #65008 ), #199414, .T. ) ;
#7729=DIRECTION ( 'NONE',  ( 1.000000000000000000, 3.265361837132813093E-16, -0.000000000000000000 ) ) ;
#7731=CARTESIAN_POINT ( 'NONE',  ( -18.59999999999999787, 9.350000000011156942, -112.6500000000000341 ) ) ;
#7746=CARTESIAN_POINT ( 'NONE',  ( 20.02499999999999858, 9.750000000011153745, -121.6500000000000341 ) ) ;
#7748=EDGE_CURVE ( 'NONE', #20386, #177453, #28214, .T. ) ;
#7749=VECTOR ( 'NONE', #234423, 1000.000000000000000 ) ;
#7762=EDGE_CURVE ( 'NONE', #89986, #28813, #7328, .T. ) ;
#7853=DIRECTION ( 'NONE',  ( -1.000000000000000000, 0.000000000000000000, 0.000000000000000000 ) ) ;
#7856=ORIENTED_EDGE ( 'NONE', *, *, #22074, .T. ) ;
#7860=ADVANCED_FACE ( 'NONE', ( #10189 ), #11475, .T. ) ;
#7867=DIRECTION ( 'NONE',  ( 0.000000000000000000, 0.000000000000000000, -1.000000000000000000 ) ) ;
#7876=LINE ( 'NONE', #251602, #135844 ) ;
#7897=CARTESIAN_POINT ( 'NONE',  ( 21.05095171578076574, 8.776179878782192745, -112.6658732766379103 ) ) ;
#7903=DIRECTION ( 'NONE',  ( -1.000000000000000000, -0.000000000000000000, 0.000000000000000000 ) ) ;
#7907=VECTOR ( 'NONE', #54135, 1000.000000000000000 ) ;
#7921=FACE_OUTER_BOUND ( 'NONE', #107218, .T. ) ;
#7953=AXIS2_PLACEMENT_3D ( 'NONE', #21126, #184014, #142314 ) ;
#7954=EDGE_CURVE ( 'NONE', #72307, #111525, #207441, .T. ) ;
#7961=EDGE_CURVE ( 'NONE', #185072, #238459, #150976, .T. ) ;
#7979=EDGE_LOOP ( 'NONE', ( #225849, #229391, #160463, #77323 ) ) ;
#7995=DIRECTION ( 'NONE',  ( 1.000000000000000000, 0.000000000000000000, 0.000000000000000000 ) ) ;
#7999=AXIS2_PLACEMENT_3D ( 'NONE', #157090, #76238, #77504 ) ;
#8023=CARTESIAN_POINT ( 'NONE',  ( 21.05000000000000071, 6.257814610487280937, -100.4022097086912311 ) ) ;
#8028=FACE_OUTER_BOUND ( 'NONE', #180203, .T. ) ;
#8031=CIRCLE ( 'NONE', #195480, 11.80000000000000426 ) ;
#8054=ORIENTED_EDGE ( 'NONE', *, *, #153797, .T. ) ;
#8063=AXIS2_PLACEMENT_3D ( 'NONE', #192755, #17942, #14128 ) ;
#8101=AXIS2_PLACEMENT_3D ( 'NONE', #7731, #5113, #84642 ) ;
#8107=VERTEX_POINT ( 'NONE', #115698 ) ;
#8108=DIRECTION ( 'NONE',  ( -0.000000000000000000, -0.000000000000000000, 1.000000000000000000 ) ) ;
#8110=ORIENTED_EDGE ( 'NONE', *, *, #93148, .F. ) ;
#8115=AXIS2_PLACEMENT_3D ( 'NONE', #112579, #13477, #92999 ) ;
#8154=EDGE_LOOP ( 'NONE', ( #211384, #232252, #151019, #196600 ) ) ;
#8179=EDGE_CURVE ( 'NONE', #168030, #125538, #49195, .T. ) ;
#8184=DIRECTION ( 'NONE',  ( -2.578261006436900068E-14, 0.1350103645451904977, -0.9908441862701597991 ) ) ;
#8208=VECTOR ( 'NONE', #11597, 1000.000000000000000 ) ;
#8209=VERTEX_POINT ( 'NONE', #141667 ) ;
#8216=CARTESIAN_POINT ( 'NONE',  ( -18.50000000000000355, -1.263275465206102233, -141.9018646667464338 ) ) ;
#8252=EDGE_CURVE ( 'NONE', #18469, #40984, #119978, .T. ) ;
#8289=EDGE_LOOP ( 'NONE', ( #122397, #183883, #202922, #205066, #55068, #46655 ) ) ;
#8329=CARTESIAN_POINT ( 'NONE',  ( 18.49999999999999645, 1.835341550235567887, -112.0551512925630249 ) ) ;
#8331=CIRCLE ( 'NONE', #158370, 0.09999999999999939493 ) ;
#8346=VECTOR ( 'NONE', #155919, 999.9999999999998863 ) ;
#8354=ORIENTED_EDGE ( 'NONE', *, *, #249123, .F. ) ;
#8370=ORIENTED_EDGE ( 'NONE', *, *, #248103, .T. ) ;
#8390=DIRECTION ( 'NONE',  ( 0.000000000000000000, -0.000000000000000000, 1.000000000000000000 ) ) ;
#8449=CARTESIAN_POINT ( 'NONE',  ( -21.14999999999999858, 11.65000000001115588, -107.2838656629781866 ) ) ;
#8478=ORIENTED_EDGE ( 'NONE', *, *, #239268, .T. ) ;
#8486=ADVANCED_FACE ( 'NONE', ( #554 ), #195158, .F. ) ;
#8505=ORIENTED_EDGE ( 'NONE', *, *, #171145, .T. ) ;
#8518=DIRECTION ( 'NONE',  ( 0.000000000000000000, 1.000000000000000000, 0.000000000000000000 ) ) ;
#8533=CARTESIAN_POINT ( 'NONE',  ( 20.96937028524355640, 10.62446937163783289, -107.9914261011696510 ) ) ;
#8536=DIRECTION ( 'NONE',  ( 0.000000000000000000, 0.000000000000000000, 1.000000000000000000 ) ) ;
#8541=EDGE_LOOP ( 'NONE', ( #3333, #149503, #134538, #48320 ) ) ;
#8555=SURFACE_SIDE_STYLE ('',( #107647 ) ) ;
#8593=ORIENTED_EDGE ( 'NONE', *, *, #120467, .F. ) ;
#8594=EDGE_CURVE ( 'NONE', #20141, #222623, #20181, .T. ) ;
#8695=ORIENTED_EDGE ( 'NONE', *, *, #46095, .T. ) ;
#8700=VERTEX_POINT ( 'NONE', #93909 ) ;
#8715=EDGE_LOOP ( 'NONE', ( #119483, #80069, #106394, #248552, #96259 ) ) ;
#8739=VERTEX_POINT ( 'NONE', #207788 ) ;
#8740=CARTESIAN_POINT ( 'NONE',  ( -18.39999999999999858, -9.599999999988844124, -107.5320693966997112 ) ) ;
#8792=ORIENTED_EDGE ( 'NONE', *, *, #73860, .T. ) ;
#8797=CARTESIAN_POINT ( 'NONE',  ( 22.50000000000000000, 0.1000000000111554016, -88.85042919245522341 ) ) ;
#8905=ORIENTED_EDGE ( 'NONE', *, *, #137376, .T. ) ;
#8957=CARTESIAN_POINT ( 'NONE',  ( 18.45139536634707156, -9.486081720270041373, -140.6405116178106880 ) ) ;
#8986=CARTESIAN_POINT ( 'NONE',  ( 21.05000000000000071, -11.74999999998883560, -130.9000000000000341 ) ) ;
#9002=DIRECTION ( 'NONE',  ( 0.000000000000000000, 0.000000000000000000, -1.000000000000000000 ) ) ;
#9011=EDGE_LOOP ( 'NONE', ( #780, #32479, #208048, #236192 ) ) ;
#9014=EDGE_CURVE ( 'NONE', #66665, #239952, #6357, .T. ) ;
#9042=DIRECTION ( 'NONE',  ( 0.000000000000000000, 0.000000000000000000, -1.000000000000000000 ) ) ;
#9052=ORIENTED_EDGE ( 'NONE', *, *, #74313, .T. ) ;
#9055=CARTESIAN_POINT ( 'NONE',  ( -23.15000000000000213, 2.500000000011156409, -113.7246219227621395 ) ) ;
#9110=EDGE_CURVE ( 'NONE', #134210, #163256, #241308, .T. ) ;
#9115=AXIS2_PLACEMENT_3D ( 'NONE', #190426, #93864, #13072 ) ;
#9126=ORIENTED_EDGE ( 'NONE', *, *, #57040, .F. ) ;
#9162=CARTESIAN_POINT ( 'NONE',  ( -21.03922262424672596, 11.62390063401586637, -107.3592080428934850 ) ) ;
#9214=CARTESIAN_POINT ( 'NONE',  ( 20.89878130938411616, 10.32747123227773045, -139.5774032850249569 ) ) ;
#9215=DIRECTION ( 'NONE',  ( 1.000000000000000000, -0.000000000000000000, -0.000000000000000000 ) ) ;
#9257=AXIS2_PLACEMENT_3D ( 'NONE', #5970, #46382, #62124 ) ;
#9261=DIRECTION ( 'NONE',  ( -1.000000000000000000, 0.000000000000000000, 0.000000000000000000 ) ) ;
#9316=ORIENTED_EDGE ( 'NONE', *, *, #201423, .F. ) ;
#9336=CARTESIAN_POINT ( 'NONE',  ( -20.85000000000000142, -1.851617760457748618, -145.6031897196037050 ) ) ;
#9355=DIRECTION ( 'NONE',  ( 0.000000000000000000, 1.000000000000000000, 0.000000000000000000 ) ) ;
#9401=AXIS2_PLACEMENT_3D ( 'NONE', #170061, #215550, #59012 ) ;
#9407=EDGE_LOOP ( 'NONE', ( #142358, #176255, #155377, #196202 ) ) ;
#9417=DIRECTION ( 'NONE',  ( 1.000000000000000000, 0.000000000000000000, 0.000000000000000000 ) ) ;
#9426=VERTEX_POINT ( 'NONE', #171582 ) ;
#9434=ORIENTED_EDGE ( 'NONE', *, *, #93467, .T. ) ;
#9449=AXIS2_PLACEMENT_3D ( 'NONE', #19687, #104318, #222994 ) ;
#9464=FACE_OUTER_BOUND ( 'NONE', #69921, .T. ) ;
#9465=DIRECTION ( 'NONE',  ( 0.000000000000000000, 0.000000000000000000, 1.000000000000000000 ) ) ;
#9471=ORIENTED_EDGE ( 'NONE', *, *, #216403, .F. ) ;
#9486=DIRECTION ( 'NONE',  ( -0.000000000000000000, -0.000000000000000000, 1.000000000000000000 ) ) ;
#9506=CARTESIAN_POINT ( 'NONE',  ( 23.25000000000000000, -9.599999999988842347, -124.1060308773475924 ) ) ;
#9540=EDGE_CURVE ( 'NONE', #138314, #164116, #104079, .T. ) ;
#9543=CIRCLE ( 'NONE', #155339, 0.09999999999999864553 ) ;
#9555=EDGE_LOOP ( 'NONE', ( #157336, #192219, #228495, #84681 ) ) ;
#9565=LINE ( 'NONE', #70863, #5143 ) ;
#9622=EDGE_CURVE ( 'NONE', #110439, #230693, #33226, .T. ) ;
#9629=ORIENTED_EDGE ( 'NONE', *, *, #93887, .T. ) ;
#9665=CARTESIAN_POINT ( 'NONE',  ( 20.94999999999999929, 11.63687328911503727, -127.1782407866755307 ) ) ;
#9706=EDGE_LOOP ( 'NONE', ( #59840, #126281, #162537, #166902 ) ) ;
#9713=DIRECTION ( 'NONE',  ( 2.694716079187272946E-16, -1.000000000000000000, 0.000000000000000000 ) ) ;
#9726=EDGE_CURVE ( 'NONE', #34898, #137137, #62421, .T. ) ;
#9752=ORIENTED_EDGE ( 'NONE', *, *, #133818, .F. ) ;
#9757=CARTESIAN_POINT ( 'NONE',  ( 20.94999999999999929, 5.000000000011153745, -121.5947339810869465 ) ) ;
#9764=DIRECTION ( 'NONE',  ( -1.000000000000000000, 0.000000000000000000, 0.000000000000000000 ) ) ;
#9813=DIRECTION ( 'NONE',  ( -3.469446951953635015E-14, 1.000000000000000000, 0.000000000000000000 ) ) ;
#9853=FACE_OUTER_BOUND ( 'NONE', #4925, .T. ) ;
#9855=SPHERICAL_SURFACE ( 'NONE', #149849, 0.1000000000000000056 ) ;
#9922=DIRECTION ( 'NONE',  ( 0.000000000000000000, 0.000000000000000000, -1.000000000000000000 ) ) ;
#9944=DIRECTION ( 'NONE',  ( 1.000000000000000000, 0.000000000000000000, 0.000000000000000000 ) ) ;
#9951=CIRCLE ( 'NONE', #34941, 0.1000000000000043493 ) ;
#9966=CARTESIAN_POINT ( 'NONE',  ( -20.54999999999999716, -9.499999999988848032, -110.3939691226524786 ) ) ;
#9974=DIRECTION ( 'NONE',  ( -0.000000000000000000, 0.8660254037844502539, 0.4999999999999799050 ) ) ;
#9975=CIRCLE ( 'NONE', #238944, 0.09999999999999971412 ) ;
#9981=CIRCLE ( 'NONE', #255638, 12.97499999999999964 ) ;
#9982=CARTESIAN_POINT ( 'NONE',  ( -18.59999999999999787, 6.982009704867601307, -137.6961521182563217 ) ) ;
#10004=VECTOR ( 'NONE', #116567, 1000.000000000000000 ) ;
#10007=ADVANCED_FACE ( 'NONE', ( #142290 ), #217956, .F. ) ;
#10027=DIRECTION ( 'NONE',  ( 1.000000000000000000, 0.000000000000000000, 0.000000000000000000 ) ) ;
#10028=ORIENTED_EDGE ( 'NONE', *, *, #149364, .F. ) ;
#10096=VECTOR ( 'NONE', #125606, 1000.000000000000114 ) ;
#10121=VECTOR ( 'NONE', #233569, 1000.000000000000114 ) ;
#10128=ORIENTED_EDGE ( 'NONE', *, *, #153797, .F. ) ;
#10133=LINE ( 'NONE', #246176, #251331 ) ;
#10154=EDGE_LOOP ( 'NONE', ( #3676, #228797, #30575, #203755 ) ) ;
#10179=LINE ( 'NONE', #109254, #246083 ) ;
#10187=ORIENTED_EDGE ( 'NONE', *, *, #42101, .T. ) ;
#10189=FACE_OUTER_BOUND ( 'NONE', #174082, .T. ) ;
#10215=ORIENTED_EDGE ( 'NONE', *, *, #128643, .F. ) ;
#10276=ADVANCED_FACE ( 'NONE', ( #249122 ), #150026, .F. ) ;
#10317=CIRCLE ( 'NONE', #185268, 0.1000000000000028644 ) ;
#10369=CIRCLE ( 'NONE', #68039, 0.1000000000000028644 ) ;
#10392=ORIENTED_EDGE ( 'NONE', *, *, #185297, .F. ) ;
#10393=ADVANCED_FACE ( 'NONE', ( #117298 ), #154839, .T. ) ;
#10425=ORIENTED_EDGE ( 'NONE', *, *, #189400, .T. ) ;
#10444=AXIS2_PLACEMENT_3D ( 'NONE', #79101, #218616, #40034 ) ;
#10455=CARTESIAN_POINT ( 'NONE',  ( -21.04999999999999361, 6.307425219576554554, -100.5168198683856957 ) ) ;
#10466=AXIS2_PLACEMENT_3D ( 'NONE', #88634, #67811, #50792 ) ;
#10472=EDGE_CURVE ( 'NONE', #135828, #188180, #198113, .T. ) ;
#10473=CARTESIAN_POINT ( 'NONE',  ( 18.59999999999999432, 1.162701749949165642, -108.6000000000000227 ) ) ;
#10482=AXIS2_PLACEMENT_3D ( 'NONE', #113974, #130983, #248364 ) ;
#10485=CARTESIAN_POINT ( 'NONE',  ( -22.50000000000000000, 0.09263750062063533242, -88.85030279295926903 ) ) ;
#10488=LINE ( 'NONE', #110861, #152418 ) ;
#10504=AXIS2_PLACEMENT_3D ( 'NONE', #225161, #68689, #46533 ) ;
#10520=CIRCLE ( 'NONE', #43828, 2.099999999999990763 ) ;
#10536=CARTESIAN_POINT ( 'NONE',  ( 21.05000000000000071, 1.115600667400684642E-11, -134.0000000000000284 ) ) ;
#10548=EDGE_LOOP ( 'NONE', ( #74657, #89380, #187565, #217233 ) ) ;
#10620=CARTESIAN_POINT ( 'NONE',  ( 23.14999999999999858, 1.115600667400684642E-11, -134.0000000000000284 ) ) ;
#10626=ORIENTED_EDGE ( 'NONE', *, *, #175711, .T. ) ;
#10628=FACE_OUTER_BOUND ( 'NONE', #51728, .T. ) ;
#10638=DIRECTION ( 'NONE',  ( 0.000000000000000000, 1.000000000000000000, 0.000000000000000000 ) ) ;
#10649=ORIENTED_EDGE ( 'NONE', *, *, #257353, .F. ) ;
#10650=DIRECTION ( 'NONE',  ( 1.000000000000000000, 2.952720810173289112E-16, -0.000000000000000000 ) ) ;
#10675=LINE ( 'NONE', #13251, #147443 ) ;
#10689=VERTEX_POINT ( 'NONE', #208408 ) ;
#10692=EDGE_CURVE ( 'NONE', #239952, #144728, #246559, .T. ) ;
#10729=ORIENTED_EDGE ( 'NONE', *, *, #175671, .T. ) ;
#10734=AXIS2_PLACEMENT_3D ( 'NONE', #195469, #156349, #234563 ) ;
#10740=ORIENTED_EDGE ( 'NONE', *, *, #158069, .F. ) ;
#10741=DIRECTION ( 'NONE',  ( -1.000000000000000000, -1.836970198721029934E-16, -3.186635328391151676E-31 ) ) ;
#10760=CARTESIAN_POINT ( 'NONE',  ( -18.59999999999999787, 5.341242990002807112, -90.69334979351201298 ) ) ;
#10784=CIRCLE ( 'NONE', #23276, 7.800000000000001599 ) ;
#10804=CARTESIAN_POINT ( 'NONE',  ( -23.15000000000000213, 4.150000000011156764, -121.6500000000000341 ) ) ;
#10883=ORIENTED_EDGE ( 'NONE', *, *, #101940, .F. ) ;
#10935=VERTEX_POINT ( 'NONE', #40048 ) ;
#10958=CARTESIAN_POINT ( 'NONE',  ( 18.59999999999999432, 1.162701749949165642, -108.5000000000000426 ) ) ;
#10963=PLANE ( 'NONE',  #26927 ) ;
#10971=DIRECTION ( 'NONE',  ( 0.000000000000000000, 0.000000000000000000, -1.000000000000000000 ) ) ;
#11004=COLOUR_RGB ( '', 0.40784314, 0.44705882, 0.49803922) ;
#11017=CARTESIAN_POINT ( 'NONE',  ( -21.05000000000000071, -0.2561057920810652089, -100.4651035583277405 ) ) ;
#11029=CIRCLE ( 'NONE', #35986, 0.09999999999999484301 ) ;
#11047=DIRECTION ( 'NONE',  ( 0.000000000000000000, 0.000000000000000000, -1.000000000000000000 ) ) ;
#11057=CARTESIAN_POINT ( 'NONE',  ( 20.94999999999999929, 10.47338541492406172, -108.0786544642485723 ) ) ;
#11058=VECTOR ( 'NONE', #234981, 1000.000000000000000 ) ;
#11078=LINE ( 'NONE', #69784, #3214 ) ;
#11083=ORIENTED_EDGE ( 'NONE', *, *, #110781, .F. ) ;
#11090=AXIS2_PLACEMENT_3D ( 'NONE', #33539, #213395, #253804 ) ;
#11091=CARTESIAN_POINT ( 'NONE',  ( 21.12642695952774119, 0.09890328320052040045, -94.12434007796485957 ) ) ;
#11105=DIRECTION ( 'NONE',  ( -1.000000000000000000, 0.000000000000000000, 0.000000000000000000 ) ) ;
#11135=DIRECTION ( 'NONE',  ( 0.000000000000000000, -0.9654727137038715545, 0.2605042016806676242 ) ) ;
#11182=CARTESIAN_POINT ( 'NONE',  ( -20.54999999999999716, -8.999999999988846255, -110.3939691226524786 ) ) ;
#11185=ORIENTED_EDGE ( 'NONE', *, *, #114312, .F. ) ;
#11187=CARTESIAN_POINT ( 'NONE',  ( -23.25000000000000000, -1.835859311432481045, -145.5044391687985694 ) ) ;
#11201=CIRCLE ( 'NONE', #36153, 11.74999999999999645 ) ;
#11206=CARTESIAN_POINT ( 'NONE',  ( 23.14999999999999858, 1.115600667400684642E-11, -134.0000000000000284 ) ) ;
#11209=CARTESIAN_POINT ( 'NONE',  ( 23.14999999999999858, 5.600000000011153389, -112.9052660189131245 ) ) ;
#11213=ORIENTED_EDGE ( 'NONE', *, *, #220478, .T. ) ;
#11250=( BOUNDED_SURFACE ( )  B_SPLINE_SURFACE ( 3, 2, ( 
 ( #101006, #120649, #163611 ),
 ( #200168, #1936, #81460 ),
 ( #3223, #162339, #123196 ),
 ( #64507, #85319, #68364 ),
 ( #9665, #224849, #86606 ),
 ( #145308, #128344, #69660 ) ),
 .UNSPECIFIED., .F., .F., .F. ) 
 B_SPLINE_SURFACE_WITH_KNOTS ( ( 4, 2, 4 ),
 ( 3, 3 ),
 ( -1.776356839400250465E-15, 0.7853981633974468357, 1.570796326794895448 ),
 ( 0.000000000000000000, 1.000000000000000000 ),
 .UNSPECIFIED. ) 
 GEOMETRIC_REPRESENTATION_ITEM ( )  RATIONAL_B_SPLINE_SURFACE ( (
 ( 1.000000000000000000, 0.5000000000000260902, 1.000000000000000000),
 ( 1.000000000000000000, 0.4993418825329626332, 1.000000000000000000),
 ( 1.000000000000000000, 0.5278258667064184007, 1.000000000000000000),
 ( 1.000000000000000000, 0.6092287576689454642, 1.000000000000000000),
 ( 1.000000000000000000, 0.6611148371783867050, 1.000000000000000000),
 ( 1.000000000000000000, 0.7071067811865597852, 1.000000000000000000) ) ) 
 REPRESENTATION_ITEM ( '' )  SURFACE ( )  );
#11265=CARTESIAN_POINT ( 'NONE',  ( 20.94999999999999929, 8.876614585098254295, -108.8850804788447135 ) ) ;
#11299=ORIENTED_EDGE ( 'NONE', *, *, #100753, .F. ) ;
#11303=CARTESIAN_POINT ( 'NONE',  ( 20.94999999999999929, 8.926614585098253229, -108.9716830192231498 ) ) ;
#11304=VERTEX_POINT ( 'NONE', #158403 ) ;
#11328=DIRECTION ( 'NONE',  ( 1.000000000000000000, 0.000000000000000000, 0.000000000000000000 ) ) ;
#11355=VECTOR ( 'NONE', #177222, 1000.000000000000000 ) ;
#11363=CARTESIAN_POINT ( 'NONE',  ( -21.05000000000000071, -0.09999999998884338825, -88.85000000000003695 ) ) ;
#11365=DIRECTION ( 'NONE',  ( 0.000000000000000000, 0.000000000000000000, -1.000000000000000000 ) ) ;
#11394=EDGE_LOOP ( 'NONE', ( #95040, #186441, #44680, #181427 ) ) ;
#11398=ADVANCED_FACE ( 'NONE', ( #148772 ), #190480, .F. ) ;
#11434=CARTESIAN_POINT ( 'NONE',  ( 18.57071067811864040, 10.17928932189250091, -121.7500000000000426 ) ) ;
#11445=CIRCLE ( 'NONE', #90516, 11.80000000000000426 ) ;
#11467=AXIS2_PLACEMENT_3D ( 'NONE', #37519, #21804, #180875 ) ;
#11475=CYLINDRICAL_SURFACE ( 'NONE', #219699, 0.09999999999999939493 ) ;
#11493=AXIS2_PLACEMENT_3D ( 'NONE', #173160, #128858, #74042 ) ;
#11508=CARTESIAN_POINT ( 'NONE',  ( 18.59999999999998721, 6.846123162363745074, -137.7377262668498759 ) ) ;
#11517=ORIENTED_EDGE ( 'NONE', *, *, #6604, .F. ) ;
#11545=AXIS2_PLACEMENT_3D ( 'NONE', #254318, #34049, #154011 ) ;
#11597=DIRECTION ( 'NONE',  ( -1.000000000000000000, 0.000000000000000000, 0.000000000000000000 ) ) ;
#11625=CIRCLE ( 'NONE', #7495, 0.3999999999999975797 ) ;
#11632=DIRECTION ( 'NONE',  ( 1.000000000000000000, 0.000000000000000000, 0.000000000000000000 ) ) ;
#11690=CARTESIAN_POINT ( 'NONE',  ( -21.14999999999999858, -0.09999999998884338825, -88.85042919245522341 ) ) ;
#11785=CARTESIAN_POINT ( 'NONE',  ( -22.50000000000000000, 11.64957080755595520, -100.4000000000000483 ) ) ;
#11799=CARTESIAN_POINT ( 'NONE',  ( 22.39999999999999503, 0.1000000000111554016, -92.70922040162665212 ) ) ;
#11801=CARTESIAN_POINT ( 'NONE',  ( 20.94999999999999929, -11.48912529306489994, -130.9000000000000341 ) ) ;
#11807=VECTOR ( 'NONE', #142907, 1000.000000000000000 ) ;
#11813=EDGE_CURVE ( 'NONE', #223255, #168502, #166768, .T. ) ;
#11831=TOROIDAL_SURFACE ( 'NONE', #45113, 0.4000000000000017431, 0.1000000000000000056 ) ;
#11861=DIRECTION ( 'NONE',  ( 1.000000000000000000, 0.000000000000000000, 0.000000000000000000 ) ) ;
#11867=AXIS2_PLACEMENT_3D ( 'NONE', #165105, #189804, #132395 ) ;
#11869=VERTEX_POINT ( 'NONE', #53199 ) ;
#11883=ORIENTED_EDGE ( 'NONE', *, *, #16699, .F. ) ;
#11892=CARTESIAN_POINT ( 'NONE',  ( 20.94999999999999929, -8.999999999988842703, -124.1060308773475924 ) ) ;
#11894=FACE_OUTER_BOUND ( 'NONE', #36096, .T. ) ;
#11899=DIRECTION ( 'NONE',  ( 0.000000000000000000, -0.9999631594459056361, -0.008583690987124413183 ) ) ;
#11909=ORIENTED_EDGE ( 'NONE', *, *, #61557, .F. ) ;
#11917=CARTESIAN_POINT ( 'NONE',  ( 21.05000000000000071, 1.115600667400684642E-11, -134.0000000000000284 ) ) ;
#11965=CARTESIAN_POINT ( 'NONE',  ( -23.15000000000000213, 11.65000000001115588, -126.9851942293460922 ) ) ;
#11989=DIRECTION ( 'NONE',  ( 0.000000000000000000, -1.000000000000000000, -0.000000000000000000 ) ) ;
#12081=B_SPLINE_CURVE_WITH_KNOTS ( 'NONE', 3,
 ( #160857, #46017, #20059, #143826, #85112, #223364, #220806, #460, #42187, #121732, #102114, #181693, #3027, #164696, #44753, #65586, #99546, #63011, #82547 ),
 .UNSPECIFIED., .F., .F.,
 ( 4, 3, 3, 3, 3, 3, 4 ),
 ( 0.000000000000000000, 7.110282409889913185E-05, 0.0001508797727291427476, 0.0002027344179858411031, 0.0002343294522349015981, 0.0002454816334821165657, 0.0002619873080085518072 ),
 .UNSPECIFIED. ) ;
#12098=FACE_OUTER_BOUND ( 'NONE', #224572, .T. ) ;
#12105=LINE ( 'NONE', #89036, #49317 ) ;
#12109=DIRECTION ( 'NONE',  ( -1.000000000000000000, 0.000000000000000000, 0.000000000000000000 ) ) ;
#12112=CIRCLE ( 'NONE', #220386, 4.049999999999998934 ) ;
#12113=LINE ( 'NONE', #90321, #616 ) ;
#12131=AXIS2_PLACEMENT_3D ( 'NONE', #118242, #154829, #55658 ) ;
#12141=ORIENTED_EDGE ( 'NONE', *, *, #145311, .T. ) ;
#12163=FACE_OUTER_BOUND ( 'NONE', #111676, .T. ) ;
#12207=DIRECTION ( 'NONE',  ( 0.000000000000000000, 1.000000000000000000, 0.000000000000000000 ) ) ;
#12217=ORIENTED_EDGE ( 'NONE', *, *, #12374, .T. ) ;
#12223=VERTEX_POINT ( 'NONE', #26938 ) ;
#12251=CIRCLE ( 'NONE', #199699, 0.09999999999999939493 ) ;
#12254=ORIENTED_EDGE ( 'NONE', *, *, #224934, .F. ) ;
#12261=DIRECTION ( 'NONE',  ( -1.000000000000000000, 0.000000000000000000, 0.000000000000000000 ) ) ;
#12285=AXIS2_PLACEMENT_3D ( 'NONE', #17310, #117675, #159387 ) ;
#12292=VERTEX_POINT ( 'NONE', #251075 ) ;
#12306=CARTESIAN_POINT ( 'NONE',  ( -23.25000000000000000, 2.600000000011156054, -113.7246219227621395 ) ) ;
#12311=AXIS2_PLACEMENT_3D ( 'NONE', #200663, #161551, #239794 ) ;
#12352=TOROIDAL_SURFACE ( 'NONE', #87148, 12.97499999999999609, 0.1000000000000000056 ) ;
#12354=LINE ( 'NONE', #35768, #114238 ) ;
#12362=AXIS2_PLACEMENT_3D ( 'NONE', #193692, #141404, #180548 ) ;
#12369=CARTESIAN_POINT ( 'NONE',  ( 18.41356215285961895, -9.499999999988869348, -107.5320693966996544 ) ) ;
#12374=EDGE_CURVE ( 'NONE', #46505, #67969, #126499, .T. ) ;
#12387=ORIENTED_EDGE ( 'NONE', *, *, #216333, .F. ) ;
#12406=CARTESIAN_POINT ( 'NONE',  ( 20.84451136049448294, 10.62014191482269965, -107.9939245595242170 ) ) ;
#12412=DIRECTION ( 'NONE',  ( 0.000000000000000000, 2.891205793294679805E-16, -1.000000000000000000 ) ) ;
#12451=DIRECTION ( 'NONE',  ( 1.000000000000000000, -7.304098846218134667E-16, -0.000000000000000000 ) ) ;
#12459=ORIENTED_EDGE ( 'NONE', *, *, #62305, .F. ) ;
#12468=VECTOR ( 'NONE', #218728, 1000.000000000000000 ) ;
#12476=DIRECTION ( 'NONE',  ( -1.000000000000000000, 9.012599976028471648E-15, 6.882867235861662930E-14 ) ) ;
#12530=CARTESIAN_POINT ( 'NONE',  ( 22.39999999999999503, 11.65000000001116298, -100.5000000000000284 ) ) ;
#12547=EDGE_LOOP ( 'NONE', ( #31027, #167974, #31048, #2302 ) ) ;
#12551=DIRECTION ( 'NONE',  ( 0.000000000000000000, 0.000000000000000000, 1.000000000000000000 ) ) ;
#12564=DIRECTION ( 'NONE',  ( 1.000000000000000000, 3.469446951953704435E-14, -2.003086131649669752E-14 ) ) ;
#12605=ORIENTED_EDGE ( 'NONE', *, *, #69057, .T. ) ;
#12608=CARTESIAN_POINT ( 'NONE',  ( -18.50000000000000000, 11.75000000001115197, -100.6000000000000369 ) ) ;
#12620=ORIENTED_EDGE ( 'NONE', *, *, #232181, .T. ) ;
#12664=ORIENTED_EDGE ( 'NONE', *, *, #6604, .T. ) ;
#12672=CARTESIAN_POINT ( 'NONE',  ( 23.25000000000000000, -11.64999999998884483, -100.5000000000000284 ) ) ;
#12711=SPHERICAL_SURFACE ( 'NONE', #84339, 0.1000000000000000056 ) ;
#12743=VECTOR ( 'NONE', #199278, 1000.000000000000114 ) ;
#12770=LINE ( 'NONE', #190108, #173725 ) ;
#12792=ORIENTED_EDGE ( 'NONE', *, *, #169314, .T. ) ;
#12807=ORIENTED_EDGE ( 'NONE', *, *, #45837, .T. ) ;
#12810=CARTESIAN_POINT ( 'NONE',  ( -18.59999999999999787, -9.321008403350132809, -107.7359382490779183 ) ) ;
#12831=DIRECTION ( 'NONE',  ( 0.000000000000000000, 0.000000000000000000, -1.000000000000000000 ) ) ;
#12854=ORIENTED_EDGE ( 'NONE', *, *, #93490, .T. ) ;
#12860=AXIS2_PLACEMENT_3D ( 'NONE', #95313, #118747, #215262 ) ;
#12916=DIRECTION ( 'NONE',  ( 1.000000000000000000, 0.000000000000000000, 0.000000000000000000 ) ) ;
#12976=ORIENTED_EDGE ( 'NONE', *, *, #6135, .F. ) ;
#13009=ORIENTED_EDGE ( 'NONE', *, *, #204131, .F. ) ;
#13031=VECTOR ( 'NONE', #158846, 1000.000000000000114 ) ;
#13042=CARTESIAN_POINT ( 'NONE',  ( 18.41832399655374886, -9.682403266662264585, -140.6568436200283543 ) ) ;
#13071=CARTESIAN_POINT ( 'NONE',  ( -23.15000000000000213, 1.115625160336667635E-11, -136.0000000000000284 ) ) ;
#13072=DIRECTION ( 'NONE',  ( 0.000000000000000000, 0.000000000000000000, 1.000000000000000000 ) ) ;
#13078=FACE_OUTER_BOUND ( 'NONE', #21071, .T. ) ;
#13095=ADVANCED_FACE ( 'NONE', ( #11894 ), #30171, .F. ) ;
#13171=CARTESIAN_POINT ( 'NONE',  ( 23.15000000000000213, -11.48912529306489994, -130.9000000000000341 ) ) ;
#13195=LINE ( 'NONE', #151430, #81613 ) ;
#13208=EDGE_CURVE ( 'NONE', #97170, #46680, #23118, .T. ) ;
#13251=CARTESIAN_POINT ( 'NONE',  ( -23.25000000000000000, -11.74999999998884448, -134.0000000000000284 ) ) ;
#13256=EDGE_CURVE ( 'NONE', #127698, #177453, #22461, .T. ) ;
#13262=EDGE_CURVE ( 'NONE', #131609, #40304, #68221, .T. ) ;
#13303=CARTESIAN_POINT ( 'NONE',  ( -23.25000000000000000, 2.000000000011154189, -120.7753780772379315 ) ) ;
#13306=ORIENTED_EDGE ( 'NONE', *, *, #237566, .F. ) ;
#13323=FACE_OUTER_BOUND ( 'NONE', #64912, .T. ) ;
#13327=AXIS2_PLACEMENT_3D ( 'NONE', #92014, #90722, #171589 ) ;
#13341=EDGE_CURVE ( 'NONE', #83495, #109956, #9951, .T. ) ;
#13361=CARTESIAN_POINT ( 'NONE',  ( 21.05000000000000071, 5.000000000011153745, -112.9052660189131245 ) ) ;
#13371=CARTESIAN_POINT ( 'NONE',  ( -20.85000000000000142, -11.74999999998884448, -134.0000000000000284 ) ) ;
#13379=DIRECTION ( 'NONE',  ( 0.000000000000000000, 0.000000000000000000, -1.000000000000000000 ) ) ;
#13411=EDGE_CURVE ( 'NONE', #93357, #218820, #230548, .T. ) ;
#13424=EDGE_CURVE ( 'NONE', #134210, #179995, #172324, .T. ) ;
#13428=ORIENTED_EDGE ( 'NONE', *, *, #206863, .T. ) ;
#13454=DIRECTION ( 'NONE',  ( 0.000000000000000000, -0.5000000000000004441, -0.8660254037844384856 ) ) ;
#13458=DIRECTION ( 'NONE',  ( 1.000000000000000000, 0.000000000000000000, 0.000000000000000000 ) ) ;
#13461=CARTESIAN_POINT ( 'NONE',  ( -21.05000000000000071, 14.05000000001115623, -106.0136950707610310 ) ) ;
#13477=DIRECTION ( 'NONE',  ( -1.000000000000000000, 0.000000000000000000, -0.000000000000000000 ) ) ;
#13495=ORIENTED_EDGE ( 'NONE', *, *, #27452, .T. ) ;
#13521=DIRECTION ( 'NONE',  ( -1.000000000000000000, -3.265361837132813093E-16, 0.000000000000000000 ) ) ;
#13524=FACE_OUTER_BOUND ( 'NONE', #125122, .T. ) ;
#13542=AXIS2_PLACEMENT_3D ( 'NONE', #18251, #76930, #219005 ) ;
#13579=EDGE_LOOP ( 'NONE', ( #19021, #178547, #89918, #87849 ) ) ;
#13591=ORIENTED_EDGE ( 'NONE', *, *, #245510, .T. ) ;
#13603=DIRECTION ( 'NONE',  ( 3.469446951953498700E-14, -0.7899159663865300551, -0.6132151058540831201 ) ) ;
#13617=CARTESIAN_POINT ( 'NONE',  ( 20.94999999999999574, -11.39257802169451672, -103.5739495798319751 ) ) ;
#13640=DIRECTION ( 'NONE',  ( 1.000000000000000000, 0.000000000000000000, 0.000000000000000000 ) ) ;
#13666=CARTESIAN_POINT ( 'NONE',  ( 20.51284917709620359, 10.31088662285602275, -108.1724731855920538 ) ) ;
#13677=ADVANCED_FACE ( 'NONE', ( #134568 ), #98005, .F. ) ;
#13687=DIRECTION ( 'NONE',  ( 1.000000000000000000, 0.000000000000000000, 0.000000000000000000 ) ) ;
#13695=ORIENTED_EDGE ( 'NONE', *, *, #198332, .T. ) ;
#13740=CARTESIAN_POINT ( 'NONE',  ( 20.94999999999999929, 1.115600667400684642E-11, -134.0000000000000284 ) ) ;
#13742=ADVANCED_FACE ( 'NONE', ( #109683 ), #93973, .T. ) ;
#13818=VERTEX_POINT ( 'NONE', #155280 ) ;
#13832=EDGE_LOOP ( 'NONE', ( #195697, #171558, #7045, #23130 ) ) ;
#13862=CARTESIAN_POINT ( 'NONE',  ( -23.15000000000000213, 1.115600667400684642E-11, -100.5000000000000284 ) ) ;
#13864=CARTESIAN_POINT ( 'NONE',  ( -20.64999999999999858, 2.500000000011154633, -120.7753780772379315 ) ) ;
#13881=ORIENTED_EDGE ( 'NONE', *, *, #116126, .T. ) ;
#13891=B_SPLINE_CURVE_WITH_KNOTS ( 'NONE', 3,
 ( #45735, #249096, #130401, #146116 ),
 .UNSPECIFIED., .F., .F.,
 ( 4, 4 ),
 ( 0.000000000000000000, 0.001767853679387101484 ),
 .UNSPECIFIED. ) ;
#13910=ORIENTED_EDGE ( 'NONE', *, *, #84486, .T. ) ;
#13922=ORIENTED_EDGE ( 'NONE', *, *, #93140, .T. ) ;
#13933=DIRECTION ( 'NONE',  ( -0.000000000000000000, 0.000000000000000000, 1.000000000000000000 ) ) ;
#13938=DIRECTION ( 'NONE',  ( 1.836970198721029934E-16, -1.000000000000000000, -0.000000000000000000 ) ) ;
#13955=EDGE_LOOP ( 'NONE', ( #62810, #164642, #41602, #51287 ) ) ;
#13988=CARTESIAN_POINT ( 'NONE',  ( -18.44448725179913851, -9.490081715472173940, -140.6289602940625514 ) ) ;
#13996=EDGE_CURVE ( 'NONE', #205, #123531, #202080, .T. ) ;
#14004=CARTESIAN_POINT ( 'NONE',  ( -22.39999999999999858, 0.1000000000111554016, -92.70922040162662370 ) ) ;
#14022=DIRECTION ( 'NONE',  ( 0.000000000000000000, 1.776356839400155604E-15, 1.000000000000000000 ) ) ;
#14047=LINE ( 'NONE', #70181, #144414 ) ;
#14076=CARTESIAN_POINT ( 'NONE',  ( -21.05000000000000071, -11.48912529306490349, -103.5000000000000426 ) ) ;
#14082=VERTEX_POINT ( 'NONE', #104233 ) ;
#14111=AXIS2_PLACEMENT_3D ( 'NONE', #18227, #97722, #256773 ) ;
#14120=CIRCLE ( 'NONE', #155774, 0.09999999999998898659 ) ;
#14128=DIRECTION ( 'NONE',  ( -1.000000000000000000, 0.000000000000000000, 0.000000000000000000 ) ) ;
#14278=ORIENTED_EDGE ( 'NONE', *, *, #121390, .F. ) ;
#14286=TOROIDAL_SURFACE ( 'NONE', #47554, 0.2000000000000000111, 0.1000000000000000056 ) ;
#14303=DIRECTION ( 'NONE',  ( 0.000000000000000000, 0.000000000000000000, -1.000000000000000000 ) ) ;
#14330=CYLINDRICAL_SURFACE ( 'NONE', #95591, 0.1000000000000028644 ) ;
#14350=CARTESIAN_POINT ( 'NONE',  ( -20.64999999999999858, 1.115623935689868526E-11, -132.1000000000000227 ) ) ;
#14367=CARTESIAN_POINT ( 'NONE',  ( 22.39999999999999503, -0.1008583690875579364, -88.75043287651064361 ) ) ;
#14388=ADVANCED_FACE ( 'NONE', ( #200483 ), #179649, .T. ) ;
#14418=VERTEX_POINT ( 'NONE', #161367 ) ;
#14430=EDGE_CURVE ( 'NONE', #88314, #243325, #118859, .T. ) ;
#14466=DIRECTION ( 'NONE',  ( 1.000000000000000000, 0.000000000000000000, 0.000000000000000000 ) ) ;
#14474=CARTESIAN_POINT ( 'NONE',  ( 21.00000000000000000, 9.750000000011153745, -121.7500000000000426 ) ) ;
#14489=CARTESIAN_POINT ( 'NONE',  ( 21.06086055315988759, 8.774707514967413857, -112.7023221551541070 ) ) ;
#14496=AXIS2_PLACEMENT_3D ( 'NONE', #220809, #159566, #239101 ) ;
#14499=ORIENTED_EDGE ( 'NONE', *, *, #214017, .T. ) ;
#14508=CARTESIAN_POINT ( 'NONE',  ( 18.39999999999999858, -9.519327731081283162, -107.4729763765593589 ) ) ;
#14520=ORIENTED_EDGE ( 'NONE', *, *, #137999, .F. ) ;
#14523=ORIENTED_EDGE ( 'NONE', *, *, #50472, .T. ) ;
#14598=ORIENTED_EDGE ( 'NONE', *, *, #102448, .F. ) ;
#14637=AXIS2_PLACEMENT_3D ( 'NONE', #62941, #223286, #43382 ) ;
#14696=CARTESIAN_POINT ( 'NONE',  ( -23.15000000000000213, -9.599999999988845900, -124.1060308773475924 ) ) ;
#14697=EDGE_CURVE ( 'NONE', #17092, #120951, #10520, .T. ) ;
#14747=AXIS2_PLACEMENT_3D ( 'NONE', #67888, #223100, #163153 ) ;
#14749=VERTEX_POINT ( 'NONE', #128028 ) ;
#14756=DIRECTION ( 'NONE',  ( 1.000000000000000000, -0.000000000000000000, 0.000000000000000000 ) ) ;
#14762=CARTESIAN_POINT ( 'NONE',  ( -18.59999999999999787, 10.33248238083634440, -139.5948465439131780 ) ) ;
#14823=EDGE_CURVE ( 'NONE', #167915, #213068, #68979, .T. ) ;
#14837=CIRCLE ( 'NONE', #152779, 0.1000000000000029060 ) ;
#14899=CARTESIAN_POINT ( 'NONE',  ( 18.60000000000000142, -9.399999999988782662, -107.7972597596633193 ) ) ;
#14913=ORIENTED_EDGE ( 'NONE', *, *, #248103, .F. ) ;
#14954=ORIENTED_EDGE ( 'NONE', *, *, #92215, .T. ) ;
#14955=CARTESIAN_POINT ( 'NONE',  ( 20.94999999999999929, 1.360870587203197646, -108.5729979270909951 ) ) ;
#14963=DIRECTION ( 'NONE',  ( 0.000000000000000000, 0.000000000000000000, -1.000000000000000000 ) ) ;
#14966=CARTESIAN_POINT ( 'NONE',  ( 20.94999999999999574, 1.750000000011155743, -112.1695115579016857 ) ) ;
#14970=CYLINDRICAL_SURFACE ( 'NONE', #234771, 0.09999999999999939493 ) ;
#14980=CARTESIAN_POINT ( 'NONE',  ( -18.59999999999999787, -1.835859311432481045, -145.5044391687985694 ) ) ;
#14988=VECTOR ( 'NONE', #78104, 1000.000000000000000 ) ;
#15016=DIRECTION ( 'NONE',  ( 1.000000000000000000, 0.000000000000000000, 0.000000000000000000 ) ) ;
#15054=EDGE_CURVE ( 'NONE', #191859, #75372, #81385, .T. ) ;
#15060=CARTESIAN_POINT ( 'NONE',  ( 23.14999999999999503, 11.65000000001116298, -112.6500000000000341 ) ) ;
#15071=FACE_OUTER_BOUND ( 'NONE', #149802, .T. ) ;
#15138=FACE_OUTER_BOUND ( 'NONE', #195856, .T. ) ;
#15159=CARTESIAN_POINT ( 'NONE',  ( 23.25000000000000000, -8.596261682231833845, -109.9501275171503210 ) ) ;
#15200=ORIENTED_EDGE ( 'NONE', *, *, #74145, .F. ) ;
#15229=DIRECTION ( 'NONE',  ( 0.000000000000000000, 0.000000000000000000, 1.000000000000000000 ) ) ;
#15276=CIRCLE ( 'NONE', #44502, 0.2000000000000057288 ) ;
#15305=ADVANCED_FACE ( 'NONE', ( #158851 ), #80535, .T. ) ;
#15364=CARTESIAN_POINT ( 'NONE',  ( -20.85000000000000142, 7.070967871809997973, -137.7465642218683399 ) ) ;
#15378=AXIS2_PLACEMENT_3D ( 'NONE', #56397, #14756, #190831 ) ;
#15436=EDGE_CURVE ( 'NONE', #75372, #204523, #223910, .T. ) ;
#15446=ORIENTED_EDGE ( 'NONE', *, *, #766, .T. ) ;
#15474=AXIS2_PLACEMENT_3D ( 'NONE', #164131, #65011, #6314 ) ;
#15502=DIRECTION ( 'NONE',  ( 0.000000000000000000, 0.000000000000000000, -1.000000000000000000 ) ) ;
#15552=CARTESIAN_POINT ( 'NONE',  ( 21.05193202509564543, 10.72393601970834354, -112.6725346033258006 ) ) ;
#15565=CARTESIAN_POINT ( 'NONE',  ( 21.53699400380799389, 6.787711793200783106, -100.4999999999817106 ) ) ;
#15567=CARTESIAN_POINT ( 'NONE',  ( -20.85000000000000142, -1.164121893230052995, -141.8148480855716684 ) ) ;
#15584=ORIENTED_EDGE ( 'NONE', *, *, #93633, .F. ) ;
#15597=DIRECTION ( 'NONE',  ( 0.000000000000000000, 0.000000000000000000, -1.000000000000000000 ) ) ;
#15613=LINE ( 'NONE', #75580, #14988 ) ;
#15617=CARTESIAN_POINT ( 'NONE',  ( 18.40916198585730967, -9.499999999988844479, -140.6001896318244349 ) ) ;
#15626=EDGE_CURVE ( 'NONE', #126709, #126005, #51679, .T. ) ;
#15636=CARTESIAN_POINT ( 'NONE',  ( -18.47653818581419927, -9.465280387751805691, -107.6259608161398518 ) ) ;
#15651=ORIENTED_EDGE ( 'NONE', *, *, #135513, .F. ) ;
#15655=EDGE_CURVE ( 'NONE', #15694, #24871, #175536, .T. ) ;
#15678=CARTESIAN_POINT ( 'NONE',  ( 20.85000000000000142, 1.115600667400684642E-11, -141.8000000000000398 ) ) ;
#15694=VERTEX_POINT ( 'NONE', #253746 ) ;
#15711=EDGE_LOOP ( 'NONE', ( #228419, #12664, #122847, #137825 ) ) ;
#15712=ORIENTED_EDGE ( 'NONE', *, *, #138285, .T. ) ;
#15715=DIRECTION ( 'NONE',  ( -0.000000000000000000, -0.000000000000000000, 1.000000000000000000 ) ) ;
#15749=DIRECTION ( 'NONE',  ( 5.603264701231745086E-32, -1.897661533703520636E-16, 1.000000000000000000 ) ) ;
#15751=EDGE_CURVE ( 'NONE', #210814, #256383, #198501, .T. ) ;
#15778=ORIENTED_EDGE ( 'NONE', *, *, #170152, .F. ) ;
#15786=AXIS2_PLACEMENT_3D ( 'NONE', #3472, #67304, #82980 ) ;
#15810=EDGE_LOOP ( 'NONE', ( #104953, #173350, #188589, #115058 ) ) ;
#15812=VERTEX_POINT ( 'NONE', #124532 ) ;
#15822=B_SPLINE_CURVE_WITH_KNOTS ( 'NONE', 3,
 ( #26798, #64600, #123311, #122019 ),
 .UNSPECIFIED., .F., .F.,
 ( 4, 4 ),
 ( 0.000000000000000000, 0.0002118541922231923684 ),
 .UNSPECIFIED. ) ;
#15830=EDGE_CURVE ( 'NONE', #237460, #100304, #161088, .T. ) ;
#15850=DIRECTION ( 'NONE',  ( 0.000000000000000000, 0.000000000000000000, -1.000000000000000000 ) ) ;
#15862=ORIENTED_EDGE ( 'NONE', *, *, #229000, .T. ) ;
#15870=AXIS2_PLACEMENT_3D ( 'NONE', #98814, #256589, #3595 ) ;
#15888=EDGE_LOOP ( 'NONE', ( #170810, #2283 ) ) ;
#15891=ORIENTED_EDGE ( 'NONE', *, *, #226891, .F. ) ;
#15905=EDGE_CURVE ( 'NONE', #146870, #227485, #91818, .T. ) ;
#15916=AXIS2_PLACEMENT_3D ( 'NONE', #141290, #220818, #60450 ) ;
#15924=CIRCLE ( 'NONE', #69898, 0.09999999999999864553 ) ;
#15936=CARTESIAN_POINT ( 'NONE',  ( -21.09316766718153247, 0.03926340232583033080, -94.12984668752531547 ) ) ;
#15976=( BOUNDED_SURFACE ( )  B_SPLINE_SURFACE ( 3, 2, ( 
 ( #241596, #184178, #60379 ),
 ( #64245, #222004, #163354 ),
 ( #43397, #160807, #122944 ),
 ( #103348, #223300, #4252 ) ),
 .UNSPECIFIED., .F., .F., .F. ) 
 B_SPLINE_SURFACE_WITH_KNOTS ( ( 4, 4 ),
 ( 3, 3 ),
 ( 1.219727444046192488E-19, 0.0003124336600439509004 ),
 ( 0.000000000000000000, 1.000000000000000000 ),
 .UNSPECIFIED. ) 
 GEOMETRIC_REPRESENTATION_ITEM ( )  RATIONAL_B_SPLINE_SURFACE ( (
 ( 1.000000000000000000, 0.7071067811865475727, 1.000000000000000000),
 ( 1.000000000000000000, 0.7089187706049692173, 1.000000000000000000),
 ( 1.000000000000000000, 0.7039288185052148261, 1.000000000000000000),
 ( 1.000000000000000000, 0.7040654476016184882, 1.000000000000000000) ) ) 
 REPRESENTATION_ITEM ( '' )  SURFACE ( )  );
#15996=CARTESIAN_POINT ( 'NONE',  ( 18.50000000000000000, -9.499999999988842703, -88.75000000000004263 ) ) ;
#16011=ORIENTED_EDGE ( 'NONE', *, *, #132796, .F. ) ;
#16043=CARTESIAN_POINT ( 'NONE',  ( -18.51697539158857353, 10.31565961587945957, -139.5364194119178478 ) ) ;
#16058=AXIS2_PLACEMENT_3D ( 'NONE', #250344, #211218, #32623 ) ;
#16060=EDGE_CURVE ( 'NONE', #249334, #173650, #96912, .T. ) ;
#16079=EDGE_CURVE ( 'NONE', #85377, #253683, #214336, .T. ) ;
#16084=FACE_OUTER_BOUND ( 'NONE', #112155, .T. ) ;
#16095=AXIS2_PLACEMENT_3D ( 'NONE', #69168, #89974, #249083 ) ;
#16111=CYLINDRICAL_SURFACE ( 'NONE', #216559, 0.09999999999998898659 ) ;
#16141=ORIENTED_EDGE ( 'NONE', *, *, #128146, .F. ) ;
#16152=DIRECTION ( 'NONE',  ( 0.000000000000000000, 0.000000000000000000, -1.000000000000000000 ) ) ;
#16194=CIRCLE ( 'NONE', #249234, 0.1000000000000028644 ) ;
#16208=DIRECTION ( 'NONE',  ( 1.000000000000000000, 2.952720810173289112E-16, -0.000000000000000000 ) ) ;
#16247=CIRCLE ( 'NONE', #249470, 0.1000000000000028644 ) ;
#16255=DIRECTION ( 'NONE',  ( -1.000000000000000000, 0.000000000000000000, 0.000000000000000000 ) ) ;
#16259=CIRCLE ( 'NONE', #228637, 0.1999999999999996503 ) ;
#16266=EDGE_CURVE ( 'NONE', #118818, #144465, #119772, .T. ) ;
#16267=FACE_OUTER_BOUND ( 'NONE', #242984, .T. ) ;
#16338=CARTESIAN_POINT ( 'NONE',  ( -21.64999999999999858, 7.350000000011155166, -112.8500000000000369 ) ) ;
#16368=CARTESIAN_POINT ( 'NONE',  ( -21.05000000000000071, 1.115600667400684642E-11, -100.5000000000000284 ) ) ;
#16381=AXIS2_PLACEMENT_3D ( 'NONE', #231492, #110235, #189786 ) ;
#16391=CIRCLE ( 'NONE', #74682, 0.2000000000000057288 ) ;
#16398=AXIS2_PLACEMENT_3D ( 'NONE', #10804, #128182, #12109 ) ;
#16406=ORIENTED_EDGE ( 'NONE', *, *, #114079, .F. ) ;
#16444=CARTESIAN_POINT ( 'NONE',  ( -20.64999999999999858, -9.499999999988848032, -110.3939691226524786 ) ) ;
#16487=LINE ( 'NONE', #255006, #131221 ) ;
#16507=CARTESIAN_POINT ( 'NONE',  ( 21.14999999999999858, 6.550000000011156231, -112.8500000000000369 ) ) ;
#16519=DIRECTION ( 'NONE',  ( 0.000000000000000000, 0.000000000000000000, -1.000000000000000000 ) ) ;
#16531=DIRECTION ( 'NONE',  ( 1.000000000000000000, 0.000000000000000000, 0.000000000000000000 ) ) ;
#16541=DIRECTION ( 'NONE',  ( 1.000000000000000000, 0.000000000000000000, 0.000000000000000000 ) ) ;
#16559=DIRECTION ( 'NONE',  ( 0.000000000000000000, 1.000000000000000000, 0.000000000000000000 ) ) ;
#16566=ORIENTED_EDGE ( 'NONE', *, *, #139765, .T. ) ;
#16619=DIRECTION ( 'NONE',  ( 0.000000000000000000, -0.8660254037844412611, -0.4999999999999956701 ) ) ;
#16668=( BOUNDED_CURVE ( )  B_SPLINE_CURVE ( 3, ( #211098, #74195, #55838, #75468 ),
 .UNSPECIFIED., .F., .F. ) 
 B_SPLINE_CURVE_WITH_KNOTS ( ( 4, 4 ),
 ( 0.000000000000000000, 1.570796326794908992 ),
 .UNSPECIFIED. ) 
 CURVE ( )  GEOMETRIC_REPRESENTATION_ITEM ( )  RATIONAL_B_SPLINE_CURVE ( ( 1.000000000000000000, 0.8047378541243619399, 0.8047378541243619399, 1.000000000000000000 ) ) 
 REPRESENTATION_ITEM ( '' )  );
#16690=CARTESIAN_POINT ( 'NONE',  ( -23.25000000000000000, 1.115600667400684642E-11, -141.9000000000000341 ) ) ;
#16699=EDGE_CURVE ( 'NONE', #7066, #257484, #11625, .T. ) ;
#16713=EDGE_CURVE ( 'NONE', #20260, #53618, #19997, .T. ) ;
#16732=EDGE_CURVE ( 'NONE', #148718, #43391, #77715, .T. ) ;
#16761=AXIS2_PLACEMENT_3D ( 'NONE', #192777, #213604, #153704 ) ;
#16770=ORIENTED_EDGE ( 'NONE', *, *, #72224, .T. ) ;
#16782=VERTEX_POINT ( 'NONE', #136389 ) ;
#16817=DIRECTION ( 'NONE',  ( 0.000000000000000000, 0.000000000000000000, -1.000000000000000000 ) ) ;
#16839=CARTESIAN_POINT ( 'NONE',  ( 22.00356870142688948, 7.254242362487860696, -100.5000000000000711 ) ) ;
#16848=ORIENTED_EDGE ( 'NONE', *, *, #61557, .T. ) ;
#16885=CARTESIAN_POINT ( 'NONE',  ( -20.64999999999999858, -8.999999999988844479, -124.1060308773475924 ) ) ;
#16897=CARTESIAN_POINT ( 'NONE',  ( -23.25000000000000000, 10.33248238083634440, -139.5948465439131780 ) ) ;
#16907=PLANE ( 'NONE',  #232 ) ;
#16939=VERTEX_POINT ( 'NONE', #7167 ) ;
#16945=DIRECTION ( 'NONE',  ( 0.000000000000000000, 0.000000000000000000, -1.000000000000000000 ) ) ;
#16947=FACE_OUTER_BOUND ( 'NONE', #55042, .T. ) ;
#16983=EDGE_CURVE ( 'NONE', #20386, #83522, #228817, .T. ) ;
#16990=DIRECTION ( 'NONE',  ( 0.000000000000000000, 0.000000000000000000, -1.000000000000000000 ) ) ;
#16995=AXIS2_PLACEMENT_3D ( 'NONE', #112690, #172710, #190964 ) ;
#17007=EDGE_LOOP ( 'NONE', ( #225484, #253190, #257005, #11909, #49282 ) ) ;
#17087=CARTESIAN_POINT ( 'NONE',  ( 23.24999999999999289, 11.65000000001116298, -100.5000000000000284 ) ) ;
#17092=VERTEX_POINT ( 'NONE', #241509 ) ;
#17126=EDGE_CURVE ( 'NONE', #163726, #110634, #74372, .T. ) ;
#17128=FACE_OUTER_BOUND ( 'NONE', #113414, .T. ) ;
#17152=DIRECTION ( 'NONE',  ( -3.440080580676165868E-14, -0.1298341882520124002, -0.9915357197604841577 ) ) ;
#17167=DIRECTION ( 'NONE',  ( 0.000000000000000000, -1.000000000000000000, 0.000000000000000000 ) ) ;
#17220=EDGE_LOOP ( 'NONE', ( #109483, #29980, #159103, #144460 ) ) ;
#17239=AXIS2_PLACEMENT_3D ( 'NONE', #115784, #171950, #239589 ) ;
#17247=EDGE_CURVE ( 'NONE', #46680, #144467, #90884, .T. ) ;
#17296=DIRECTION ( 'NONE',  ( -1.000000000000000000, -1.836970198721029934E-16, 0.000000000000000000 ) ) ;
#17302=CARTESIAN_POINT ( 'NONE',  ( -18.59999999999999787, 1.250000000011155299, -108.5000000000000426 ) ) ;
#17310=CARTESIAN_POINT ( 'NONE',  ( -23.15000000000000213, 1.115600667400684642E-11, -134.0000000000000284 ) ) ;
#17317=DIRECTION ( 'NONE',  ( -1.000000000000000000, 0.000000000000000000, 0.000000000000000000 ) ) ;
#17326=DIRECTION ( 'NONE',  ( 1.000000000000000000, -0.000000000000000000, -0.000000000000000000 ) ) ;
#17359=CARTESIAN_POINT ( 'NONE',  ( 22.50000000000000000, 1.115600667400684642E-11, -100.5000000000000284 ) ) ;
#17388=CIRCLE ( 'NONE', #21493, 0.1000000000000028644 ) ;
#17392=EDGE_CURVE ( 'NONE', #55645, #208604, #241152, .T. ) ;
#17402=CARTESIAN_POINT ( 'NONE',  ( 23.14999999999999503, 11.65000000001116298, -112.7500000000000284 ) ) ;
#17403=ORIENTED_EDGE ( 'NONE', *, *, #240845, .F. ) ;
#17427=CARTESIAN_POINT ( 'NONE',  ( 21.07928932188134397, 1.115600667400684642E-11, -100.5000000000000284 ) ) ;
#17434=CARTESIAN_POINT ( 'NONE',  ( 20.94999999999999929, -1.135018845899022466, -141.7169768834323520 ) ) ;
#17458=CARTESIAN_POINT ( 'NONE',  ( 20.94999999999999929, -9.499999999988848032, -110.3939691226524786 ) ) ;
#17501=DIRECTION ( 'NONE',  ( 2.952720810173288619E-16, -1.000000000000000000, 0.000000000000000000 ) ) ;
#17508=DIRECTION ( 'NONE',  ( 0.000000000000000000, -1.000000000000000000, 0.000000000000000000 ) ) ;
#17512=CARTESIAN_POINT ( 'NONE',  ( 21.09107601085557349, 0.03930716472865622424, -94.13612202464047130 ) ) ;
#17513=VERTEX_POINT ( 'NONE', #178871 ) ;
#17522=CIRCLE ( 'NONE', #250583, 0.9750000000000036415 ) ;
#17536=EDGE_CURVE ( 'NONE', #76942, #170174, #104400, .T. ) ;
#17590=ORIENTED_EDGE ( 'NONE', *, *, #137929, .T. ) ;
#17599=VECTOR ( 'NONE', #181137, 1000.000000000000000 ) ;
#17624=CARTESIAN_POINT ( 'NONE',  ( -20.94999999999999929, -1.835341550213255957, -112.0551512925630249 ) ) ;
#17629=AXIS2_PLACEMENT_3D ( 'NONE', #71131, #251004, #86799 ) ;
#17633=DIRECTION ( 'NONE',  ( 0.000000000000000000, 0.000000000000000000, -1.000000000000000000 ) ) ;
#17639=DIRECTION ( 'NONE',  ( 0.000000000000000000, -0.6728971962616697722, 0.7397360091702875895 ) ) ;
#17652=DIRECTION ( 'NONE',  ( 0.000000000000000000, 0.000000000000000000, -1.000000000000000000 ) ) ;
#17669=ORIENTED_EDGE ( 'NONE', *, *, #219163, .T. ) ;
#17672=AXIS2_PLACEMENT_3D ( 'NONE', #217629, #42875, #220242 ) ;
#17673=CARTESIAN_POINT ( 'NONE',  ( -23.25000000000000000, 1.115600667400684642E-11, -104.5500000000000256 ) ) ;
#17679=EDGE_CURVE ( 'NONE', #104851, #164361, #13891, .T. ) ;
#17712=LINE ( 'NONE', #102365, #60358 ) ;
#17733=CIRCLE ( 'NONE', #221741, 0.09999999999998898659 ) ;
#17770=CIRCLE ( 'NONE', #80108, 2.000000000000002665 ) ;
#17796=ORIENTED_EDGE ( 'NONE', *, *, #30452, .T. ) ;
#17800=CIRCLE ( 'NONE', #109387, 0.09999999999999939493 ) ;
#17830=CIRCLE ( 'NONE', #84431, 0.09999999999999939493 ) ;
#17872=FACE_OUTER_BOUND ( 'NONE', #111409, .T. ) ;
#17918=FACE_OUTER_BOUND ( 'NONE', #213726, .T. ) ;
#17930=CARTESIAN_POINT ( 'NONE',  ( 18.39999999999999858, -9.499999999988842703, -140.6001893912220737 ) ) ;
#17936=DIRECTION ( 'NONE',  ( 0.000000000000000000, 1.000000000000000000, 0.000000000000000000 ) ) ;
#17942=DIRECTION ( 'NONE',  ( 0.000000000000000000, 0.000000000000000000, -1.000000000000000000 ) ) ;
#17962=CIRCLE ( 'NONE', #221955, 0.1999999999999996503 ) ;
#17963=ORIENTED_EDGE ( 'NONE', *, *, #253019, .F. ) ;
#18025=DIRECTION ( 'NONE',  ( 0.000000000000000000, 0.000000000000000000, -1.000000000000000000 ) ) ;
#18027=ORIENTED_EDGE ( 'NONE', *, *, #8179, .F. ) ;
#18032=TOROIDAL_SURFACE ( 'NONE', #234509, 0.2000000000000000111, 0.1000000000000000056 ) ;
#18046=CARTESIAN_POINT ( 'NONE',  ( -20.64999999999999858, 1.115600667400684642E-11, -134.0000000000000284 ) ) ;
#18056=EDGE_LOOP ( 'NONE', ( #141498, #146830, #40717, #137068, #129026 ) ) ;
#18066=VECTOR ( 'NONE', #54822, 1000.000000000000114 ) ;
#18083=DIRECTION ( 'NONE',  ( 0.000000000000000000, 0.000000000000000000, 1.000000000000000000 ) ) ;
#18084=CIRCLE ( 'NONE', #172268, 0.1000000000000000472 ) ;
#18093=DIRECTION ( 'NONE',  ( 0.000000000000000000, 0.000000000000000000, 1.000000000000000000 ) ) ;
#18120=EDGE_CURVE ( 'NONE', #10689, #133593, #53474, .T. ) ;
#18128=AXIS2_PLACEMENT_3D ( 'NONE', #57365, #99052, #236016 ) ;
#18144=CARTESIAN_POINT ( 'NONE',  ( -21.05000000000000071, -11.48912529306489994, -131.1000000000000227 ) ) ;
#18171=ORIENTED_EDGE ( 'NONE', *, *, #255441, .F. ) ;
#18175=ORIENTED_EDGE ( 'NONE', *, *, #200424, .T. ) ;
#18176=LINE ( 'NONE', #135541, #112676 ) ;
#18186=ORIENTED_EDGE ( 'NONE', *, *, #203589, .F. ) ;
#18197=DIRECTION ( 'NONE',  ( 1.000000000000000000, 0.000000000000000000, 0.000000000000000000 ) ) ;
#18227=CARTESIAN_POINT ( 'NONE',  ( 18.59999999999999432, 1.728086936805619311, -87.38443500516778784 ) ) ;
#18251=CARTESIAN_POINT ( 'NONE',  ( -23.25000000000000000, 1.115600667400684642E-11, -100.5000000000000284 ) ) ;
#18254=CARTESIAN_POINT ( 'NONE',  ( 18.49999999999999289, 10.41716543472752932, -125.3499999994178182 ) ) ;
#18263=ADVANCED_FACE ( 'NONE', ( #21712 ), #236896, .T. ) ;
#18273=ORIENTED_EDGE ( 'NONE', *, *, #72639, .F. ) ;
#18352=AXIS2_PLACEMENT_3D ( 'NONE', #18144, #37738, #160255 ) ;
#18381=AXIS2_PLACEMENT_3D ( 'NONE', #166151, #181823, #146525 ) ;
#18384=ORIENTED_EDGE ( 'NONE', *, *, #8252, .T. ) ;
#18386=DIRECTION ( 'NONE',  ( 0.000000000000000000, -1.000000000000000000, -2.891205793294679805E-16 ) ) ;
#18394=EDGE_CURVE ( 'NONE', #80403, #53303, #85484, .T. ) ;
#18406=CARTESIAN_POINT ( 'NONE',  ( -20.64999999999999858, 7.150000000011155876, -121.7500000000000426 ) ) ;
#18431=EDGE_CURVE ( 'NONE', #213938, #150130, #207428, .T. ) ;
#18469=VERTEX_POINT ( 'NONE', #170253 ) ;
#18474=CARTESIAN_POINT ( 'NONE',  ( -21.08884785362073089, 0.04978309507788075683, -94.14280663257441972 ) ) ;
#18491=FACE_OUTER_BOUND ( 'NONE', #39288, .T. ) ;
#18496=DIRECTION ( 'NONE',  ( -1.000000000000000000, -0.000000000000000000, -0.000000000000000000 ) ) ;
#18538=DIRECTION ( 'NONE',  ( 1.000000000000000000, 1.875376730785737719E-16, 0.000000000000000000 ) ) ;
#18564=FACE_OUTER_BOUND ( 'NONE', #95049, .T. ) ;
#18589=CARTESIAN_POINT ( 'NONE',  ( -18.58222699835055280, 10.33200063080771969, -139.5931674956643462 ) ) ;
#18603=DIRECTION ( 'NONE',  ( 0.000000000000000000, 0.000000000000000000, 1.000000000000000000 ) ) ;
#18612=DIRECTION ( 'NONE',  ( 0.000000000000000000, 0.000000000000000000, -1.000000000000000000 ) ) ;
#18620=FACE_OUTER_BOUND ( 'NONE', #50980, .T. ) ;
#18624=LINE ( 'NONE', #138541, #150946 ) ;
#18653=LINE ( 'NONE', #138561, #49958 ) ;
#18709=CARTESIAN_POINT ( 'NONE',  ( -23.15000000000000213, 2.000000000011154189, -120.7753780772379315 ) ) ;
#18742=CIRCLE ( 'NONE', #143640, 0.09999999999999939493 ) ;
#18755=CARTESIAN_POINT ( 'NONE',  ( -21.44999999999999929, 7.250000000011155521, -121.7500000000000426 ) ) ;
#18773=VECTOR ( 'NONE', #2930, 1000.000000000000000 ) ;
#18776=EDGE_CURVE ( 'NONE', #144062, #183616, #166111, .T. ) ;
#18793=CARTESIAN_POINT ( 'NONE',  ( 23.24999999999999645, 5.000000000011153745, -121.5947339810869465 ) ) ;
#18808=ORIENTED_EDGE ( 'NONE', *, *, #35537, .T. ) ;
#18828=EDGE_LOOP ( 'NONE', ( #206792, #162092, #39824, #21012 ) ) ;
#18889=( BOUNDED_SURFACE ( )  B_SPLINE_SURFACE ( 3, 2, ( 
 ( #247768, #224349, #108270 ),
 ( #243906, #6583, #208664 ),
 ( #9162, #65277, #165692 ),
 ( #86092, #164390, #104378 ),
 ( #206081, #223061, #123986 ),
 ( #126543, #168282, #45715 ) ),
 .UNSPECIFIED., .F., .F., .F. ) 
 B_SPLINE_SURFACE_WITH_KNOTS ( ( 4, 2, 4 ),
 ( 3, 3 ),
 ( 1.570796326794895448, 2.356194490192343505, 3.141592653589791784 ),
 ( 0.000000000000000000, 1.000000000000000000 ),
 .UNSPECIFIED. ) 
 GEOMETRIC_REPRESENTATION_ITEM ( )  RATIONAL_B_SPLINE_SURFACE ( (
 ( 1.000000000000000000, 0.7071067811865597852, 1.000000000000000000),
 ( 1.000000000000000000, 0.6611148371788475586, 1.000000000000000000),
 ( 1.000000000000000000, 0.6092287576683730332, 1.000000000000000000),
 ( 1.000000000000000000, 0.5278258667070037102, 1.000000000000000000),
 ( 1.000000000000000000, 0.4993418825324473231, 1.000000000000000000),
 ( 1.000000000000000000, 0.4999999999999960587, 1.000000000000000000) ) ) 
 REPRESENTATION_ITEM ( '' )  SURFACE ( )  );
#18904=VERTEX_POINT ( 'NONE', #181151 ) ;
#18920=AXIS2_PLACEMENT_3D ( 'NONE', #42348, #22810, #102276 ) ;
#18939=FACE_OUTER_BOUND ( 'NONE', #59178, .T. ) ;
#18941=DIRECTION ( 'NONE',  ( 0.000000000000000000, 0.008583690987127625890, 0.9999631594459055250 ) ) ;
#18961=CYLINDRICAL_SURFACE ( 'NONE', #121716, 0.09999999999999939493 ) ;
#18971=AXIS2_PLACEMENT_3D ( 'NONE', #74171, #33772, #97508 ) ;
#18988=CARTESIAN_POINT ( 'NONE',  ( -21.05000000000000071, 1.115600667400684642E-11, -100.5000000000000284 ) ) ;
#18989=VERTEX_POINT ( 'NONE', #159031 ) ;
#19016=CARTESIAN_POINT ( 'NONE',  ( 21.05000000000000071, 6.304516329275134723, -100.5211033080587413 ) ) ;
#19021=ORIENTED_EDGE ( 'NONE', *, *, #170538, .T. ) ;
#19034=CIRCLE ( 'NONE', #119018, 0.09999999999999939493 ) ;
#19037=DIRECTION ( 'NONE',  ( 1.000000000000000000, -0.000000000000000000, -0.000000000000000000 ) ) ;
#19050=DIRECTION ( 'NONE',  ( 0.000000000000000000, 0.000000000000000000, 1.000000000000000000 ) ) ;
#19054=CARTESIAN_POINT ( 'NONE',  ( -22.57320508075687115, 11.75000000001115552, -100.5000000000000284 ) ) ;
#19104=CARTESIAN_POINT ( 'NONE',  ( -21.05000000000000071, 1.115600667400684642E-11, -130.0000000000000284 ) ) ;
#19108=TOROIDAL_SURFACE ( 'NONE', #64891, 0.6000000000000013101, 0.1000000000000000056 ) ;
#19110=CARTESIAN_POINT ( 'NONE',  ( 23.14999999999999858, 4.000000000011155521, -134.0000000000000284 ) ) ;
#19134=AXIS2_PLACEMENT_3D ( 'NONE', #86575, #145278, #187016 ) ;
#19154=DIRECTION ( 'NONE',  ( 1.000000000000000000, 0.000000000000000000, 0.000000000000000000 ) ) ;
#19162=DIRECTION ( 'NONE',  ( 0.000000000000000000, 1.000000000000000000, 0.000000000000000000 ) ) ;
#19178=ORIENTED_EDGE ( 'NONE', *, *, #184566, .F. ) ;
#19197=TOROIDAL_SURFACE ( 'NONE', #227467, 0.4000000000000012990, 0.1000000000000000056 ) ;
#19198=ORIENTED_EDGE ( 'NONE', *, *, #104441, .F. ) ;
#19222=LINE ( 'NONE', #195322, #253293 ) ;
#19236=ORIENTED_EDGE ( 'NONE', *, *, #150576, .T. ) ;
#19258=CARTESIAN_POINT ( 'NONE',  ( 18.49999999999999645, 5.950000000011100632, -110.8057023050348988 ) ) ;
#19325=DIRECTION ( 'NONE',  ( 0.000000000000000000, 0.000000000000000000, -1.000000000000000000 ) ) ;
#19421=ORIENTED_EDGE ( 'NONE', *, *, #22886, .T. ) ;
#19423=DIRECTION ( 'NONE',  ( -1.000000000000000000, 0.000000000000000000, 0.000000000000000000 ) ) ;
#19449=CIRCLE ( 'NONE', #219344, 0.1999999999999987899 ) ;
#19467=CIRCLE ( 'NONE', #15378, 0.1000000000000028644 ) ;
#19502=CIRCLE ( 'NONE', #73677, 0.09999999999999363565 ) ;
#19515=CARTESIAN_POINT ( 'NONE',  ( 18.49999999999996803, 7.070967871809997973, -137.7465642218683399 ) ) ;
#19516=CARTESIAN_POINT ( 'NONE',  ( 23.24999999999999645, 1.115600667400684642E-11, -100.5000000000000284 ) ) ;
#19526=VERTEX_POINT ( 'NONE', #73732 ) ;
#19595=FACE_OUTER_BOUND ( 'NONE', #231651, .T. ) ;
#19610=CARTESIAN_POINT ( 'NONE',  ( 21.09787244211732471, 8.775370707348422172, -112.7392533843174789 ) ) ;
#19643=CARTESIAN_POINT ( 'NONE',  ( 21.05000000000000071, 5.900000000011162093, -123.7809002353436654 ) ) ;
#19647=( BOUNDED_CURVE ( )  B_SPLINE_CURVE ( 3, ( #170511, #70101, #27131, #51767 ),
 .UNSPECIFIED., .F., .F. ) 
 B_SPLINE_CURVE_WITH_KNOTS ( ( 4, 4 ),
 ( 3.141592653589793116, 4.712388980384689674 ),
 .UNSPECIFIED. ) 
 CURVE ( )  GEOMETRIC_REPRESENTATION_ITEM ( )  RATIONAL_B_SPLINE_CURVE ( ( 1.000000000000000000, 0.8047378541243649375, 0.8047378541243649375, 1.000000000000000000 ) ) 
 REPRESENTATION_ITEM ( '' )  );
#19661=ADVANCED_FACE ( 'NONE', ( #196214 ), #116677, .T. ) ;
#19668=CARTESIAN_POINT ( 'NONE',  ( 21.14999999999999503, 11.65000000001116298, -100.6000000000000369 ) ) ;
#19680=EDGE_CURVE ( 'NONE', #203793, #188954, #99657, .T. ) ;
#19687=CARTESIAN_POINT ( 'NONE',  ( -18.59999999999999787, 9.150000000011157653, -112.8500000000000369 ) ) ;
#19714=CARTESIAN_POINT ( 'NONE',  ( 21.05000000000000071, 1.115600667400684642E-11, -100.5000000000000284 ) ) ;
#19732=CARTESIAN_POINT ( 'NONE',  ( 21.05000000000000071, 11.60000000001116227, -127.0717967697245143 ) ) ;
#19791=FACE_OUTER_BOUND ( 'NONE', #66512, .T. ) ;
#19795=CARTESIAN_POINT ( 'NONE',  ( 20.04142135623730070, 11.65000000001115943, -121.8500000000000369 ) ) ;
#19804=DIRECTION ( 'NONE',  ( 1.000000000000000000, 0.000000000000000000, -0.000000000000000000 ) ) ;
#19815=ORIENTED_EDGE ( 'NONE', *, *, #127575, .F. ) ;
#19830=LINE ( 'NONE', #220581, #151305 ) ;
#19835=DIRECTION ( 'NONE',  ( 1.000000000000000000, 0.000000000000000000, -0.000000000000000000 ) ) ;
#19839=DIRECTION ( 'NONE',  ( 0.000000000000000000, 0.000000000000000000, 1.000000000000000000 ) ) ;
#19848=ORIENTED_EDGE ( 'NONE', *, *, #207468, .T. ) ;
#19873=DIRECTION ( 'NONE',  ( 0.000000000000000000, -0.000000000000000000, 1.000000000000000000 ) ) ;
#19919=CARTESIAN_POINT ( 'NONE',  ( -18.59999999999999787, -1.249999999988843369, -141.8004807544151333 ) ) ;
#19932=AXIS2_PLACEMENT_3D ( 'NONE', #24134, #241869, #81480 ) ;
#19938=ORIENTED_EDGE ( 'NONE', *, *, #100397, .T. ) ;
#19959=CIRCLE ( 'NONE', #140744, 0.6000000000000033085 ) ;
#19963=EDGE_CURVE ( 'NONE', #10689, #92883, #29768, .T. ) ;
#19996=ORIENTED_EDGE ( 'NONE', *, *, #220432, .F. ) ;
#19997=CIRCLE ( 'NONE', #107465, 0.2000000000000057288 ) ;
#20029=DIRECTION ( 'NONE',  ( 0.000000000000000000, -1.000000000000000000, 0.000000000000000000 ) ) ;
#20059=CARTESIAN_POINT ( 'NONE',  ( 21.13498764882293557, 6.495618143485025975, -100.4983436052687011 ) ) ;
#20071=DIRECTION ( 'NONE',  ( -0.000000000000000000, 0.01283462868039629209, -0.9999176327611372095 ) ) ;
#20079=AXIS2_PLACEMENT_3D ( 'NONE', #415, #79927, #121687 ) ;
#20106=CARTESIAN_POINT ( 'NONE',  ( 21.07928932188134397, 0.09889514566578934407, -94.17148334360132367 ) ) ;
#20121=AXIS2_PLACEMENT_3D ( 'NONE', #29095, #168612, #239434 ) ;
#20138=ORIENTED_EDGE ( 'NONE', *, *, #70099, .F. ) ;
#20141=VERTEX_POINT ( 'NONE', #45831 ) ;
#20154=EDGE_LOOP ( 'NONE', ( #198621, #116720, #205322, #235928 ) ) ;
#20169=CARTESIAN_POINT ( 'NONE',  ( 18.59999999999999432, 1.162701749949165642, -108.6000000000000227 ) ) ;
#20181=CIRCLE ( 'NONE', #53491, 0.09999999999999939493 ) ;
#20186=CARTESIAN_POINT ( 'NONE',  ( -22.45305610364634674, -0.1008583690875579225, -88.75043287651064361 ) ) ;
#20198=ADVANCED_FACE ( 'NONE', ( #43272 ), #181513, .F. ) ;
#20202=CARTESIAN_POINT ( 'NONE',  ( 20.95512820512820440, 10.62384868372303615, -108.1649135690876449 ) ) ;
#20204=ORIENTED_EDGE ( 'NONE', *, *, #133147, .F. ) ;
#20206=EDGE_CURVE ( 'NONE', #123531, #219752, #66687, .T. ) ;
#20228=CARTESIAN_POINT ( 'NONE',  ( -20.54999999999999716, 7.250000000011155521, -112.7500000000000284 ) ) ;
#20233=CARTESIAN_POINT ( 'NONE',  ( 23.15000000000000213, -11.74999999998883737, -121.8500000000000369 ) ) ;
#20249=DIRECTION ( 'NONE',  ( 1.000000000000000000, 0.000000000000000000, 0.000000000000000000 ) ) ;
#20256=CARTESIAN_POINT ( 'NONE',  ( 23.14999999999999858, 1.115600667400684642E-11, -136.0000000000000284 ) ) ;
#20260=VERTEX_POINT ( 'NONE', #49683 ) ;
#20269=CIRCLE ( 'NONE', #136763, 0.2000000000000057288 ) ;
#20270=DIRECTION ( 'NONE',  ( 1.000000000000000000, 0.000000000000000000, 0.000000000000000000 ) ) ;
#20300=LINE ( 'NONE', #219753, #148240 ) ;
#20311=CIRCLE ( 'NONE', #174478, 0.09999999999999939493 ) ;
#20326=CARTESIAN_POINT ( 'NONE',  ( 21.11833042828144258, 6.445644693866450226, -100.4928994909406015 ) ) ;
#20333=DIRECTION ( 'NONE',  ( 3.265361837132813093E-16, -1.000000000000000000, -0.000000000000000000 ) ) ;
#20349=AXIS2_PLACEMENT_3D ( 'NONE', #18046, #61016, #57149 ) ;
#20364=ORIENTED_EDGE ( 'NONE', *, *, #164826, .F. ) ;
#20386=VERTEX_POINT ( 'NONE', #84458 ) ;
#20442=DIRECTION ( 'NONE',  ( 1.000000000000000000, -0.000000000000000000, -0.000000000000000000 ) ) ;
#20445=( BOUNDED_CURVE ( )  B_SPLINE_CURVE ( 3, ( #191354, #72689, #152227, #193903 ),
 .UNSPECIFIED., .F., .F. ) 
 B_SPLINE_CURVE_WITH_KNOTS ( ( 4, 4 ),
 ( 4.712388980384689674, 6.283185307179586232 ),
 .UNSPECIFIED. ) 
 CURVE ( )  GEOMETRIC_REPRESENTATION_ITEM ( )  RATIONAL_B_SPLINE_CURVE ( ( 1.000000000000000000, 0.8047378541243649375, 0.8047378541243649375, 1.000000000000000000 ) ) 
 REPRESENTATION_ITEM ( '' )  );
#20449=ORIENTED_EDGE ( 'NONE', *, *, #240835, .F. ) ;
#20482=ADVANCED_FACE ( 'NONE', ( #54360 ), #203106, .F. ) ;
#20510=VECTOR ( 'NONE', #28449, 1000.000000000000000 ) ;
#20531=DIRECTION ( 'NONE',  ( -1.000000000000000000, 0.000000000000000000, 0.000000000000000000 ) ) ;
#20534=AXIS2_PLACEMENT_3D ( 'NONE', #117440, #136989, #215250 ) ;
#20535=CARTESIAN_POINT ( 'NONE',  ( -23.15000000000000213, 2.000000000011154189, -120.7753780772379315 ) ) ;
#20536=DIRECTION ( 'NONE',  ( 0.000000000000000000, -1.000000000000000000, -0.000000000000000000 ) ) ;
#20583=CARTESIAN_POINT ( 'NONE',  ( -20.54999999999999716, 4.250000000011156409, -112.7500000000000284 ) ) ;
#20585=DIRECTION ( 'NONE',  ( 1.000000000000000000, 0.000000000000000000, 0.000000000000000000 ) ) ;
#20604=CIRCLE ( 'NONE', #87206, 0.09999999999999939493 ) ;
#20624=ADVANCED_FACE ( 'NONE', ( #221982 ), #115816, .T. ) ;
#20642=ORIENTED_EDGE ( 'NONE', *, *, #76503, .F. ) ;
#20654=ORIENTED_EDGE ( 'NONE', *, *, #148612, .F. ) ;
#20662=VECTOR ( 'NONE', #67998, 1000.000000000000000 ) ;
#20665=FACE_OUTER_BOUND ( 'NONE', #39601, .T. ) ;
#20668=AXIS2_PLACEMENT_3D ( 'NONE', #40370, #198116, #1180 ) ;
#20695=CARTESIAN_POINT ( 'NONE',  ( 22.47007471830798053, 7.720710651937614522, -100.5000000000000426 ) ) ;
#20709=ORIENTED_EDGE ( 'NONE', *, *, #227856, .F. ) ;
#20729=VERTEX_POINT ( 'NONE', #185461 ) ;
#20748=ORIENTED_EDGE ( 'NONE', *, *, #170138, .T. ) ;
#20801=CARTESIAN_POINT ( 'NONE',  ( -21.30740335185486245, 0.09893452578700702438, -93.94334207797203362 ) ) ;
#20805=CARTESIAN_POINT ( 'NONE',  ( 18.59999999999999076, 6.550000000011156231, -121.7500000000000426 ) ) ;
#20846=DIRECTION ( 'NONE',  ( -1.000000000000000000, -1.836970198721029934E-16, 0.000000000000000000 ) ) ;
#20870=ADVANCED_FACE ( 'NONE', ( #203101 ), #23214, .F. ) ;
#20883=VECTOR ( 'NONE', #73841, 1000.000000000000000 ) ;
#20941=CARTESIAN_POINT ( 'NONE',  ( 21.05000000000000071, 1.115600667400684642E-11, -100.6000000000000227 ) ) ;
#20947=CARTESIAN_POINT ( 'NONE',  ( -18.59999999999999787, 1.162701749949165642, -108.6000000000000227 ) ) ;
#20965=VERTEX_POINT ( 'NONE', #70037 ) ;
#20970=DIRECTION ( 'NONE',  ( 1.000000000000000000, -0.000000000000000000, -0.000000000000000000 ) ) ;
#21012=ORIENTED_EDGE ( 'NONE', *, *, #89721, .F. ) ;
#21036=AXIS2_PLACEMENT_3D ( 'NONE', #945, #162639, #80481 ) ;
#21071=EDGE_LOOP ( 'NONE', ( #165927, #192719, #58350, #117630 ) ) ;
#21086=CARTESIAN_POINT ( 'NONE',  ( -21.14999999999999858, 1.115526128501326264E-11, -93.95934304829879125 ) ) ;
#21120=DIRECTION ( 'NONE',  ( 0.000000000000000000, 0.000000000000000000, -1.000000000000000000 ) ) ;
#21126=CARTESIAN_POINT ( 'NONE',  ( -18.59999999999999787, 1.115600667400684642E-11, -134.0000000000000284 ) ) ;
#21136=CARTESIAN_POINT ( 'NONE',  ( 21.05000000000000071, 6.257814610487280937, -100.4022097086912311 ) ) ;
#21188=ADVANCED_FACE ( 'NONE', ( #63275 ), #46689, .T. ) ;
#21198=EDGE_CURVE ( 'NONE', #208145, #229099, #244483, .T. ) ;
#21276=AXIS2_PLACEMENT_3D ( 'NONE', #209536, #93425, #128723 ) ;
#21302=EDGE_CURVE ( 'NONE', #90545, #245055, #4576, .T. ) ;
#21304=AXIS2_PLACEMENT_3D ( 'NONE', #244922, #204502, #188798 ) ;
#21310=ADVANCED_FACE ( 'NONE', ( #68429 ), #144084, .T. ) ;
#21314=DIRECTION ( 'NONE',  ( -1.000000000000000000, 0.000000000000000000, 0.000000000000000000 ) ) ;
#21423=CARTESIAN_POINT ( 'NONE',  ( -21.14999999999999858, -0.1008583690875562017, -88.75043287651064361 ) ) ;
#21431=DIRECTION ( 'NONE',  ( 3.469446951953728416E-14, -0.8660254037844309360, 0.5000000000000134337 ) ) ;
#21450=LINE ( 'NONE', #200066, #240705 ) ;
#21483=VERTEX_POINT ( 'NONE', #17434 ) ;
#21493=AXIS2_PLACEMENT_3D ( 'NONE', #214849, #115754, #34978 ) ;
#21495=CARTESIAN_POINT ( 'NONE',  ( 20.95575313997065336, 10.61455330328599089, -108.1212907019448579 ) ) ;
#21505=DIRECTION ( 'NONE',  ( 1.000000000000000000, 0.000000000000000000, 0.000000000000000000 ) ) ;
#21516=DIRECTION ( 'NONE',  ( 0.000000000000000000, 0.000000000000000000, 1.000000000000000000 ) ) ;
#21524=DIRECTION ( 'NONE',  ( 1.000000000000000000, 0.000000000000000000, 0.000000000000000000 ) ) ;
#21528=VERTEX_POINT ( 'NONE', #136072 ) ;
#21571=CIRCLE ( 'NONE', #192437, 11.80000000000000426 ) ;
#21573=EDGE_CURVE ( 'NONE', #13818, #207918, #194745, .T. ) ;
#21576=ORIENTED_EDGE ( 'NONE', *, *, #32785, .T. ) ;
#21581=DIRECTION ( 'NONE',  ( -2.952720810173289112E-16, 1.000000000000000000, 0.000000000000000000 ) ) ;
#21583=DIRECTION ( 'NONE',  ( 1.301042606982683418E-14, -0.8660254037844330455, 0.5000000000000096589 ) ) ;
#21595=ORIENTED_EDGE ( 'NONE', *, *, #21670, .F. ) ;
#21651=CARTESIAN_POINT ( 'NONE',  ( -20.85000000000000142, -1.164121893230052995, -141.9148480855716343 ) ) ;
#21670=EDGE_CURVE ( 'NONE', #241932, #113797, #232341, .T. ) ;
#21699=ORIENTED_EDGE ( 'NONE', *, *, #51324, .F. ) ;
#21705=ADVANCED_FACE ( 'NONE', ( #66841 ), #88948, .F. ) ;
#21712=FACE_OUTER_BOUND ( 'NONE', #28908, .T. ) ;
#21747=CYLINDRICAL_SURFACE ( 'NONE', #248921, 0.09999999999998898659 ) ;
#21754=DIRECTION ( 'NONE',  ( -1.000000000000000000, -0.000000000000000000, -0.000000000000000000 ) ) ;
#21804=DIRECTION ( 'NONE',  ( 0.000000000000000000, 0.01562499999998609446, -0.9998779222360101304 ) ) ;
#21823=ORIENTED_EDGE ( 'NONE', *, *, #23974, .T. ) ;
#21835=CARTESIAN_POINT ( 'NONE',  ( -21.44999999999999929, 7.350000000011155166, -121.7500000000000426 ) ) ;
#21848=CARTESIAN_POINT ( 'NONE',  ( -22.39999999999999858, 1.115600667400684642E-11, -100.4000000000000341 ) ) ;
#21850=CARTESIAN_POINT ( 'NONE',  ( 20.95083306685154056, 8.916842641901356004, -108.9773248532583807 ) ) ;
#21866=ORIENTED_EDGE ( 'NONE', *, *, #22698, .F. ) ;
#21872=DIRECTION ( 'NONE',  ( 0.000000000000000000, -1.000000000000000000, 0.000000000000000000 ) ) ;
#21879=EDGE_CURVE ( 'NONE', #219752, #205, #121408, .T. ) ;
#21885=AXIS2_PLACEMENT_3D ( 'NONE', #39525, #81162, #119036 ) ;
#21901=ADVANCED_FACE ( 'NONE', ( #178813 ), #236174, .F. ) ;
#21910=TOROIDAL_SURFACE ( 'NONE', #138576, 0.2000000000000000111, 0.1000000000000000056 ) ;
#21914=CARTESIAN_POINT ( 'NONE',  ( -18.47130263965439667, -9.471155585952804046, -140.6834047654767801 ) ) ;
#21924=CIRCLE ( 'NONE', #9257, 0.09999999999998898659 ) ;
#21935=CIRCLE ( 'NONE', #9449, 0.09999999999999939493 ) ;
#21941=DIRECTION ( 'NONE',  ( -1.000000000000000000, -0.000000000000000000, -0.000000000000000000 ) ) ;
#21989=ORIENTED_EDGE ( 'NONE', *, *, #38278, .F. ) ;
#21994=DIRECTION ( 'NONE',  ( -6.938893903907222067E-15, 1.000000000000000000, 2.891205793294679805E-16 ) ) ;
#22000=ORIENTED_EDGE ( 'NONE', *, *, #166144, .T. ) ;
#22048=AXIS2_PLACEMENT_3D ( 'NONE', #192538, #129966, #11328 ) ;
#22054=AXIS2_PLACEMENT_3D ( 'NONE', #156096, #98609, #40002 ) ;
#22056=ADVANCED_FACE ( 'NONE', ( #70981 ), #151797, .T. ) ;
#22060=CARTESIAN_POINT ( 'NONE',  ( -20.64999999999999858, 7.150000000011155876, -112.8500000000000369 ) ) ;
#22074=EDGE_CURVE ( 'NONE', #169135, #96459, #133491, .T. ) ;
#22112=VECTOR ( 'NONE', #214716, 1000.000000000000000 ) ;
#22122=CARTESIAN_POINT ( 'NONE',  ( 21.05000000000000071, 1.115600667400684642E-11, -112.6500000000000341 ) ) ;
#22155=AXIS2_PLACEMENT_3D ( 'NONE', #150769, #12564, #72533 ) ;
#22177=VERTEX_POINT ( 'NONE', #270 ) ;
#22204=EDGE_CURVE ( 'NONE', #172421, #183119, #61997, .T. ) ;
#22208=CARTESIAN_POINT ( 'NONE',  ( -22.59999970745345976, -0.009356377315827653016, -88.74948679233081350 ) ) ;
#22218=CARTESIAN_POINT ( 'NONE',  ( -20.94999999999999929, 11.65000000001115232, -127.2161343370219413 ) ) ;
#22262=DIRECTION ( 'NONE',  ( 0.000000000000000000, -0.000000000000000000, 1.000000000000000000 ) ) ;
#22281=ADVANCED_FACE ( 'NONE', ( #242729 ), #107074, .T. ) ;
#22309=AXIS2_PLACEMENT_3D ( 'NONE', #163183, #178918, #235 ) ;
#22317=DIRECTION ( 'NONE',  ( -0.000000000000000000, 1.000000000000000000, -0.000000000000000000 ) ) ;
#22318=EDGE_CURVE ( 'NONE', #164116, #238428, #20311, .T. ) ;
#22362=DIRECTION ( 'NONE',  ( 1.000000000000000000, 0.000000000000000000, -0.000000000000000000 ) ) ;
#22381=EDGE_CURVE ( 'NONE', #234552, #131734, #66076, .T. ) ;
#22451=DIRECTION ( 'NONE',  ( 1.000000000000000000, 0.000000000000000000, 0.000000000000000000 ) ) ;
#22461=CIRCLE ( 'NONE', #238922, 0.2000000000000057288 ) ;
#22511=DIRECTION ( 'NONE',  ( 0.000000000000000000, -1.224646799142185182E-16, 1.000000000000000000 ) ) ;
#22519=AXIS2_PLACEMENT_3D ( 'NONE', #226202, #47589, #127146 ) ;
#22533=CARTESIAN_POINT ( 'NONE',  ( 20.94999999999999574, -11.74999999998883560, -103.4000000000000341 ) ) ;
#22609=CARTESIAN_POINT ( 'NONE',  ( -21.05000000000000071, -1.162701749926853712, -108.6000000000000227 ) ) ;
#22627=CARTESIAN_POINT ( 'NONE',  ( -21.02374657821588855, 11.60000000083177696, -127.0717967701983326 ) ) ;
#22630=CARTESIAN_POINT ( 'NONE',  ( 23.24999999999997513, 11.75000000001116263, -126.9851942293460922 ) ) ;
#22678=EDGE_CURVE ( 'NONE', #203793, #250577, #112077, .T. ) ;
#22698=EDGE_CURVE ( 'NONE', #67239, #188768, #107969, .T. ) ;
#22746=EDGE_CURVE ( 'NONE', #87387, #25027, #137008, .T. ) ;
#22763=DIRECTION ( 'NONE',  ( 0.000000000000000000, -1.000000000000000000, 0.000000000000000000 ) ) ;
#22765=AXIS2_PLACEMENT_3D ( 'NONE', #192821, #152428, #154988 ) ;
#22792=ORIENTED_EDGE ( 'NONE', *, *, #25139, .T. ) ;
#22798=DIRECTION ( 'NONE',  ( -1.000000000000000000, -0.000000000000000000, -0.000000000000000000 ) ) ;
#22810=DIRECTION ( 'NONE',  ( 1.000000000000000000, -0.000000000000000000, -0.000000000000000000 ) ) ;
#22812=( BOUNDED_SURFACE ( )  B_SPLINE_SURFACE ( 3, 2, ( 
 ( #50829, #92537, #113403 ),
 ( #15617, #33916, #13042 ),
 ( #189088, #191691, #30039 ),
 ( #172133, #230801, #132979 ),
 ( #95119, #169569, #211214 ),
 ( #247771, #114683, #148691 ),
 ( #71722, #251628, #73029 ),
 ( #249078, #151258, #74309 ),
 ( #52124, #32620, #130383 ),
 ( #152562, #49575, #232083 ) ),
 .UNSPECIFIED., .F., .F., .F. ) 
 B_SPLINE_SURFACE_WITH_KNOTS ( ( 4, 2, 2, 2, 4 ),
 ( 3, 3 ),
 ( 0.0001701955120502345899, 0.0002247052511886083901, 0.0002792149903269822175, 0.0003882344686037298722, 0.0006062734251572251274 ),
 ( 0.000000000000000000, 1.000000000000000000 ),
 .UNSPECIFIED. ) 
 GEOMETRIC_REPRESENTATION_ITEM ( )  RATIONAL_B_SPLINE_SURFACE ( (
 ( 1.000000000000000000, 0.2966190024560962923, 1.000000000000000000),
 ( 1.000000000000000000, 0.2964522492710705004, 1.000000000000000000),
 ( 1.000000000000000000, 0.3059923531883924630, 1.000000000000000000),
 ( 1.000000000000000000, 0.3355751146944598862, 1.000000000000000000),
 ( 1.000000000000000000, 0.3550672384962806349, 1.000000000000000000),
 ( 1.000000000000000000, 0.4157034672182661761, 1.000000000000000000),
 ( 1.000000000000000000, 0.4588031877658533819, 1.000000000000000000),
 ( 1.000000000000000000, 0.5771441759652413683, 1.000000000000000000),
 ( 1.000000000000000000, 0.6469377121778552286, 1.000000000000000000),
 ( 1.000000000000000000, 0.7071067811865475727, 1.000000000000000000) ) ) 
 REPRESENTATION_ITEM ( '' )  SURFACE ( )  );
#22828=AXIS2_PLACEMENT_3D ( 'NONE', #19795, #99289, #120201 ) ;
#22837=DIRECTION ( 'NONE',  ( 0.000000000000000000, 1.000000000000000000, 1.734723475976807292E-15 ) ) ;
#22865=EDGE_CURVE ( 'NONE', #79905, #132946, #253879, .T. ) ;
#22869=CIRCLE ( 'NONE', #118729, 0.1000000000000001860 ) ;
#22876=DIRECTION ( 'NONE',  ( -2.915501640297154283E-16, 1.000000000000000000, 0.000000000000000000 ) ) ;
#22886=EDGE_CURVE ( 'NONE', #29706, #56434, #166446, .T. ) ;
#22892=LINE ( 'NONE', #204060, #149472 ) ;
#22922=EDGE_CURVE ( 'NONE', #81295, #122312, #174841, .T. ) ;
#22953=DIRECTION ( 'NONE',  ( 1.000000000000000000, 0.000000000000000000, 0.000000000000000000 ) ) ;
#22956=ADVANCED_FACE ( 'NONE', ( #100013 ), #195662, .T. ) ;
#22992=CARTESIAN_POINT ( 'NONE',  ( 20.77526135991775291, 8.932009016633136511, -108.9685685427243698 ) ) ;
#23033=CARTESIAN_POINT ( 'NONE',  ( 18.49999999999999645, 1.115600667400684642E-11, -134.0000000000000284 ) ) ;
#23045=DIRECTION ( 'NONE',  ( 0.000000000000000000, -0.8700118002898321601, 0.4930308989875230030 ) ) ;
#23062=CARTESIAN_POINT ( 'NONE',  ( -22.39999999999999858, 7.790779598384560245, -100.4000000000000341 ) ) ;
#23089=AXIS2_PLACEMENT_3D ( 'NONE', #197665, #19037, #164972 ) ;
#23102=CARTESIAN_POINT ( 'NONE',  ( 22.39999999999999503, 1.115541036281197940E-11, -92.70922040162665212 ) ) ;
#23111=AXIS2_PLACEMENT_3D ( 'NONE', #186466, #46924, #67791 ) ;
#23117=ORIENTED_EDGE ( 'NONE', *, *, #164826, .T. ) ;
#23118=LINE ( 'NONE', #42654, #138902 ) ;
#23124=ADVANCED_FACE ( 'NONE', ( #122193 ), #38814, .F. ) ;
#23130=ORIENTED_EDGE ( 'NONE', *, *, #187435, .F. ) ;
#23173=ORIENTED_EDGE ( 'NONE', *, *, #237921, .T. ) ;
#23201=CARTESIAN_POINT ( 'NONE',  ( -23.15000000000000213, 1.115600667400684642E-11, -134.0000000000000284 ) ) ;
#23214=CYLINDRICAL_SURFACE ( 'NONE', #132563, 11.80000000000000426 ) ;
#23247=DIRECTION ( 'NONE',  ( 0.000000000000000000, -0.8660254037844459241, -0.4999999999999873990 ) ) ;
#23253=DIRECTION ( 'NONE',  ( 0.000000000000000000, 0.000000000000000000, -1.000000000000000000 ) ) ;
#23276=AXIS2_PLACEMENT_3D ( 'NONE', #112411, #73304, #111113 ) ;
#23290=FACE_OUTER_BOUND ( 'NONE', #114693, .T. ) ;
#23306=STYLED_ITEM ( 'NONE', ( #148067 ), #194461 ) ;
#23322=EDGE_CURVE ( 'NONE', #174781, #103006, #4091, .T. ) ;
#23343=CIRCLE ( 'NONE', #69116, 0.1000000000000028644 ) ;
#23351=CARTESIAN_POINT ( 'NONE',  ( -23.15000000000000213, -8.663551401858001100, -124.4758988819327215 ) ) ;
#23363=DIRECTION ( 'NONE',  ( 1.000000000000000000, 0.000000000000000000, 0.000000000000000000 ) ) ;
#23381=CIRCLE ( 'NONE', #198130, 0.09999999999999939493 ) ;
#23399=CARTESIAN_POINT ( 'NONE',  ( -23.25000000000000000, -9.682403433465239573, -140.6568433774128266 ) ) ;
#23406=EDGE_CURVE ( 'NONE', #70151, #155284, #141641, .T. ) ;
#23416=CARTESIAN_POINT ( 'NONE',  ( 20.85000000000000142, -1.135018845899022466, -141.7169768834323520 ) ) ;
#23430=VERTEX_POINT ( 'NONE', #197552 ) ;
#23434=DIRECTION ( 'NONE',  ( 0.000000000000000000, 0.000000000000000000, 1.000000000000000000 ) ) ;
#23453=CIRCLE ( 'NONE', #31826, 12.77499999999999503 ) ;
#23456=ADVANCED_FACE ( 'NONE', ( #85288 ), #73394, .T. ) ;
#23474=ORIENTED_EDGE ( 'NONE', *, *, #155622, .T. ) ;
#23487=CARTESIAN_POINT ( 'NONE',  ( 18.59999999999999076, 10.20857864377385127, -121.8500000000000369 ) ) ;
#23495=AXIS2_PLACEMENT_3D ( 'NONE', #232023, #151192, #53366 ) ;
#23529=DIRECTION ( 'NONE',  ( -0.000000000000000000, -0.000000000000000000, 1.000000000000000000 ) ) ;
#23536=EDGE_CURVE ( 'NONE', #37861, #186401, #212408, .T. ) ;
#23539=DIRECTION ( 'NONE',  ( 0.000000000000000000, -0.1350103645451904977, -0.9908441862701596881 ) ) ;
#23545=AXIS2_PLACEMENT_3D ( 'NONE', #14980, #54083, #252274 ) ;
#23548=LINE ( 'NONE', #171706, #76741 ) ;
#23572=DIRECTION ( 'NONE',  ( 1.000000000000000000, 0.000000000000000000, 0.000000000000000000 ) ) ;
#23608=EDGE_CURVE ( 'NONE', #234652, #245055, #116531, .T. ) ;
#23671=DIRECTION ( 'NONE',  ( -0.000000000000000000, -0.1350103645451904977, 0.9908441862701596881 ) ) ;
#23672=DIRECTION ( 'NONE',  ( 1.000000000000000000, -0.000000000000000000, -0.000000000000000000 ) ) ;
#23723=VERTEX_POINT ( 'NONE', #102945 ) ;
#23731=FACE_OUTER_BOUND ( 'NONE', #93064, .T. ) ;
#23757=DIRECTION ( 'NONE',  ( -1.000000000000000000, 0.000000000000000000, 0.000000000000000000 ) ) ;
#23793=EDGE_LOOP ( 'NONE', ( #192427, #103359, #38538, #255459 ) ) ;
#23854=AXIS2_PLACEMENT_3D ( 'NONE', #217575, #158938, #119807 ) ;
#23856=EDGE_CURVE ( 'NONE', #217484, #167927, #175201, .T. ) ;
#23857=ORIENTED_EDGE ( 'NONE', *, *, #207576, .T. ) ;
#23891=ADVANCED_FACE ( 'NONE', ( #225807 ), #86295, .T. ) ;
#23897=ORIENTED_EDGE ( 'NONE', *, *, #235188, .F. ) ;
#23954=DIRECTION ( 'NONE',  ( 0.000000000000000000, 0.000000000000000000, -1.000000000000000000 ) ) ;
#23956=LINE ( 'NONE', #142576, #2795 ) ;
#23963=FACE_OUTER_BOUND ( 'NONE', #125830, .T. ) ;
#23974=EDGE_CURVE ( 'NONE', #25027, #50700, #33547, .T. ) ;
#24080=CARTESIAN_POINT ( 'NONE',  ( -21.07928932188134041, 6.328516656409859387, -100.4011048543454052 ) ) ;
#24091=DIRECTION ( 'NONE',  ( 1.000000000000000000, 0.000000000000000000, 0.000000000000000000 ) ) ;
#24134=CARTESIAN_POINT ( 'NONE',  ( -23.15000000000000213, 1.115600667400684642E-11, -134.0000000000000284 ) ) ;
#24138=ORIENTED_EDGE ( 'NONE', *, *, #104441, .T. ) ;
#24151=CYLINDRICAL_SURFACE ( 'NONE', #113123, 0.09999999999999939493 ) ;
#24172=ORIENTED_EDGE ( 'NONE', *, *, #100580, .F. ) ;
#24179=EDGE_CURVE ( 'NONE', #113797, #235011, #125277, .T. ) ;
#24198=VERTEX_POINT ( 'NONE', #254361 ) ;
#24204=VECTOR ( 'NONE', #81302, 1000.000000000000000 ) ;
#24208=VECTOR ( 'NONE', #64109, 1000.000000000000000 ) ;
#24212=DIRECTION ( 'NONE',  ( 1.000000000000000000, -0.000000000000000000, -0.000000000000000000 ) ) ;
#24220=CARTESIAN_POINT ( 'NONE',  ( 21.05000000000000071, 10.48459288120601229, -107.9567135705844265 ) ) ;
#24228=AXIS2_PLACEMENT_3D ( 'NONE', #233876, #209168, #30561 ) ;
#24253=CARTESIAN_POINT ( 'NONE',  ( 19.90621891164687440, 11.75000000001116263, -125.3284452778770373 ) ) ;
#24266=AXIS2_PLACEMENT_3D ( 'NONE', #138487, #116399, #218028 ) ;
#24278=FACE_OUTER_BOUND ( 'NONE', #113620, .T. ) ;
#24347=DIRECTION ( 'NONE',  ( 0.000000000000000000, 1.897661533703519897E-16, -1.000000000000000000 ) ) ;
#24352=DIRECTION ( 'NONE',  ( 1.000000000000000000, 0.000000000000000000, 0.000000000000000000 ) ) ;
#24356=EDGE_LOOP ( 'NONE', ( #41788, #67222, #19848, #182333 ) ) ;
#24424=DIRECTION ( 'NONE',  ( 0.000000000000000000, 0.000000000000000000, -1.000000000000000000 ) ) ;
#24453=ORIENTED_EDGE ( 'NONE', *, *, #240644, .F. ) ;
#24507=TOROIDAL_SURFACE ( 'NONE', #149413, 6.258578643762712446, 0.1000000000000000056 ) ;
#24517=AXIS2_PLACEMENT_3D ( 'NONE', #215731, #239167, #180482 ) ;
#24530=AXIS2_PLACEMENT_3D ( 'NONE', #213616, #35028, #31180 ) ;
#24596=AXIS2_PLACEMENT_3D ( 'NONE', #197127, #257059, #78460 ) ;
#24605=CIRCLE ( 'NONE', #216100, 0.09999999999998898659 ) ;
#24638=CARTESIAN_POINT ( 'NONE',  ( 23.14999999999999503, 6.450000000011156587, -121.6500000000000341 ) ) ;
#24639=EDGE_CURVE ( 'NONE', #241144, #176862, #125458, .T. ) ;
#24654=FACE_OUTER_BOUND ( 'NONE', #17220, .T. ) ;
#24670=CARTESIAN_POINT ( 'NONE',  ( -23.25000000000000000, 11.75000000001115552, -88.75000000000004263 ) ) ;
#24685=ORIENTED_EDGE ( 'NONE', *, *, #39610, .T. ) ;
#24686=CARTESIAN_POINT ( 'NONE',  ( -20.94999999999999929, -1.162701749926853712, -108.5000000000000426 ) ) ;
#24703=DIRECTION ( 'NONE',  ( 0.000000000000000000, 0.000000000000000000, 1.000000000000000000 ) ) ;
#24705=TOROIDAL_SURFACE ( 'NONE', #224398, 11.65000000000000036, 0.1000000000000000056 ) ;
#24709=CIRCLE ( 'NONE', #57966, 0.09999999999999939493 ) ;
#24714=ORIENTED_EDGE ( 'NONE', *, *, #6404, .F. ) ;
#24727=AXIS2_PLACEMENT_3D ( 'NONE', #179860, #177312, #218959 ) ;
#24758=LINE ( 'NONE', #6437, #53332 ) ;
#24760=CARTESIAN_POINT ( 'NONE',  ( -21.05000000000000071, 1.162701749949165642, -108.5000000000000426 ) ) ;
#24795=ORIENTED_EDGE ( 'NONE', *, *, #39886, .T. ) ;
#24800=ORIENTED_EDGE ( 'NONE', *, *, #110919, .T. ) ;
#24802=AXIS2_PLACEMENT_3D ( 'NONE', #20535, #255218, #156203 ) ;
#24828=AXIS2_PLACEMENT_3D ( 'NONE', #164276, #207258, #202110 ) ;
#24849=ORIENTED_EDGE ( 'NONE', *, *, #184261, .T. ) ;
#24871=VERTEX_POINT ( 'NONE', #107836 ) ;
#24881=CARTESIAN_POINT ( 'NONE',  ( 18.48536876927967754, -9.463527249856181101, -107.5486182650831495 ) ) ;
#24891=EDGE_CURVE ( 'NONE', #2430, #159306, #34628, .T. ) ;
#24908=AXIS2_PLACEMENT_3D ( 'NONE', #145320, #185750, #144034 ) ;
#24921=VERTEX_POINT ( 'NONE', #148245 ) ;
#24945=DIRECTION ( 'NONE',  ( 0.7071067811865475727, -0.7071067811865475727, 0.000000000000000000 ) ) ;
#24958=CIRCLE ( 'NONE', #108708, 0.2000000000000057288 ) ;
#24963=ADVANCED_FACE ( 'NONE', ( #118105 ), #18032, .F. ) ;
#25027=VERTEX_POINT ( 'NONE', #213339 ) ;
#25052=AXIS2_PLACEMENT_3D ( 'NONE', #53926, #210450, #190904 ) ;
#25139=EDGE_CURVE ( 'NONE', #109188, #253865, #42282, .T. ) ;
#25167=CIRCLE ( 'NONE', #229345, 0.1000000000000028644 ) ;
#25199=AXIS2_PLACEMENT_3D ( 'NONE', #47915, #164035, #46621 ) ;
#25202=CARTESIAN_POINT ( 'NONE',  ( 23.14999999999999858, 2.100000000011158274, -134.0000000000000284 ) ) ;
#25253=ORIENTED_EDGE ( 'NONE', *, *, #32517, .T. ) ;
#25271=DIRECTION ( 'NONE',  ( 0.000000000000000000, 1.000000000000000000, -0.000000000000000000 ) ) ;
#25307=ORIENTED_EDGE ( 'NONE', *, *, #238884, .F. ) ;
#25381=DIRECTION ( 'NONE',  ( 0.000000000000000000, 0.000000000000000000, -1.000000000000000000 ) ) ;
#25404=CARTESIAN_POINT ( 'NONE',  ( -18.46946985241266859, -9.509317228700410851, -107.4866625654996852 ) ) ;
#25405=DIRECTION ( 'NONE',  ( 1.000000000000000000, 1.836970198721029934E-16, 0.000000000000000000 ) ) ;
#25406=ORIENTED_EDGE ( 'NONE', *, *, #213135, .F. ) ;
#25408=CIRCLE ( 'NONE', #58681, 0.1000000000000028644 ) ;
#25414=DIRECTION ( 'NONE',  ( 0.000000000000000000, 0.000000000000000000, -1.000000000000000000 ) ) ;
#25419=EDGE_CURVE ( 'NONE', #85377, #143803, #244554, .T. ) ;
#25435=ORIENTED_EDGE ( 'NONE', *, *, #66318, .T. ) ;
#25440=ORIENTED_EDGE ( 'NONE', *, *, #218853, .T. ) ;
#25465=CIRCLE ( 'NONE', #121361, 0.1000000000000028644 ) ;
#25474=EDGE_LOOP ( 'NONE', ( #220724, #120115, #32362, #245121 ) ) ;
#25510=EDGE_CURVE ( 'NONE', #160408, #85652, #106480, .T. ) ;
#25529=LINE ( 'NONE', #158638, #204106 ) ;
#25543=DIRECTION ( 'NONE',  ( -1.000000000000000000, 0.000000000000000000, 0.000000000000000000 ) ) ;
#25553=DIRECTION ( 'NONE',  ( -1.000000000000000000, 0.000000000000000000, 0.000000000000000000 ) ) ;
#25563=VERTEX_POINT ( 'NONE', #135037 ) ;
#25613=DIRECTION ( 'NONE',  ( 1.000000000000000000, -0.000000000000000000, -0.000000000000000000 ) ) ;
#25631=DIRECTION ( 'NONE',  ( -5.603264701231743991E-32, 1.897661533703519897E-16, -1.000000000000000000 ) ) ;
#25695=DIRECTION ( 'NONE',  ( 1.000000000000000000, 0.000000000000000000, 0.000000000000000000 ) ) ;
#25696=DIRECTION ( 'NONE',  ( -1.000000000000000000, 0.000000000000000000, 0.000000000000000000 ) ) ;
#25727=CARTESIAN_POINT ( 'NONE',  ( -20.54999999999999716, -8.999999999988844479, -124.1060308773475924 ) ) ;
#25735=ORIENTED_EDGE ( 'NONE', *, *, #215812, .T. ) ;
#25739=AXIS2_PLACEMENT_3D ( 'NONE', #95733, #76174, #114018 ) ;
#25743=CARTESIAN_POINT ( 'NONE',  ( -18.50000000000000000, 9.350000000011156942, -112.6500000000000341 ) ) ;
#25787=FACE_OUTER_BOUND ( 'NONE', #247418, .T. ) ;
#25814=CARTESIAN_POINT ( 'NONE',  ( -18.50000000000000000, 5.950000000011100632, -110.8057023050348988 ) ) ;
#25856=ORIENTED_EDGE ( 'NONE', *, *, #194515, .F. ) ;
#25867=DIRECTION ( 'NONE',  ( 1.000000000000000000, 0.000000000000000000, 0.000000000000000000 ) ) ;
#25869=CARTESIAN_POINT ( 'NONE',  ( -20.64999999999999858, -8.999999999988844479, -124.1060308773475924 ) ) ;
#25930=FACE_OUTER_BOUND ( 'NONE', #64146, .T. ) ;
#25942=AXIS2_PLACEMENT_3D ( 'NONE', #123696, #85800, #4993 ) ;
#25970=AXIS2_PLACEMENT_3D ( 'NONE', #81099, #22451, #240206 ) ;
#26013=ORIENTED_EDGE ( 'NONE', *, *, #142777, .T. ) ;
#26021=AXIS2_PLACEMENT_3D ( 'NONE', #59572, #139107, #218667 ) ;
#26046=DIRECTION ( 'NONE',  ( 0.000000000000000000, -0.1350103645451876944, -0.9908441862701601321 ) ) ;
#26109=VERTEX_POINT ( 'NONE', #81066 ) ;
#26151=CARTESIAN_POINT ( 'NONE',  ( 18.47073956224755875, -9.471729412460639708, -107.6086857528181753 ) ) ;
#26161=ADVANCED_FACE ( 'NONE', ( #51889 ), #32387, .F. ) ;
#26165=ORIENTED_EDGE ( 'NONE', *, *, #235985, .T. ) ;
#26180=DIRECTION ( 'NONE',  ( 0.000000000000000000, 0.000000000000000000, 1.000000000000000000 ) ) ;
#26182=AXIS2_PLACEMENT_3D ( 'NONE', #72214, #34383, #214279 ) ;
#26260=ORIENTED_EDGE ( 'NONE', *, *, #29561, .T. ) ;
#26271=CARTESIAN_POINT ( 'NONE',  ( 21.05000000000000071, 5.400000000011154988, -124.1060308773475924 ) ) ;
#26288=CARTESIAN_POINT ( 'NONE',  ( -21.05000000000000071, 1.835341550235567887, -112.0551512925630249 ) ) ;
#26291=CARTESIAN_POINT ( 'NONE',  ( -23.15000000000000213, 1.115600667400684642E-11, -113.2750000000000341 ) ) ;
#26300=LINE ( 'NONE', #66706, #30567 ) ;
#26317=AXIS2_PLACEMENT_3D ( 'NONE', #104831, #22798, #102264 ) ;
#26323=ORIENTED_EDGE ( 'NONE', *, *, #7762, .T. ) ;
#26335=TOROIDAL_SURFACE ( 'NONE', #42900, 0.2000000000000000111, 0.1000000000000000056 ) ;
#26337=VECTOR ( 'NONE', #87608, 1000.000000000000000 ) ;
#26340=DIRECTION ( 'NONE',  ( -0.7071067811865475727, -0.7071067811865475727, 0.000000000000000000 ) ) ;
#26343=ADVANCED_FACE ( 'NONE', ( #235670 ), #234388, .F. ) ;
#26361=DIRECTION ( 'NONE',  ( -1.000000000000000000, 0.000000000000000000, 0.000000000000000000 ) ) ;
#26397=FACE_OUTER_BOUND ( 'NONE', #131974, .T. ) ;
#26411=VERTEX_POINT ( 'NONE', #142972 ) ;
#26443=ORIENTED_EDGE ( 'NONE', *, *, #221047, .F. ) ;
#26447=TOROIDAL_SURFACE ( 'NONE', #168137, 2.100000000000002309, 0.1000000000000000056 ) ;
#26470=ORIENTED_EDGE ( 'NONE', *, *, #98361, .F. ) ;
#26473=DIRECTION ( 'NONE',  ( 1.000000000000000000, -0.000000000000000000, 0.000000000000000000 ) ) ;
#26484=AXIS2_PLACEMENT_3D ( 'NONE', #249881, #126062, #106485 ) ;
#26501=AXIS2_PLACEMENT_3D ( 'NONE', #135975, #233821, #133431 ) ;
#26524=FACE_OUTER_BOUND ( 'NONE', #104992, .T. ) ;
#26550=DIRECTION ( 'NONE',  ( 0.000000000000000000, 0.3738317757009345654, 0.9274965247785492695 ) ) ;
#26572=CARTESIAN_POINT ( 'NONE',  ( -21.44999999999999929, 7.350000000011155166, -112.7500000000000284 ) ) ;
#26617=ADVANCED_FACE ( 'NONE', ( #97105 ), #209939, .F. ) ;
#26619=ORIENTED_EDGE ( 'NONE', *, *, #92914, .F. ) ;
#26627=CYLINDRICAL_SURFACE ( 'NONE', #183009, 0.09999999999999939493 ) ;
#26636=DIRECTION ( 'NONE',  ( -0.000000000000000000, -0.000000000000000000, 1.000000000000000000 ) ) ;
#26647=VERTEX_POINT ( 'NONE', #80106 ) ;
#26672=VECTOR ( 'NONE', #209686, 1000.000000000000000 ) ;
#26680=CARTESIAN_POINT ( 'NONE',  ( 21.05000000000000071, -8.999999999988842703, -124.1060308773475924 ) ) ;
#26728=CIRCLE ( 'NONE', #1747, 0.09999999999999939493 ) ;
#26746=LINE ( 'NONE', #245775, #4624 ) ;
#26756=EDGE_CURVE ( 'NONE', #216892, #250368, #193187, .T. ) ;
#26758=DIRECTION ( 'NONE',  ( 0.000000000000000000, 0.000000000000000000, -1.000000000000000000 ) ) ;
#26763=DIRECTION ( 'NONE',  ( 0.000000000000000000, -0.6728971962616697722, -0.7397360091702875895 ) ) ;
#26764=CARTESIAN_POINT ( 'NONE',  ( -23.15000000000000213, 4.150000000011156764, -88.75000000000004263 ) ) ;
#26788=ADVANCED_FACE ( 'NONE', ( #27918 ), #80724, .T. ) ;
#26798=CARTESIAN_POINT ( 'NONE',  ( 21.05000000000000071, 8.776282895303632259, -109.0586289951409924 ) ) ;
#26823=CARTESIAN_POINT ( 'NONE',  ( 23.24999999999997513, 11.65000000001116298, -126.9851942293460922 ) ) ;
#26856=CARTESIAN_POINT ( 'NONE',  ( -22.47007471830798764, 7.720710651937634061, -100.5000000000000426 ) ) ;
#26889=VECTOR ( 'NONE', #235669, 1000.000000000000000 ) ;
#26927=AXIS2_PLACEMENT_3D ( 'NONE', #188302, #107483, #187052 ) ;
#26938=CARTESIAN_POINT ( 'NONE',  ( 20.94999999999999929, 10.29270135741298731, -139.4573618871519614 ) ) ;
#26939=EDGE_CURVE ( 'NONE', #173551, #9426, #239146, .T. ) ;
#26943=CIRCLE ( 'NONE', #6052, 0.1000000000000028644 ) ;
#26961=CARTESIAN_POINT ( 'NONE',  ( 21.46681500597533798, 1.115541036281197940E-11, -93.64248884056873123 ) ) ;
#26997=EDGE_CURVE ( 'NONE', #90910, #257108, #77268, .T. ) ;
#27007=VERTEX_POINT ( 'NONE', #34335 ) ;
#27069=CARTESIAN_POINT ( 'NONE',  ( -18.44232395689893877, -9.552282557039065480, -140.8422519848076888 ) ) ;
#27119=FACE_OUTER_BOUND ( 'NONE', #66142, .T. ) ;
#27131=CARTESIAN_POINT ( 'NONE',  ( 18.55857864376267941, 10.36715728753653565, -125.2500000000000284 ) ) ;
#27138=ORIENTED_EDGE ( 'NONE', *, *, #102861, .T. ) ;
#27183=ORIENTED_EDGE ( 'NONE', *, *, #32302, .F. ) ;
#27184=VERTEX_POINT ( 'NONE', #104513 ) ;
#27207=EDGE_LOOP ( 'NONE', ( #213639, #76160, #254074, #12217 ) ) ;
#27227=AXIS2_PLACEMENT_3D ( 'NONE', #11799, #135551, #152598 ) ;
#27241=CARTESIAN_POINT ( 'NONE',  ( -23.15000000000000213, -9.499999999988848032, -110.3939691226524786 ) ) ;
#27261=AXIS2_PLACEMENT_3D ( 'NONE', #109048, #12551, #216826 ) ;
#27270=DIRECTION ( 'NONE',  ( 1.000000000000000000, 0.000000000000000000, 0.000000000000000000 ) ) ;
#27275=CARTESIAN_POINT ( 'NONE',  ( 18.50000000000000000, -9.399999999988843058, -140.8820418481727188 ) ) ;
#27291=DIRECTION ( 'NONE',  ( 0.000000000000000000, 0.000000000000000000, 1.000000000000000000 ) ) ;
#27298=EDGE_CURVE ( 'NONE', #8107, #224679, #22869, .T. ) ;
#27317=EDGE_CURVE ( 'NONE', #53973, #105004, #122823, .T. ) ;
#27325=ADVANCED_FACE ( 'NONE', ( #8028 ), #109665, .T. ) ;
#27349=EDGE_LOOP ( 'NONE', ( #42808, #174363, #196948, #176358 ) ) ;
#27367=CARTESIAN_POINT ( 'NONE',  ( 18.59999999999999076, 1.250000000011167511, -108.5000000000000426 ) ) ;
#27372=CIRCLE ( 'NONE', #214756, 0.09999999999999939493 ) ;
#27401=ORIENTED_EDGE ( 'NONE', *, *, #57928, .F. ) ;
#27403=EDGE_LOOP ( 'NONE', ( #121604, #251272, #180042, #43087, #13009 ) ) ;
#27413=( BOUNDED_SURFACE ( )  B_SPLINE_SURFACE ( 3, 2, ( 
 ( #159072, #143325, #160363 ),
 ( #118661, #61228, #142041 ),
 ( #161640, #221558, #196881 ),
 ( #239879, #177362, #83324 ),
 ( #119954, #138176, #18254 ),
 ( #3822, #241165, #121248 ) ),
 .UNSPECIFIED., .F., .F., .F. ) 
 B_SPLINE_SURFACE_WITH_KNOTS ( ( 4, 2, 4 ),
 ( 3, 3 ),
 ( 3.141592653589793116, 3.926990816987241395, 4.712388980384689674 ),
 ( 0.000000000000000000, 1.000000000000000000 ),
 .UNSPECIFIED. ) 
 GEOMETRIC_REPRESENTATION_ITEM ( )  RATIONAL_B_SPLINE_SURFACE ( (
 ( 1.000000000000000000, 0.9238795325112820755, 1.000000000000000000),
 ( 1.000000000000000000, 0.9240297172239489987, 1.000000000000000000),
 ( 1.000000000000000000, 0.9038128468044698272, 1.000000000000000000),
 ( 1.000000000000000000, 0.8282379607644166919, 1.000000000000000000),
 ( 1.000000000000000000, 0.7727932973495217350, 1.000000000000000000),
 ( 1.000000000000000000, 0.7071067811865475727, 1.000000000000000000) ) ) 
 REPRESENTATION_ITEM ( '' )  SURFACE ( )  );
#27425=DIRECTION ( 'NONE',  ( -1.000000000000000000, -0.000000000000000000, -0.000000000000000000 ) ) ;
#27446=AXIS2_PLACEMENT_3D ( 'NONE', #142429, #160750, #22511 ) ;
#27452=EDGE_CURVE ( 'NONE', #219174, #200879, #133101, .T. ) ;
#27501=VECTOR ( 'NONE', #230037, 999.9999999999998863 ) ;
#27512=DIRECTION ( 'NONE',  ( 0.000000000000000000, -1.000000000000000000, 0.000000000000000000 ) ) ;
#27546=CARTESIAN_POINT ( 'NONE',  ( 21.95218792049437795, 7.201507561257818324, -100.4009715602001194 ) ) ;
#27555=CARTESIAN_POINT ( 'NONE',  ( -21.04999999999999716, -0.08574093702224511171, -94.08617371118702977 ) ) ;
#27558=VERTEX_POINT ( 'NONE', #88155 ) ;
#27567=DIRECTION ( 'NONE',  ( 1.000000000000000000, -0.000000000000000000, -0.000000000000000000 ) ) ;
#27601=ORIENTED_EDGE ( 'NONE', *, *, #69175, .F. ) ;
#27610=CARTESIAN_POINT ( 'NONE',  ( -20.64999999999999858, 7.250000000011155521, -112.7500000000000284 ) ) ;
#27614=CARTESIAN_POINT ( 'NONE',  ( 21.05000000000000071, 11.65000000001116298, -126.9851942293460922 ) ) ;
#27628=CARTESIAN_POINT ( 'NONE',  ( -21.14999999999999858, 11.65000000001115588, -100.6000000000000369 ) ) ;
#27671=VECTOR ( 'NONE', #50516, 1000.000000000000000 ) ;
#27775=EDGE_CURVE ( 'NONE', #5506, #219593, #168819, .T. ) ;
#27798=ADVANCED_FACE ( 'NONE', ( #4487 ), #240548, .F. ) ;
#27819=FACE_OUTER_BOUND ( 'NONE', #237072, .T. ) ;
#27911=VECTOR ( 'NONE', #201033, 1000.000000000000000 ) ;
#27916=ORIENTED_EDGE ( 'NONE', *, *, #150576, .F. ) ;
#27918=FACE_OUTER_BOUND ( 'NONE', #215240, .T. ) ;
#27920=EDGE_CURVE ( 'NONE', #52329, #106008, #73137, .T. ) ;
#27954=DIRECTION ( 'NONE',  ( -0.9880948137434723000, 0.1538461538461483591, -0.000000000000000000 ) ) ;
#27964=EDGE_LOOP ( 'NONE', ( #43749, #8695, #202720, #83736 ) ) ;
#27973=AXIS2_PLACEMENT_3D ( 'NONE', #131276, #32204, #111719 ) ;
#27990=FACE_OUTER_BOUND ( 'NONE', #70536, .T. ) ;
#27998=CARTESIAN_POINT ( 'NONE',  ( -20.85000000000000142, 1.115600667400684642E-11, -134.0000000000000284 ) ) ;
#28017=CIRCLE ( 'NONE', #119593, 0.2000000000000057288 ) ;
#28041=VERTEX_POINT ( 'NONE', #135984 ) ;
#28064=CARTESIAN_POINT ( 'NONE',  ( -20.94999999999999929, -1.249999999988843369, -108.5000000000000426 ) ) ;
#28066=AXIS2_PLACEMENT_3D ( 'NONE', #186263, #217971, #67587 ) ;
#28083=CARTESIAN_POINT ( 'NONE',  ( 20.95512820512820085, 10.62384868372303615, -108.1649135690876449 ) ) ;
#28086=EDGE_CURVE ( 'NONE', #64377, #76616, #153045, .T. ) ;
#28106=CARTESIAN_POINT ( 'NONE',  ( 21.22070241538126467, 0.09891903054618129965, -94.03005372713040799 ) ) ;
#28114=ADVANCED_FACE ( 'NONE', ( #176440 ), #19108, .T. ) ;
#28121=DIRECTION ( 'NONE',  ( 0.000000000000000000, -0.1350103645451904977, 0.9908441862701596881 ) ) ;
#28158=CARTESIAN_POINT ( 'NONE',  ( 21.05000000000000071, -11.29603075032412640, -130.9521008403361861 ) ) ;
#28167=ORIENTED_EDGE ( 'NONE', *, *, #100327, .T. ) ;
#28175=VECTOR ( 'NONE', #251630, 1000.000000000000000 ) ;
#28190=DIRECTION ( 'NONE',  ( 1.000000000000000000, -0.000000000000000000, -0.000000000000000000 ) ) ;
#28195=DIRECTION ( 'NONE',  ( 1.000000000000000000, 3.265361837132813093E-16, -0.000000000000000000 ) ) ;
#28210=CARTESIAN_POINT ( 'NONE',  ( -20.64999999999999858, 7.250000000011155521, -112.8500000000000369 ) ) ;
#28214=CIRCLE ( 'NONE', #161466, 0.1000000000000000472 ) ;
#28248=CARTESIAN_POINT ( 'NONE',  ( 21.07094088545368393, 0.09889370256337753906, -94.17983277808291120 ) ) ;
#28253=TOROIDAL_SURFACE ( 'NONE', #15786, 11.90000000000000391, 0.1000000000000000056 ) ;
#28312=EDGE_LOOP ( 'NONE', ( #115394, #123553, #75543, #164624 ) ) ;
#28316=CIRCLE ( 'NONE', #144787, 0.1000000000000028644 ) ;
#28333=CARTESIAN_POINT ( 'NONE',  ( 20.95429402530545815, 8.876194151113343977, -109.0230866979378703 ) ) ;
#28334=CARTESIAN_POINT ( 'NONE',  ( -21.14999999999999858, 11.75000000001115552, -100.6000000000000369 ) ) ;
#28339=CARTESIAN_POINT ( 'NONE',  ( -21.05000000000000071, 1.736257131608553550, -112.0686523290175245 ) ) ;
#28350=AXIS2_PLACEMENT_3D ( 'NONE', #195416, #235788, #58413 ) ;
#28351=DIRECTION ( 'NONE',  ( 1.000000000000000000, 0.000000000000000000, 0.000000000000000000 ) ) ;
#28359=CARTESIAN_POINT ( 'NONE',  ( 18.50000324121758055, 10.29307482169091692, -139.4586421466940180 ) ) ;
#28373=AXIS2_PLACEMENT_3D ( 'NONE', #217312, #196477, #98627 ) ;
#28374=EDGE_CURVE ( 'NONE', #37339, #188850, #13195, .T. ) ;
#28381=VERTEX_POINT ( 'NONE', #233529 ) ;
#28405=LINE ( 'NONE', #188715, #254829 ) ;
#28407=ORIENTED_EDGE ( 'NONE', *, *, #223415, .T. ) ;
#28419=ORIENTED_EDGE ( 'NONE', *, *, #195233, .F. ) ;
#28445=ORIENTED_EDGE ( 'NONE', *, *, #113747, .T. ) ;
#28449=DIRECTION ( 'NONE',  ( 1.000000000000000000, 0.000000000000000000, 0.000000000000000000 ) ) ;
#28479=CARTESIAN_POINT ( 'NONE',  ( -23.25000000000000000, 5.950000000011167245, -123.6942976949652149 ) ) ;
#28496=DIRECTION ( 'NONE',  ( 0.000000000000000000, 0.1350103645451876666, 0.9908441862701600211 ) ) ;
#28525=ORIENTED_EDGE ( 'NONE', *, *, #223054, .F. ) ;
#28550=VECTOR ( 'NONE', #68715, 1000.000000000000000 ) ;
#28566=ORIENTED_EDGE ( 'NONE', *, *, #84449, .F. ) ;
#28582=DIRECTION ( 'NONE',  ( 0.000000000000000000, 0.000000000000000000, -1.000000000000000000 ) ) ;
#28594=CIRCLE ( 'NONE', #174327, 0.2000000000000057288 ) ;
#28607=CARTESIAN_POINT ( 'NONE',  ( 21.14999999999999503, 11.75000000001115552, -100.5000000000000284 ) ) ;
#28625=EDGE_CURVE ( 'NONE', #223382, #247168, #77524, .T. ) ;
#28643=AXIS2_PLACEMENT_3D ( 'NONE', #195645, #54809, #153979 ) ;
#28658=CARTESIAN_POINT ( 'NONE',  ( -22.39999999999999858, 1.115600667400684642E-11, -88.85042919245522341 ) ) ;
#28682=EDGE_LOOP ( 'NONE', ( #118973, #195369, #200109, #248051 ) ) ;
#28692=CIRCLE ( 'NONE', #124505, 2.000000000000001776 ) ;
#28705=DIRECTION ( 'NONE',  ( -1.000000000000000000, 0.000000000000000000, 0.000000000000000000 ) ) ;
#28722=AXIS2_PLACEMENT_3D ( 'NONE', #75970, #79789, #155541 ) ;
#28750=ORIENTED_EDGE ( 'NONE', *, *, #165988, .F. ) ;
#28755=CARTESIAN_POINT ( 'NONE',  ( 21.14999999999999858, 6.650000000011155876, -112.8500000000000369 ) ) ;
#28776=CARTESIAN_POINT ( 'NONE',  ( 21.10710606213542206, 8.776894023904366904, -112.7409965263994565 ) ) ;
#28810=EDGE_CURVE ( 'NONE', #80843, #156398, #115167, .T. ) ;
#28813=VERTEX_POINT ( 'NONE', #38532 ) ;
#28824=EDGE_CURVE ( 'NONE', #234572, #94985, #145318, .T. ) ;
#28830=AXIS2_PLACEMENT_3D ( 'NONE', #137122, #233662, #214088 ) ;
#28848=ORIENTED_EDGE ( 'NONE', *, *, #169483, .T. ) ;
#28883=CIRCLE ( 'NONE', #241235, 0.1000000000000028644 ) ;
#28891=ORIENTED_EDGE ( 'NONE', *, *, #172474, .F. ) ;
#28898=EDGE_LOOP ( 'NONE', ( #10883, #69102, #185220, #136669 ) ) ;
#28904=AXIS2_PLACEMENT_3D ( 'NONE', #60186, #23671, #65327 ) ;
#28908=EDGE_LOOP ( 'NONE', ( #37303, #51139, #223001, #247615 ) ) ;
#28913=DIRECTION ( 'NONE',  ( 0.000000000000000000, 0.9876197685951252359, -0.1568667991644863424 ) ) ;
#28925=CARTESIAN_POINT ( 'NONE',  ( -20.85000000000000142, 11.75000000001115197, -127.1583993101029790 ) ) ;
#28932=CARTESIAN_POINT ( 'NONE',  ( -20.15000000000000568, 9.291421356248463326, -121.7500000000000426 ) ) ;
#28933=ORIENTED_EDGE ( 'NONE', *, *, #132373, .T. ) ;
#28951=ORIENTED_EDGE ( 'NONE', *, *, #108045, .F. ) ;
#28956=ORIENTED_EDGE ( 'NONE', *, *, #205647, .T. ) ;
#29003=DIRECTION ( 'NONE',  ( -0.000000000000000000, 0.000000000000000000, -1.000000000000000000 ) ) ;
#29006=ORIENTED_EDGE ( 'NONE', *, *, #85586, .F. ) ;
#29037=DIRECTION ( 'NONE',  ( 0.000000000000000000, 0.000000000000000000, -1.000000000000000000 ) ) ;
#29090=AXIS2_PLACEMENT_3D ( 'NONE', #41273, #16559, #136463 ) ;
#29095=CARTESIAN_POINT ( 'NONE',  ( 23.24999999999999645, 5.000000000011153745, -112.9052660189131245 ) ) ;
#29238=AXIS2_PLACEMENT_3D ( 'NONE', #190098, #170586, #28496 ) ;
#29278=DIRECTION ( 'NONE',  ( 1.000000000000000000, 0.000000000000000000, 0.000000000000000000 ) ) ;
#29294=ORIENTED_EDGE ( 'NONE', *, *, #124729, .T. ) ;
#29308=ORIENTED_EDGE ( 'NONE', *, *, #24639, .F. ) ;
#29361=CARTESIAN_POINT ( 'NONE',  ( 20.94999999999999929, -8.999999999988844479, -110.3939691226524786 ) ) ;
#29366=ORIENTED_EDGE ( 'NONE', *, *, #258057, .T. ) ;
#29377=EDGE_CURVE ( 'NONE', #135831, #160208, #90386, .T. ) ;
#29380=CARTESIAN_POINT ( 'NONE',  ( 20.95595624212412744, 10.62389120310530544, -108.1296329141269297 ) ) ;
#29387=EDGE_LOOP ( 'NONE', ( #183662, #67204, #175535, #137051 ) ) ;
#29395=CARTESIAN_POINT ( 'NONE',  ( -21.05000000000000071, 14.00000000001115374, -128.5729074696175473 ) ) ;
#29416=FACE_OUTER_BOUND ( 'NONE', #32294, .T. ) ;
#29435=EDGE_CURVE ( 'NONE', #188768, #31301, #82171, .T. ) ;
#29469=ORIENTED_EDGE ( 'NONE', *, *, #44, .T. ) ;
#29483=AXIS2_PLACEMENT_3D ( 'NONE', #119114, #239056, #175267 ) ;
#29494=FACE_OUTER_BOUND ( 'NONE', #166338, .T. ) ;
#29501=CARTESIAN_POINT ( 'NONE',  ( -20.94999999999999929, -1.835859311432479268, -145.5044391687985694 ) ) ;
#29561=EDGE_CURVE ( 'NONE', #215032, #132946, #164066, .T. ) ;
#29600=AXIS2_PLACEMENT_3D ( 'NONE', #65360, #144884, #70535 ) ;
#29610=CARTESIAN_POINT ( 'NONE',  ( 21.05000000000000071, 1.115600667400684642E-11, -134.0000000000000284 ) ) ;
#29611=EDGE_CURVE ( 'NONE', #124696, #20141, #254374, .T. ) ;
#29612=ORIENTED_EDGE ( 'NONE', *, *, #121762, .F. ) ;
#29667=ORIENTED_EDGE ( 'NONE', *, *, #229853, .F. ) ;
#29706=VERTEX_POINT ( 'NONE', #178759 ) ;
#29715=DIRECTION ( 'NONE',  ( 0.000000000000000000, 0.000000000000000000, -1.000000000000000000 ) ) ;
#29734=ORIENTED_EDGE ( 'NONE', *, *, #243354, .F. ) ;
#29768=CIRCLE ( 'NONE', #237825, 0.1000000000000001860 ) ;
#29771=CARTESIAN_POINT ( 'NONE',  ( -21.59142135623730852, 7.850000000011158718, -112.8500000000000369 ) ) ;
#29778=CARTESIAN_POINT ( 'NONE',  ( -22.50000000000000000, 11.65000000001115588, -100.5000000000000284 ) ) ;
#29782=CARTESIAN_POINT ( 'NONE',  ( 20.94999999999999929, -9.399999999988846611, -110.3939691226524786 ) ) ;
#29799=ORIENTED_EDGE ( 'NONE', *, *, #71590, .T. ) ;
#29811=DIRECTION ( 'NONE',  ( 0.000000000000000000, 0.000000000000000000, -1.000000000000000000 ) ) ;
#29824=CARTESIAN_POINT ( 'NONE',  ( -21.05000000000000071, 1.115653327213047955E-11, -96.20000000000007390 ) ) ;
#29829=ORIENTED_EDGE ( 'NONE', *, *, #220723, .F. ) ;
#29834=AXIS2_PLACEMENT_3D ( 'NONE', #163692, #204081, #86686 ) ;
#29837=CARTESIAN_POINT ( 'NONE',  ( -20.54999999999999716, -8.663551401858004652, -110.0241011180673354 ) ) ;
#29862=VECTOR ( 'NONE', #163179, 1000.000000000000000 ) ;
#29918=CARTESIAN_POINT ( 'NONE',  ( 23.14999999999999858, -1.999999999988846699, -134.0000000000000284 ) ) ;
#29939=ORIENTED_EDGE ( 'NONE', *, *, #153006, .T. ) ;
#29980=ORIENTED_EDGE ( 'NONE', *, *, #116315, .F. ) ;
#29992=CARTESIAN_POINT ( 'NONE',  ( -21.55000000000000426, 7.708578643773852157, -121.7500000000000426 ) ) ;
#30004=VECTOR ( 'NONE', #236237, 1000.000000000000000 ) ;
#30018=CARTESIAN_POINT ( 'NONE',  ( -21.45000000000000284, 7.708578643773852157, -112.7500000000000284 ) ) ;
#30039=CARTESIAN_POINT ( 'NONE',  ( 18.43630871534871218, -9.679800874791856913, -140.6606320679840394 ) ) ;
#30054=ORIENTED_EDGE ( 'NONE', *, *, #100706, .F. ) ;
#30063=CARTESIAN_POINT ( 'NONE',  ( -22.49999999999999645, 11.74956712350054744, -100.3991416309013402 ) ) ;
#30105=CARTESIAN_POINT ( 'NONE',  ( -21.05000000000000071, 0.09779029131994770863, -94.24218538952392521 ) ) ;
#30161=CARTESIAN_POINT ( 'NONE',  ( 21.04999999999999716, 6.304455821958816486, -100.5210354765401632 ) ) ;
#30165=EDGE_LOOP ( 'NONE', ( #255883, #219928, #179320, #23474 ) ) ;
#30171=PLANE ( 'NONE',  #168040 ) ;
#30213=ORIENTED_EDGE ( 'NONE', *, *, #31471, .F. ) ;
#30248=LINE ( 'NONE', #188030, #136595 ) ;
#30266=ORIENTED_EDGE ( 'NONE', *, *, #226009, .F. ) ;
#30282=ORIENTED_EDGE ( 'NONE', *, *, #107879, .T. ) ;
#30286=CARTESIAN_POINT ( 'NONE',  ( 18.39999999999999858, -9.499999999988842703, -140.9146583429697159 ) ) ;
#30304=ORIENTED_EDGE ( 'NONE', *, *, #37990, .F. ) ;
#30305=DIRECTION ( 'NONE',  ( -1.000000000000000000, 0.000000000000000000, 0.000000000000000000 ) ) ;
#30316=ADVANCED_FACE ( 'NONE', ( #191268 ), #37316, .T. ) ;
#30361=DIRECTION ( 'NONE',  ( -4.701977403289178058E-30, 1.734723475976807094E-14, -1.000000000000000000 ) ) ;
#30395=CIRCLE ( 'NONE', #142773, 0.5000000000000004441 ) ;
#30405=DIRECTION ( 'NONE',  ( 1.000000000000000000, -0.000000000000000000, -0.000000000000000000 ) ) ;
#30448=CYLINDRICAL_SURFACE ( 'NONE', #36577, 0.1000000000000028644 ) ;
#30452=EDGE_CURVE ( 'NONE', #159714, #210115, #17712, .T. ) ;
#30460=DIRECTION ( 'NONE',  ( -0.000000000000000000, -0.8660254037844411501, -0.4999999999999956701 ) ) ;
#30490=CIRCLE ( 'NONE', #205235, 12.87499999999999822 ) ;
#30496=LINE ( 'NONE', #87852, #230901 ) ;
#30504=CIRCLE ( 'NONE', #176250, 11.69999999999998863 ) ;
#30531=EDGE_CURVE ( 'NONE', #20260, #64097, #118656, .T. ) ;
#30533=DIRECTION ( 'NONE',  ( 1.000000000000000000, 0.000000000000000000, 0.000000000000000000 ) ) ;
#30534=DIRECTION ( 'NONE',  ( 0.000000000000000000, 0.000000000000000000, -1.000000000000000000 ) ) ;
#30536=ORIENTED_EDGE ( 'NONE', *, *, #127293, .F. ) ;
#30561=DIRECTION ( 'NONE',  ( 0.000000000000000000, -0.9915357197604972583, 0.1298341882519109536 ) ) ;
#30562=ORIENTED_EDGE ( 'NONE', *, *, #249441, .F. ) ;
#30567=VECTOR ( 'NONE', #23757, 1000.000000000000000 ) ;
#30575=ORIENTED_EDGE ( 'NONE', *, *, #218753, .F. ) ;
#30626=AXIS2_PLACEMENT_3D ( 'NONE', #181802, #4433, #43580 ) ;
#30644=CARTESIAN_POINT ( 'NONE',  ( 18.39999999999999858, -9.499999999988842703, -107.5320693966997112 ) ) ;
#30645=CARTESIAN_POINT ( 'NONE',  ( 21.05000000000000071, 10.47338541492406172, -108.0786544642485580 ) ) ;
#30650=VERTEX_POINT ( 'NONE', #117498 ) ;
#30695=CARTESIAN_POINT ( 'NONE',  ( 22.39999999999999503, 11.75000000001115552, -100.5000000000000284 ) ) ;
#30698=ORIENTED_EDGE ( 'NONE', *, *, #220432, .T. ) ;
#30708=EDGE_CURVE ( 'NONE', #255159, #226146, #34146, .T. ) ;
#30712=CIRCLE ( 'NONE', #80147, 0.1999999999999987899 ) ;
#30717=ORIENTED_EDGE ( 'NONE', *, *, #234814, .F. ) ;
#30758=CIRCLE ( 'NONE', #243111, 0.09999999999999971412 ) ;
#30768=CYLINDRICAL_SURFACE ( 'NONE', #2946, 0.1000000000000028644 ) ;
#30799=CARTESIAN_POINT ( 'NONE',  ( -18.50000000000000000, -9.399999999988850163, -140.9146583429697159 ) ) ;
#30820=EDGE_LOOP ( 'NONE', ( #190188, #14913, #51772, #27183, #242192 ) ) ;
#30844=EDGE_CURVE ( 'NONE', #239256, #46494, #6379, .T. ) ;
#30859=DIRECTION ( 'NONE',  ( -0.000000000000000000, -0.8700118002898321601, 0.4930308989875230030 ) ) ;
#30866=EDGE_CURVE ( 'NONE', #231172, #4043, #239569, .T. ) ;
#30870=TOROIDAL_SURFACE ( 'NONE', #251600, 4.149999999999999467, 0.1000000000000000056 ) ;
#30896=EDGE_CURVE ( 'NONE', #182032, #243821, #35653, .T. ) ;
#30909=CARTESIAN_POINT ( 'NONE',  ( -23.15000000000000213, 2.000000000011154189, -121.3753780772379258 ) ) ;
#30919=VERTEX_POINT ( 'NONE', #36255 ) ;
#30922=CARTESIAN_POINT ( 'NONE',  ( 18.51697539158856998, 10.31565961587946312, -139.5364194119178478 ) ) ;
#30923=ORIENTED_EDGE ( 'NONE', *, *, #72199, .F. ) ;
#30942=AXIS2_PLACEMENT_3D ( 'NONE', #195752, #135738, #237424 ) ;
#30958=CARTESIAN_POINT ( 'NONE',  ( 22.39999999999999503, 11.75000000001115552, -100.4000000000000483 ) ) ;
#30962=DIRECTION ( 'NONE',  ( -1.000000000000000000, 0.000000000000000000, 0.000000000000000000 ) ) ;
#30991=DIRECTION ( 'NONE',  ( 1.000000000000000000, 0.000000000000000000, 0.000000000000000000 ) ) ;
#30997=ORIENTED_EDGE ( 'NONE', *, *, #132529, .F. ) ;
#31014=ORIENTED_EDGE ( 'NONE', *, *, #146766, .T. ) ;
#31024=DIRECTION ( 'NONE',  ( 1.000000000000000000, 0.000000000000000000, 0.000000000000000000 ) ) ;
#31027=ORIENTED_EDGE ( 'NONE', *, *, #115834, .T. ) ;
#31036=CARTESIAN_POINT ( 'NONE',  ( 20.94999999999999929, 1.115600667400684642E-11, -113.3750000000000284 ) ) ;
#31048=ORIENTED_EDGE ( 'NONE', *, *, #126834, .F. ) ;
#31106=CARTESIAN_POINT ( 'NONE',  ( -18.58671080940900566, -9.406932858815460818, -107.6241544649047484 ) ) ;
#31138=VECTOR ( 'NONE', #114597, 1000.000000000000000 ) ;
#31142=EDGE_LOOP ( 'NONE', ( #219803, #246834, #149935, #193703 ) ) ;
#31158=DIRECTION ( 'NONE',  ( 0.000000000000000000, 0.000000000000000000, -1.000000000000000000 ) ) ;
#31180=DIRECTION ( 'NONE',  ( 0.000000000000000000, 0.000000000000000000, -1.000000000000000000 ) ) ;
#31195=AXIS2_PLACEMENT_3D ( 'NONE', #186781, #31576, #250575 ) ;
#31252=DIRECTION ( 'NONE',  ( 1.000000000000000000, 3.265361837132813093E-16, -0.000000000000000000 ) ) ;
#31259=VERTEX_POINT ( 'NONE', #96500 ) ;
#31281=DIRECTION ( 'NONE',  ( 0.000000000000000000, 1.000000000000000000, 0.000000000000000000 ) ) ;
#31290=FACE_OUTER_BOUND ( 'NONE', #52720, .T. ) ;
#31301=VERTEX_POINT ( 'NONE', #216462 ) ;
#31309=CARTESIAN_POINT ( 'NONE',  ( -20.00857864376270001, 9.350000000011156942, -121.7500000000000426 ) ) ;
#31321=VECTOR ( 'NONE', #7278, 1000.000000000000000 ) ;
#31333=CARTESIAN_POINT ( 'NONE',  ( -21.05000000000000426, 6.477046381801003783, -100.6000000000000512 ) ) ;
#31340=CARTESIAN_POINT ( 'NONE',  ( -20.15000000000000568, 9.291421356248463326, -112.8500000000000369 ) ) ;
#31343=DIRECTION ( 'NONE',  ( 0.000000000000000000, 0.000000000000000000, 1.000000000000000000 ) ) ;
#31366=DIRECTION ( 'NONE',  ( 0.000000000000000000, 0.000000000000000000, 1.000000000000000000 ) ) ;
#31371=DIRECTION ( 'NONE',  ( 0.000000000000000000, 0.000000000000000000, -1.000000000000000000 ) ) ;
#31383=EDGE_CURVE ( 'NONE', #25563, #63872, #19034, .T. ) ;
#31429=ORIENTED_EDGE ( 'NONE', *, *, #116822, .F. ) ;
#31434=LINE ( 'NONE', #62518, #81964 ) ;
#31435=CARTESIAN_POINT ( 'NONE',  ( -23.15000000000000213, 11.75000000001115907, -127.1583993101029790 ) ) ;
#31447=LINE ( 'NONE', #113514, #116036 ) ;
#31463=DIRECTION ( 'NONE',  ( -1.000000000000000000, 0.000000000000000000, -0.000000000000000000 ) ) ;
#31471=EDGE_CURVE ( 'NONE', #14418, #129536, #84615, .T. ) ;
#31499=ORIENTED_EDGE ( 'NONE', *, *, #49651, .F. ) ;
#31501=DIRECTION ( 'NONE',  ( 0.000000000000000000, 0.000000000000000000, -1.000000000000000000 ) ) ;
#31504=ORIENTED_EDGE ( 'NONE', *, *, #15751, .T. ) ;
#31511=CARTESIAN_POINT ( 'NONE',  ( -23.25000000000000000, 6.982009704867601307, -137.6961521182563217 ) ) ;
#31541=CIRCLE ( 'NONE', #27446, 0.09999999999998898659 ) ;
#31544=DIRECTION ( 'NONE',  ( 0.000000000000000000, 6.938893903907270030E-14, 1.000000000000000000 ) ) ;
#31558=ORIENTED_EDGE ( 'NONE', *, *, #190035, .T. ) ;
#31576=DIRECTION ( 'NONE',  ( -0.000000000000000000, 0.1350103645451904977, 0.9908441862701597991 ) ) ;
#31638=AXIS2_PLACEMENT_3D ( 'NONE', #197420, #80011, #117880 ) ;
#31649=ADVANCED_FACE ( 'NONE', ( #54515 ), #53242, .T. ) ;
#31652=ORIENTED_EDGE ( 'NONE', *, *, #46954, .F. ) ;
#31690=ORIENTED_EDGE ( 'NONE', *, *, #45837, .F. ) ;
#31692=CARTESIAN_POINT ( 'NONE',  ( 21.00000000000000000, 9.750000000011153745, -112.7500000000000284 ) ) ;
#31702=CIRCLE ( 'NONE', #223196, 0.1000000000000028644 ) ;
#31726=ORIENTED_EDGE ( 'NONE', *, *, #82426, .F. ) ;
#31729=VECTOR ( 'NONE', #58942, 1000.000000000000000 ) ;
#31756=ORIENTED_EDGE ( 'NONE', *, *, #85209, .T. ) ;
#31761=DIRECTION ( 'NONE',  ( -1.000000000000000000, -2.952720810173289112E-16, 0.000000000000000000 ) ) ;
#31823=EDGE_CURVE ( 'NONE', #173790, #239952, #190250, .T. ) ;
#31825=CARTESIAN_POINT ( 'NONE',  ( 21.14999999999999858, 1.115600667400684642E-11, -93.95934304829877703 ) ) ;
#31826=AXIS2_PLACEMENT_3D ( 'NONE', #219683, #137567, #58025 ) ;
#31829=CYLINDRICAL_SURFACE ( 'NONE', #124996, 0.1000000000000028644 ) ;
#31913=ORIENTED_EDGE ( 'NONE', *, *, #45168, .T. ) ;
#31931=CARTESIAN_POINT ( 'NONE',  ( 21.05000000000000071, 10.42338541492406989, -107.9920519238701218 ) ) ;
#31934=CARTESIAN_POINT ( 'NONE',  ( 18.50000000000000000, -9.419209763398095347, -107.7477694627589955 ) ) ;
#31970=CARTESIAN_POINT ( 'NONE',  ( 20.74897398619109268, 10.59569302167756888, -108.1793114562555473 ) ) ;
#31974=CIRCLE ( 'NONE', #65267, 11.90000000000000746 ) ;
#32002=DIRECTION ( 'NONE',  ( 0.000000000000000000, -0.9915357197604853789, 0.1298341882520022694 ) ) ;
#32022=ADVANCED_FACE ( 'NONE', ( #119020 ), #198537, .T. ) ;
#32032=EDGE_CURVE ( 'NONE', #223382, #239014, #39717, .T. ) ;
#32053=EDGE_CURVE ( 'NONE', #100676, #92189, #122870, .T. ) ;
#32069=VECTOR ( 'NONE', #225806, 1000.000000000000000 ) ;
#32076=CARTESIAN_POINT ( 'NONE',  ( -18.59999999999999787, 9.350000000011156942, -121.8500000000000369 ) ) ;
#32080=CARTESIAN_POINT ( 'NONE',  ( -18.59999999999999787, 1.261786168576181755, -108.5864989635455089 ) ) ;
#32128=LINE ( 'NONE', #111637, #251558 ) ;
#32151=FACE_OUTER_BOUND ( 'NONE', #89994, .T. ) ;
#32170=CARTESIAN_POINT ( 'NONE',  ( 20.95263205890712399, 8.895740107905208305, -108.9895084069416527 ) ) ;
#32183=AXIS2_PLACEMENT_3D ( 'NONE', #225145, #223866, #187345 ) ;
#32198=ORIENTED_EDGE ( 'NONE', *, *, #22865, .F. ) ;
#32204=DIRECTION ( 'NONE',  ( 1.836970198721029934E-16, -1.000000000000000000, -0.000000000000000000 ) ) ;
#32226=ORIENTED_EDGE ( 'NONE', *, *, #38117, .F. ) ;
#32231=DIRECTION ( 'NONE',  ( 0.000000000000000000, 0.000000000000000000, -1.000000000000000000 ) ) ;
#32235=SPHERICAL_SURFACE ( 'NONE', #102584, 0.1000000000000000056 ) ;
#32249=VERTEX_POINT ( 'NONE', #112294 ) ;
#32294=EDGE_LOOP ( 'NONE', ( #97764, #44918, #251117, #64978 ) ) ;
#32302=EDGE_CURVE ( 'NONE', #214263, #207792, #210557, .T. ) ;
#32339=ORIENTED_EDGE ( 'NONE', *, *, #204639, .F. ) ;
#32362=ORIENTED_EDGE ( 'NONE', *, *, #246313, .F. ) ;
#32387=CYLINDRICAL_SURFACE ( 'NONE', #5517, 4.049999999999998046 ) ;
#32416=DIRECTION ( 'NONE',  ( 1.000000000000000000, -0.000000000000000000, -0.000000000000000000 ) ) ;
#32461=AXIS2_PLACEMENT_3D ( 'NONE', #16885, #36463, #132981 ) ;
#32470=DIRECTION ( 'NONE',  ( 0.000000000000000000, -1.000000000000000000, 0.000000000000000000 ) ) ;
#32479=ORIENTED_EDGE ( 'NONE', *, *, #247528, .F. ) ;
#32499=CIRCLE ( 'NONE', #178230, 11.80000000000000426 ) ;
#32511=ORIENTED_EDGE ( 'NONE', *, *, #140296, .T. ) ;
#32517=EDGE_CURVE ( 'NONE', #89986, #228873, #224202, .T. ) ;
#32563=CIRCLE ( 'NONE', #44995, 0.2000000000000005107 ) ;
#32589=VERTEX_POINT ( 'NONE', #105513 ) ;
#32620=CARTESIAN_POINT ( 'NONE',  ( 18.48197441911542072, -9.517954794695242526, -140.8902116422106872 ) ) ;
#32623=DIRECTION ( 'NONE',  ( 0.000000000000000000, 0.000000000000000000, 1.000000000000000000 ) ) ;
#32633=ORIENTED_EDGE ( 'NONE', *, *, #29561, .F. ) ;
#32649=EDGE_LOOP ( 'NONE', ( #191886, #49503, #117546, #144557 ) ) ;
#32651=CARTESIAN_POINT ( 'NONE',  ( -22.39999999999999858, 1.115600667400684642E-11, -88.85042919245522341 ) ) ;
#32670=CARTESIAN_POINT ( 'NONE',  ( -18.59999999999999787, 9.350000000011156942, -112.8500000000000369 ) ) ;
#32679=CARTESIAN_POINT ( 'NONE',  ( 20.88420186297724612, 10.33025634372637391, -139.5870929282639281 ) ) ;
#32717=DIRECTION ( 'NONE',  ( 1.000000000000000000, 0.000000000000000000, 0.000000000000000000 ) ) ;
#32738=FACE_OUTER_BOUND ( 'NONE', #72940, .T. ) ;
#32758=LINE ( 'NONE', #250470, #63953 ) ;
#32763=DIRECTION ( 'NONE',  ( 1.000000000000000000, 0.000000000000000000, 0.000000000000000000 ) ) ;
#32773=ORIENTED_EDGE ( 'NONE', *, *, #16699, .T. ) ;
#32785=EDGE_CURVE ( 'NONE', #70123, #167341, #89928, .T. ) ;
#32799=PLANE ( 'NONE',  #118425 ) ;
#32832=ORIENTED_EDGE ( 'NONE', *, *, #151028, .T. ) ;
#32856=CARTESIAN_POINT ( 'NONE',  ( 18.60000000000000142, -9.321008403350125704, -107.7359382490779325 ) ) ;
#32859=EDGE_LOOP ( 'NONE', ( #80990, #192450, #231165, #120100, #23857, #125199, #253172 ) ) ;
#32871=ORIENTED_EDGE ( 'NONE', *, *, #161975, .F. ) ;
#32923=ORIENTED_EDGE ( 'NONE', *, *, #225315, .T. ) ;
#32944=DIRECTION ( 'NONE',  ( -1.000000000000000000, 0.000000000000000000, 0.000000000000000000 ) ) ;
#32961=EDGE_CURVE ( 'NONE', #143803, #94061, #180001, .T. ) ;
#32990=DIRECTION ( 'NONE',  ( 0.000000000000000000, 0.000000000000000000, -1.000000000000000000 ) ) ;
#33020=DIRECTION ( 'NONE',  ( -0.000000000000000000, 1.000000000000000000, 0.000000000000000000 ) ) ;
#33029=DIRECTION ( 'NONE',  ( 0.000000000000000000, 1.000000000000000000, 0.000000000000000000 ) ) ;
#33040=CARTESIAN_POINT ( 'NONE',  ( -18.50000000000000000, 6.846123162363745074, -137.7377262668498759 ) ) ;
#33044=CARTESIAN_POINT ( 'NONE',  ( 21.05000000000000071, -11.64999999998883595, -131.1000000000000227 ) ) ;
#33046=DIRECTION ( 'NONE',  ( 1.000000000000000000, 0.000000000000000000, 0.000000000000000000 ) ) ;
#33067=DIRECTION ( 'NONE',  ( 0.000000000000000000, 0.4999999999999956701, -0.8660254037844411501 ) ) ;
#33071=CARTESIAN_POINT ( 'NONE',  ( 20.94999999999999929, 6.550000000011156231, -110.5170271704400591 ) ) ;
#33079=CARTESIAN_POINT ( 'NONE',  ( 21.05000000000000071, -11.48912529306489994, -131.1000000000000227 ) ) ;
#33092=CARTESIAN_POINT ( 'NONE',  ( 23.24999999999999289, 11.75000000001116263, -88.75000000000004263 ) ) ;
#33101=DIRECTION ( 'NONE',  ( 1.000000000000000000, -0.000000000000000000, -0.000000000000000000 ) ) ;
#33155=ADVANCED_FACE ( 'NONE', ( #90793 ), #76362, .T. ) ;
#33223=CARTESIAN_POINT ( 'NONE',  ( -23.25000000000000000, 1.115600667400684642E-11, -134.0000000000000284 ) ) ;
#33226=CIRCLE ( 'NONE', #12362, 11.70000000000000284 ) ;
#33233=EDGE_CURVE ( 'NONE', #60618, #161835, #123447, .T. ) ;
#33247=ORIENTED_EDGE ( 'NONE', *, *, #8594, .F. ) ;
#33251=ORIENTED_EDGE ( 'NONE', *, *, #179841, .F. ) ;
#33253=CARTESIAN_POINT ( 'NONE',  ( 21.07928932188134397, 0.09889514566555242248, -94.17148334360672379 ) ) ;
#33277=ADVANCED_FACE ( 'NONE', ( #80193 ), #110972, .T. ) ;
#33282=ORIENTED_EDGE ( 'NONE', *, *, #204337, .F. ) ;
#33305=CARTESIAN_POINT ( 'NONE',  ( -20.85882249326303040, 10.33248238083634796, -139.5948465439131780 ) ) ;
#33355=CARTESIAN_POINT ( 'NONE',  ( 21.13461538461538325, 8.885417037985616773, -112.8500000000000369 ) ) ;
#33374=DIRECTION ( 'NONE',  ( 0.000000000000000000, 0.000000000000000000, -1.000000000000000000 ) ) ;
#33377=CARTESIAN_POINT ( 'NONE',  ( -20.00857864376270001, 9.150000000011157653, -112.7500000000000284 ) ) ;
#33412=CIRCLE ( 'NONE', #183225, 0.09999999999999892308 ) ;
#33414=CARTESIAN_POINT ( 'NONE',  ( -21.05000000000000071, 11.75000000001115552, -126.9851942293460922 ) ) ;
#33445=( BOUNDED_CURVE ( )  B_SPLINE_CURVE ( 3, ( #161457, #59742, #122317, #201845 ),
 .UNSPECIFIED., .F., .F. ) 
 B_SPLINE_CURVE_WITH_KNOTS ( ( 4, 4 ),
 ( 3.141592653589793116, 4.712388980384689674 ),
 .UNSPECIFIED. ) 
 CURVE ( )  GEOMETRIC_REPRESENTATION_ITEM ( )  RATIONAL_B_SPLINE_CURVE ( ( 1.000000000000000000, 0.8047378541243649375, 0.8047378541243649375, 1.000000000000000000 ) ) 
 REPRESENTATION_ITEM ( '' )  );
#33465=DIRECTION ( 'NONE',  ( 1.000000000000000000, 0.000000000000000000, -0.000000000000000000 ) ) ;
#33466=FACE_OUTER_BOUND ( 'NONE', #35139, .T. ) ;
#33469=ORIENTED_EDGE ( 'NONE', *, *, #213918, .T. ) ;
#33483=ADVANCED_FACE ( 'NONE', ( #185755 ), #111154, .T. ) ;
#33506=EDGE_LOOP ( 'NONE', ( #221197, #160908, #8110, #3475 ) ) ;
#33539=CARTESIAN_POINT ( 'NONE',  ( -23.15000000000000213, -8.999999999988844479, -124.1060308773475924 ) ) ;
#33547=CIRCLE ( 'NONE', #145916, 0.1000000000000106914 ) ;
#33550=VECTOR ( 'NONE', #16255, 1000.000000000000000 ) ;
#33587=ORIENTED_EDGE ( 'NONE', *, *, #202985, .T. ) ;
#33591=CARTESIAN_POINT ( 'NONE',  ( 23.14999999999999858, 1.115600667400684642E-11, -100.5000000000000284 ) ) ;
#33615=EDGE_CURVE ( 'NONE', #60618, #102466, #182584, .T. ) ;
#33684=DIRECTION ( 'NONE',  ( -0.000000000000000000, -0.8700118002898321601, 0.4930308989875230030 ) ) ;
#33702=CARTESIAN_POINT ( 'NONE',  ( 21.06280952165527154, 10.62713230061232927, -112.7040538867790076 ) ) ;
#33772=DIRECTION ( 'NONE',  ( -1.000000000000000000, -2.952720810173289112E-16, 0.000000000000000000 ) ) ;
#33828=CIRCLE ( 'NONE', #87913, 0.5000000000000004441 ) ;
#33839=VERTEX_POINT ( 'NONE', #226821 ) ;
#33853=CARTESIAN_POINT ( 'NONE',  ( 21.05000000000000071, 10.72371710471867701, -112.6611902941274650 ) ) ;
#33888=CARTESIAN_POINT ( 'NONE',  ( 21.97500000000000497, 9.750000000011153745, -112.8500000000000369 ) ) ;
#33916=CARTESIAN_POINT ( 'NONE',  ( 18.36493879433272625, -9.500000806178645618, -140.9221486603523488 ) ) ;
#33932=ORIENTED_EDGE ( 'NONE', *, *, #126028, .T. ) ;
#33966=CARTESIAN_POINT ( 'NONE',  ( 20.92356734117541706, 10.31973158071402175, -139.5505334713354841 ) ) ;
#33974=CARTESIAN_POINT ( 'NONE',  ( 22.49436431346199683, 11.64995094766461392, -100.4330964702777749 ) ) ;
#33975=ADVANCED_FACE ( 'NONE', ( #134123 ), #165516, .T. ) ;
#33985=LINE ( 'NONE', #73104, #184224 ) ;
#34007=CARTESIAN_POINT ( 'NONE',  ( -20.54999999999999716, -8.730841121484173684, -110.0980747189843640 ) ) ;
#34029=AXIS2_PLACEMENT_3D ( 'NONE', #243704, #50619, #65065 ) ;
#34049=DIRECTION ( 'NONE',  ( -0.000000000000000000, -1.000000000000000000, -5.421010862427649374E-16 ) ) ;
#34053=ORIENTED_EDGE ( 'NONE', *, *, #86983, .T. ) ;
#34065=FACE_OUTER_BOUND ( 'NONE', #32649, .T. ) ;
#34070=CIRCLE ( 'NONE', #159141, 0.1000000000000106914 ) ;
#34077=ORIENTED_EDGE ( 'NONE', *, *, #246609, .F. ) ;
#34079=VERTEX_POINT ( 'NONE', #183543 ) ;
#34088=CARTESIAN_POINT ( 'NONE',  ( -21.05000000000000071, -1.162701749926853712, -108.4000000000000341 ) ) ;
#34130=EDGE_CURVE ( 'NONE', #5081, #236424, #136623, .T. ) ;
#34146=LINE ( 'NONE', #97893, #164440 ) ;
#34152=VECTOR ( 'NONE', #190077, 1000.000000000000000 ) ;
#34179=DIRECTION ( 'NONE',  ( -0.000000000000000000, 0.1350103645451876666, 0.9908441862701600211 ) ) ;
#34211=ORIENTED_EDGE ( 'NONE', *, *, #42198, .T. ) ;
#34227=ORIENTED_EDGE ( 'NONE', *, *, #6135, .T. ) ;
#34240=ORIENTED_EDGE ( 'NONE', *, *, #92151, .F. ) ;
#34246=CARTESIAN_POINT ( 'NONE',  ( -21.05000000000000071, -1.851028230129704522, -112.1539132694225316 ) ) ;
#34273=FACE_OUTER_BOUND ( 'NONE', #177477, .T. ) ;
#34295=CARTESIAN_POINT ( 'NONE',  ( -18.50000000000000000, 11.65000000001115232, -112.6500000000000341 ) ) ;
#34306=FACE_OUTER_BOUND ( 'NONE', #114165, .T. ) ;
#34319=CARTESIAN_POINT ( 'NONE',  ( -20.64999999999999858, 2.000000000011154189, -121.2753780772379315 ) ) ;
#34335=CARTESIAN_POINT ( 'NONE',  ( 21.05000000000000071, -0.09999999998884338825, -93.95934304829877703 ) ) ;
#34339=ORIENTED_EDGE ( 'NONE', *, *, #119025, .F. ) ;
#34362=EDGE_CURVE ( 'NONE', #123327, #39467, #215737, .T. ) ;
#34373=CARTESIAN_POINT ( 'NONE',  ( 20.85000000000000142, -1.835859311432481045, -145.5044391687985694 ) ) ;
#34383=DIRECTION ( 'NONE',  ( 0.000000000000000000, 0.8660254037844482555, 0.4999999999999837907 ) ) ;
#34401=EDGE_CURVE ( 'NONE', #227485, #229941, #19959, .T. ) ;
#34456=VERTEX_POINT ( 'NONE', #252054 ) ;
#34475=EDGE_LOOP ( 'NONE', ( #190714, #9316, #175642, #62577 ) ) ;
#34483=CARTESIAN_POINT ( 'NONE',  ( -21.05000000000000071, 1.115600667400684642E-11, -100.5000000000000284 ) ) ;
#34485=VERTEX_POINT ( 'NONE', #172577 ) ;
#34502=DIRECTION ( 'NONE',  ( 1.000000000000000000, 0.000000000000000000, 0.000000000000000000 ) ) ;
#34511=DIRECTION ( 'NONE',  ( -1.000000000000000000, 0.000000000000000000, 0.000000000000000000 ) ) ;
#34530=DIRECTION ( 'NONE',  ( -1.000000000000000000, -2.952720810173289112E-16, 0.000000000000000000 ) ) ;
#34549=DIRECTION ( 'NONE',  ( 0.000000000000000000, 0.000000000000000000, 1.000000000000000000 ) ) ;
#34555=EDGE_CURVE ( 'NONE', #160408, #46245, #233330, .T. ) ;
#34559=CARTESIAN_POINT ( 'NONE',  ( -18.59999999999999787, 1.162701749949165642, -108.6000000000000227 ) ) ;
#34579=VECTOR ( 'NONE', #74903, 1000.000000000000000 ) ;
#34581=DIRECTION ( 'NONE',  ( 0.000000000000000000, -0.9908441862701600211, -0.1350103645451876666 ) ) ;
#34597=AXIS2_PLACEMENT_3D ( 'NONE', #107538, #228796, #147964 ) ;
#34622=EDGE_CURVE ( 'NONE', #226312, #74036, #157729, .T. ) ;
#34628=CIRCLE ( 'NONE', #242888, 0.1000000000000028644 ) ;
#34636=DIRECTION ( 'NONE',  ( 1.000000000000000000, -0.000000000000000000, -0.000000000000000000 ) ) ;
#34651=DIRECTION ( 'NONE',  ( 0.000000000000000000, 0.000000000000000000, -1.000000000000000000 ) ) ;
#34695=VECTOR ( 'NONE', #26758, 1000.000000000000000 ) ;
#34709=FACE_OUTER_BOUND ( 'NONE', #90007, .T. ) ;
#34742=EDGE_LOOP ( 'NONE', ( #143964, #144133, #93515, #119356 ) ) ;
#34771=CARTESIAN_POINT ( 'NONE',  ( 18.59117750673696534, 10.33248238083634796, -139.5948465439131780 ) ) ;
#34806=DIRECTION ( 'NONE',  ( -1.000000000000000000, 0.000000000000000000, 0.000000000000000000 ) ) ;
#34822=ORIENTED_EDGE ( 'NONE', *, *, #85730, .T. ) ;
#34846=VERTEX_POINT ( 'NONE', #149306 ) ;
#34852=CARTESIAN_POINT ( 'NONE',  ( -18.41418431465368144, -9.499999999989071853, -140.6001893912215053 ) ) ;
#34880=ORIENTED_EDGE ( 'NONE', *, *, #58526, .F. ) ;
#34898=VERTEX_POINT ( 'NONE', #30644 ) ;
#34903=AXIS2_PLACEMENT_3D ( 'NONE', #229761, #70719, #148963 ) ;
#34915=CARTESIAN_POINT ( 'NONE',  ( -20.85000000000000142, -11.74999999998884448, -131.1000000000000227 ) ) ;
#34941=AXIS2_PLACEMENT_3D ( 'NONE', #127331, #189873, #206866 ) ;
#34942=CYLINDRICAL_SURFACE ( 'NONE', #181509, 0.09999999999999939493 ) ;
#34944=DIRECTION ( 'NONE',  ( 0.000000000000000000, 0.000000000000000000, -1.000000000000000000 ) ) ;
#34960=VERTEX_POINT ( 'NONE', #158309 ) ;
#34972=EDGE_LOOP ( 'NONE', ( #67721, #117200, #70153, #241024 ) ) ;
#34978=DIRECTION ( 'NONE',  ( 0.000000000000000000, 0.000000000000000000, -1.000000000000000000 ) ) ;
#35016=ORIENTED_EDGE ( 'NONE', *, *, #253795, .T. ) ;
#35028=DIRECTION ( 'NONE',  ( 1.000000000000000000, 0.000000000000000000, 0.000000000000000000 ) ) ;
#35061=DIRECTION ( 'NONE',  ( 1.000000000000000000, 0.000000000000000000, 0.000000000000000000 ) ) ;
#35099=CIRCLE ( 'NONE', #118268, 0.8750000000000007772 ) ;
#35118=EDGE_CURVE ( 'NONE', #254860, #18904, #12081, .T. ) ;
#35127=FACE_OUTER_BOUND ( 'NONE', #100594, .T. ) ;
#35131=CARTESIAN_POINT ( 'NONE',  ( 18.49999999999999645, -1.362429037182155023, -141.8888812479212334 ) ) ;
#35139=EDGE_LOOP ( 'NONE', ( #216889, #11883, #256656, #144417 ) ) ;
#35147=ORIENTED_EDGE ( 'NONE', *, *, #47046, .F. ) ;
#35152=ORIENTED_EDGE ( 'NONE', *, *, #124650, .F. ) ;
#35173=EDGE_CURVE ( 'NONE', #97978, #182621, #159563, .T. ) ;
#35196=CARTESIAN_POINT ( 'NONE',  ( -18.50000000000000000, -9.399999999988850163, -140.8820418481727188 ) ) ;
#35197=AXIS2_PLACEMENT_3D ( 'NONE', #217908, #97956, #232387 ) ;
#35206=CARTESIAN_POINT ( 'NONE',  ( -18.44362607810620958, -9.490496158073669974, -107.5579538668471571 ) ) ;
#35233=CARTESIAN_POINT ( 'NONE',  ( -20.94999999999999929, -1.164121893230052995, -141.7148480855716457 ) ) ;
#35246=CARTESIAN_POINT ( 'NONE',  ( -23.15000000000000213, 4.350000000011156054, -121.6500000000000341 ) ) ;
#35260=CARTESIAN_POINT ( 'NONE',  ( 23.15000000000000213, -11.64999999998883595, -130.9000000000000341 ) ) ;
#35276=ADVANCED_FACE ( 'NONE', ( #9464 ), #166089, .T. ) ;
#35353=VECTOR ( 'NONE', #120466, 1000.000000000000000 ) ;
#35443=DIRECTION ( 'NONE',  ( 0.000000000000000000, 1.000000000000000000, 0.000000000000000000 ) ) ;
#35530=VERTEX_POINT ( 'NONE', #107940 ) ;
#35537=EDGE_CURVE ( 'NONE', #25563, #76942, #160564, .T. ) ;
#35541=AXIS2_PLACEMENT_3D ( 'NONE', #184555, #22953, #45057 ) ;
#35544=DIRECTION ( 'NONE',  ( 1.000000000000000000, 0.000000000000000000, 0.000000000000000000 ) ) ;
#35552=CARTESIAN_POINT ( 'NONE',  ( 22.50000000000000000, 0.1000000000111554016, -88.75000000000004263 ) ) ;
#35570=EDGE_LOOP ( 'NONE', ( #200552, #8792, #232446, #183605, #130923, #63170 ) ) ;
#35616=EDGE_CURVE ( 'NONE', #219593, #172822, #74247, .T. ) ;
#35643=CARTESIAN_POINT ( 'NONE',  ( 21.30000000000002558, 1.115600667400684642E-11, -96.45000000000003126 ) ) ;
#35645=AXIS2_PLACEMENT_3D ( 'NONE', #40881, #220772, #64267 ) ;
#35653=CIRCLE ( 'NONE', #139636, 0.09999999999999917288 ) ;
#35656=AXIS2_PLACEMENT_3D ( 'NONE', #114228, #154670, #135050 ) ;
#35662=EDGE_CURVE ( 'NONE', #83495, #182032, #3929, .T. ) ;
#35680=CARTESIAN_POINT ( 'NONE',  ( -20.54999999999999716, 4.350000000011156054, -112.8500000000000369 ) ) ;
#35688=CYLINDRICAL_SURFACE ( 'NONE', #37982, 0.5000000000000004441 ) ;
#35724=EDGE_LOOP ( 'NONE', ( #85782, #196392, #117903, #176631 ) ) ;
#35725=ORIENTED_EDGE ( 'NONE', *, *, #89291, .F. ) ;
#35731=AXIS2_PLACEMENT_3D ( 'NONE', #95457, #57602, #175052 ) ;
#35743=ORIENTED_EDGE ( 'NONE', *, *, #114055, .T. ) ;
#35768=CARTESIAN_POINT ( 'NONE',  ( -18.59999999999999787, 9.250000000011157297, -121.7500000000000426 ) ) ;
#35783=CARTESIAN_POINT ( 'NONE',  ( -21.07928932188134041, 1.115600667400684642E-11, -100.5000000000000284 ) ) ;
#35793=EDGE_CURVE ( 'NONE', #137271, #196016, #112451, .T. ) ;
#35832=ORIENTED_EDGE ( 'NONE', *, *, #111558, .F. ) ;
#35856=ORIENTED_EDGE ( 'NONE', *, *, #62930, .F. ) ;
#35872=AXIS2_PLACEMENT_3D ( 'NONE', #67475, #226525, #167897 ) ;
#35873=CARTESIAN_POINT ( 'NONE',  ( -21.07928932188134041, 6.328516656404449492, -100.4011048543456468 ) ) ;
#35884=AXIS2_PLACEMENT_3D ( 'NONE', #114689, #149996, #31343 ) ;
#35889=DIRECTION ( 'NONE',  ( 0.000000000000000000, 0.000000000000000000, -1.000000000000000000 ) ) ;
#35921=FACE_OUTER_BOUND ( 'NONE', #149682, .T. ) ;
#35931=FACE_OUTER_BOUND ( 'NONE', #87602, .T. ) ;
#35943=AXIS2_PLACEMENT_3D ( 'NONE', #169184, #149614, #229129 ) ;
#35947=DIRECTION ( 'NONE',  ( 0.000000000000000000, 0.000000000000000000, 1.000000000000000000 ) ) ;
#35986=AXIS2_PLACEMENT_3D ( 'NONE', #146841, #47744, #106425 ) ;
#35998=EDGE_LOOP ( 'NONE', ( #186244, #34240, #204342, #32871 ) ) ;
#36009=ADVANCED_FACE ( 'NONE', ( #67217 ), #161734, .T. ) ;
#36060=VECTOR ( 'NONE', #25405, 1000.000000000000000 ) ;
#36096=EDGE_LOOP ( 'NONE', ( #121320, #145298, #10187, #210488 ) ) ;
#36125=DIRECTION ( 'NONE',  ( -1.000000000000000000, -7.304098846218135653E-16, 4.607487905232624742E-31 ) ) ;
#36153=AXIS2_PLACEMENT_3D ( 'NONE', #246339, #67698, #147231 ) ;
#36156=DIRECTION ( 'NONE',  ( 0.000000000000000000, 1.192622389734062135E-14, -1.000000000000000000 ) ) ;
#36191=EDGE_CURVE ( 'NONE', #126005, #167562, #57905, .T. ) ;
#36210=DIRECTION ( 'NONE',  ( 0.000000000000000000, 0.000000000000000000, -1.000000000000000000 ) ) ;
#36248=DIRECTION ( 'NONE',  ( 0.000000000000000000, 0.000000000000000000, -1.000000000000000000 ) ) ;
#36255=CARTESIAN_POINT ( 'NONE',  ( -18.59999999999999787, 11.65000000001115232, -107.4148057706540271 ) ) ;
#36264=ORIENTED_EDGE ( 'NONE', *, *, #232293, .T. ) ;
#36268=ORIENTED_EDGE ( 'NONE', *, *, #250852, .F. ) ;
#36318=CARTESIAN_POINT ( 'NONE',  ( 18.59999999999999076, 10.20857864377385127, -125.2500000000000284 ) ) ;
#36365=ORIENTED_EDGE ( 'NONE', *, *, #119828, .F. ) ;
#36367=AXIS2_PLACEMENT_3D ( 'NONE', #252630, #16619, #251349 ) ;
#36390=DIRECTION ( 'NONE',  ( -1.000000000000000000, 0.000000000000000000, 0.000000000000000000 ) ) ;
#36398=DIRECTION ( 'NONE',  ( 0.000000000000000000, 0.000000000000000000, -1.000000000000000000 ) ) ;
#36424=ORIENTED_EDGE ( 'NONE', *, *, #169314, .F. ) ;
#36453=VERTEX_POINT ( 'NONE', #245564 ) ;
#36463=DIRECTION ( 'NONE',  ( 1.000000000000000000, 0.000000000000000000, 0.000000000000000000 ) ) ;
#36483=CARTESIAN_POINT ( 'NONE',  ( -21.05000000000000071, -11.64999999998884306, -130.9000000000000341 ) ) ;
#36490=CIRCLE ( 'NONE', #107539, 2.000000000000001776 ) ;
#36520=AXIS2_PLACEMENT_3D ( 'NONE', #134835, #73639, #213115 ) ;
#36541=CARTESIAN_POINT ( 'NONE',  ( 20.94999999999999929, 6.846123162363745074, -137.7377262668498759 ) ) ;
#36565=ORIENTED_EDGE ( 'NONE', *, *, #37990, .T. ) ;
#36577=AXIS2_PLACEMENT_3D ( 'NONE', #109959, #90394, #169990 ) ;
#36586=CARTESIAN_POINT ( 'NONE',  ( -20.64999999999999858, 7.150000000011155876, -112.8500000000000369 ) ) ;
#36632=EDGE_CURVE ( 'NONE', #46505, #141039, #77182, .T. ) ;
#36664=ADVANCED_FACE ( 'NONE', ( #156759, #236262, #217960 ), #57610, .F. ) ;
#36670=ADVANCED_FACE ( 'NONE', ( #180160 ), #221809, .F. ) ;
#36700=EDGE_LOOP ( 'NONE', ( #28933, #37671, #95510, #25406 ) ) ;
#36723=DIRECTION ( 'NONE',  ( 1.000000000000000000, 2.952720810173289112E-16, -0.000000000000000000 ) ) ;
#36733=DIRECTION ( 'NONE',  ( 1.000000000000000000, 0.000000000000000000, 0.000000000000000000 ) ) ;
#36752=AXIS2_PLACEMENT_3D ( 'NONE', #76534, #175656, #96088 ) ;
#36762=EDGE_CURVE ( 'NONE', #126637, #2822, #153798, .T. ) ;
#36946=AXIS2_PLACEMENT_3D ( 'NONE', #202139, #23539, #103017 ) ;
#36951=AXIS2_PLACEMENT_3D ( 'NONE', #244563, #28121, #145461 ) ;
#37008=AXIS2_PLACEMENT_3D ( 'NONE', #21848, #57088, #156249 ) ;
#37038=CARTESIAN_POINT ( 'NONE',  ( 20.94999999999999929, 11.65000000001115943, -127.2161343370219413 ) ) ;
#37042=CARTESIAN_POINT ( 'NONE',  ( -20.85000000000000142, 1.115600667400684642E-11, -134.0000000000000284 ) ) ;
#37050=ADVANCED_FACE ( 'NONE', ( #239826 ), #102840, .T. ) ;
#37081=DIRECTION ( 'NONE',  ( -1.000000000000000000, -0.000000000000000000, -0.000000000000000000 ) ) ;
#37097=ORIENTED_EDGE ( 'NONE', *, *, #71042, .F. ) ;
#37101=DIRECTION ( 'NONE',  ( 3.616040088954497272E-32, -1.224646799147352961E-16, 1.000000000000000000 ) ) ;
#37167=DIRECTION ( 'NONE',  ( 0.000000000000000000, 1.000000000000000000, 0.000000000000000000 ) ) ;
#37185=CIRCLE ( 'NONE', #166197, 11.75000000000001066 ) ;
#37211=CARTESIAN_POINT ( 'NONE',  ( -21.05000000000000071, 6.478078221105989520, -100.5999999353071246 ) ) ;
#37219=CARTESIAN_POINT ( 'NONE',  ( -23.25000000000000000, 4.350000000011156054, -112.8500000000000369 ) ) ;
#37230=CARTESIAN_POINT ( 'NONE',  ( -20.94999999999999929, 1.261786168576181755, -108.5864989635455089 ) ) ;
#37232=DIRECTION ( 'NONE',  ( 8.673617379884087537E-15, -0.000000000000000000, 1.000000000000000000 ) ) ;
#37233=ADVANCED_FACE ( 'NONE', ( #91004 ), #190119, .F. ) ;
#37234=DIRECTION ( 'NONE',  ( 0.000000000000000000, 1.000000000000000000, 0.000000000000000000 ) ) ;
#37239=ORIENTED_EDGE ( 'NONE', *, *, #152818, .F. ) ;
#37272=CARTESIAN_POINT ( 'NONE',  ( -20.94999999999999929, 1.360870587203197646, -108.5729979270909951 ) ) ;
#37286=ORIENTED_EDGE ( 'NONE', *, *, #66396, .F. ) ;
#37303=ORIENTED_EDGE ( 'NONE', *, *, #34555, .T. ) ;
#37306=ORIENTED_EDGE ( 'NONE', *, *, #192717, .T. ) ;
#37310=EDGE_CURVE ( 'NONE', #119449, #159714, #215745, .T. ) ;
#37316=SPHERICAL_SURFACE ( 'NONE', #235161, 0.1000000000000000056 ) ;
#37339=VERTEX_POINT ( 'NONE', #77505 ) ;
#37362=CARTESIAN_POINT ( 'NONE',  ( -18.59999999999999787, 7.021664781911246322, -137.8335654018973457 ) ) ;
#37388=EDGE_LOOP ( 'NONE', ( #26013, #57193, #33247, #29366 ) ) ;
#37391=DIRECTION ( 'NONE',  ( 0.000000000000000000, 0.000000000000000000, -1.000000000000000000 ) ) ;
#37416=ORIENTED_EDGE ( 'NONE', *, *, #107684, .T. ) ;
#37444=DIRECTION ( 'NONE',  ( 0.000000000000000000, -0.4999999999999949485, 0.8660254037844415942 ) ) ;
#37457=ORIENTED_EDGE ( 'NONE', *, *, #30531, .F. ) ;
#37505=DIRECTION ( 'NONE',  ( 0.000000000000000000, -1.000000000000000000, 0.000000000000000000 ) ) ;
#37519=CARTESIAN_POINT ( 'NONE',  ( 21.14999999999999858, 6.257814610487280937, -100.4022097086912311 ) ) ;
#37565=FACE_OUTER_BOUND ( 'NONE', #253775, .T. ) ;
#37616=VERTEX_POINT ( 'NONE', #53817 ) ;
#37626=PLANE ( 'NONE',  #233513 ) ;
#37645=EDGE_CURVE ( 'NONE', #46758, #198608, #141807, .T. ) ;
#37671=ORIENTED_EDGE ( 'NONE', *, *, #116113, .F. ) ;
#37689=DIRECTION ( 'NONE',  ( 0.000000000000000000, -1.000000000000000000, -0.000000000000000000 ) ) ;
#37703=DIRECTION ( 'NONE',  ( 0.000000000000000000, 0.000000000000000000, -1.000000000000000000 ) ) ;
#37718=CARTESIAN_POINT ( 'NONE',  ( 21.30000000000002558, 1.115600667400684642E-11, -100.5000000000000284 ) ) ;
#37734=SPHERICAL_SURFACE ( 'NONE', #88537, 0.1000000000000000056 ) ;
#37738=DIRECTION ( 'NONE',  ( -0.000000000000000000, 1.000000000000000000, -0.000000000000000000 ) ) ;
#37792=AXIS2_PLACEMENT_3D ( 'NONE', #138863, #55473, #157216 ) ;
#37797=EDGE_LOOP ( 'NONE', ( #119108, #91543, #38905, #178264 ) ) ;
#37843=CARTESIAN_POINT ( 'NONE',  ( -20.54999999999999716, 4.350000000011156054, -121.6500000000000341 ) ) ;
#37855=CARTESIAN_POINT ( 'NONE',  ( 21.14999999999999858, 1.115600667400684642E-11, -100.5000000000000284 ) ) ;
#37861=VERTEX_POINT ( 'NONE', #178937 ) ;
#37868=EDGE_CURVE ( 'NONE', #84341, #185932, #137694, .T. ) ;
#37869=CIRCLE ( 'NONE', #145986, 0.1000000000000000472 ) ;
#37935=DIRECTION ( 'NONE',  ( 0.000000000000000000, 0.000000000000000000, 1.000000000000000000 ) ) ;
#37949=VERTEX_POINT ( 'NONE', #21136 ) ;
#37966=AXIS2_PLACEMENT_3D ( 'NONE', #88164, #131169, #227695 ) ;
#37982=AXIS2_PLACEMENT_3D ( 'NONE', #209145, #189606, #172652 ) ;
#37989=CIRCLE ( 'NONE', #62903, 0.1000000000000002692 ) ;
#37990=EDGE_CURVE ( 'NONE', #141039, #60627, #171289, .T. ) ;
#38008=CARTESIAN_POINT ( 'NONE',  ( 20.94999999999999929, -9.499999999988844479, -124.1060308773475924 ) ) ;
#38039=EDGE_LOOP ( 'NONE', ( #238620, #256698 ) ) ;
#38060=CARTESIAN_POINT ( 'NONE',  ( -21.07933241753356413, 0.09337959043042065588, -94.17135405162028405 ) ) ;
#38061=CYLINDRICAL_SURFACE ( 'NONE', #199301, 0.09999999999999939493 ) ;
#38088=EDGE_CURVE ( 'NONE', #40984, #196505, #62897, .T. ) ;
#38114=LINE ( 'NONE', #178931, #156928 ) ;
#38117=EDGE_CURVE ( 'NONE', #110815, #257268, #241947, .T. ) ;
#38132=ORIENTED_EDGE ( 'NONE', *, *, #116606, .T. ) ;
#38159=CARTESIAN_POINT ( 'NONE',  ( 20.02499999999999858, 9.750000000011153745, -121.7500000000000426 ) ) ;
#38164=ORIENTED_EDGE ( 'NONE', *, *, #35662, .F. ) ;
#38178=ORIENTED_EDGE ( 'NONE', *, *, #150503, .T. ) ;
#38203=CARTESIAN_POINT ( 'NONE',  ( 23.14999999999999858, 1.115600667400684642E-11, -134.0000000000000284 ) ) ;
#38215=ORIENTED_EDGE ( 'NONE', *, *, #173587, .T. ) ;
#38276=ORIENTED_EDGE ( 'NONE', *, *, #85505, .F. ) ;
#38278=EDGE_CURVE ( 'NONE', #45367, #85652, #17733, .T. ) ;
#38281=AXIS2_PLACEMENT_3D ( 'NONE', #194503, #35443, #174970 ) ;
#38340=CIRCLE ( 'NONE', #246434, 0.09999999999999939493 ) ;
#38379=ORIENTED_EDGE ( 'NONE', *, *, #45168, .F. ) ;
#38401=EDGE_LOOP ( 'NONE', ( #155166, #99335 ) ) ;
#38425=AXIS2_PLACEMENT_3D ( 'NONE', #13461, #33067, #147839 ) ;
#38454=ORIENTED_EDGE ( 'NONE', *, *, #233844, .T. ) ;
#38473=AXIS2_PLACEMENT_3D ( 'NONE', #61207, #39100, #179888 ) ;
#38479=B_SPLINE_CURVE_WITH_KNOTS ( 'NONE', 3,
 ( #55901, #33853, #15552, #95053, #117194, #76772, #156351, #93765, #173364, #135453, #53367, #153806, #214997, #174652, #57189, #252838 ),
 .UNSPECIFIED., .F., .F.,
 ( 4, 3, 3, 3, 3, 4 ),
 ( 0.000000000000000000, 3.357088238233684694E-05, 6.714213034887935657E-05, 0.0001007408646121008016, 0.0001343627955914262746, 0.0001573956632896011476 ),
 .UNSPECIFIED. ) ;
#38481=VERTEX_POINT ( 'NONE', #52845 ) ;
#38510=CARTESIAN_POINT ( 'NONE',  ( 23.14999999999999858, 5.500000000011153745, -112.9052660189131245 ) ) ;
#38532=CARTESIAN_POINT ( 'NONE',  ( 23.14999999999999503, 6.550000000011156231, -121.6500000000000341 ) ) ;
#38538=ORIENTED_EDGE ( 'NONE', *, *, #189707, .F. ) ;
#38541=DIRECTION ( 'NONE',  ( 0.000000000000000000, 0.9908441862701596881, 0.1350103645451904977 ) ) ;
#38544=CARTESIAN_POINT ( 'NONE',  ( -23.15000000000000213, 1.115600667400684642E-11, -100.5000000000000284 ) ) ;
#38567=CYLINDRICAL_SURFACE ( 'NONE', #234487, 0.09999999999999939493 ) ;
#38578=TOROIDAL_SURFACE ( 'NONE', #96812, 7.800000000000000711, 0.1000000000000000056 ) ;
#38581=DIRECTION ( 'NONE',  ( 1.000000000000000000, 0.000000000000000000, 0.000000000000000000 ) ) ;
#38584=DIRECTION ( 'NONE',  ( 0.000000000000000000, 0.000000000000000000, 1.000000000000000000 ) ) ;
#38616=LINE ( 'NONE', #114290, #77676 ) ;
#38625=ORIENTED_EDGE ( 'NONE', *, *, #102448, .T. ) ;
#38663=CARTESIAN_POINT ( 'NONE',  ( 18.49999999999999645, 1.637172712981537659, -112.0821533654720525 ) ) ;
#38680=FACE_OUTER_BOUND ( 'NONE', #164115, .T. ) ;
#38721=EDGE_LOOP ( 'NONE', ( #178997, #16406, #251022, #223042 ) ) ;
#38731=VERTEX_POINT ( 'NONE', #102213 ) ;
#38739=EDGE_LOOP ( 'NONE', ( #139695, #157056, #178377, #59298 ) ) ;
#38766=AXIS2_PLACEMENT_3D ( 'NONE', #150694, #247213, #244645 ) ;
#38773=DIRECTION ( 'NONE',  ( 2.694716079187272946E-16, -1.000000000000000000, 0.000000000000000000 ) ) ;
#38781=CARTESIAN_POINT ( 'NONE',  ( -21.14999999999999858, 6.540656951712397138, -100.6000000000000369 ) ) ;
#38794=PLANE ( 'NONE',  #69984 ) ;
#38795=EDGE_CURVE ( 'NONE', #197646, #129441, #209473, .T. ) ;
#38798=AXIS2_PLACEMENT_3D ( 'NONE', #73434, #96781, #17296 ) ;
#38812=DIRECTION ( 'NONE',  ( 1.000000000000000000, 0.000000000000000000, 0.000000000000000000 ) ) ;
#38813=EDGE_LOOP ( 'NONE', ( #190694, #208642, #53782, #235912 ) ) ;
#38814=( BOUNDED_SURFACE ( )  B_SPLINE_SURFACE ( 3, 2, ( 
 ( #23102, #145581, #225102 ),
 ( #46473, #126018, #205549 ),
 ( #26961, #182162, #83015 ),
 ( #162601, #63475, #28248 ) ),
 .UNSPECIFIED., .F., .F., .T. ) 
 B_SPLINE_SURFACE_WITH_KNOTS ( ( 4, 4 ),
 ( 3, 3 ),
 ( -3.469446951953614189E-18, 0.001979672783031532438 ),
 ( 0.000000000000000000, 1.000000000000000000 ),
 .UNSPECIFIED. ) 
 GEOMETRIC_REPRESENTATION_ITEM ( )  RATIONAL_B_SPLINE_SURFACE ( (
 ( 1.000000000000000000, 0.7103081912008198939, 1.000000000000000000),
 ( 1.000000000000000000, 0.7104998333558888435, 1.000000000000000000),
 ( 1.000000000000000000, 0.7107238315754828006, 1.000000000000000000),
 ( 1.000000000000000000, 0.7110073749539717047, 1.000000000000000000) ) ) 
 REPRESENTATION_ITEM ( '' )  SURFACE ( )  );
#38855=ORIENTED_EDGE ( 'NONE', *, *, #250962, .F. ) ;
#38870=ORIENTED_EDGE ( 'NONE', *, *, #160481, .F. ) ;
#38885=DIRECTION ( 'NONE',  ( 1.000000000000000000, -0.000000000000000000, -0.000000000000000000 ) ) ;
#38892=EDGE_CURVE ( 'NONE', #20386, #247339, #1360, .T. ) ;
#38905=ORIENTED_EDGE ( 'NONE', *, *, #13341, .F. ) ;
#38906=DIRECTION ( 'NONE',  ( 0.000000000000000000, -0.4930308989874653269, -0.8700118002898649117 ) ) ;
#38935=ORIENTED_EDGE ( 'NONE', *, *, #62930, .T. ) ;
#38949=VECTOR ( 'NONE', #30460, 999.9999999999998863 ) ;
#38953=CYLINDRICAL_SURFACE ( 'NONE', #80719, 4.000000000000003553 ) ;
#38959=ORIENTED_EDGE ( 'NONE', *, *, #179077, .T. ) ;
#38967=ADVANCED_FACE ( 'NONE', ( #53842 ), #251146, .T. ) ;
#38973=ORIENTED_EDGE ( 'NONE', *, *, #175200, .T. ) ;
#38999=CARTESIAN_POINT ( 'NONE',  ( -20.54999999999999716, 1.925233644870967487, -121.2697564668739005 ) ) ;
#39032=CARTESIAN_POINT ( 'NONE',  ( -23.24999999999999645, -9.599999999988845900, -140.6001893912220737 ) ) ;
#39033=ADVANCED_FACE ( 'NONE', ( #34306 ), #26335, .T. ) ;
#39082=CARTESIAN_POINT ( 'NONE',  ( -22.32929514600008503, 0.09907567812507747651, -92.92135243462352889 ) ) ;
#39089=CIRCLE ( 'NONE', #51495, 0.1000000000000096922 ) ;
#39100=DIRECTION ( 'NONE',  ( -1.000000000000000000, -0.000000000000000000, -0.000000000000000000 ) ) ;
#39106=EDGE_CURVE ( 'NONE', #222832, #75372, #93130, .T. ) ;
#39119=DIRECTION ( 'NONE',  ( 1.000000000000000000, 2.952720810173289112E-16, -0.000000000000000000 ) ) ;
#39185=ORIENTED_EDGE ( 'NONE', *, *, #186209, .T. ) ;
#39206=FACE_OUTER_BOUND ( 'NONE', #188703, .T. ) ;
#39235=ORIENTED_EDGE ( 'NONE', *, *, #210773, .F. ) ;
#39288=EDGE_LOOP ( 'NONE', ( #195741, #80677, #65666 ) ) ;
#39292=ORIENTED_EDGE ( 'NONE', *, *, #6804, .T. ) ;
#39298=ORIENTED_EDGE ( 'NONE', *, *, #7954, .F. ) ;
#39316=CIRCLE ( 'NONE', #201599, 0.09999999999998807065 ) ;
#39345=AXIS2_PLACEMENT_3D ( 'NONE', #26288, #105782, #65400 ) ;
#39346=ORIENTED_EDGE ( 'NONE', *, *, #42449, .F. ) ;
#39354=EDGE_CURVE ( 'NONE', #182621, #70011, #138880, .T. ) ;
#39361=DIRECTION ( 'NONE',  ( 0.000000000000000000, 0.000000000000000000, 1.000000000000000000 ) ) ;
#39371=CARTESIAN_POINT ( 'NONE',  ( -23.15000000000000213, 4.250000000011156409, -121.7500000000000426 ) ) ;
#39374=DIRECTION ( 'NONE',  ( 0.000000000000000000, 1.000000000000000000, 1.626303258728238113E-15 ) ) ;
#39383=AXIS2_PLACEMENT_3D ( 'NONE', #89448, #69924, #110304 ) ;
#39384=CARTESIAN_POINT ( 'NONE',  ( -23.25000000000000000, 1.115600667400684642E-11, -100.5000000000000284 ) ) ;
#39393=ADVANCED_FACE ( 'NONE', ( #52228 ), #68197, .T. ) ;
#39412=DIRECTION ( 'NONE',  ( -1.000000000000000000, -3.265361837132813093E-16, 0.000000000000000000 ) ) ;
#39414=CARTESIAN_POINT ( 'NONE',  ( -20.94999999999999929, 11.65000000001115232, -134.0000000000000284 ) ) ;
#39421=TOROIDAL_SURFACE ( 'NONE', #110109, 2.100000000000002309, 0.1000000000000000056 ) ;
#39463=CARTESIAN_POINT ( 'NONE',  ( -18.50000000000000000, -1.835859311432484375, -145.5044391687985694 ) ) ;
#39467=VERTEX_POINT ( 'NONE', #97763 ) ;
#39497=ORIENTED_EDGE ( 'NONE', *, *, #17392, .T. ) ;
#39509=DIRECTION ( 'NONE',  ( 1.000000000000000000, 0.000000000000000000, 0.000000000000000000 ) ) ;
#39518=AXIS2_PLACEMENT_3D ( 'NONE', #236680, #200144, #197559 ) ;
#39525=CARTESIAN_POINT ( 'NONE',  ( -18.59999999999999787, -9.499999999988849808, -108.6000000000000227 ) ) ;
#39536=DIRECTION ( 'NONE',  ( 1.000000000000000000, -0.000000000000000000, -0.000000000000000000 ) ) ;
#39551=TOROIDAL_SURFACE ( 'NONE', #226954, 0.9750000000000019762, 0.1000000000000000056 ) ;
#39576=ORIENTED_EDGE ( 'NONE', *, *, #159199, .T. ) ;
#39597=DIRECTION ( 'NONE',  ( -1.000000000000000000, -0.000000000000000000, 0.000000000000000000 ) ) ;
#39601=EDGE_LOOP ( 'NONE', ( #100469, #50117, #78629, #178357 ) ) ;
#39610=EDGE_CURVE ( 'NONE', #131734, #7066, #178097, .T. ) ;
#39631=VECTOR ( 'NONE', #15749, 1000.000000000000000 ) ;
#39682=DIRECTION ( 'NONE',  ( 0.000000000000000000, -1.000000000000000000, 0.000000000000000000 ) ) ;
#39687=CIRCLE ( 'NONE', #27227, 0.1000000000000021289 ) ;
#39688=EDGE_CURVE ( 'NONE', #96459, #104969, #148875, .T. ) ;
#39689=CARTESIAN_POINT ( 'NONE',  ( 21.05000000000000071, 0.03201369319892944515, -94.24115727646220364 ) ) ;
#39717=CIRCLE ( 'NONE', #85428, 0.1000000000000000472 ) ;
#39751=CYLINDRICAL_SURFACE ( 'NONE', #61490, 0.1000000000000028644 ) ;
#39753=CARTESIAN_POINT ( 'NONE',  ( 21.04999999999999716, -0.08561306079281386094, -94.08624026618971925 ) ) ;
#39756=EDGE_LOOP ( 'NONE', ( #95402, #218047, #208242, #56597 ) ) ;
#39790=CARTESIAN_POINT ( 'NONE',  ( 21.05000000000000071, 1.115650877919449575E-11, -129.9000000000000341 ) ) ;
#39812=VERTEX_POINT ( 'NONE', #143977 ) ;
#39824=ORIENTED_EDGE ( 'NONE', *, *, #158554, .T. ) ;
#39850=CARTESIAN_POINT ( 'NONE',  ( 20.94999999999999929, 1.115600667400684642E-11, -134.0000000000000284 ) ) ;
#39886=EDGE_CURVE ( 'NONE', #7281, #129441, #4468, .T. ) ;
#39889=DIRECTION ( 'NONE',  ( 1.000000000000000000, 0.000000000000000000, -0.000000000000000000 ) ) ;
#39930=CARTESIAN_POINT ( 'NONE',  ( -20.54999999999999716, 2.500000000011156409, -113.7246219227621395 ) ) ;
#39937=DIRECTION ( 'NONE',  ( -1.000000000000000000, 0.000000000000000000, 0.000000000000000000 ) ) ;
#39955=EDGE_CURVE ( 'NONE', #164361, #27007, #115731, .T. ) ;
#39960=LINE ( 'NONE', #199003, #103175 ) ;
#39977=CARTESIAN_POINT ( 'NONE',  ( 19.94784844284930969, 11.71308993304057999, -125.2021987172991260 ) ) ;
#40002=DIRECTION ( 'NONE',  ( 0.000000000000000000, 0.000000000000000000, -1.000000000000000000 ) ) ;
#40007=DIRECTION ( 'NONE',  ( -1.000000000000000000, -0.000000000000000000, -0.000000000000000000 ) ) ;
#40020=AXIS2_PLACEMENT_3D ( 'NONE', #75080, #55445, #129869 ) ;
#40034=DIRECTION ( 'NONE',  ( 0.000000000000000000, 0.000000000000000000, -1.000000000000000000 ) ) ;
#40048=CARTESIAN_POINT ( 'NONE',  ( -23.15000000000000213, 1.115600667400684642E-11, -104.5500000000000256 ) ) ;
#40113=CYLINDRICAL_SURFACE ( 'NONE', #96393, 0.1000000000000028644 ) ;
#40130=ORIENTED_EDGE ( 'NONE', *, *, #23536, .F. ) ;
#40148=CIRCLE ( 'NONE', #169345, 0.09999999999999939493 ) ;
#40155=FACE_OUTER_BOUND ( 'NONE', #117662, .T. ) ;
#40189=VECTOR ( 'NONE', #150661, 1000.000000000000000 ) ;
#40212=DIRECTION ( 'NONE',  ( -1.000000000000000000, -0.000000000000000000, -0.000000000000000000 ) ) ;
#40240=ORIENTED_EDGE ( 'NONE', *, *, #209427, .F. ) ;
#40241=CARTESIAN_POINT ( 'NONE',  ( 20.94999999999999929, 5.000000000011153745, -121.5947339810869465 ) ) ;
#40253=FACE_OUTER_BOUND ( 'NONE', #93501, .T. ) ;
#40264=MECHANICAL_DESIGN_GEOMETRIC_PRESENTATION_REPRESENTATION('',(#231784),#161039);
#40276=CARTESIAN_POINT ( 'NONE',  ( 18.59999999999999076, 10.49142135624846439, -125.3500000000000512 ) ) ;
#40278=VECTOR ( 'NONE', #102111, 1000.000000000000000 ) ;
#40285=ORIENTED_EDGE ( 'NONE', *, *, #16079, .T. ) ;
#40295=CYLINDRICAL_SURFACE ( 'NONE', #73827, 0.09999999999999939493 ) ;
#40298=ORIENTED_EDGE ( 'NONE', *, *, #107879, .F. ) ;
#40300=DIRECTION ( 'NONE',  ( 0.000000000000000000, 0.000000000000000000, 1.000000000000000000 ) ) ;
#40304=VERTEX_POINT ( 'NONE', #88824 ) ;
#40322=VECTOR ( 'NONE', #210785, 1000.000000000000000 ) ;
#40332=CIRCLE ( 'NONE', #57008, 0.09999999999998898659 ) ;
#40349=AXIS2_PLACEMENT_3D ( 'NONE', #89954, #147371, #108251 ) ;
#40361=CARTESIAN_POINT ( 'NONE',  ( -20.94999999999999929, -1.360870587180885716, -108.5729979270909951 ) ) ;
#40370=CARTESIAN_POINT ( 'NONE',  ( -23.15000000000000213, 11.75000000001115552, -130.9000000000000341 ) ) ;
#40396=DIRECTION ( 'NONE',  ( 1.000000000000000000, 2.952720810173289112E-16, -0.000000000000000000 ) ) ;
#40408=ORIENTED_EDGE ( 'NONE', *, *, #70623, .F. ) ;
#40417=DIRECTION ( 'NONE',  ( 1.000000000000000000, -0.000000000000000000, -0.000000000000000000 ) ) ;
#40420=DIRECTION ( 'NONE',  ( -0.000000000000000000, 1.000000000000000000, 0.000000000000000000 ) ) ;
#40440=AXIS2_PLACEMENT_3D ( 'NONE', #99953, #119568, #240785 ) ;
#40455=AXIS2_PLACEMENT_3D ( 'NONE', #250824, #151765, #116471 ) ;
#40485=CARTESIAN_POINT ( 'NONE',  ( 21.05000000000000071, 8.776282889879928106, -112.6762151410681696 ) ) ;
#40511=CARTESIAN_POINT ( 'NONE',  ( -22.50047199487802274, 0.04490605193189570188, -88.74995258108347684 ) ) ;
#40527=DIRECTION ( 'NONE',  ( -0.000000000000000000, 1.000000000000000000, -0.000000000000000000 ) ) ;
#40562=CARTESIAN_POINT ( 'NONE',  ( -21.05000000000000071, 1.835341550235567887, -112.0551512925630249 ) ) ;
#40568=EDGE_CURVE ( 'NONE', #81511, #10689, #153559, .T. ) ;
#40571=ORIENTED_EDGE ( 'NONE', *, *, #126182, .T. ) ;
#40594=ORIENTED_EDGE ( 'NONE', *, *, #155929, .T. ) ;
#40606=CARTESIAN_POINT ( 'NONE',  ( -21.05000000000000071, -11.64999999998884483, -103.5000000000000426 ) ) ;
#40616=EDGE_CURVE ( 'NONE', #163148, #138064, #41736, .T. ) ;
#40640=ADVANCED_FACE ( 'NONE', ( #19595 ), #99091, .F. ) ;
#40663=CIRCLE ( 'NONE', #98833, 0.2000000000000057288 ) ;
#40667=CARTESIAN_POINT ( 'NONE',  ( -21.07954763557533084, 0.06587591862964220502, -94.17070900996139926 ) ) ;
#40701=DIRECTION ( 'NONE',  ( -0.000000000000000000, 0.000000000000000000, 1.000000000000000000 ) ) ;
#40717=ORIENTED_EDGE ( 'NONE', *, *, #27317, .F. ) ;
#40753=CARTESIAN_POINT ( 'NONE',  ( -20.85000000000000142, 1.115600667400684642E-11, -134.0000000000000284 ) ) ;
#40756=DIRECTION ( 'NONE',  ( -0.000000000000000000, 0.000000000000000000, 1.000000000000000000 ) ) ;
#40759=VERTEX_POINT ( 'NONE', #245050 ) ;
#40844=ORIENTED_EDGE ( 'NONE', *, *, #51324, .T. ) ;
#40861=CARTESIAN_POINT ( 'NONE',  ( -21.07094088545368749, 0.09889370256337755294, -94.17983277808291120 ) ) ;
#40865=ORIENTED_EDGE ( 'NONE', *, *, #218623, .F. ) ;
#40869=VERTEX_POINT ( 'NONE', #170700 ) ;
#40881=CARTESIAN_POINT ( 'NONE',  ( -20.94999999999999929, -1.162701749926853712, -108.6000000000000227 ) ) ;
#40906=ORIENTED_EDGE ( 'NONE', *, *, #18394, .T. ) ;
#40911=EDGE_CURVE ( 'NONE', #53303, #213938, #87018, .T. ) ;
#40927=CARTESIAN_POINT ( 'NONE',  ( -20.54999999999999716, 4.250000000011156409, -112.8500000000000369 ) ) ;
#40933=ADVANCED_FACE ( 'NONE', ( #139192 ), #157546, .F. ) ;
#40953=VERTEX_POINT ( 'NONE', #120968 ) ;
#40984=VERTEX_POINT ( 'NONE', #77948 ) ;
#41015=ORIENTED_EDGE ( 'NONE', *, *, #13996, .F. ) ;
#41029=CARTESIAN_POINT ( 'NONE',  ( 21.05000000000000071, 0.09779029131994770863, -94.24218538952391100 ) ) ;
#41046=CARTESIAN_POINT ( 'NONE',  ( -22.57848426163147693, -0.004264329271961095000, -88.74994169310971870 ) ) ;
#41052=EDGE_CURVE ( 'NONE', #240102, #182294, #257673, .T. ) ;
#41081=CARTESIAN_POINT ( 'NONE',  ( 22.59999999999999432, 11.74956712350054566, -100.3991416309013260 ) ) ;
#41104=ADVANCED_FACE ( 'NONE', ( #7398, #45253 ), #148201, .F. ) ;
#41130=AXIS2_PLACEMENT_3D ( 'NONE', #154607, #213250, #34651 ) ;
#41188=ORIENTED_EDGE ( 'NONE', *, *, #37645, .T. ) ;
#41194=VERTEX_POINT ( 'NONE', #71260 ) ;
#41230=DIRECTION ( 'NONE',  ( -1.000000000000000000, 0.000000000000000000, 0.000000000000000000 ) ) ;
#41252=CARTESIAN_POINT ( 'NONE',  ( -18.59999999999999787, 1.637172712981537659, -112.0821533654720525 ) ) ;
#41273=CARTESIAN_POINT ( 'NONE',  ( -22.39999999999999858, 7.790779598384560245, -100.4000000000000341 ) ) ;
#41283=CIRCLE ( 'NONE', #7953, 7.899999999999990585 ) ;
#41297=ORIENTED_EDGE ( 'NONE', *, *, #214017, .F. ) ;
#41313=CARTESIAN_POINT ( 'NONE',  ( 18.59999999999999076, -1.835859311432481045, -145.5044391687985694 ) ) ;
#41319=ORIENTED_EDGE ( 'NONE', *, *, #235985, .F. ) ;
#41356=AXIS2_PLACEMENT_3D ( 'NONE', #143328, #24703, #202033 ) ;
#41363=DIRECTION ( 'NONE',  ( 0.000000000000000000, -1.000000000000000000, 0.000000000000000000 ) ) ;
#41371=EDGE_CURVE ( 'NONE', #62504, #164965, #238001, .T. ) ;
#41381=DIRECTION ( 'NONE',  ( 0.000000000000000000, 0.000000000000000000, 1.000000000000000000 ) ) ;
#41440=ADVANCED_FACE ( 'NONE', ( #44956 ), #3234, .T. ) ;
#41444=ORIENTED_EDGE ( 'NONE', *, *, #64035, .F. ) ;
#41456=DIRECTION ( 'NONE',  ( 0.000000000000000000, 0.000000000000000000, -1.000000000000000000 ) ) ;
#41462=ORIENTED_EDGE ( 'NONE', *, *, #172685, .F. ) ;
#41477=DIRECTION ( 'NONE',  ( 0.000000000000000000, 1.224646799142015331E-16, 1.000000000000000000 ) ) ;
#41503=DIRECTION ( 'NONE',  ( -0.7071067811865474617, -0.7071067811865474617, -0.000000000000000000 ) ) ;
#41508=VECTOR ( 'NONE', #62837, 1000.000000000000000 ) ;
#41602=ORIENTED_EDGE ( 'NONE', *, *, #63015, .F. ) ;
#41647=ORIENTED_EDGE ( 'NONE', *, *, #162049, .F. ) ;
#41681=CARTESIAN_POINT ( 'NONE',  ( -18.59999999999999787, -1.835341550213255957, -112.0551512925630107 ) ) ;
#41689=DIRECTION ( 'NONE',  ( 1.000000000000000000, 0.000000000000000000, 0.000000000000000000 ) ) ;
#41702=DIRECTION ( 'NONE',  ( 0.000000000000000000, 0.000000000000000000, -1.000000000000000000 ) ) ;
#41736=LINE ( 'NONE', #82093, #220150 ) ;
#41788=ORIENTED_EDGE ( 'NONE', *, *, #84327, .F. ) ;
#41875=ORIENTED_EDGE ( 'NONE', *, *, #112567, .T. ) ;
#41888=CARTESIAN_POINT ( 'NONE',  ( 20.94999999999999929, 1.115624548013267999E-11, -132.1000000000000227 ) ) ;
#41932=CARTESIAN_POINT ( 'NONE',  ( -23.15000000000000213, -8.663551401858004652, -110.0241011180673354 ) ) ;
#41938=TOROIDAL_SURFACE ( 'NONE', #79298, 0.2000000000000000111, 0.1000000000000000056 ) ;
#41947=CARTESIAN_POINT ( 'NONE',  ( 20.94999999999999929, 5.400000000011154988, -124.1060308773475924 ) ) ;
#42002=ORIENTED_EDGE ( 'NONE', *, *, #119535, .F. ) ;
#42061=DIRECTION ( 'NONE',  ( 0.7071067811865388020, -0.7071067811865561215, 0.000000000000000000 ) ) ;
#42062=AXIS2_PLACEMENT_3D ( 'NONE', #134998, #35947, #5764 ) ;
#42079=ADVANCED_FACE ( 'NONE', ( #241990 ), #676, .T. ) ;
#42086=CIRCLE ( 'NONE', #79634, 0.2000000000000057288 ) ;
#42101=EDGE_CURVE ( 'NONE', #23723, #131609, #25529, .T. ) ;
#42110=CARTESIAN_POINT ( 'NONE',  ( -21.14999999999999858, 11.75000000001115552, -107.2838656629781866 ) ) ;
#42133=CARTESIAN_POINT ( 'NONE',  ( -22.00411653889212005, 0.09903810579721090968, -93.24655713235959809 ) ) ;
#42173=EDGE_CURVE ( 'NONE', #79959, #239049, #189728, .T. ) ;
#42187=CARTESIAN_POINT ( 'NONE',  ( 21.09316766718127667, 6.370153312485567376, -100.4607365976853401 ) ) ;
#42194=CARTESIAN_POINT ( 'NONE',  ( 23.24999999999999645, 1.115600667400684642E-11, -100.5000000000000284 ) ) ;
#42195=ORIENTED_EDGE ( 'NONE', *, *, #82631, .F. ) ;
#42198=EDGE_CURVE ( 'NONE', #80403, #62956, #3833, .T. ) ;
#42199=DIRECTION ( 'NONE',  ( -1.000000000000000000, 0.000000000000000000, 0.000000000000000000 ) ) ;
#42258=DIRECTION ( 'NONE',  ( 3.469446951953243109E-14, 0.4999999999999608646, 0.8660254037844612451 ) ) ;
#42265=CARTESIAN_POINT ( 'NONE',  ( 18.59999999999999076, 6.650000000011155876, -121.6500000000000341 ) ) ;
#42275=CARTESIAN_POINT ( 'NONE',  ( -21.45000000000000284, 7.708578643773852157, -112.8500000000000369 ) ) ;
#42282=B_SPLINE_CURVE_WITH_KNOTS ( 'NONE', 3,
 ( #44992, #183222, #81507, #60675, #161097, #201480, #243176, #178099, #99792, #43705 ),
 .UNSPECIFIED., .F., .F.,
 ( 4, 3, 3, 4 ),
 ( 0.000000000000000000, 0.0002000000000008585893, 0.001000000000082977483, 0.001967863649483336721 ),
 .UNSPECIFIED. ) ;
#42305=EDGE_CURVE ( 'NONE', #41194, #126005, #249553, .T. ) ;
#42320=CARTESIAN_POINT ( 'NONE',  ( -23.25000000000000000, -11.64999999998884483, -103.6000000000000369 ) ) ;
#42324=CARTESIAN_POINT ( 'NONE',  ( 20.95545211741311320, 10.58641331155510379, -108.0861468595883252 ) ) ;
#42348=CARTESIAN_POINT ( 'NONE',  ( 20.94999999999999929, 1.115600667400684642E-11, -134.0000000000000284 ) ) ;
#42349=EDGE_CURVE ( 'NONE', #114076, #149886, #124636, .T. ) ;
#42351=EDGE_LOOP ( 'NONE', ( #143890, #192807, #248057, #54736 ) ) ;
#42369=LINE ( 'NONE', #104866, #200058 ) ;
#42389=CARTESIAN_POINT ( 'NONE',  ( -18.59999999999999787, 11.65000000001115232, -112.6500000000000341 ) ) ;
#42409=DIRECTION ( 'NONE',  ( 1.000000000000000000, 1.836970198721029934E-16, 0.000000000000000000 ) ) ;
#42436=CIRCLE ( 'NONE', #150595, 0.09999999999999939493 ) ;
#42449=EDGE_CURVE ( 'NONE', #234552, #221499, #166185, .T. ) ;
#42494=DIRECTION ( 'NONE',  ( 0.000000000000000000, 0.9908441862701596881, 0.1350103645451904977 ) ) ;
#42500=CARTESIAN_POINT ( 'NONE',  ( 19.75857864376269291, 11.65000000001116476, -125.2500000000000568 ) ) ;
#42530=AXIS2_PLACEMENT_3D ( 'NONE', #42320, #236657, #121868 ) ;
#42542=CARTESIAN_POINT ( 'NONE',  ( 21.05000000000000071, 1.115600667400684642E-11, -100.5000000000000284 ) ) ;
#42551=ORIENTED_EDGE ( 'NONE', *, *, #255603, .T. ) ;
#42577=EDGE_CURVE ( 'NONE', #257618, #79905, #211238, .T. ) ;
#42583=DIRECTION ( 'NONE',  ( 0.000000000000000000, 0.000000000000000000, 1.000000000000000000 ) ) ;
#42651=DIRECTION ( 'NONE',  ( -1.000000000000000000, -0.000000000000000000, -0.000000000000000000 ) ) ;
#42654=CARTESIAN_POINT ( 'NONE',  ( 22.50000000000000000, 7.750000000011162626, -100.4000000000000341 ) ) ;
#42655=LINE ( 'NONE', #158788, #147305 ) ;
#42676=EDGE_CURVE ( 'NONE', #45367, #12292, #228870, .T. ) ;
#42755=AXIS2_PLACEMENT_3D ( 'NONE', #222933, #2603, #242506 ) ;
#42773=ORIENTED_EDGE ( 'NONE', *, *, #115097, .T. ) ;
#42780=ADVANCED_FACE ( 'NONE', ( #213803 ), #62271, .T. ) ;
#42790=EDGE_CURVE ( 'NONE', #14749, #243821, #189530, .T. ) ;
#42807=EDGE_CURVE ( 'NONE', #249313, #197578, #84511, .T. ) ;
#42808=ORIENTED_EDGE ( 'NONE', *, *, #204639, .T. ) ;
#42812=AXIS2_PLACEMENT_3D ( 'NONE', #191052, #12412, #213149 ) ;
#42825=CARTESIAN_POINT ( 'NONE',  ( -22.50000000000000000, 1.115600667400684642E-11, -100.5000000000000284 ) ) ;
#42833=FACE_OUTER_BOUND ( 'NONE', #73963, .T. ) ;
#42839=CARTESIAN_POINT ( 'NONE',  ( -18.59999999999999787, -1.135018845899022466, -141.7169768834323520 ) ) ;
#42853=DIRECTION ( 'NONE',  ( 1.000000000000000000, 0.000000000000000000, -0.000000000000000000 ) ) ;
#42873=DIRECTION ( 'NONE',  ( 1.000000000000000000, 0.000000000000000000, 0.000000000000000000 ) ) ;
#42875=DIRECTION ( 'NONE',  ( 0.000000000000000000, -1.000000000000000000, 0.000000000000000000 ) ) ;
#42891=AXIS2_PLACEMENT_3D ( 'NONE', #7564, #104070, #204468 ) ;
#42900=AXIS2_PLACEMENT_3D ( 'NONE', #33044, #94241, #173843 ) ;
#42903=DIRECTION ( 'NONE',  ( -0.000000000000000000, -0.000000000000000000, -1.000000000000000000 ) ) ;
#42920=PLANE ( 'NONE',  #250492 ) ;
#42924=DIRECTION ( 'NONE',  ( 0.000000000000000000, -1.000000000000000000, 0.000000000000000000 ) ) ;
#42930=VECTOR ( 'NONE', #118133, 1000.000000000000000 ) ;
#42942=CIRCLE ( 'NONE', #201150, 0.1000000000000000472 ) ;
#42944=CARTESIAN_POINT ( 'NONE',  ( -20.94999999999999929, 5.900000000011162093, -123.7809002353436654 ) ) ;
#42961=DIRECTION ( 'NONE',  ( -1.000000000000000000, 0.000000000000000000, 0.000000000000000000 ) ) ;
#42967=ORIENTED_EDGE ( 'NONE', *, *, #216949, .F. ) ;
#42968=DIRECTION ( 'NONE',  ( 0.000000000000000000, 0.000000000000000000, -1.000000000000000000 ) ) ;
#42979=DIRECTION ( 'NONE',  ( 1.000000000000000000, 1.734723475976817507E-14, 0.000000000000000000 ) ) ;
#43017=AXIS2_PLACEMENT_3D ( 'NONE', #244375, #7054, #1904 ) ;
#43020=CARTESIAN_POINT ( 'NONE',  ( 21.05000000000000071, 8.776282895303626930, -112.6500000000000341 ) ) ;
#43034=ORIENTED_EDGE ( 'NONE', *, *, #147994, .F. ) ;
#43055=CARTESIAN_POINT ( 'NONE',  ( -21.05000000000000071, 11.60000000001115517, -127.0717967697245143 ) ) ;
#43076=AXIS2_PLACEMENT_3D ( 'NONE', #57916, #120509, #1796 ) ;
#43080=CARTESIAN_POINT ( 'NONE',  ( -21.45000000000000284, 7.708578643773852157, -121.6500000000000341 ) ) ;
#43087=ORIENTED_EDGE ( 'NONE', *, *, #140996, .T. ) ;
#43143=CARTESIAN_POINT ( 'NONE',  ( 18.46082813847998949, -9.480749650896306946, -107.5843701027156811 ) ) ;
#43209=DIRECTION ( 'NONE',  ( 1.000000000000000000, 0.000000000000000000, 0.000000000000000000 ) ) ;
#43222=CARTESIAN_POINT ( 'NONE',  ( 22.42357213249528769, 7.672932386371071445, -100.4009130359984709 ) ) ;
#43256=CARTESIAN_POINT ( 'NONE',  ( -23.25000000000000000, -8.999999999988844479, -124.1060308773475924 ) ) ;
#43272=FACE_OUTER_BOUND ( 'NONE', #34742, .T. ) ;
#43296=EDGE_CURVE ( 'NONE', #182032, #129536, #105193, .T. ) ;
#43305=CARTESIAN_POINT ( 'NONE',  ( -23.15000000000000213, 11.75000000001116263, -112.6500000000000341 ) ) ;
#43307=CARTESIAN_POINT ( 'NONE',  ( 20.85000000000000142, 7.070967871809997973, -137.7465642218683399 ) ) ;
#43315=ORIENTED_EDGE ( 'NONE', *, *, #197340, .T. ) ;
#43348=EDGE_CURVE ( 'NONE', #204472, #103006, #91951, .T. ) ;
#43350=EDGE_CURVE ( 'NONE', #127135, #53973, #107330, .T. ) ;
#43376=CARTESIAN_POINT ( 'NONE',  ( -21.14999999999999503, 11.75000000001115019, -107.4191472459587828 ) ) ;
#43382=DIRECTION ( 'NONE',  ( 0.000000000000000000, -1.000000000000000000, 0.000000000000000000 ) ) ;
#43391=VERTEX_POINT ( 'NONE', #128520 ) ;
#43397=CARTESIAN_POINT ( 'NONE',  ( 22.45463910399148233, 1.026727559903827464E-11, -88.85042918981690718 ) ) ;
#43405=VERTEX_POINT ( 'NONE', #136179 ) ;
#43430=AXIS2_PLACEMENT_3D ( 'NONE', #253757, #136356, #38581 ) ;
#43439=ORIENTED_EDGE ( 'NONE', *, *, #1658, .F. ) ;
#43453=CARTESIAN_POINT ( 'NONE',  ( -21.05000000000000071, -11.29603075032412463, -130.9521008403361861 ) ) ;
#43528=EDGE_CURVE ( 'NONE', #177002, #97776, #83456, .T. ) ;
#43537=DIRECTION ( 'NONE',  ( 0.000000000000000000, 0.000000000000000000, -1.000000000000000000 ) ) ;
#43545=CARTESIAN_POINT ( 'NONE',  ( -23.15000000000000213, 11.65000000001115588, -126.9851942293460922 ) ) ;
#43551=VERTEX_POINT ( 'NONE', #60510 ) ;
#43573=AXIS2_PLACEMENT_3D ( 'NONE', #20228, #61915, #218393 ) ;
#43580=DIRECTION ( 'NONE',  ( 0.000000000000000000, 0.1568667991644863147, -0.9876197685951252359 ) ) ;
#43674=CIRCLE ( 'NONE', #135416, 0.09999999999999939493 ) ;
#43702=EDGE_CURVE ( 'NONE', #213681, #149981, #225109, .T. ) ;
#43705=CARTESIAN_POINT ( 'NONE',  ( -22.47071067811865319, 7.720074744509219933, -100.4009075452974287 ) ) ;
#43749=ORIENTED_EDGE ( 'NONE', *, *, #229863, .F. ) ;
#43763=CARTESIAN_POINT ( 'NONE',  ( 21.04999999999963478, 10.54375127550701485, -108.0563878086650789 ) ) ;
#43785=ORIENTED_EDGE ( 'NONE', *, *, #242760, .T. ) ;
#43828=AXIS2_PLACEMENT_3D ( 'NONE', #103294, #104569, #168481 ) ;
#43872=ORIENTED_EDGE ( 'NONE', *, *, #3752, .T. ) ;
#43901=CARTESIAN_POINT ( 'NONE',  ( -21.29999999999995808, 1.115600667400684642E-11, -104.5500000000000256 ) ) ;
#43945=EDGE_CURVE ( 'NONE', #56434, #126637, #221021, .T. ) ;
#43951=ORIENTED_EDGE ( 'NONE', *, *, #223325, .T. ) ;
#43960=LINE ( 'NONE', #158804, #100288 ) ;
#43976=AXIS2_PLACEMENT_3D ( 'NONE', #89595, #252518, #32231 ) ;
#44000=ORIENTED_EDGE ( 'NONE', *, *, #200424, .F. ) ;
#44010=DIRECTION ( 'NONE',  ( 1.000000000000000000, -0.000000000000000000, -0.000000000000000000 ) ) ;
#44036=CARTESIAN_POINT ( 'NONE',  ( -18.49372193242239959, -9.442484523346882597, -140.7647812600350505 ) ) ;
#44074=CARTESIAN_POINT ( 'NONE',  ( 22.39999999999999503, 1.115600667400684642E-11, -88.85042919245522341 ) ) ;
#44084=CARTESIAN_POINT ( 'NONE',  ( -18.50000000000000000, 1.866714910068465239, -112.2526752462820525 ) ) ;
#44139=FACE_OUTER_BOUND ( 'NONE', #155613, .T. ) ;
#44144=CARTESIAN_POINT ( 'NONE',  ( 23.14999999999998437, -11.74999999998884448, -100.5000000000000284 ) ) ;
#44183=DIRECTION ( 'NONE',  ( -0.000000000000000000, -0.000000000000000000, 1.000000000000000000 ) ) ;
#44188=DIRECTION ( 'NONE',  ( -1.000000000000000000, 0.000000000000000000, 0.000000000000000000 ) ) ;
#44208=VECTOR ( 'NONE', #103974, 1000.000000000000000 ) ;
#44240=DIRECTION ( 'NONE',  ( 0.000000000000000000, 0.000000000000000000, -1.000000000000000000 ) ) ;
#44241=DIRECTION ( 'NONE',  ( 0.000000000000000000, 1.000000000000000000, -1.224646799147353207E-16 ) ) ;
#44258=LINE ( 'NONE', #143337, #85854 ) ;
#44288=LINE ( 'NONE', #65115, #109900 ) ;
#44300=VECTOR ( 'NONE', #120142, 1000.000000000000000 ) ;
#44325=DIRECTION ( 'NONE',  ( 0.000000000000000000, 0.000000000000000000, 1.000000000000000000 ) ) ;
#44369=ADVANCED_FACE ( 'NONE', ( #183403 ), #125980, .F. ) ;
#44371=CARTESIAN_POINT ( 'NONE',  ( -21.14999999999999858, 11.75000000001115552, -100.6000000000000369 ) ) ;
#44397=DIRECTION ( 'NONE',  ( 0.000000000000000000, 0.000000000000000000, -1.000000000000000000 ) ) ;
#44401=EDGE_LOOP ( 'NONE', ( #149393, #59549, #55896 ) ) ;
#44419=ORIENTED_EDGE ( 'NONE', *, *, #159199, .F. ) ;
#44429=DIRECTION ( 'NONE',  ( 1.000000000000000000, 0.000000000000000000, 0.000000000000000000 ) ) ;
#44430=FACE_OUTER_BOUND ( 'NONE', #207425, .T. ) ;
#44432=ADVANCED_FACE ( 'NONE', ( #29494 ), #247208, .F. ) ;
#44449=VERTEX_POINT ( 'NONE', #148124 ) ;
#44466=EDGE_CURVE ( 'NONE', #107194, #151151, #154797, .T. ) ;
#44476=ORIENTED_EDGE ( 'NONE', *, *, #87882, .F. ) ;
#44484=AXIS2_PLACEMENT_3D ( 'NONE', #33888, #114658, #14303 ) ;
#44496=DIRECTION ( 'NONE',  ( 0.000000000000000000, 0.000000000000000000, 1.000000000000000000 ) ) ;
#44502=AXIS2_PLACEMENT_3D ( 'NONE', #71197, #42961, #230245 ) ;
#44518=VECTOR ( 'NONE', #11989, 1000.000000000000000 ) ;
#44519=DIRECTION ( 'NONE',  ( -1.000000000000000000, 0.000000000000000000, 0.000000000000000000 ) ) ;
#44521=ORIENTED_EDGE ( 'NONE', *, *, #71062, .F. ) ;
#44525=ORIENTED_EDGE ( 'NONE', *, *, #3196, .T. ) ;
#44545=ORIENTED_EDGE ( 'NONE', *, *, #61847, .T. ) ;
#44554=CARTESIAN_POINT ( 'NONE',  ( 23.14999999999999503, 11.65000000001116298, -112.6500000000000341 ) ) ;
#44559=DIRECTION ( 'NONE',  ( -1.000000000000000000, -7.304098846218134667E-16, 0.000000000000000000 ) ) ;
#44583=DIRECTION ( 'NONE',  ( 0.000000000000000000, -2.428612866367527723E-14, -1.000000000000000000 ) ) ;
#44602=ORIENTED_EDGE ( 'NONE', *, *, #82280, .F. ) ;
#44678=PRODUCT_DEFINITION_FORMATION_WITH_SPECIFIED_SOURCE ( 'ANY', '', #209720, .NOT_KNOWN. ) ;
#44680=ORIENTED_EDGE ( 'NONE', *, *, #175671, .F. ) ;
#44730=FACE_OUTER_BOUND ( 'NONE', #77515, .T. ) ;
#44735=AXIS2_PLACEMENT_3D ( 'NONE', #4027, #83534, #242632 ) ;
#44753=CARTESIAN_POINT ( 'NONE',  ( 21.08078803292165659, 6.333012964448271553, -100.4208140128422571 ) ) ;
#44814=VECTOR ( 'NONE', #190915, 1000.000000000000000 ) ;
#44824=( BOUNDED_SURFACE ( )  B_SPLINE_SURFACE ( 3, 2, ( 
 ( #210781, #189940, #11303 ),
 ( #248622, #72574, #32170 ),
 ( #208234, #90817, #28333 ),
 ( #50397, #171690, #112972 ) ),
 .UNSPECIFIED., .F., .F., .F. ) 
 B_SPLINE_SURFACE_WITH_KNOTS ( ( 4, 4 ),
 ( 3, 3 ),
 ( 0.0002700421466196717673, 0.0004789321604330994782 ),
 ( 0.000000000000000000, 1.000000000000000000 ),
 .UNSPECIFIED. ) 
 GEOMETRIC_REPRESENTATION_ITEM ( )  RATIONAL_B_SPLINE_SURFACE ( (
 ( 1.000000000000000000, 0.7071067811865475727, 1.000000000000000000),
 ( 1.000000000000000000, 0.7163411249511767442, 1.000000000000000000),
 ( 1.000000000000000000, 0.7221957104841900676, 1.000000000000000000),
 ( 1.000000000000000000, 0.7250110520819876836, 1.000000000000000000) ) ) 
 REPRESENTATION_ITEM ( '' )  SURFACE ( )  );
#44858=AXIS2_PLACEMENT_3D ( 'NONE', #235244, #37081, #256038 ) ;
#44872=CARTESIAN_POINT ( 'NONE',  ( -20.94999999999999929, 14.05000000001115623, -106.0136950707610310 ) ) ;
#44893=CARTESIAN_POINT ( 'NONE',  ( 23.14999999999999858, 4.775700934590591196, -122.1512318959540693 ) ) ;
#44918=ORIENTED_EDGE ( 'NONE', *, *, #49663, .F. ) ;
#44930=CARTESIAN_POINT ( 'NONE',  ( -22.16821283564876666, 7.558973340791935058, -100.5000000000000284 ) ) ;
#44956=FACE_OUTER_BOUND ( 'NONE', #48553, .T. ) ;
#44965=EDGE_CURVE ( 'NONE', #66771, #153726, #250811, .T. ) ;
#44992=CARTESIAN_POINT ( 'NONE',  ( -21.07928932188134041, 6.328516656404449492, -100.4011048543456468 ) ) ;
#44995=AXIS2_PLACEMENT_3D ( 'NONE', #30018, #75560, #169546 ) ;
#45016=PLANE ( 'NONE',  #72166 ) ;
#45038=CARTESIAN_POINT ( 'NONE',  ( 23.15000000000000213, -8.663551401858002876, -110.0241011180673354 ) ) ;
#45057=DIRECTION ( 'NONE',  ( 0.000000000000000000, 0.000000000000000000, -1.000000000000000000 ) ) ;
#45073=CYLINDRICAL_SURFACE ( 'NONE', #240999, 0.09999999999999939493 ) ;
#45076=CARTESIAN_POINT ( 'NONE',  ( 19.97071067695831559, 11.72071067696947644, -125.1762534328032217 ) ) ;
#45083=DIRECTION ( 'NONE',  ( 0.000000000000000000, 0.2605042016806672911, -0.9654727137038716656 ) ) ;
#45089=CARTESIAN_POINT ( 'NONE',  ( 20.22894356738321164, 9.278498222849551169, -108.7685229062446552 ) ) ;
#45103=CARTESIAN_POINT ( 'NONE',  ( -22.00356870142647026, 7.254242362488315443, -100.5000000000000426 ) ) ;
#45105=ADVANCED_FACE ( 'NONE', ( #221883 ), #109324, .F. ) ;
#45113=AXIS2_PLACEMENT_3D ( 'NONE', #58472, #138015, #3651 ) ;
#45114=ORIENTED_EDGE ( 'NONE', *, *, #189441, .T. ) ;
#45115=VERTEX_POINT ( 'NONE', #182808 ) ;
#45126=CARTESIAN_POINT ( 'NONE',  ( -20.90851465518105812, 10.32532329027886320, -139.5699343018359855 ) ) ;
#45137=CARTESIAN_POINT ( 'NONE',  ( 20.95512820512820440, 10.62384868372303615, -108.1649135690876449 ) ) ;
#45151=CIRCLE ( 'NONE', #165799, 11.75000000000001066 ) ;
#45168=EDGE_CURVE ( 'NONE', #155920, #90910, #221561, .T. ) ;
#45221=DIRECTION ( 'NONE',  ( 0.000000000000000000, 0.000000000000000000, -1.000000000000000000 ) ) ;
#45253=FACE_OUTER_BOUND ( 'NONE', #193239, .T. ) ;
#45283=CARTESIAN_POINT ( 'NONE',  ( 20.85000000000000142, -11.74999999998883560, -131.0000000000000284 ) ) ;
#45306=ORIENTED_EDGE ( 'NONE', *, *, #22318, .T. ) ;
#45317=CARTESIAN_POINT ( 'NONE',  ( -18.44204374631830845, -9.491036389587215183, -140.6262012702210598 ) ) ;
#45340=CIRCLE ( 'NONE', #224405, 0.09999999999999910349 ) ;
#45341=DIRECTION ( 'NONE',  ( -1.000000000000000000, -0.000000000000000000, -0.000000000000000000 ) ) ;
#45350=LINE ( 'NONE', #186147, #56657 ) ;
#45367=VERTEX_POINT ( 'NONE', #105322 ) ;
#45374=ORIENTED_EDGE ( 'NONE', *, *, #161349, .F. ) ;
#45395=EDGE_CURVE ( 'NONE', #131609, #193670, #165344, .T. ) ;
#45421=AXIS2_PLACEMENT_3D ( 'NONE', #152263, #109243, #14022 ) ;
#45438=CARTESIAN_POINT ( 'NONE',  ( -22.49806830649814060, 11.64988965485023620, -100.4225356836745249 ) ) ;
#45473=ADVANCED_FACE ( 'NONE', ( #226575 ), #12711, .T. ) ;
#45488=CARTESIAN_POINT ( 'NONE',  ( -21.44999999999999929, 7.350000000011155166, -121.7500000000000426 ) ) ;
#45530=CARTESIAN_POINT ( 'NONE',  ( 23.14999999999998437, 1.115600667400684642E-11, -100.5000000000000284 ) ) ;
#45581=CARTESIAN_POINT ( 'NONE',  ( 23.24999999999999289, 6.450000000011156587, -88.75000000000004263 ) ) ;
#45591=EDGE_CURVE ( 'NONE', #16939, #233320, #113625, .T. ) ;
#45606=CARTESIAN_POINT ( 'NONE',  ( 18.59999999999999076, 10.20857864377385127, -121.7500000000000426 ) ) ;
#45701=AXIS2_PLACEMENT_3D ( 'NONE', #16368, #175445, #218377 ) ;
#45715=CARTESIAN_POINT ( 'NONE',  ( -20.94999999999999929, 11.75000000001115197, -107.5148057706540357 ) ) ;
#45724=CIRCLE ( 'NONE', #133209, 0.1000000000000028644 ) ;
#45735=CARTESIAN_POINT ( 'NONE',  ( 22.39999999999999503, 1.115600667400684642E-11, -92.70922040162665212 ) ) ;
#45750=DIRECTION ( 'NONE',  ( -0.000000000000000000, 0.8660254037844411501, 0.4999999999999956701 ) ) ;
#45781=ADVANCED_FACE ( 'NONE', ( #172864 ), #88843, .T. ) ;
#45822=CARTESIAN_POINT ( 'NONE',  ( -21.05000000000000071, 1.115600667400684642E-11, -134.0000000000000284 ) ) ;
#45831=CARTESIAN_POINT ( 'NONE',  ( 18.52928932188133970, 10.27928932189250411, -125.1500000000000341 ) ) ;
#45837=EDGE_CURVE ( 'NONE', #27007, #114076, #159976, .T. ) ;
#45902=EDGE_CURVE ( 'NONE', #29706, #209835, #126275, .T. ) ;
#45927=ADVANCED_FACE ( 'NONE', ( #80087 ), #1852, .T. ) ;
#45941=DIRECTION ( 'NONE',  ( 2.952720810173289112E-16, -1.000000000000000000, 0.000000000000000000 ) ) ;
#45947=AXIS2_PLACEMENT_3D ( 'NONE', #127353, #7392, #246021 ) ;
#45950=CARTESIAN_POINT ( 'NONE',  ( 21.00000000000000000, 9.750000000011153745, -112.8500000000000369 ) ) ;
#45974=CARTESIAN_POINT ( 'NONE',  ( -18.39999999999999858, -9.499999999988849808, -107.5320693966997112 ) ) ;
#45995=DIRECTION ( 'NONE',  ( 0.000000000000000000, 0.000000000000000000, -1.000000000000000000 ) ) ;
#46015=DIRECTION ( 'NONE',  ( 0.000000000000000000, -5.204170427930272346E-14, 1.000000000000000000 ) ) ;
#46017=CARTESIAN_POINT ( 'NONE',  ( 21.14250536705908345, 6.518172176891880554, -100.5000000000000284 ) ) ;
#46027=CARTESIAN_POINT ( 'NONE',  ( 21.05000000000000426, 10.56275983746218472, -107.9568139579186692 ) ) ;
#46044=EDGE_CURVE ( 'NONE', #190470, #70151, #113978, .T. ) ;
#46066=CARTESIAN_POINT ( 'NONE',  ( -21.44999999999999929, 7.350000000011155166, -112.8500000000000369 ) ) ;
#46095=EDGE_CURVE ( 'NONE', #197589, #163018, #118081, .T. ) ;
#46099=ORIENTED_EDGE ( 'NONE', *, *, #154278, .T. ) ;
#46113=CARTESIAN_POINT ( 'NONE',  ( -23.15000000000000213, 11.75000000001115552, -88.75000000000004263 ) ) ;
#46127=AXIS2_PLACEMENT_3D ( 'NONE', #112607, #254645, #250818 ) ;
#46137=CARTESIAN_POINT ( 'NONE',  ( 20.94999999999999929, 6.450000000011156587, -110.5170271704400591 ) ) ;
#46142=AXIS2_PLACEMENT_3D ( 'NONE', #123613, #225247, #181030 ) ;
#46147=LINE ( 'NONE', #44872, #38949 ) ;
#46160=DIRECTION ( 'NONE',  ( 0.000000000000000000, -1.000000000000000000, 0.000000000000000000 ) ) ;
#46220=CARTESIAN_POINT ( 'NONE',  ( -18.60000000000000142, -9.321008403350123928, -107.7359382490779325 ) ) ;
#46240=ADVANCED_FACE ( 'NONE', ( #222854 ), #163884, .T. ) ;
#46245=VERTEX_POINT ( 'NONE', #123772 ) ;
#46262=EDGE_LOOP ( 'NONE', ( #87935, #215426, #183338, #66768 ) ) ;
#46267=DIRECTION ( 'NONE',  ( 0.000000000000000000, 0.000000000000000000, -1.000000000000000000 ) ) ;
#46292=AXIS2_PLACEMENT_3D ( 'NONE', #26823, #5920, #183302 ) ;
#46332=ORIENTED_EDGE ( 'NONE', *, *, #220594, .T. ) ;
#46345=ORIENTED_EDGE ( 'NONE', *, *, #123563, .T. ) ;
#46346=CARTESIAN_POINT ( 'NONE',  ( 20.94999999999999929, 1.115625160336667635E-11, -132.0000000000000284 ) ) ;
#46368=CARTESIAN_POINT ( 'NONE',  ( -21.07016717456945898, 6.320940838111400950, -100.5000000000000426 ) ) ;
#46371=ORIENTED_EDGE ( 'NONE', *, *, #105381, .T. ) ;
#46373=AXIS2_PLACEMENT_3D ( 'NONE', #41313, #157419, #239492 ) ;
#46382=DIRECTION ( 'NONE',  ( -1.000000000000000000, 9.012599976028471648E-15, 6.882867235861662930E-14 ) ) ;
#46385=FACE_OUTER_BOUND ( 'NONE', #27964, .T. ) ;
#46390=CARTESIAN_POINT ( 'NONE',  ( 20.95512820512820440, 10.62384868372303615, -112.6500000000000341 ) ) ;
#46400=ORIENTED_EDGE ( 'NONE', *, *, #139284, .F. ) ;
#46413=EDGE_LOOP ( 'NONE', ( #162419, #123834, #21866 ) ) ;
#46426=CARTESIAN_POINT ( 'NONE',  ( 18.59999999999998366, 1.115600667400684642E-11, -134.0000000000000284 ) ) ;
#46448=ORIENTED_EDGE ( 'NONE', *, *, #232618, .F. ) ;
#46469=DIRECTION ( 'NONE',  ( -1.000000000000000000, 0.000000000000000000, 0.000000000000000000 ) ) ;
#46473=CARTESIAN_POINT ( 'NONE',  ( 21.93340585898357631, 1.115541036281197940E-11, -93.17585297786898479 ) ) ;
#46492=DIRECTION ( 'NONE',  ( 0.000000000000000000, 0.000000000000000000, -1.000000000000000000 ) ) ;
#46494=VERTEX_POINT ( 'NONE', #76619 ) ;
#46502=VECTOR ( 'NONE', #45750, 999.9999999999998863 ) ;
#46505=VERTEX_POINT ( 'NONE', #174505 ) ;
#46533=DIRECTION ( 'NONE',  ( -3.265361837132813586E-16, 1.000000000000000000, 0.000000000000000000 ) ) ;
#46575=AXIS2_PLACEMENT_3D ( 'NONE', #104183, #44241, #66361 ) ;
#46581=ORIENTED_EDGE ( 'NONE', *, *, #230760, .T. ) ;
#46611=CARTESIAN_POINT ( 'NONE',  ( -20.85000000000000142, 11.65000000001115232, -134.0000000000000284 ) ) ;
#46619=VERTEX_POINT ( 'NONE', #63467 ) ;
#46621=DIRECTION ( 'NONE',  ( -3.265361837132813093E-16, 1.000000000000000000, 0.000000000000000000 ) ) ;
#46638=ORIENTED_EDGE ( 'NONE', *, *, #69103, .F. ) ;
#46655=ORIENTED_EDGE ( 'NONE', *, *, #105900, .F. ) ;
#46673=DIRECTION ( 'NONE',  ( 0.000000000000000000, 1.000000000000000000, 0.000000000000000000 ) ) ;
#46680=VERTEX_POINT ( 'NONE', #150725 ) ;
#46688=AXIS2_PLACEMENT_3D ( 'NONE', #175743, #216115, #93614 ) ;
#46689=( BOUNDED_SURFACE ( )  B_SPLINE_SURFACE ( 3, 2, ( 
 ( #222325, #142794, #102373 ),
 ( #198933, #157276, #98508 ),
 ( #181956, #97229, #19016 ),
 ( #20326, #159835, #118124 ),
 ( #161114, #217201, #257569 ),
 ( #78962, #158559, #60696 ) ),
 .UNSPECIFIED., .F., .F., .T. ) 
 B_SPLINE_SURFACE_WITH_KNOTS ( ( 4, 2, 4 ),
 ( 3, 3 ),
 ( 0.0001792624049599545865, 0.0003686986002124822948, 0.0005581347954650100031 ),
 ( 0.000000000000000000, 1.000000000000000000 ),
 .UNSPECIFIED. ) 
 GEOMETRIC_REPRESENTATION_ITEM ( )  RATIONAL_B_SPLINE_SURFACE ( (
 ( 1.000000000000000000, 0.9238795325112834078, 1.000000000000000000),
 ( 1.000000000000000000, 0.9229318695230264158, 1.000000000000000000),
 ( 1.000000000000000000, 0.8926288119241689856, 1.000000000000000000),
 ( 1.000000000000000000, 0.8123777807260450512, 1.000000000000000000),
 ( 1.000000000000000000, 0.7629087100939330179, 1.000000000000000000),
 ( 1.000000000000000000, 0.7071067811865966446, 1.000000000000000000) ) ) 
 REPRESENTATION_ITEM ( '' )  SURFACE ( )  );
#46727=EDGE_CURVE ( 'NONE', #16782, #172822, #172899, .T. ) ;
#46739=EDGE_CURVE ( 'NONE', #164082, #185160, #72691, .T. ) ;
#46752=DIRECTION ( 'NONE',  ( 1.000000000000000000, 0.000000000000000000, 0.000000000000000000 ) ) ;
#46758=VERTEX_POINT ( 'NONE', #254891 ) ;
#46766=ORIENTED_EDGE ( 'NONE', *, *, #53008, .F. ) ;
#46769=AXIS2_PLACEMENT_3D ( 'NONE', #195170, #230415, #16519 ) ;
#46794=DIRECTION ( 'NONE',  ( 0.000000000000000000, -1.000000000000000000, 0.000000000000000000 ) ) ;
#46824=TOROIDAL_SURFACE ( 'NONE', #171776, 12.77499999999999858, 0.1000000000000000056 ) ;
#46859=CIRCLE ( 'NONE', #242508, 0.1000000000000000472 ) ;
#46907=ADVANCED_FACE ( 'NONE', ( #15071 ), #72320, .T. ) ;
#46924=DIRECTION ( 'NONE',  ( -1.000000000000000000, 0.000000000000000000, 0.000000000000000000 ) ) ;
#46937=VERTEX_POINT ( 'NONE', #202683 ) ;
#46954=EDGE_CURVE ( 'NONE', #168568, #164082, #138684, .T. ) ;
#46973=ORIENTED_EDGE ( 'NONE', *, *, #36191, .F. ) ;
#47046=EDGE_CURVE ( 'NONE', #197646, #63374, #30496, .T. ) ;
#47072=DIRECTION ( 'NONE',  ( 0.000000000000000000, -0.8660254037844411501, -0.4999999999999956146 ) ) ;
#47107=LINE ( 'NONE', #27610, #1181 ) ;
#47110=ADVANCED_FACE ( 'NONE', ( #108728 ), #90433, .F. ) ;
#47114=DIRECTION ( 'NONE',  ( 0.000000000000000000, 0.000000000000000000, -1.000000000000000000 ) ) ;
#47128=ORIENTED_EDGE ( 'NONE', *, *, #88420, .F. ) ;
#47154=ORIENTED_EDGE ( 'NONE', *, *, #240732, .F. ) ;
#47200=DIRECTION ( 'NONE',  ( 1.000000000000000000, -0.000000000000000000, -0.000000000000000000 ) ) ;
#47229=EDGE_LOOP ( 'NONE', ( #238607, #174008, #158280 ) ) ;
#47234=AXIS2_PLACEMENT_3D ( 'NONE', #1002, #238362, #38906 ) ;
#47245=DIRECTION ( 'NONE',  ( 0.000000000000000000, 0.000000000000000000, -1.000000000000000000 ) ) ;
#47246=ADVANCED_FACE ( 'NONE', ( #252086 ), #255889, .F. ) ;
#47270=AXIS2_PLACEMENT_3D ( 'NONE', #68984, #168107, #31158 ) ;
#47304=CIRCLE ( 'NONE', #34903, 0.09999999999999344136 ) ;
#47309=ORIENTED_EDGE ( 'NONE', *, *, #73362, .T. ) ;
#47328=AXIS2_PLACEMENT_3D ( 'NONE', #182476, #27270, #44240 ) ;
#47329=CARTESIAN_POINT ( 'NONE',  ( -21.05000000000000426, 11.60000000001115872, -107.4282032302755852 ) ) ;
#47346=CYLINDRICAL_SURFACE ( 'NONE', #61087, 0.09999999999998898659 ) ;
#47349=AXIS2_PLACEMENT_3D ( 'NONE', #106994, #69197, #228256 ) ;
#47422=CIRCLE ( 'NONE', #143295, 0.1999999999999987899 ) ;
#47435=DIRECTION ( 'NONE',  ( 1.000000000000000000, 0.000000000000000000, 0.000000000000000000 ) ) ;
#47436=DIRECTION ( 'NONE',  ( 0.000000000000000000, 0.3738317757009345654, 0.9274965247785492695 ) ) ;
#47437=DIRECTION ( 'NONE',  ( -1.000000000000000000, 0.000000000000000000, 0.000000000000000000 ) ) ;
#47443=VECTOR ( 'NONE', #151103, 1000.000000000000000 ) ;
#47445=EDGE_LOOP ( 'NONE', ( #99182, #7597, #173079, #80956 ) ) ;
#47489=DIRECTION ( 'NONE',  ( -1.000000000000000000, 0.000000000000000000, 0.000000000000000000 ) ) ;
#47496=CARTESIAN_POINT ( 'NONE',  ( -18.51991288638537725, -9.392436789662212959, -107.6432664039581795 ) ) ;
#47516=CARTESIAN_POINT ( 'NONE',  ( -23.25000000000000000, 11.75000000001115552, -134.0000000000000284 ) ) ;
#47554=AXIS2_PLACEMENT_3D ( 'NONE', #154803, #135189, #77780 ) ;
#47560=CARTESIAN_POINT ( 'NONE',  ( 21.05000000000000071, -8.663551401858002876, -110.0241011180673354 ) ) ;
#47564=DIRECTION ( 'NONE',  ( 0.000000000000000000, -0.000000000000000000, 1.000000000000000000 ) ) ;
#47589=DIRECTION ( 'NONE',  ( 1.000000000000000000, 0.000000000000000000, 0.000000000000000000 ) ) ;
#47611=ORIENTED_EDGE ( 'NONE', *, *, #68990, .F. ) ;
#47663=TOROIDAL_SURFACE ( 'NONE', #64257, 4.149999999999999467, 0.1000000000000000056 ) ;
#47680=DIRECTION ( 'NONE',  ( 0.000000000000000000, 0.000000000000000000, 1.000000000000000000 ) ) ;
#47699=EDGE_CURVE ( 'NONE', #196043, #219593, #241224, .T. ) ;
#47715=EDGE_CURVE ( 'NONE', #198727, #39812, #239937, .T. ) ;
#47744=DIRECTION ( 'NONE',  ( 2.259780016855445309E-14, 0.9875055080513753802, -0.1575844902526748192 ) ) ;
#47807=DIRECTION ( 'NONE',  ( 0.000000000000000000, 0.000000000000000000, -1.000000000000000000 ) ) ;
#47817=AXIS2_PLACEMENT_3D ( 'NONE', #247936, #71894, #31501 ) ;
#47830=CARTESIAN_POINT ( 'NONE',  ( -20.64999999999999858, 1.115600667400684642E-11, -134.0000000000000284 ) ) ;
#47871=AXIS2_PLACEMENT_3D ( 'NONE', #105131, #66045, #46469 ) ;
#47915=CARTESIAN_POINT ( 'NONE',  ( 18.59999999999999787, -1.835341550213255957, -112.0551512925630107 ) ) ;
#47924=EDGE_LOOP ( 'NONE', ( #174326, #54841, #193144, #18808 ) ) ;
#47952=EDGE_LOOP ( 'NONE', ( #255619, #228541, #258016, #234877 ) ) ;
#47988=DIRECTION ( 'NONE',  ( 0.000000000000000000, 0.000000000000000000, -1.000000000000000000 ) ) ;
#48004=AXIS2_PLACEMENT_3D ( 'NONE', #158291, #115272, #56546 ) ;
#48068=CIRCLE ( 'NONE', #193826, 0.09999999999999939493 ) ;
#48093=LINE ( 'NONE', #187631, #251867 ) ;
#48098=ORIENTED_EDGE ( 'NONE', *, *, #139375, .T. ) ;
#48130=ORIENTED_EDGE ( 'NONE', *, *, #190809, .F. ) ;
#48154=CARTESIAN_POINT ( 'NONE',  ( -22.39999999999999858, 1.115600667400684642E-11, -94.25000000000002842 ) ) ;
#48160=DIRECTION ( 'NONE',  ( -0.000000000000000000, 1.000000000000000000, -0.000000000000000000 ) ) ;
#48167=EDGE_LOOP ( 'NONE', ( #255064, #182450, #109313 ) ) ;
#48214=CARTESIAN_POINT ( 'NONE',  ( -23.25000000000000000, -1.149570369564537842, -141.8159124845019790 ) ) ;
#48220=ADVANCED_FACE ( 'NONE', ( #13524 ), #39551, .F. ) ;
#48228=DIRECTION ( 'NONE',  ( -0.000000000000000000, 0.000000000000000000, 1.000000000000000000 ) ) ;
#48250=VECTOR ( 'NONE', #249972, 1000.000000000000000 ) ;
#48277=EDGE_LOOP ( 'NONE', ( #169431, #48310, #36365, #66969 ) ) ;
#48298=ORIENTED_EDGE ( 'NONE', *, *, #79784, .F. ) ;
#48310=ORIENTED_EDGE ( 'NONE', *, *, #141211, .T. ) ;
#48311=CARTESIAN_POINT ( 'NONE',  ( -22.48660254037844197, 11.75000000001114842, -100.4500000000000313 ) ) ;
#48320=ORIENTED_EDGE ( 'NONE', *, *, #234624, .T. ) ;
#48323=VECTOR ( 'NONE', #223975, 1000.000000000000000 ) ;
#48334=LINE ( 'NONE', #127883, #162368 ) ;
#48352=CIRCLE ( 'NONE', #165059, 0.3999999999999975797 ) ;
#48362=DIRECTION ( 'NONE',  ( -1.000000000000000000, -0.000000000000000000, -0.000000000000000000 ) ) ;
#48363=ADVANCED_FACE ( 'NONE', ( #119045 ), #106120, .T. ) ;
#48364=LINE ( 'NONE', #228302, #150208 ) ;
#48398=CYLINDRICAL_SURFACE ( 'NONE', #39345, 0.1000000000000028644 ) ;
#48408=CARTESIAN_POINT ( 'NONE',  ( 21.05000000000000071, 6.477067021135911595, -100.6000000000000369 ) ) ;
#48440=CIRCLE ( 'NONE', #148412, 0.1000000000000028644 ) ;
#48496=EDGE_CURVE ( 'NONE', #163018, #140720, #6171, .T. ) ;
#48510=CIRCLE ( 'NONE', #85902, 0.09999999999999939493 ) ;
#48523=ORIENTED_EDGE ( 'NONE', *, *, #19963, .T. ) ;
#48553=EDGE_LOOP ( 'NONE', ( #155524, #67570, #88171, #106546, #130672, #117430 ) ) ;
#48554=DIRECTION ( 'NONE',  ( 0.000000000000000000, 0.000000000000000000, -1.000000000000000000 ) ) ;
#48607=CARTESIAN_POINT ( 'NONE',  ( -20.15000000000000568, 9.291421356248463326, -121.6500000000000341 ) ) ;
#48626=FACE_OUTER_BOUND ( 'NONE', #28898, .T. ) ;
#48632=DIRECTION ( 'NONE',  ( 1.000000000000000000, -0.000000000000000000, -0.000000000000000000 ) ) ;
#48670=CONICAL_SURFACE ( 'NONE', #190345, 4.049999999999998046, 0.7853981633974604915 ) ;
#48685=AXIS2_PLACEMENT_3D ( 'NONE', #90041, #206153, #125337 ) ;
#48691=DIRECTION ( 'NONE',  ( -1.000000000000000000, -0.000000000000000000, -0.000000000000000000 ) ) ;
#48720=VERTEX_POINT ( 'NONE', #17087 ) ;
#48721=AXIS2_PLACEMENT_3D ( 'NONE', #86916, #89494, #169090 ) ;
#48745=ORIENTED_EDGE ( 'NONE', *, *, #36191, .T. ) ;
#48746=ADVANCED_FACE ( 'NONE', ( #53630 ), #234832, .T. ) ;
#48794=CARTESIAN_POINT ( 'NONE',  ( -18.47079683080347223, -9.471664105233722708, -107.6088605409924952 ) ) ;
#48800=CIRCLE ( 'NONE', #52890, 0.5000000000000004441 ) ;
#48811=CARTESIAN_POINT ( 'NONE',  ( -21.07928932188134041, 6.328516656404449492, -100.4011048543456468 ) ) ;
#48818=DIRECTION ( 'NONE',  ( -1.000000000000000000, -3.265361837132813093E-16, 0.000000000000000000 ) ) ;
#48823=CARTESIAN_POINT ( 'NONE',  ( -23.15000000000000213, -9.499999999988848032, -110.3939691226524786 ) ) ;
#48835=LINE ( 'NONE', #232642, #181411 ) ;
#48844=DIRECTION ( 'NONE',  ( 0.000000000000000000, 0.000000000000000000, 1.000000000000000000 ) ) ;
#48861=DIRECTION ( 'NONE',  ( 0.7071359030027766224, -0.7070776581709024011, 0.000000000000000000 ) ) ;
#48871=CARTESIAN_POINT ( 'NONE',  ( -18.39999999999999858, -9.599999999988849453, -140.6001893912220737 ) ) ;
#48878=AXIS2_PLACEMENT_3D ( 'NONE', #109737, #207589, #228437 ) ;
#48916=DIRECTION ( 'NONE',  ( 1.000000000000000000, 0.000000000000000000, 0.000000000000000000 ) ) ;
#48933=DIRECTION ( 'NONE',  ( 0.000000000000000000, 0.000000000000000000, 1.000000000000000000 ) ) ;
#48972=CARTESIAN_POINT ( 'NONE',  ( 21.05000000000000071, 11.75000000001116263, -126.9851942293460922 ) ) ;
#48975=ORIENTED_EDGE ( 'NONE', *, *, #238774, .T. ) ;
#48983=CARTESIAN_POINT ( 'NONE',  ( 20.46382478191414833, 10.59862044130854031, -108.1778144693454919 ) ) ;
#49018=CARTESIAN_POINT ( 'NONE',  ( 20.94999999999999574, 10.42338541492406279, -107.9920519238701218 ) ) ;
#49019=FACE_OUTER_BOUND ( 'NONE', #96455, .T. ) ;
#49106=CIRCLE ( 'NONE', #182218, 0.1000000000000020595 ) ;
#49122=AXIS2_PLACEMENT_3D ( 'NONE', #63018, #202539, #109846 ) ;
#49142=DIRECTION ( 'NONE',  ( 0.000000000000000000, 0.000000000000000000, -1.000000000000000000 ) ) ;
#49154=DIRECTION ( 'NONE',  ( 1.000000000000000000, 0.000000000000000000, 0.000000000000000000 ) ) ;
#49161=CARTESIAN_POINT ( 'NONE',  ( 18.49999999999998934, 10.29288807859941457, -139.4580020160121876 ) ) ;
#49191=DIRECTION ( 'NONE',  ( 0.000000000000000000, 0.000000000000000000, -1.000000000000000000 ) ) ;
#49195=CIRCLE ( 'NONE', #157391, 0.1000000000000008937 ) ;
#49196=LINE ( 'NONE', #11363, #48250 ) ;
#49207=EDGE_LOOP ( 'NONE', ( #14278, #69401, #96800, #57535 ) ) ;
#49259=EDGE_CURVE ( 'NONE', #115014, #5081, #244523, .T. ) ;
#49268=ORIENTED_EDGE ( 'NONE', *, *, #107633, .T. ) ;
#49282=ORIENTED_EDGE ( 'NONE', *, *, #23406, .F. ) ;
#49317=VECTOR ( 'NONE', #207730, 1000.000000000000000 ) ;
#49328=ORIENTED_EDGE ( 'NONE', *, *, #24179, .T. ) ;
#49369=CARTESIAN_POINT ( 'NONE',  ( 21.05000000000000071, 10.72371711693665652, -112.6762396011380218 ) ) ;
#49403=DIRECTION ( 'NONE',  ( -3.787827842127535236E-15, 0.7397360091702777085, 0.6728971962616808744 ) ) ;
#49406=EDGE_LOOP ( 'NONE', ( #35832, #119218, #185011, #74697 ) ) ;
#49456=CARTESIAN_POINT ( 'NONE',  ( -20.54999999999999716, 1.115600667400684642E-11, -134.0000000000000284 ) ) ;
#49495=ADVANCED_FACE ( 'NONE', ( #121544 ), #201045, .T. ) ;
#49503=ORIENTED_EDGE ( 'NONE', *, *, #66261, .T. ) ;
#49509=EDGE_LOOP ( 'NONE', ( #31014, #147591, #70686, #120474 ) ) ;
#49536=CARTESIAN_POINT ( 'NONE',  ( -18.59999999999999787, 9.350000000011156942, -121.6500000000000341 ) ) ;
#49539=CARTESIAN_POINT ( 'NONE',  ( 21.05000000000000071, 10.72371710471867701, -100.5000000000000284 ) ) ;
#49575=CARTESIAN_POINT ( 'NONE',  ( 18.50000000000000355, -9.480686695267811714, -140.9411151687578467 ) ) ;
#49579=CARTESIAN_POINT ( 'NONE',  ( -23.15000000000000213, 4.250000000011156409, -121.6500000000000341 ) ) ;
#49580=ADVANCED_FACE ( 'NONE', ( #168395 ), #249171, .F. ) ;
#49595=DIRECTION ( 'NONE',  ( 0.000000000000000000, -0.1350103645451876666, -0.9908441862701600211 ) ) ;
#49602=CARTESIAN_POINT ( 'NONE',  ( -22.50000000000000000, 0.1000000000111554016, -88.85042919245522341 ) ) ;
#49625=CARTESIAN_POINT ( 'NONE',  ( 20.89192007715127986, 10.32898536001801304, -139.5826683222764757 ) ) ;
#49626=AXIS2_PLACEMENT_3D ( 'NONE', #182146, #2195, #3484 ) ;
#49651=EDGE_CURVE ( 'NONE', #54193, #67239, #210052, .T. ) ;
#49663=EDGE_CURVE ( 'NONE', #218579, #40869, #120096, .T. ) ;
#49667=VERTEX_POINT ( 'NONE', #37843 ) ;
#49683=CARTESIAN_POINT ( 'NONE',  ( 21.05000000000000071, -1.360870587180885716, -108.5729979270909951 ) ) ;
#49689=LINE ( 'NONE', #69270, #157622 ) ;
#49694=DIRECTION ( 'NONE',  ( -1.000000000000000000, 0.000000000000000000, 0.000000000000000000 ) ) ;
#49711=DIRECTION ( 'NONE',  ( -6.938893903907222067E-15, 1.000000000000000000, 0.000000000000000000 ) ) ;
#49740=AXIS2_PLACEMENT_3D ( 'NONE', #116001, #30361, #68188 ) ;
#49757=DIRECTION ( 'NONE',  ( -1.000000000000000000, 0.000000000000000000, 0.000000000000000000 ) ) ;
#49761=CARTESIAN_POINT ( 'NONE',  ( -23.15000000000000213, 2.000000000011154189, -120.7753780772379315 ) ) ;
#49792=ADVANCED_FACE ( 'NONE', ( #242420 ), #27413, .T. ) ;
#49819=ADVANCED_FACE ( 'NONE', ( #117357 ), #236953, .T. ) ;
#49837=ORIENTED_EDGE ( 'NONE', *, *, #52531, .T. ) ;
#49847=AXIS2_PLACEMENT_3D ( 'NONE', #58866, #178882, #257042 ) ;
#49849=CARTESIAN_POINT ( 'NONE',  ( -22.47071067811865319, 7.720074744509219933, -100.4009075452974287 ) ) ;
#49870=DIRECTION ( 'NONE',  ( 0.000000000000000000, -0.01283462868041947667, -0.9999176327611367654 ) ) ;
#49876=FACE_OUTER_BOUND ( 'NONE', #120161, .T. ) ;
#49886=EDGE_CURVE ( 'NONE', #115014, #186169, #226707, .T. ) ;
#49917=CIRCLE ( 'NONE', #216514, 0.1000000000000028644 ) ;
#49931=ORIENTED_EDGE ( 'NONE', *, *, #111803, .T. ) ;
#49958=VECTOR ( 'NONE', #39536, 1000.000000000000000 ) ;
#49978=CARTESIAN_POINT ( 'NONE',  ( 21.14999999999999503, -11.74999999998883560, -88.75000000000004263 ) ) ;
#49987=CARTESIAN_POINT ( 'NONE',  ( 21.05000000000000071, -9.499999999988844479, -124.1060308773475924 ) ) ;
#49988=DIRECTION ( 'NONE',  ( 1.713247197920696616E-14, 0.9876197685951252359, -0.1568667991644863424 ) ) ;
#50003=ORIENTED_EDGE ( 'NONE', *, *, #67045, .F. ) ;
#50014=DIRECTION ( 'NONE',  ( 1.000000000000000000, 0.000000000000000000, 0.000000000000000000 ) ) ;
#50021=DIRECTION ( 'NONE',  ( -0.000000000000000000, 1.000000000000000000, -0.000000000000000000 ) ) ;
#50025=CYLINDRICAL_SURFACE ( 'NONE', #182036, 0.09999999999999781286 ) ;
#50034=DIRECTION ( 'NONE',  ( -0.000000000000000000, -1.000000000000000000, 0.000000000000000000 ) ) ;
#50038=CARTESIAN_POINT ( 'NONE',  ( 18.49999999999999289, 11.75000000001115907, -88.75000000000004263 ) ) ;
#50039=CARTESIAN_POINT ( 'NONE',  ( 18.39999999999999858, -9.682403433465241349, -140.6568433774128266 ) ) ;
#50067=AXIS2_PLACEMENT_3D ( 'NONE', #86143, #64046, #83574 ) ;
#50079=CARTESIAN_POINT ( 'NONE',  ( -18.45037301276681418, -9.490200447530819261, -107.5126741364140912 ) ) ;
#50117=ORIENTED_EDGE ( 'NONE', *, *, #163596, .F. ) ;
#50155=DIRECTION ( 'NONE',  ( 1.000000000000000000, -0.000000000000000000, -0.000000000000000000 ) ) ;
#50239=CARTESIAN_POINT ( 'NONE',  ( -20.94983749550516450, 10.29766095125282810, -139.4743663933276139 ) ) ;
#50377=VERTEX_POINT ( 'NONE', #63473 ) ;
#50382=VECTOR ( 'NONE', #75753, 1000.000000000000000 ) ;
#50397=CARTESIAN_POINT ( 'NONE',  ( 21.05000000000000071, 8.776282895303630482, -109.0586289951409924 ) ) ;
#50423=CARTESIAN_POINT ( 'NONE',  ( 18.50596464788227280, 10.30632246271648889, -139.5041836778896425 ) ) ;
#50444=ORIENTED_EDGE ( 'NONE', *, *, #224934, .T. ) ;
#50471=CARTESIAN_POINT ( 'NONE',  ( -23.25000000000000000, -8.999999999988844479, -124.7060308773475867 ) ) ;
#50472=EDGE_CURVE ( 'NONE', #169534, #152480, #16391, .T. ) ;
#50513=ORIENTED_EDGE ( 'NONE', *, *, #96556, .F. ) ;
#50516=DIRECTION ( 'NONE',  ( -0.000000000000000000, -0.000000000000000000, -1.000000000000000000 ) ) ;
#50523=CARTESIAN_POINT ( 'NONE',  ( -18.59999999999999787, 1.162701749949165642, -108.6000000000000227 ) ) ;
#50552=FACE_OUTER_BOUND ( 'NONE', #72286, .T. ) ;
#50561=VERTEX_POINT ( 'NONE', #244055 ) ;
#50604=CIRCLE ( 'NONE', #125627, 0.5000000000000004441 ) ;
#50609=CARTESIAN_POINT ( 'NONE',  ( 20.85000000000000142, 6.982009704867603972, -137.6961521182563217 ) ) ;
#50619=DIRECTION ( 'NONE',  ( -1.000000000000000000, 0.000000000000000000, 0.000000000000000000 ) ) ;
#50628=CARTESIAN_POINT ( 'NONE',  ( 18.42636655943170965, -9.496944315759476396, -140.6090805711555731 ) ) ;
#50642=CARTESIAN_POINT ( 'NONE',  ( 23.15000000000000213, -8.999999999988842703, -124.1060308773475924 ) ) ;
#50697=ADVANCED_FACE ( 'NONE', ( #228364 ), #90107, .T. ) ;
#50700=VERTEX_POINT ( 'NONE', #229642 ) ;
#50719=DIRECTION ( 'NONE',  ( -1.000000000000000000, 0.000000000000000000, 0.000000000000000000 ) ) ;
#50749=AXIS2_PLACEMENT_3D ( 'NONE', #94960, #175809, #76678 ) ;
#50792=DIRECTION ( 'NONE',  ( 0.000000000000000000, -1.000000000000000000, 0.000000000000000000 ) ) ;
#50801=ADVANCED_FACE ( 'NONE', ( #155272 ), #220574, .F. ) ;
#50816=AXIS2_PLACEMENT_3D ( 'NONE', #174798, #32717, #152650 ) ;
#50829=CARTESIAN_POINT ( 'NONE',  ( 18.39999999999999858, -9.499999999988844479, -140.6001893912220737 ) ) ;
#50837=VECTOR ( 'NONE', #204548, 1000.000000000000000 ) ;
#50851=CARTESIAN_POINT ( 'NONE',  ( -22.57320508075687115, 11.75000000001115552, -100.5000000000000568 ) ) ;
#50860=FACE_OUTER_BOUND ( 'NONE', #183331, .T. ) ;
#50889=AXIS2_PLACEMENT_3D ( 'NONE', #117694, #219356, #18603 ) ;
#50938=CARTESIAN_POINT ( 'NONE',  ( -20.94999999999999929, 1.115600667400684642E-11, -134.0000000000000284 ) ) ;
#50980=EDGE_LOOP ( 'NONE', ( #224987, #224957, #160430, #163059 ) ) ;
#51052=ORIENTED_EDGE ( 'NONE', *, *, #115761, .F. ) ;
#51072=AXIS2_PLACEMENT_3D ( 'NONE', #244511, #127145, #11047 ) ;
#51077=EDGE_CURVE ( 'NONE', #85652, #195772, #91761, .T. ) ;
#51079=ADVANCED_FACE ( 'NONE', ( #74140 ), #175012, .F. ) ;
#51104=CARTESIAN_POINT ( 'NONE',  ( 20.94999999999999929, 6.650000000011155876, -110.5170271704400591 ) ) ;
#51106=CARTESIAN_POINT ( 'NONE',  ( -18.59999999999999787, -1.249999999988843369, -108.5000000000000426 ) ) ;
#51139=ORIENTED_EDGE ( 'NONE', *, *, #178116, .F. ) ;
#51155=EDGE_LOOP ( 'NONE', ( #242542, #254870, #188337, #138643 ) ) ;
#51202=CARTESIAN_POINT ( 'NONE',  ( -23.15000000000000213, 5.950000000011163692, -123.6942976949652149 ) ) ;
#51232=CYLINDRICAL_SURFACE ( 'NONE', #231491, 0.09999999999999781286 ) ;
#51287=ORIENTED_EDGE ( 'NONE', *, *, #175888, .F. ) ;
#51293=DIRECTION ( 'NONE',  ( -3.265361837132813093E-16, 1.000000000000000000, 0.000000000000000000 ) ) ;
#51304=ORIENTED_EDGE ( 'NONE', *, *, #136770, .F. ) ;
#51324=EDGE_CURVE ( 'NONE', #253084, #176862, #43960, .T. ) ;
#51325=FACE_OUTER_BOUND ( 'NONE', #179683, .T. ) ;
#51330=FACE_OUTER_BOUND ( 'NONE', #20154, .T. ) ;
#51348=CIRCLE ( 'NONE', #226332, 0.1000000000000028644 ) ;
#51371=VECTOR ( 'NONE', #52952, 1000.000000000000000 ) ;
#51376=CARTESIAN_POINT ( 'NONE',  ( 21.05000000000000071, 1.115600667400684642E-11, -113.4750000000000369 ) ) ;
#51418=VERTEX_POINT ( 'NONE', #246018 ) ;
#51431=CARTESIAN_POINT ( 'NONE',  ( -18.58735405345342073, -9.566478620325447935, -140.8227146462660357 ) ) ;
#51444=ORIENTED_EDGE ( 'NONE', *, *, #86594, .T. ) ;
#51456=ORIENTED_EDGE ( 'NONE', *, *, #21302, .T. ) ;
#51462=CARTESIAN_POINT ( 'NONE',  ( 21.59780538579342135, 0.09897866960914131207, -93.65290947005678390 ) ) ;
#51475=CARTESIAN_POINT ( 'NONE',  ( 20.87631937322880304, 10.47149503677605509, -108.0797458745812065 ) ) ;
#51488=ORIENTED_EDGE ( 'NONE', *, *, #54816, .T. ) ;
#51495=AXIS2_PLACEMENT_3D ( 'NONE', #120400, #83757, #199916 ) ;
#51519=FACE_OUTER_BOUND ( 'NONE', #172681, .T. ) ;
#51554=DIRECTION ( 'NONE',  ( 1.000000000000000000, -0.000000000000000000, -0.000000000000000000 ) ) ;
#51579=CIRCLE ( 'NONE', #230705, 0.09999999999999939493 ) ;
#51597=ADVANCED_FACE ( 'NONE', ( #116768 ), #136302, .F. ) ;
#51616=CIRCLE ( 'NONE', #84946, 0.09999999999999736877 ) ;
#51674=ORIENTED_EDGE ( 'NONE', *, *, #7954, .T. ) ;
#51679=LINE ( 'NONE', #131244, #40322 ) ;
#51728=EDGE_LOOP ( 'NONE', ( #215816, #62853, #130353, #147900 ) ) ;
#51751=ORIENTED_EDGE ( 'NONE', *, *, #205647, .F. ) ;
#51764=AXIS2_PLACEMENT_3D ( 'NONE', #183160, #207880, #25381 ) ;
#51767=CARTESIAN_POINT ( 'NONE',  ( 18.59999999999999076, 10.49142135624846439, -125.2500000000000284 ) ) ;
#51772=ORIENTED_EDGE ( 'NONE', *, *, #167134, .T. ) ;
#51823=DIRECTION ( 'NONE',  ( 1.000000000000000000, 0.000000000000000000, 0.000000000000000000 ) ) ;
#51824=CARTESIAN_POINT ( 'NONE',  ( -20.94999999999999929, 1.162701749949165642, -108.4000000000000341 ) ) ;
#51833=ORIENTED_EDGE ( 'NONE', *, *, #209889, .T. ) ;
#51866=ADVANCED_FACE ( 'NONE', ( #51330 ), #35688, .F. ) ;
#51889=FACE_OUTER_BOUND ( 'NONE', #132625, .T. ) ;
#51906=CARTESIAN_POINT ( 'NONE',  ( 18.46905048506369340, -9.473744257371240707, -140.6759862922554589 ) ) ;
#51953=PLANE ( 'NONE',  #237318 ) ;
#51956=FACE_OUTER_BOUND ( 'NONE', #155277, .T. ) ;
#51963=CARTESIAN_POINT ( 'NONE',  ( 20.94999999999999929, 1.115600667400684642E-11, -141.8000000000000398 ) ) ;
#52004=EDGE_LOOP ( 'NONE', ( #35856, #31504, #125818 ) ) ;
#52050=CYLINDRICAL_SURFACE ( 'NONE', #1244, 0.1000000000000028644 ) ;
#52055=ORIENTED_EDGE ( 'NONE', *, *, #147574, .T. ) ;
#52099=DIRECTION ( 'NONE',  ( 0.000000000000000000, 1.734723475976997999E-14, -1.000000000000000000 ) ) ;
#52109=EDGE_LOOP ( 'NONE', ( #177345, #204119, #147307, #8593 ) ) ;
#52124=CARTESIAN_POINT ( 'NONE',  ( 18.50000000000000355, -9.421074344976428705, -140.8244720594310593 ) ) ;
#52152=ORIENTED_EDGE ( 'NONE', *, *, #220723, .T. ) ;
#52163=CIRCLE ( 'NONE', #197907, 0.9750000000000036415 ) ;
#52166=CARTESIAN_POINT ( 'NONE',  ( 22.50000000000000000, 0.1000000000111554016, -92.70922040162665212 ) ) ;
#52204=DIRECTION ( 'NONE',  ( 0.000000000000000000, -1.000000000000000000, -0.000000000000000000 ) ) ;
#52222=DIRECTION ( 'NONE',  ( 0.000000000000000000, 1.224646799142185182E-16, 1.000000000000000000 ) ) ;
#52226=CARTESIAN_POINT ( 'NONE',  ( -23.25000000000000000, -8.596261682231832069, -124.5498724828497501 ) ) ;
#52228=FACE_OUTER_BOUND ( 'NONE', #139952, .T. ) ;
#52248=DIRECTION ( 'NONE',  ( 0.5000000000001141309, 0.000000000000000000, -0.8660254037843729824 ) ) ;
#52329=VERTEX_POINT ( 'NONE', #249275 ) ;
#52334=ORIENTED_EDGE ( 'NONE', *, *, #136102, .T. ) ;
#52377=CYLINDRICAL_SURFACE ( 'NONE', #91287, 0.09999999999999939493 ) ;
#52386=AXIS2_PLACEMENT_3D ( 'NONE', #135221, #54415, #193944 ) ;
#52401=CARTESIAN_POINT ( 'NONE',  ( -23.25000000000000000, -11.74999999998884448, -88.75000000000004263 ) ) ;
#52440=ORIENTED_EDGE ( 'NONE', *, *, #110384, .T. ) ;
#52455=CARTESIAN_POINT ( 'NONE',  ( -22.59999999999999787, 1.115600667400684642E-11, -100.5000000000000284 ) ) ;
#52459=CARTESIAN_POINT ( 'NONE',  ( 20.94999999999999929, 4.850467289730776344, -121.9657325909983570 ) ) ;
#52467=DIRECTION ( 'NONE',  ( 1.000000000000000000, 0.000000000000000000, 0.000000000000000000 ) ) ;
#52474=CYLINDRICAL_SURFACE ( 'NONE', #172271, 11.74999999999999645 ) ;
#52483=ORIENTED_EDGE ( 'NONE', *, *, #235684, .F. ) ;
#52488=EDGE_CURVE ( 'NONE', #85468, #187769, #63245, .T. ) ;
#52531=EDGE_CURVE ( 'NONE', #85365, #163018, #234122, .T. ) ;
#52562=AXIS2_PLACEMENT_3D ( 'NONE', #76514, #214747, #136471 ) ;
#52601=CARTESIAN_POINT ( 'NONE',  ( 18.60000000000000142, -9.523946312306554418, -140.8820279953382908 ) ) ;
#52633=CARTESIAN_POINT ( 'NONE',  ( -2.995603634470891112E-16, -11.74999999998884448, -125.2500000000000284 ) ) ;
#52640=DIRECTION ( 'NONE',  ( 1.000000000000000000, 0.000000000000000000, 0.000000000000000000 ) ) ;
#52648=FACE_OUTER_BOUND ( 'NONE', #139348, .T. ) ;
#52652=DIRECTION ( 'NONE',  ( 0.000000000000000000, -0.8700118002898322711, 0.4930308989875231140 ) ) ;
#52720=EDGE_LOOP ( 'NONE', ( #123761, #15712, #17403, #205999 ) ) ;
#52724=B_SPLINE_CURVE_WITH_KNOTS ( 'NONE', 3,
 ( #27275, #230583, #207169, #166782, #51906, #8957, #228005, #50628, #248856, #70246 ),
 .UNSPECIFIED., .F., .F.,
 ( 4, 2, 2, 2, 4 ),
 ( 0.000000000000000000, 0.0001660831991681949865, 0.0002491247987522924798, 0.0002906455985443746198, 0.0003321663983364568141 ),
 .UNSPECIFIED. ) ;
#52742=CARTESIAN_POINT ( 'NONE',  ( 18.46858270002952196, -9.474202674699409243, -107.6020219347038704 ) ) ;
#52751=ORIENTED_EDGE ( 'NONE', *, *, #188211, .F. ) ;
#52756=EDGE_LOOP ( 'NONE', ( #108647, #181132, #222340, #44602 ) ) ;
#52772=CARTESIAN_POINT ( 'NONE',  ( 20.50589344624992449, 10.48318793148740546, -108.0729949786726536 ) ) ;
#52802=CARTESIAN_POINT ( 'NONE',  ( 20.85000000000000142, -1.835859311432481045, -145.5044391687985694 ) ) ;
#52845=CARTESIAN_POINT ( 'NONE',  ( -21.05000000000000071, -11.64999999998884483, -100.5000000000000284 ) ) ;
#52857=DIRECTION ( 'NONE',  ( 0.000000000000000000, 4.336808689942043768E-15, -1.000000000000000000 ) ) ;
#52886=ADVANCED_FACE ( 'NONE', ( #3353 ), #184574, .T. ) ;
#52890=AXIS2_PLACEMENT_3D ( 'NONE', #80711, #198112, #157757 ) ;
#52908=EDGE_CURVE ( 'NONE', #153129, #75064, #46859, .T. ) ;
#52914=DIRECTION ( 'NONE',  ( 0.000000000000000000, 0.000000000000000000, -1.000000000000000000 ) ) ;
#52926=CIRCLE ( 'NONE', #186222, 0.09999999999999939493 ) ;
#52945=ORIENTED_EDGE ( 'NONE', *, *, #107713, .F. ) ;
#52950=ORIENTED_EDGE ( 'NONE', *, *, #196797, .T. ) ;
#52951=CARTESIAN_POINT ( 'NONE',  ( -20.64999999999999858, 1.115600667400684642E-11, -113.3750000000000284 ) ) ;
#52952=DIRECTION ( 'NONE',  ( 1.000000000000000000, -0.000000000000000000, -0.000000000000000000 ) ) ;
#52974=CARTESIAN_POINT ( 'NONE',  ( 18.59999999999999076, 6.982009704867611077, -137.6961521182563501 ) ) ;
#52981=VECTOR ( 'NONE', #125152, 1000.000000000000000 ) ;
#52985=ORIENTED_EDGE ( 'NONE', *, *, #229216, .T. ) ;
#52988=ORIENTED_EDGE ( 'NONE', *, *, #139293, .F. ) ;
#53008=EDGE_CURVE ( 'NONE', #204472, #6436, #180175, .T. ) ;
#53021=CARTESIAN_POINT ( 'NONE',  ( 22.39999999999999503, -0.1008583690875579364, -88.75043287651064361 ) ) ;
#53025=CIRCLE ( 'NONE', #69630, 0.09999999999998898659 ) ;
#53036=AXIS2_PLACEMENT_3D ( 'NONE', #156379, #235867, #237172 ) ;
#53043=EDGE_LOOP ( 'NONE', ( #51674, #116303, #157612, #19815 ) ) ;
#53068=CIRCLE ( 'NONE', #32461, 0.5000000000000004441 ) ;
#53122=ORIENTED_EDGE ( 'NONE', *, *, #78876, .T. ) ;
#53127=CARTESIAN_POINT ( 'NONE',  ( -18.59999999999999787, 11.65000000001115232, -112.6500000000000341 ) ) ;
#53128=CARTESIAN_POINT ( 'NONE',  ( -18.59999999999999787, 11.65000000001115232, -121.7500000000000426 ) ) ;
#53182=CARTESIAN_POINT ( 'NONE',  ( -18.59999999999999787, 11.65000000001115232, -88.75000000000004263 ) ) ;
#53199=CARTESIAN_POINT ( 'NONE',  ( -20.94999999999999929, -11.29603075032412640, -130.9521008403361861 ) ) ;
#53233=AXIS2_PLACEMENT_3D ( 'NONE', #155922, #112921, #232893 ) ;
#53242=CYLINDRICAL_SURFACE ( 'NONE', #156053, 0.09999999999999781286 ) ;
#53267=FACE_BOUND ( 'NONE', #207674, .T. ) ;
#53275=( LENGTH_UNIT ( ) NAMED_UNIT ( * ) SI_UNIT ( .MILLI., .METRE. ) );
#53300=DIRECTION ( 'NONE',  ( 1.000000000000000000, 0.000000000000000000, 0.000000000000000000 ) ) ;
#53303=VERTEX_POINT ( 'NONE', #203834 ) ;
#53324=DIRECTION ( 'NONE',  ( 0.000000000000000000, -0.1298341882520022694, -0.9915357197604853789 ) ) ;
#53332=VECTOR ( 'NONE', #204629, 1000.000000000000000 ) ;
#53345=AXIS2_PLACEMENT_3D ( 'NONE', #159362, #180206, #101905 ) ;
#53349=CIRCLE ( 'NONE', #11867, 0.09999999999999939493 ) ;
#53366=DIRECTION ( 'NONE',  ( 0.000000000000000000, -0.1568667991644863147, 0.9876197685951252359 ) ) ;
#53367=CARTESIAN_POINT ( 'NONE',  ( 21.10642757222115407, 10.72315628916975250, -112.7406975237852436 ) ) ;
#53408=DIRECTION ( 'NONE',  ( 0.000000000000000000, 0.000000000000000000, -1.000000000000000000 ) ) ;
#53442=VERTEX_POINT ( 'NONE', #72052 ) ;
#53450=CARTESIAN_POINT ( 'NONE',  ( 21.05000000000000071, 5.850000000011105428, -110.6324972242780120 ) ) ;
#53473=DIRECTION ( 'NONE',  ( -1.000000000000000000, 0.000000000000000000, 0.000000000000000000 ) ) ;
#53474=CIRCLE ( 'NONE', #36752, 0.1000000000000004774 ) ;
#53479=DIRECTION ( 'NONE',  ( -0.000000000000000000, 0.1350103645451876666, -0.9908441862701600211 ) ) ;
#53491=AXIS2_PLACEMENT_3D ( 'NONE', #237895, #138756, #61839 ) ;
#53493=ADVANCED_FACE ( 'NONE', ( #189426 ), #171188, .F. ) ;
#53495=CIRCLE ( 'NONE', #136677, 0.1000000000000028644 ) ;
#53496=CYLINDRICAL_SURFACE ( 'NONE', #98948, 0.1000000000000000472 ) ;
#53506=CARTESIAN_POINT ( 'NONE',  ( 21.05000000000000071, 1.115600667400684642E-11, -112.6500000000000341 ) ) ;
#53559=FACE_OUTER_BOUND ( 'NONE', #118808, .T. ) ;
#53565=ORIENTED_EDGE ( 'NONE', *, *, #245231, .T. ) ;
#53574=DIRECTION ( 'NONE',  ( 0.000000000000000000, -0.01283462868041947667, -0.9999176327611367654 ) ) ;
#53581=ORIENTED_EDGE ( 'NONE', *, *, #185770, .T. ) ;
#53604=CARTESIAN_POINT ( 'NONE',  ( -23.24999999999999645, -9.599999999988845900, -140.7001893912220680 ) ) ;
#53618=VERTEX_POINT ( 'NONE', #115018 ) ;
#53630=FACE_OUTER_BOUND ( 'NONE', #143178, .T. ) ;
#53635=AXIS2_PLACEMENT_3D ( 'NONE', #150280, #68157, #128141 ) ;
#53641=AXIS2_PLACEMENT_3D ( 'NONE', #7148, #243195, #106239 ) ;
#53655=DIRECTION ( 'NONE',  ( 1.000000000000000000, -0.000000000000000000, -0.000000000000000000 ) ) ;
#53659=LINE ( 'NONE', #194480, #223545 ) ;
#53750=ADVANCED_FACE ( 'NONE', ( #4991 ), #71639, .T. ) ;
#53777=CARTESIAN_POINT ( 'NONE',  ( -23.25000000000000000, 1.115600667400684642E-11, -100.5000000000000284 ) ) ;
#53782=ORIENTED_EDGE ( 'NONE', *, *, #210505, .T. ) ;
#53788=DIRECTION ( 'NONE',  ( 0.000000000000000000, -0.000000000000000000, 1.000000000000000000 ) ) ;
#53817=CARTESIAN_POINT ( 'NONE',  ( -20.94999999999999929, 6.846123162363745074, -137.7377262668498759 ) ) ;
#53828=EDGE_LOOP ( 'NONE', ( #66511, #107201, #88079, #54882 ) ) ;
#53832=CARTESIAN_POINT ( 'NONE',  ( 21.03675099975492202, 8.875180032795963569, -112.8255421367780826 ) ) ;
#53842=FACE_OUTER_BOUND ( 'NONE', #48277, .T. ) ;
#53882=CARTESIAN_POINT ( 'NONE',  ( 18.49999999999999645, -1.835341550213255957, -112.0551512925630107 ) ) ;
#53926=CARTESIAN_POINT ( 'NONE',  ( 20.94999999999999929, 7.021664781911246322, -137.8335654018973457 ) ) ;
#53969=DIRECTION ( 'NONE',  ( -0.000000000000000000, 0.8660254037844411501, 0.4999999999999956701 ) ) ;
#53973=VERTEX_POINT ( 'NONE', #195240 ) ;
#54012=EDGE_CURVE ( 'NONE', #237605, #34456, #88532, .T. ) ;
#54020=DIRECTION ( 'NONE',  ( 0.000000000000000000, 0.000000000000000000, -1.000000000000000000 ) ) ;
#54031=CARTESIAN_POINT ( 'NONE',  ( 20.95262331984769588, 10.50415726280101403, -108.0608883295933396 ) ) ;
#54036=VERTEX_POINT ( 'NONE', #84179 ) ;
#54037=EDGE_CURVE ( 'NONE', #233320, #27558, #21924, .T. ) ;
#54046=CIRCLE ( 'NONE', #120718, 0.09999999999999693856 ) ;
#54067=AXIS2_PLACEMENT_3D ( 'NONE', #157039, #34530, #17501 ) ;
#54083=DIRECTION ( 'NONE',  ( 1.000000000000000000, 0.000000000000000000, 0.000000000000000000 ) ) ;
#54098=CARTESIAN_POINT ( 'NONE',  ( 20.84999999999998721, 11.75000000001115552, -134.0000000000000284 ) ) ;
#54111=DIRECTION ( 'NONE',  ( 1.000000000000000000, 2.952720810173289112E-16, -0.000000000000000000 ) ) ;
#54135=DIRECTION ( 'NONE',  ( 1.000000000000000000, -0.000000000000000000, -0.000000000000000000 ) ) ;
#54138=CARTESIAN_POINT ( 'NONE',  ( 21.05000000000000071, -0.09999999998884338825, -93.95934304829877703 ) ) ;
#54144=DIRECTION ( 'NONE',  ( 0.000000000000000000, 0.000000000000000000, -1.000000000000000000 ) ) ;
#54193=VERTEX_POINT ( 'NONE', #206761 ) ;
#54199=EDGE_LOOP ( 'NONE', ( #69775, #184814, #234399, #229474, #77403 ) ) ;
#54205=ORIENTED_EDGE ( 'NONE', *, *, #39106, .T. ) ;
#54220=PLANE ( 'NONE',  #37792 ) ;
#54234=DIRECTION ( 'NONE',  ( 0.000000000000000000, 0.1350103645451904977, -0.9908441862701596881 ) ) ;
#54258=ADVANCED_FACE ( 'NONE', ( #228896 ), #150639, .F. ) ;
#54275=EDGE_CURVE ( 'NONE', #189217, #46937, #17800, .T. ) ;
#54277=FACE_OUTER_BOUND ( 'NONE', #85047, .T. ) ;
#54280=DIRECTION ( 'NONE',  ( 0.000000000000000000, 1.000000000000000000, 0.000000000000000000 ) ) ;
#54291=ORIENTED_EDGE ( 'NONE', *, *, #222807, .T. ) ;
#54295=AXIS2_PLACEMENT_3D ( 'NONE', #29771, #226636, #126255 ) ;
#54332=AXIS2_PLACEMENT_3D ( 'NONE', #255138, #236911, #115692 ) ;
#54339=ORIENTED_EDGE ( 'NONE', *, *, #153960, .F. ) ;
#54341=DIRECTION ( 'NONE',  ( 1.000000000000000000, 3.265361837132813093E-16, -0.000000000000000000 ) ) ;
#54348=EDGE_CURVE ( 'NONE', #198727, #188180, #142704, .T. ) ;
#54360=FACE_OUTER_BOUND ( 'NONE', #73262, .T. ) ;
#54414=DIRECTION ( 'NONE',  ( -1.000000000000000000, -0.000000000000000000, -0.000000000000000000 ) ) ;
#54415=DIRECTION ( 'NONE',  ( -1.000000000000000000, -2.952720810173289112E-16, 0.000000000000000000 ) ) ;
#54491=CARTESIAN_POINT ( 'NONE',  ( 21.05000012384953223, 10.62872029888669978, -112.6779773300352332 ) ) ;
#54498=CARTESIAN_POINT ( 'NONE',  ( 20.95420533658165141, 10.54586447477073285, -108.0675060206932727 ) ) ;
#54505=ORIENTED_EDGE ( 'NONE', *, *, #9726, .T. ) ;
#54515=FACE_OUTER_BOUND ( 'NONE', #187466, .T. ) ;
#54520=CARTESIAN_POINT ( 'NONE',  ( -21.65000000000000213, 7.708578643773852157, -121.7500000000000426 ) ) ;
#54544=ORIENTED_EDGE ( 'NONE', *, *, #104928, .F. ) ;
#54568=CIRCLE ( 'NONE', #96254, 0.2000000000000057288 ) ;
#54613=ORIENTED_EDGE ( 'NONE', *, *, #158967, .T. ) ;
#54651=CARTESIAN_POINT ( 'NONE',  ( 21.93340585971692747, 7.324147022868173984, -100.5000000000000426 ) ) ;
#54665=AXIS2_PLACEMENT_3D ( 'NONE', #141056, #19835, #143611 ) ;
#54693=ADVANCED_FACE ( 'NONE', ( #34273 ), #152936, .T. ) ;
#54707=LINE ( 'NONE', #235900, #28175 ) ;
#54731=DIRECTION ( 'NONE',  ( -0.000000000000000000, 0.000000000000000000, -1.000000000000000000 ) ) ;
#54736=ORIENTED_EDGE ( 'NONE', *, *, #223473, .T. ) ;
#54740=DIRECTION ( 'NONE',  ( 1.000000000000000000, -0.000000000000000000, -0.000000000000000000 ) ) ;
#54798=CARTESIAN_POINT ( 'NONE',  ( 23.14999999999999858, 1.115600667400684642E-11, -134.0000000000000284 ) ) ;
#54809=DIRECTION ( 'NONE',  ( -1.000000000000000000, -0.000000000000000000, 0.000000000000000000 ) ) ;
#54816=EDGE_CURVE ( 'NONE', #217495, #118818, #19830, .T. ) ;
#54821=VERTEX_POINT ( 'NONE', #240148 ) ;
#54822=DIRECTION ( 'NONE',  ( -4.408576920032448588E-17, 0.1350103645451876666, -0.9908441862701600211 ) ) ;
#54841=ORIENTED_EDGE ( 'NONE', *, *, #225689, .T. ) ;
#54853=AXIS2_PLACEMENT_3D ( 'NONE', #243626, #225324, #83241 ) ;
#54862=ADVANCED_FACE ( 'NONE', ( #199753 ), #99317, .T. ) ;
#54874=ADVANCED_FACE ( 'NONE', ( #238857 ), #81040, .F. ) ;
#54882=ORIENTED_EDGE ( 'NONE', *, *, #90224, .T. ) ;
#54909=EDGE_CURVE ( 'NONE', #120853, #123327, #88903, .T. ) ;
#54914=VERTEX_POINT ( 'NONE', #243981 ) ;
#54920=CARTESIAN_POINT ( 'NONE',  ( 18.43565242384934422, -9.519327731081284938, -107.4729763765593731 ) ) ;
#55001=CARTESIAN_POINT ( 'NONE',  ( -21.09813707148783379, 0.03135149954058890492, -94.11493789426334899 ) ) ;
#55029=ORIENTED_EDGE ( 'NONE', *, *, #42173, .F. ) ;
#55031=DIRECTION ( 'NONE',  ( 0.000000000000000000, 1.000000000000000000, 0.000000000000000000 ) ) ;
#55042=EDGE_LOOP ( 'NONE', ( #141445, #80553, #87928, #41444 ) ) ;
#55045=EDGE_LOOP ( 'NONE', ( #229172, #106642, #69090, #163384 ) ) ;
#55062=ORIENTED_EDGE ( 'NONE', *, *, #85724, .F. ) ;
#55065=LINE ( 'NONE', #178932, #98178 ) ;
#55067=CARTESIAN_POINT ( 'NONE',  ( -23.25000000000000000, 11.75000000001115552, -121.8500000000000227 ) ) ;
#55068=ORIENTED_EDGE ( 'NONE', *, *, #69602, .F. ) ;
#55071=ORIENTED_EDGE ( 'NONE', *, *, #148795, .F. ) ;
#55105=CARTESIAN_POINT ( 'NONE',  ( -18.50211644919735932, 10.30207779525983192, -139.4895520716782755 ) ) ;
#55136=DIRECTION ( 'NONE',  ( -6.938893903907222856E-15, 1.000000000000000000, 2.891205793294679805E-16 ) ) ;
#55142=CARTESIAN_POINT ( 'NONE',  ( 23.14999999999999503, 6.450000000011156587, -88.75000000000004263 ) ) ;
#55143=ORIENTED_EDGE ( 'NONE', *, *, #47046, .T. ) ;
#55169=DIRECTION ( 'NONE',  ( 0.000000000000000000, 0.000000000000000000, 1.000000000000000000 ) ) ;
#55188=AXIS2_PLACEMENT_3D ( 'NONE', #97418, #156172, #235668 ) ;
#55212=ADVANCED_FACE ( 'NONE', ( #117323 ), #196843, .T. ) ;
#55213=SPHERICAL_SURFACE ( 'NONE', #58864, 0.1000000000000000056 ) ;
#55223=CARTESIAN_POINT ( 'NONE',  ( 18.49999999999999289, 11.75000000001115552, -125.3500000000000512 ) ) ;
#55254=ORIENTED_EDGE ( 'NONE', *, *, #233955, .F. ) ;
#55265=ORIENTED_EDGE ( 'NONE', *, *, #95038, .T. ) ;
#55272=EDGE_CURVE ( 'NONE', #247168, #224679, #97245, .T. ) ;
#55285=EDGE_CURVE ( 'NONE', #96459, #34079, #251416, .T. ) ;
#55307=CARTESIAN_POINT ( 'NONE',  ( -23.15000000000000213, 11.65000000001115588, -121.8500000000000369 ) ) ;
#55326=CARTESIAN_POINT ( 'NONE',  ( 23.15000000000000213, -9.599999999988842347, -124.1060308773475924 ) ) ;
#55343=DIRECTION ( 'NONE',  ( 0.000000000000000000, 0.1575844902526876978, 0.9875055080513731598 ) ) ;
#55360=ORIENTED_EDGE ( 'NONE', *, *, #128003, .F. ) ;
#55369=AXIS2_PLACEMENT_3D ( 'NONE', #172974, #249905, #189930 ) ;
#55393=CARTESIAN_POINT ( 'NONE',  ( 21.04999999999999716, -0.03753606327451301794, -94.16772772606439901 ) ) ;
#55405=DIRECTION ( 'NONE',  ( -1.836970198721029934E-16, 1.000000000000000000, 0.000000000000000000 ) ) ;
#55445=DIRECTION ( 'NONE',  ( 0.000000000000000000, -0.9893560106964500722, 0.1455152366551550613 ) ) ;
#55473=DIRECTION ( 'NONE',  ( 0.000000000000000000, -6.308085367188393199E-16, -1.000000000000000000 ) ) ;
#55479=ADVANCED_FACE ( 'NONE', ( #177958 ), #30870, .T. ) ;
#55575=LINE ( 'NONE', #39930, #117992 ) ;
#55582=CARTESIAN_POINT ( 'NONE',  ( -20.64999999999999858, 7.250000000011155521, -121.6500000000000341 ) ) ;
#55613=VERTEX_POINT ( 'NONE', #123117 ) ;
#55645=VERTEX_POINT ( 'NONE', #203924 ) ;
#55647=CARTESIAN_POINT ( 'NONE',  ( 20.94999999999999929, 11.65000000001115943, -134.0000000000000284 ) ) ;
#55648=ORIENTED_EDGE ( 'NONE', *, *, #213135, .T. ) ;
#55658=DIRECTION ( 'NONE',  ( 0.000000000000000000, 0.000000000000000000, -1.000000000000000000 ) ) ;
#55795=( NAMED_UNIT ( * ) PLANE_ANGLE_UNIT ( ) SI_UNIT ( $, .RADIAN. ) );
#55807=LINE ( 'NONE', #135367, #247865 ) ;
#55810=CYLINDRICAL_SURFACE ( 'NONE', #81193, 0.09999999999999939493 ) ;
#55823=AXIS2_PLACEMENT_3D ( 'NONE', #169244, #190055, #109216 ) ;
#55838=CARTESIAN_POINT ( 'NONE',  ( 19.92426406871192412, 11.75000000001116085, -125.3500000000000512 ) ) ;
#55843=ORIENTED_EDGE ( 'NONE', *, *, #159153, .T. ) ;
#55858=AXIS2_PLACEMENT_3D ( 'NONE', #226267, #208039, #9813 ) ;
#55861=VECTOR ( 'NONE', #143385, 1000.000000000000000 ) ;
#55884=ADVANCED_FACE ( 'NONE', ( #95534 ), #216762, .T. ) ;
#55887=ORIENTED_EDGE ( 'NONE', *, *, #85209, .F. ) ;
#55896=ORIENTED_EDGE ( 'NONE', *, *, #185421, .F. ) ;
#55901=CARTESIAN_POINT ( 'NONE',  ( 21.05000000000000071, 10.72371710471867701, -112.6500000000000341 ) ) ;
#55907=EDGE_CURVE ( 'NONE', #157934, #253084, #164316, .T. ) ;
#55947=ORIENTED_EDGE ( 'NONE', *, *, #72850, .T. ) ;
#55951=CARTESIAN_POINT ( 'NONE',  ( 21.05000000000000071, 1.115600667400684642E-11, -134.0000000000000284 ) ) ;
#56014=ORIENTED_EDGE ( 'NONE', *, *, #154436, .F. ) ;
#56022=ADVANCED_FACE ( 'NONE', ( #240198 ), #141093, .F. ) ;
#56065=DIRECTION ( 'NONE',  ( 0.000000000000000000, 0.000000000000000000, 1.000000000000000000 ) ) ;
#56082=DIRECTION ( 'NONE',  ( 0.000000000000000000, 0.000000000000000000, -1.000000000000000000 ) ) ;
#56108=SPHERICAL_SURFACE ( 'NONE', #244961, 0.1000000000000000056 ) ;
#56133=LINE ( 'NONE', #139528, #192262 ) ;
#56160=B_SPLINE_CURVE_WITH_KNOTS ( 'NONE', 3,
 ( #79785, #178952, #116383, #53832, #195928, #156816 ),
 .UNSPECIFIED., .F., .F.,
 ( 4, 2, 4 ),
 ( 0.000000000000000000, 0.0001496588209255844779, 0.0002993176418511689558 ),
 .UNSPECIFIED. ) ;
#56217=ORIENTED_EDGE ( 'NONE', *, *, #38088, .F. ) ;
#56226=DIRECTION ( 'NONE',  ( 0.000000000000000000, 0.000000000000000000, -1.000000000000000000 ) ) ;
#56233=AXIS2_PLACEMENT_3D ( 'NONE', #55142, #156881, #134697 ) ;
#56268=ORIENTED_EDGE ( 'NONE', *, *, #19963, .F. ) ;
#56397=CARTESIAN_POINT ( 'NONE',  ( -21.44999999999999929, 7.150000000011155876, -121.6500000000000341 ) ) ;
#56433=DIRECTION ( 'NONE',  ( -0.7071067811865389130, 0.000000000000000000, 0.7071067811865561215 ) ) ;
#56434=VERTEX_POINT ( 'NONE', #74877 ) ;
#56443=DIRECTION ( 'NONE',  ( -0.000000000000000000, -0.1298341882520022694, -0.9915357197604853789 ) ) ;
#56504=ORIENTED_EDGE ( 'NONE', *, *, #191577, .T. ) ;
#56517=CARTESIAN_POINT ( 'NONE',  ( -23.15000000000000213, 2.600000000011154278, -120.7753780772379315 ) ) ;
#56535=ORIENTED_EDGE ( 'NONE', *, *, #55285, .F. ) ;
#56546=DIRECTION ( 'NONE',  ( 1.000000000000000000, 7.304098846218134667E-16, 0.000000000000000000 ) ) ;
#56572=EDGE_LOOP ( 'NONE', ( #194, #73275, #195619, #233594 ) ) ;
#56576=ORIENTED_EDGE ( 'NONE', *, *, #72005, .F. ) ;
#56586=ORIENTED_EDGE ( 'NONE', *, *, #256226, .T. ) ;
#56597=ORIENTED_EDGE ( 'NONE', *, *, #253795, .F. ) ;
#56606=DIRECTION ( 'NONE',  ( 0.000000000000000000, 0.000000000000000000, 1.000000000000000000 ) ) ;
#56618=VECTOR ( 'NONE', #242433, 1000.000000000000000 ) ;
#56633=DIRECTION ( 'NONE',  ( 0.000000000000000000, 0.000000000000000000, -1.000000000000000000 ) ) ;
#56650=CARTESIAN_POINT ( 'NONE',  ( -21.05000000000000071, 1.750000000011155743, -112.1695115579016857 ) ) ;
#56657=VECTOR ( 'NONE', #126153, 1000.000000000000000 ) ;
#56741=DIRECTION ( 'NONE',  ( 0.000000000000000000, 0.000000000000000000, 1.000000000000000000 ) ) ;
#56750=EDGE_LOOP ( 'NONE', ( #169294, #252716, #10128 ) ) ;
#56756=ADVANCED_FACE ( 'NONE', ( #250281 ), #172064, .T. ) ;
#56773=ORIENTED_EDGE ( 'NONE', *, *, #169361, .T. ) ;
#56774=ORIENTED_EDGE ( 'NONE', *, *, #176082, .T. ) ;
#56799=DIRECTION ( 'NONE',  ( -2.840903330521631775E-16, 0.8700118002898321601, -0.4930308989875230030 ) ) ;
#56831=CARTESIAN_POINT ( 'NONE',  ( 18.58222699835054570, 10.33200063080772324, -139.5931674956643462 ) ) ;
#56876=ORIENTED_EDGE ( 'NONE', *, *, #217989, .T. ) ;
#56928=DIRECTION ( 'NONE',  ( 0.000000000000000000, -1.000000000000000000, 0.000000000000000000 ) ) ;
#56938=EDGE_LOOP ( 'NONE', ( #253881, #88453, #99022, #173525, #59059, #32923, #233563 ) ) ;
#57008=AXIS2_PLACEMENT_3D ( 'NONE', #40276, #237167, #37703 ) ;
#57032=CARTESIAN_POINT ( 'NONE',  ( 21.05000000000000071, 5.500000000011153745, -121.5947339810869465 ) ) ;
#57040=EDGE_CURVE ( 'NONE', #157934, #104851, #45350, .T. ) ;
#57045=CIRCLE ( 'NONE', #86084, 11.74999999999999645 ) ;
#57050=EDGE_CURVE ( 'NONE', #179995, #21528, #144420, .T. ) ;
#57051=EDGE_CURVE ( 'NONE', #95316, #86438, #110869, .T. ) ;
#57068=ADVANCED_FACE ( 'NONE', ( #148307 ), #204410, .T. ) ;
#57079=CARTESIAN_POINT ( 'NONE',  ( -20.54999999999999716, -9.499999999988846255, -124.1060308773475924 ) ) ;
#57088=DIRECTION ( 'NONE',  ( 0.000000000000000000, 1.000000000000000000, -6.308085367188393199E-16 ) ) ;
#57102=DIRECTION ( 'NONE',  ( -3.265361837132813093E-16, 1.000000000000000000, 0.000000000000000000 ) ) ;
#57103=CIRCLE ( 'NONE', #102899, 0.1000000000000028644 ) ;
#57109=AXIS2_PLACEMENT_3D ( 'NONE', #123007, #184246, #120462 ) ;
#57132=CARTESIAN_POINT ( 'NONE',  ( 23.14999999999998437, 4.050000000011155343, -100.5000000000000284 ) ) ;
#57138=CARTESIAN_POINT ( 'NONE',  ( -18.50000000000000000, 11.75000000001115197, -88.75000000000004263 ) ) ;
#57148=ORIENTED_EDGE ( 'NONE', *, *, #32053, .T. ) ;
#57149=DIRECTION ( 'NONE',  ( 0.000000000000000000, 0.000000000000000000, -1.000000000000000000 ) ) ;
#57168=CARTESIAN_POINT ( 'NONE',  ( -20.00857864376270001, 9.150000000011157653, -121.6500000000000341 ) ) ;
#57175=ORIENTED_EDGE ( 'NONE', *, *, #9110, .T. ) ;
#57189=CARTESIAN_POINT ( 'NONE',  ( 21.14261333020286671, 10.71569264926606202, -112.7500000000002558 ) ) ;
#57193=ORIENTED_EDGE ( 'NONE', *, *, #197179, .T. ) ;
#57245=CARTESIAN_POINT ( 'NONE',  ( -21.05000000000000071, 1.162701749949165642, -108.5000000000000426 ) ) ;
#57269=EDGE_CURVE ( 'NONE', #108506, #99810, #123520, .T. ) ;
#57296=CARTESIAN_POINT ( 'NONE',  ( -20.54999999999999716, 2.000000000011154189, -120.7753780772379315 ) ) ;
#57308=VECTOR ( 'NONE', #137593, 1000.000000000000000 ) ;
#57315=EDGE_CURVE ( 'NONE', #146245, #46505, #148470, .T. ) ;
#57350=DIRECTION ( 'NONE',  ( 0.000000000000000000, 0.000000000000000000, -1.000000000000000000 ) ) ;
#57365=CARTESIAN_POINT ( 'NONE',  ( -18.59999999999999787, 9.350000000011156942, -121.6500000000000341 ) ) ;
#57367=ORIENTED_EDGE ( 'NONE', *, *, #247528, .T. ) ;
#57435=ORIENTED_EDGE ( 'NONE', *, *, #189707, .T. ) ;
#57454=ORIENTED_EDGE ( 'NONE', *, *, #194739, .T. ) ;
#57456=VECTOR ( 'NONE', #132956, 1000.000000000000000 ) ;
#57535=ORIENTED_EDGE ( 'NONE', *, *, #77891, .F. ) ;
#57602=DIRECTION ( 'NONE',  ( 0.000000000000000000, 1.000000000000000000, 0.000000000000000000 ) ) ;
#57610=PLANE ( 'NONE',  #24596 ) ;
#57623=EDGE_CURVE ( 'NONE', #161165, #27184, #210542, .T. ) ;
#57638=ORIENTED_EDGE ( 'NONE', *, *, #66168, .F. ) ;
#57673=ORIENTED_EDGE ( 'NONE', *, *, #39955, .F. ) ;
#57683=ADVANCED_FACE ( 'NONE', ( #196118 ), #248028, .T. ) ;
#57708=AXIS2_PLACEMENT_3D ( 'NONE', #199808, #180236, #100649 ) ;
#57745=ORIENTED_EDGE ( 'NONE', *, *, #101940, .T. ) ;
#57772=CARTESIAN_POINT ( 'NONE',  ( -22.39999999999999858, 11.65000000001115588, -100.4000000000000483 ) ) ;
#57833=ORIENTED_EDGE ( 'NONE', *, *, #120516, .F. ) ;
#57853=DIRECTION ( 'NONE',  ( 2.940209281316622495E-16, -1.000000000000000000, -2.352167425053297996E-15 ) ) ;
#57867=DIRECTION ( 'NONE',  ( -1.000000000000000000, -0.000000000000000000, -0.000000000000000000 ) ) ;
#57874=DIRECTION ( 'NONE',  ( 0.000000000000000000, 0.5000000000000078826, -0.8660254037844340447 ) ) ;
#57890=EDGE_CURVE ( 'NONE', #128969, #24871, #231305, .T. ) ;
#57905=LINE ( 'NONE', #14966, #66656 ) ;
#57916=CARTESIAN_POINT ( 'NONE',  ( -21.05000000000000071, 1.115600667400684642E-11, -100.5000000000000284 ) ) ;
#57928=EDGE_CURVE ( 'NONE', #53442, #114232, #14837, .T. ) ;
#57946=DIRECTION ( 'NONE',  ( 0.000000000000000000, 1.000000000000000000, 0.000000000000000000 ) ) ;
#57949=DIRECTION ( 'NONE',  ( 0.000000000000000000, 0.000000000000000000, -1.000000000000000000 ) ) ;
#57961=DIRECTION ( 'NONE',  ( 0.000000000000000000, 0.5000000000000078826, -0.8660254037844340447 ) ) ;
#57966=AXIS2_PLACEMENT_3D ( 'NONE', #11209, #33374, #95853 ) ;
#58013=CARTESIAN_POINT ( 'NONE',  ( -21.05000000000000071, 6.440770893673045450, -100.5175971870084908 ) ) ;
#58025=DIRECTION ( 'NONE',  ( 0.000000000000000000, 1.776356839400310418E-15, -1.000000000000000000 ) ) ;
#58054=LINE ( 'NONE', #115476, #75175 ) ;
#58064=CARTESIAN_POINT ( 'NONE',  ( -18.50000000000000000, -1.835341550213255957, -112.0551512925630107 ) ) ;
#58071=DIRECTION ( 'NONE',  ( 1.000000000000000000, 0.000000000000000000, 0.000000000000000000 ) ) ;
#58131=ADVANCED_FACE ( 'NONE', ( #195837 ), #216654, .T. ) ;
#58140=EDGE_LOOP ( 'NONE', ( #148620, #95803, #92289 ) ) ;
#58177=CARTESIAN_POINT ( 'NONE',  ( 18.59999999999999076, 1.835341550235567887, -112.0551512925630249 ) ) ;
#58199=CARTESIAN_POINT ( 'NONE',  ( -22.39999999999999858, 7.790779598384560245, -100.4000000000000341 ) ) ;
#58221=EDGE_LOOP ( 'NONE', ( #146090, #190715, #30536, #177692 ) ) ;
#58285=EDGE_CURVE ( 'NONE', #97978, #100999, #60753, .T. ) ;
#58286=ORIENTED_EDGE ( 'NONE', *, *, #39354, .F. ) ;
#58297=DIRECTION ( 'NONE',  ( 1.000000000000000000, 0.000000000000000000, 0.000000000000000000 ) ) ;
#58321=CARTESIAN_POINT ( 'NONE',  ( -22.50000000000000000, 1.115600667400684642E-11, -94.25000000000002842 ) ) ;
#58327=CARTESIAN_POINT ( 'NONE',  ( -23.15000000000000213, -8.999999999988846255, -110.3939691226524786 ) ) ;
#58334=DIRECTION ( 'NONE',  ( 0.000000000000000000, 0.000000000000000000, -1.000000000000000000 ) ) ;
#58343=ADVANCED_FACE ( 'NONE', ( #104386 ), #221762, .F. ) ;
#58346=ORIENTED_EDGE ( 'NONE', *, *, #167776, .F. ) ;
#58350=ORIENTED_EDGE ( 'NONE', *, *, #201833, .F. ) ;
#58369=FACE_OUTER_BOUND ( 'NONE', #122510, .T. ) ;
#58378=CARTESIAN_POINT ( 'NONE',  ( 20.12500000000000355, 9.258049272928479567, -108.8633388371424644 ) ) ;
#58382=DIRECTION ( 'NONE',  ( 1.000000000000000000, 3.265361837132813093E-16, -0.000000000000000000 ) ) ;
#58413=DIRECTION ( 'NONE',  ( 0.000000000000000000, 0.000000000000000000, -1.000000000000000000 ) ) ;
#58422=FACE_OUTER_BOUND ( 'NONE', #187783, .T. ) ;
#58429=VERTEX_POINT ( 'NONE', #49579 ) ;
#58439=EDGE_LOOP ( 'NONE', ( #235205, #20204, #77339, #212753 ) ) ;
#58452=CARTESIAN_POINT ( 'NONE',  ( 23.14999999999999503, 11.65000000001116298, -121.7500000000000426 ) ) ;
#58458=ORIENTED_EDGE ( 'NONE', *, *, #211675, .T. ) ;
#58461=EDGE_CURVE ( 'NONE', #208327, #105004, #148695, .T. ) ;
#58472=CARTESIAN_POINT ( 'NONE',  ( -20.64999999999999858, 2.000000000011154189, -113.7246219227621395 ) ) ;
#58481=ORIENTED_EDGE ( 'NONE', *, *, #124650, .T. ) ;
#58525=CARTESIAN_POINT ( 'NONE',  ( 21.05000000000000071, -9.499999999988844479, -124.1060308773475924 ) ) ;
#58526=EDGE_CURVE ( 'NONE', #39812, #135828, #2684, .T. ) ;
#58538=DIRECTION ( 'NONE',  ( 0.000000000000000000, 0.000000000000000000, -1.000000000000000000 ) ) ;
#58555=DIRECTION ( 'NONE',  ( 1.000000000000000000, -0.000000000000000000, -0.000000000000000000 ) ) ;
#58559=EDGE_CURVE ( 'NONE', #128415, #22177, #149349, .T. ) ;
#58560=DIRECTION ( 'NONE',  ( 0.000000000000000000, -1.000000000000000000, 0.000000000000000000 ) ) ;
#58585=CARTESIAN_POINT ( 'NONE',  ( -20.64999999999999858, 1.115600667400684642E-11, -100.5000000000000284 ) ) ;
#58609=VECTOR ( 'NONE', #205833, 1000.000000000000000 ) ;
#58610=DIRECTION ( 'NONE',  ( 4.336808689942128177E-15, 0.8660254037844330455, -0.5000000000000096589 ) ) ;
#58626=AXIS2_PLACEMENT_3D ( 'NONE', #199322, #237162, #140609 ) ;
#58681=AXIS2_PLACEMENT_3D ( 'NONE', #30909, #214325, #16152 ) ;
#58697=CARTESIAN_POINT ( 'NONE',  ( 21.09546886439552438, 8.878553113026075749, -112.7370938505550413 ) ) ;
#58778=VERTEX_POINT ( 'NONE', #153207 ) ;
#58797=EDGE_CURVE ( 'NONE', #193670, #168409, #223443, .T. ) ;
#58807=ORIENTED_EDGE ( 'NONE', *, *, #212165, .T. ) ;
#58864=AXIS2_PLACEMENT_3D ( 'NONE', #76090, #209503, #10027 ) ;
#58866=CARTESIAN_POINT ( 'NONE',  ( 21.05000000000000071, 5.000000000011153745, -112.9052660189131245 ) ) ;
#58869=CARTESIAN_POINT ( 'NONE',  ( -21.09096482362058111, 0.03944827878523731596, -94.13645563459554921 ) ) ;
#58875=CARTESIAN_POINT ( 'NONE',  ( -20.64999999999999858, -9.399999999988850163, -110.3939691226524786 ) ) ;
#58876=CARTESIAN_POINT ( 'NONE',  ( 20.94999999999999929, 1.115600667400684642E-11, -100.5000000000000284 ) ) ;
#58886=AXIS2_PLACEMENT_3D ( 'NONE', #68590, #150689, #226345 ) ;
#58892=EDGE_LOOP ( 'NONE', ( #2082, #229861, #224542, #146085 ) ) ;
#58942=DIRECTION ( 'NONE',  ( 1.000000000000000000, -7.304098846218133681E-16, 4.217023435051677994E-16 ) ) ;
#58979=B_SPLINE_CURVE_WITH_KNOTS ( 'NONE', 3,
 ( #215129, #156475, #76891, #39082, #255485, #238539, #79450, #195590, #20801, #159035 ),
 .UNSPECIFIED., .F., .F.,
 ( 4, 3, 3, 4 ),
 ( 0.000000000000000000, 0.0002000000000002884074, 0.001000000000045107602, 0.001967863649472132576 ),
 .UNSPECIFIED. ) ;
#58980=DIRECTION ( 'NONE',  ( -1.000000000000000000, -2.952720810173289112E-16, 0.000000000000000000 ) ) ;
#58986=ORIENTED_EDGE ( 'NONE', *, *, #36762, .F. ) ;
#58992=ADVANCED_FACE ( 'NONE', ( #64352 ), #125597, .T. ) ;
#59012=DIRECTION ( 'NONE',  ( -1.000000000000000000, 0.000000000000000000, 0.000000000000000000 ) ) ;
#59018=ADVANCED_FACE ( 'NONE', ( #48626 ), #222103, .T. ) ;
#59059=ORIENTED_EDGE ( 'NONE', *, *, #238403, .F. ) ;
#59117=VECTOR ( 'NONE', #71296, 1000.000000000000000 ) ;
#59120=EDGE_CURVE ( 'NONE', #172421, #81295, #134570, .T. ) ;
#59128=CARTESIAN_POINT ( 'NONE',  ( 18.59999999999998366, 7.021664781911246322, -137.8335654018973457 ) ) ;
#59137=AXIS2_PLACEMENT_3D ( 'NONE', #249546, #206553, #7059 ) ;
#59138=VERTEX_POINT ( 'NONE', #109877 ) ;
#59175=CARTESIAN_POINT ( 'NONE',  ( 21.05000000000000071, -0.08559286335111412902, -94.08633726513041040 ) ) ;
#59178=EDGE_LOOP ( 'NONE', ( #160985, #113885, #107660, #169795 ) ) ;
#59195=AXIS2_PLACEMENT_3D ( 'NONE', #51824, #131380, #197771 ) ;
#59242=ORIENTED_EDGE ( 'NONE', *, *, #246609, .T. ) ;
#59266=DIRECTION ( 'NONE',  ( -0.000000000000000000, -0.000000000000000000, 1.000000000000000000 ) ) ;
#59290=LINE ( 'NONE', #102275, #239913 ) ;
#59298=ORIENTED_EDGE ( 'NONE', *, *, #73456, .F. ) ;
#59321=CARTESIAN_POINT ( 'NONE',  ( 21.05000000000000071, -8.999999999988842703, -124.1060308773475924 ) ) ;
#59335=CARTESIAN_POINT ( 'NONE',  ( -21.05000000000000071, 5.900000000011102586, -110.7190997646564483 ) ) ;
#59349=EDGE_CURVE ( 'NONE', #8739, #186134, #87472, .T. ) ;
#59383=CARTESIAN_POINT ( 'NONE',  ( -20.94999999999999929, 1.115600667400684642E-11, -134.0000000000000284 ) ) ;
#59403=ORIENTED_EDGE ( 'NONE', *, *, #178712, .T. ) ;
#59438=ORIENTED_EDGE ( 'NONE', *, *, #140611, .T. ) ;
#59464=CARTESIAN_POINT ( 'NONE',  ( 20.00000000000000355, 11.75000000001116263, -125.1500000000000341 ) ) ;
#59509=CARTESIAN_POINT ( 'NONE',  ( -18.50000000000000000, 7.021664781911246322, -137.8335654018973457 ) ) ;
#59534=DIRECTION ( 'NONE',  ( 0.000000000000000000, 0.6728971962616697722, -0.7397360091702875895 ) ) ;
#59549=ORIENTED_EDGE ( 'NONE', *, *, #234814, .T. ) ;
#59568=ORIENTED_EDGE ( 'NONE', *, *, #223244, .T. ) ;
#59572=CARTESIAN_POINT ( 'NONE',  ( 20.94999999999999929, 5.850000000011105428, -110.6324972242780120 ) ) ;
#59573=CARTESIAN_POINT ( 'NONE',  ( 23.14999999999999858, 1.115600667400684642E-11, -100.5000000000000284 ) ) ;
#59584=DIRECTION ( 'NONE',  ( 0.000000000000000000, 0.000000000000000000, -1.000000000000000000 ) ) ;
#59592=CIRCLE ( 'NONE', #22054, 0.09999999999998898659 ) ;
#59639=CARTESIAN_POINT ( 'NONE',  ( -20.54999999999999716, 4.350000000011156054, -117.2500000000000284 ) ) ;
#59652=AXIS2_PLACEMENT_3D ( 'NONE', #35783, #57867, #257315 ) ;
#59663=CARTESIAN_POINT ( 'NONE',  ( -23.15000000000000213, 1.115600667400684642E-11, -113.3750000000000284 ) ) ;
#59670=ORIENTED_EDGE ( 'NONE', *, *, #150001, .T. ) ;
#59696=ORIENTED_EDGE ( 'NONE', *, *, #211255, .T. ) ;
#59697=DIRECTION ( 'NONE',  ( -1.000000000000000000, 0.000000000000000000, 0.000000000000000000 ) ) ;
#59706=AXIS2_PLACEMENT_3D ( 'NONE', #197679, #157313, #19050 ) ;
#59734=CIRCLE ( 'NONE', #222236, 0.1000000000000028644 ) ;
#59742=CARTESIAN_POINT ( 'NONE',  ( -21.00857864376268935, 11.60000000001115161, -107.4282032302755852 ) ) ;
#59758=TOROIDAL_SURFACE ( 'NONE', #84698, 11.70000000000000639, 0.1000000000000000056 ) ;
#59767=CARTESIAN_POINT ( 'NONE',  ( -20.94999999999999929, 1.750000000011155743, -112.1695115579016857 ) ) ;
#59797=CARTESIAN_POINT ( 'NONE',  ( 20.94999999999999574, -11.41227409413852989, -103.4000000000000341 ) ) ;
#59812=CARTESIAN_POINT ( 'NONE',  ( 23.15000000000000213, -8.999999999988842703, -124.6060308773475924 ) ) ;
#59837=DIRECTION ( 'NONE',  ( 0.000000000000000000, 0.000000000000000000, -1.000000000000000000 ) ) ;
#59840=ORIENTED_EDGE ( 'NONE', *, *, #217935, .T. ) ;
#59875=VERTEX_POINT ( 'NONE', #187566 ) ;
#59892=ORIENTED_EDGE ( 'NONE', *, *, #15905, .T. ) ;
#59894=CARTESIAN_POINT ( 'NONE',  ( -20.64999999999999858, -8.999999999988846255, -109.8939691226524786 ) ) ;
#59910=VECTOR ( 'NONE', #192797, 1000.000000000000000 ) ;
#59920=DIRECTION ( 'NONE',  ( -1.836970198721029934E-16, 1.000000000000000000, 0.000000000000000000 ) ) ;
#59998=ORIENTED_EDGE ( 'NONE', *, *, #137352, .T. ) ;
#60001=EDGE_CURVE ( 'NONE', #117118, #149981, #26746, .T. ) ;
#60069=CARTESIAN_POINT ( 'NONE',  ( -20.94999999999999929, -11.41227409413852811, -131.1000000000000227 ) ) ;
#60080=ADVANCED_FACE ( 'NONE', ( #251425 ), #229305, .T. ) ;
#60113=VERTEX_POINT ( 'NONE', #111935 ) ;
#60186=CARTESIAN_POINT ( 'NONE',  ( 18.59999999999999432, 1.637172712981537659, -112.0821533654720525 ) ) ;
#60189=CARTESIAN_POINT ( 'NONE',  ( -20.94999999999999929, 1.115600667400684642E-11, -100.5000000000000284 ) ) ;
#60201=EDGE_CURVE ( 'NONE', #255700, #226146, #183726, .T. ) ;
#60224=AXIS2_PLACEMENT_3D ( 'NONE', #171493, #11105, #8536 ) ;
#60236=DIRECTION ( 'NONE',  ( 1.000000000000000000, 7.304098846218134667E-16, -0.000000000000000000 ) ) ;
#60249=TOROIDAL_SURFACE ( 'NONE', #206009, 0.2000000000000000111, 0.1000000000000000056 ) ;
#60253=DIRECTION ( 'NONE',  ( 0.000000000000000000, 1.000000000000000000, 0.000000000000000000 ) ) ;
#60263=CARTESIAN_POINT ( 'NONE',  ( -20.94999999999999929, -1.835341550213255957, -112.1551512925630192 ) ) ;
#60270=FACE_OUTER_BOUND ( 'NONE', #4352, .T. ) ;
#60308=CARTESIAN_POINT ( 'NONE',  ( 21.51976009735019346, 6.910458441670357388, -100.5000000000000284 ) ) ;
#60313=VECTOR ( 'NONE', #17633, 1000.000000000000000 ) ;
#60318=EDGE_CURVE ( 'NONE', #211247, #66896, #50604, .T. ) ;
#60319=CYLINDRICAL_SURFACE ( 'NONE', #171084, 0.1000000000000101225 ) ;
#60329=AXIS2_PLACEMENT_3D ( 'NONE', #29361, #206673, #69745 ) ;
#60330=AXIS2_PLACEMENT_3D ( 'NONE', #66386, #84613, #145904 ) ;
#60334=DIRECTION ( 'NONE',  ( 0.000000000000000000, 0.000000000000000000, -1.000000000000000000 ) ) ;
#60358=VECTOR ( 'NONE', #118117, 1000.000000000000000 ) ;
#60378=AXIS2_PLACEMENT_3D ( 'NONE', #165203, #120969, #122232 ) ;
#60379=CARTESIAN_POINT ( 'NONE',  ( 22.59999999999999432, 0.1008583691098678403, -88.75043287651062940 ) ) ;
#60380=ORIENTED_EDGE ( 'NONE', *, *, #221047, .T. ) ;
#60440=CARTESIAN_POINT ( 'NONE',  ( -20.64999999999999858, -8.663551401858001100, -124.4758988819327215 ) ) ;
#60447=DIRECTION ( 'NONE',  ( 2.978066053179067751E-16, -1.000000000000000000, 0.000000000000000000 ) ) ;
#60449=ADVANCED_FACE ( 'NONE', ( #6070 ), #40113, .T. ) ;
#60450=DIRECTION ( 'NONE',  ( 0.000000000000000000, 0.000000000000000000, 1.000000000000000000 ) ) ;
#60458=ORIENTED_EDGE ( 'NONE', *, *, #204232, .F. ) ;
#60467=ORIENTED_EDGE ( 'NONE', *, *, #66022, .F. ) ;
#60493=ORIENTED_EDGE ( 'NONE', *, *, #220478, .F. ) ;
#60510=CARTESIAN_POINT ( 'NONE',  ( 20.94999999999999929, -9.399999999988844834, -124.1060308773475924 ) ) ;
#60512=CARTESIAN_POINT ( 'NONE',  ( 20.85000000000000142, 11.65000000001115943, -134.0000000000000284 ) ) ;
#60553=DIRECTION ( 'NONE',  ( 0.000000000000000000, 1.000000000000000000, 0.000000000000000000 ) ) ;
#60591=ORIENTED_EDGE ( 'NONE', *, *, #255726, .F. ) ;
#60618=VERTEX_POINT ( 'NONE', #172910 ) ;
#60627=VERTEX_POINT ( 'NONE', #254902 ) ;
#60648=DIRECTION ( 'NONE',  ( 1.000000000000000000, 0.000000000000000000, 0.000000000000000000 ) ) ;
#60661=AXIS2_PLACEMENT_3D ( 'NONE', #49018, #227650, #106403 ) ;
#60675=CARTESIAN_POINT ( 'NONE',  ( -21.22070241538126112, 6.469946272880768845, -100.4010809694650135 ) ) ;
#60686=CARTESIAN_POINT ( 'NONE',  ( 18.59999999999999432, -1.736257131586239844, -112.0686523290175245 ) ) ;
#60696=CARTESIAN_POINT ( 'NONE',  ( 21.05000000000000071, 6.540656951712399803, -100.6000000000000512 ) ) ;
#60717=ORIENTED_EDGE ( 'NONE', *, *, #61188, .F. ) ;
#60735=CARTESIAN_POINT ( 'NONE',  ( -18.59999999999999787, 1.115600667400684642E-11, -100.5000000000000284 ) ) ;
#60743=AXIS2_PLACEMENT_3D ( 'NONE', #102709, #105265, #205675 ) ;
#60744=ORIENTED_EDGE ( 'NONE', *, *, #132711, .T. ) ;
#60753=CIRCLE ( 'NONE', #85676, 0.09999999999999864553 ) ;
#60773=DIRECTION ( 'NONE',  ( 1.000000000000000000, 0.000000000000000000, 0.000000000000000000 ) ) ;
#60875=EDGE_CURVE ( 'NONE', #219752, #69817, #250705, .T. ) ;
#60903=FACE_BOUND ( 'NONE', #38401, .T. ) ;
#60914=DIRECTION ( 'NONE',  ( 1.000000000000000000, 0.000000000000000000, -0.000000000000000000 ) ) ;
#60946=DIRECTION ( 'NONE',  ( -1.000000000000000000, 0.000000000000000000, 0.000000000000000000 ) ) ;
#60965=CARTESIAN_POINT ( 'NONE',  ( 21.05000000000000071, 6.650000000011155876, -112.6500000000000341 ) ) ;
#61005=LINE ( 'NONE', #127413, #146002 ) ;
#61016=DIRECTION ( 'NONE',  ( 1.000000000000000000, 0.000000000000000000, 0.000000000000000000 ) ) ;
#61058=CARTESIAN_POINT ( 'NONE',  ( -18.59999999999999787, -1.835859311432481045, -145.5044391687985694 ) ) ;
#61076=B_SPLINE_CURVE_WITH_KNOTS ( 'NONE', 3,
 ( #159693, #20186, #140097, #41046, #236642, #99679 ),
 .UNSPECIFIED., .F., .F.,
 ( 4, 2, 4 ),
 ( 0.000000000000000000, 0.0001568709654583421050, 0.0003137419309166842099 ),
 .UNSPECIFIED. ) ;
#61087=AXIS2_PLACEMENT_3D ( 'NONE', #183039, #4375, #126911 ) ;
#61110=DIRECTION ( 'NONE',  ( 0.000000000000000000, -0.1298341882520079038, -0.9915357197604846018 ) ) ;
#61113=ORIENTED_EDGE ( 'NONE', *, *, #58285, .T. ) ;
#61116=ORIENTED_EDGE ( 'NONE', *, *, #200275, .F. ) ;
#61183=ORIENTED_EDGE ( 'NONE', *, *, #176614, .F. ) ;
#61188=EDGE_CURVE ( 'NONE', #128969, #101017, #18624, .T. ) ;
#61192=CARTESIAN_POINT ( 'NONE',  ( 18.49999999999999645, 1.115600667400684642E-11, -134.0000000000000284 ) ) ;
#61199=DIRECTION ( 'NONE',  ( 0.000000000000000000, 1.000000000000000000, 0.000000000000000000 ) ) ;
#61207=CARTESIAN_POINT ( 'NONE',  ( 20.85000000000000142, 1.115600667400684642E-11, -134.0000000000000284 ) ) ;
#61228=CARTESIAN_POINT ( 'NONE',  ( 18.49999999999999289, 10.25000000263022670, -125.1871719496316615 ) ) ;
#61265=DIRECTION ( 'NONE',  ( 1.000000000000000000, 7.304098846218134667E-16, -0.000000000000000000 ) ) ;
#61273=CARTESIAN_POINT ( 'NONE',  ( -21.98333005346336932, 1.115600667400684642E-11, -93.12592467094334836 ) ) ;
#61274=DIRECTION ( 'NONE',  ( 0.000000000000000000, 0.000000000000000000, 1.000000000000000000 ) ) ;
#61278=VERTEX_POINT ( 'NONE', #152395 ) ;
#61280=CARTESIAN_POINT ( 'NONE',  ( -1.820710678118657944, -9.929289321870186313, -125.2500000000000284 ) ) ;
#61289=DIRECTION ( 'NONE',  ( -1.000000000000000000, -0.000000000000000000, -0.000000000000000000 ) ) ;
#61319=FACE_OUTER_BOUND ( 'NONE', #37797, .T. ) ;
#61335=EDGE_CURVE ( 'NONE', #173164, #27007, #211057, .T. ) ;
#61347=ORIENTED_EDGE ( 'NONE', *, *, #123348, .T. ) ;
#61388=ADVANCED_FACE ( 'NONE', ( #37565 ), #178369, .F. ) ;
#61389=ORIENTED_EDGE ( 'NONE', *, *, #127897, .T. ) ;
#61391=DIRECTION ( 'NONE',  ( 1.000000000000000000, 0.000000000000000000, 0.000000000000000000 ) ) ;
#61454=AXIS2_PLACEMENT_3D ( 'NONE', #175855, #194140, #15502 ) ;
#61490=AXIS2_PLACEMENT_3D ( 'NONE', #201358, #80085, #239203 ) ;
#61492=LINE ( 'NONE', #41947, #111250 ) ;
#61556=DIRECTION ( 'NONE',  ( -1.000000000000000000, -0.000000000000000000, -0.000000000000000000 ) ) ;
#61557=EDGE_CURVE ( 'NONE', #155284, #218820, #17830, .T. ) ;
#61621=CIRCLE ( 'NONE', #140729, 0.09999999999998898659 ) ;
#61630=CIRCLE ( 'NONE', #15870, 4.299999999999956302 ) ;
#61646=AXIS2_PLACEMENT_3D ( 'NONE', #212174, #30991, #253834 ) ;
#61667=VERTEX_POINT ( 'NONE', #132489 ) ;
#61682=CIRCLE ( 'NONE', #207444, 0.09999999999998898659 ) ;
#61689=VERTEX_POINT ( 'NONE', #90775 ) ;
#61700=EDGE_CURVE ( 'NONE', #50700, #87387, #134537, .T. ) ;
#61747=CARTESIAN_POINT ( 'NONE',  ( 21.05000000000000071, 10.48443348965288990, -107.9568058014919245 ) ) ;
#61750=FACE_OUTER_BOUND ( 'NONE', #62672, .T. ) ;
#61784=CIRCLE ( 'NONE', #144976, 0.8750000000000007772 ) ;
#61800=EDGE_LOOP ( 'NONE', ( #165894, #26260, #106023 ) ) ;
#61809=FACE_OUTER_BOUND ( 'NONE', #160071, .T. ) ;
#61812=AXIS2_PLACEMENT_3D ( 'NONE', #38008, #97918, #161804 ) ;
#61819=CARTESIAN_POINT ( 'NONE',  ( -23.25000000000000000, -8.596261682231835621, -109.9501275171503210 ) ) ;
#61839=DIRECTION ( 'NONE',  ( -1.000000000000000000, -1.040834085586090568E-13, 0.000000000000000000 ) ) ;
#61847=EDGE_CURVE ( 'NONE', #28813, #221229, #172211, .T. ) ;
#61848=CARTESIAN_POINT ( 'NONE',  ( -23.25000000000000000, 4.150000000011156764, -112.8500000000000369 ) ) ;
#61850=CIRCLE ( 'NONE', #186955, 0.2000000000000057288 ) ;
#61862=CARTESIAN_POINT ( 'NONE',  ( -1.820710678118658388, -9.929289321870186313, -125.1500000000000341 ) ) ;
#61868=ORIENTED_EDGE ( 'NONE', *, *, #85730, .F. ) ;
#61878=ORIENTED_EDGE ( 'NONE', *, *, #4399, .T. ) ;
#61881=CARTESIAN_POINT ( 'NONE',  ( 18.39999999999999858, -9.599999999988842347, -107.5320693966997112 ) ) ;
#61905=CARTESIAN_POINT ( 'NONE',  ( 22.49999999999999645, 11.64987090377453960, -100.4174801091270979 ) ) ;
#61911=CIRCLE ( 'NONE', #28643, 4.049999999999998046 ) ;
#61914=VERTEX_POINT ( 'NONE', #232899 ) ;
#61915=DIRECTION ( 'NONE',  ( 0.000000000000000000, -1.000000000000000000, -0.000000000000000000 ) ) ;
#61948=VERTEX_POINT ( 'NONE', #20256 ) ;
#61980=ORIENTED_EDGE ( 'NONE', *, *, #245231, .F. ) ;
#61996=CIRCLE ( 'NONE', #199383, 0.1000000000000028644 ) ;
#61997=CIRCLE ( 'NONE', #28722, 0.09999999999999939493 ) ;
#61998=AXIS2_PLACEMENT_3D ( 'NONE', #139360, #98941, #242327 ) ;
#62078=ORIENTED_EDGE ( 'NONE', *, *, #185770, .F. ) ;
#62083=ORIENTED_EDGE ( 'NONE', *, *, #95603, .T. ) ;
#62119=ORIENTED_EDGE ( 'NONE', *, *, #83397, .F. ) ;
#62124=DIRECTION ( 'NONE',  ( 6.938893903907991995E-14, 0.000000000000000000, 1.000000000000000000 ) ) ;
#62160=TOROIDAL_SURFACE ( 'NONE', #16381, 0.2000000000000000111, 0.1000000000000000056 ) ;
#62165=ORIENTED_EDGE ( 'NONE', *, *, #90000, .T. ) ;
#62232=CARTESIAN_POINT ( 'NONE',  ( -18.59999999999999787, 11.65000000001115232, -107.5148057706540357 ) ) ;
#62252=AXIS2_PLACEMENT_3D ( 'NONE', #91105, #213611, #251457 ) ;
#62270=CIRCLE ( 'NONE', #141372, 1.900000000000012790 ) ;
#62271=TOROIDAL_SURFACE ( 'NONE', #78987, 11.65000000000000036, 0.1000000000000000056 ) ;
#62305=EDGE_CURVE ( 'NONE', #243146, #159674, #109972, .T. ) ;
#62316=AXIS2_PLACEMENT_3D ( 'NONE', #225450, #222894, #168118 ) ;
#62317=EDGE_CURVE ( 'NONE', #238459, #14749, #68298, .T. ) ;
#62334=LINE ( 'NONE', #178457, #205708 ) ;
#62339=EDGE_CURVE ( 'NONE', #114911, #114550, #47422, .T. ) ;
#62368=ORIENTED_EDGE ( 'NONE', *, *, #158967, .F. ) ;
#62373=CARTESIAN_POINT ( 'NONE',  ( 21.07094088545303734, 6.320167221927647461, -100.4011062974478250 ) ) ;
#62384=ORIENTED_EDGE ( 'NONE', *, *, #16983, .F. ) ;
#62419=PLANE ( 'NONE',  #165532 ) ;
#62421=CIRCLE ( 'NONE', #208170, 0.1000000000000028644 ) ;
#62429=ORIENTED_EDGE ( 'NONE', *, *, #151567, .T. ) ;
#62462=CARTESIAN_POINT ( 'NONE',  ( 20.94999999999999574, -11.48912529306490349, -103.6000000000000369 ) ) ;
#62468=CARTESIAN_POINT ( 'NONE',  ( -20.94999999999999929, -1.162701749926853712, -108.4000000000000341 ) ) ;
#62497=CARTESIAN_POINT ( 'NONE',  ( 18.59999999999999076, 11.65000000001115943, -125.3500000000000512 ) ) ;
#62504=VERTEX_POINT ( 'NONE', #86306 ) ;
#62518=CARTESIAN_POINT ( 'NONE',  ( 21.05000000000000071, -12.41227409413852811, -131.0000000000000284 ) ) ;
#62529=DIRECTION ( 'NONE',  ( 2.952720810173289112E-16, -1.000000000000000000, -0.000000000000000000 ) ) ;
#62551=TOROIDAL_SURFACE ( 'NONE', #108345, 12.77499999999999858, 0.1000000000000000056 ) ;
#62577=ORIENTED_EDGE ( 'NONE', *, *, #117671, .F. ) ;
#62598=CYLINDRICAL_SURFACE ( 'NONE', #176322, 0.1000000000000000472 ) ;
#62603=ADVANCED_FACE ( 'NONE', ( #146303 ), #150180, .T. ) ;
#62669=ORIENTED_EDGE ( 'NONE', *, *, #246560, .T. ) ;
#62672=EDGE_LOOP ( 'NONE', ( #40408, #37239, #165348, #223868 ) ) ;
#62696=EDGE_LOOP ( 'NONE', ( #192711, #86312, #256500 ) ) ;
#62702=CARTESIAN_POINT ( 'NONE',  ( 18.40000000000000213, -9.499999999988844479, -107.5320693966997112 ) ) ;
#62712=CIRCLE ( 'NONE', #45947, 4.000000000000003553 ) ;
#62773=DIRECTION ( 'NONE',  ( -0.000000000000000000, 0.000000000000000000, 1.000000000000000000 ) ) ;
#62788=DIRECTION ( 'NONE',  ( -0.000000000000000000, -1.000000000000000000, -1.734723475976807292E-15 ) ) ;
#62795=ORIENTED_EDGE ( 'NONE', *, *, #150679, .T. ) ;
#62799=CARTESIAN_POINT ( 'NONE',  ( 20.99999999999997868, 1.115600667400684642E-11, -100.5000000000000284 ) ) ;
#62810=ORIENTED_EDGE ( 'NONE', *, *, #217766, .F. ) ;
#62837=DIRECTION ( 'NONE',  ( -0.000000000000000000, -0.000000000000000000, 1.000000000000000000 ) ) ;
#62853=ORIENTED_EDGE ( 'NONE', *, *, #80809, .F. ) ;
#62888=DIRECTION ( 'NONE',  ( -1.000000000000000000, -0.000000000000000000, -0.000000000000000000 ) ) ;
#62897=CIRCLE ( 'NONE', #204540, 0.5000000000000004441 ) ;
#62902=CARTESIAN_POINT ( 'NONE',  ( 20.85000000000000142, 11.75000000001115907, -134.0000000000000284 ) ) ;
#62903=AXIS2_PLACEMENT_3D ( 'NONE', #23062, #202947, #183402 ) ;
#62929=CARTESIAN_POINT ( 'NONE',  ( 20.94999999999999929, 5.500000000011153745, -112.9052660189131245 ) ) ;
#62930=EDGE_CURVE ( 'NONE', #210814, #100043, #101344, .T. ) ;
#62941=CARTESIAN_POINT ( 'NONE',  ( 23.14999999999999858, 1.115600667400684642E-11, -134.0000000000000284 ) ) ;
#62956=VERTEX_POINT ( 'NONE', #203420 ) ;
#62957=CARTESIAN_POINT ( 'NONE',  ( -21.93340585899455419, 1.115541036281197940E-11, -93.17585297787972820 ) ) ;
#62959=ORIENTED_EDGE ( 'NONE', *, *, #126166, .F. ) ;
#62961=EDGE_LOOP ( 'NONE', ( #10028, #163116, #185389, #14499 ) ) ;
#62981=CARTESIAN_POINT ( 'NONE',  ( 20.94999999999999929, -8.999999999988844479, -110.3939691226524786 ) ) ;
#62993=CARTESIAN_POINT ( 'NONE',  ( 20.94999999999999574, 10.47338541492405994, -108.0786544642485865 ) ) ;
#63011=CARTESIAN_POINT ( 'NONE',  ( 21.07933241753356768, 6.328645948390904330, -100.4066204095807393 ) ) ;
#63015=EDGE_CURVE ( 'NONE', #201244, #31259, #68083, .T. ) ;
#63018=CARTESIAN_POINT ( 'NONE',  ( 23.24999999999999645, 1.115600667400684642E-11, -100.5000000000000284 ) ) ;
#63056=DIRECTION ( 'NONE',  ( -1.000000000000000000, 0.000000000000000000, 0.000000000000000000 ) ) ;
#63083=DIRECTION ( 'NONE',  ( 0.000000000000000000, 0.000000000000000000, -1.000000000000000000 ) ) ;
#63105=ADVANCED_FACE ( 'NONE', ( #218462 ), #38567, .T. ) ;
#63133=CIRCLE ( 'NONE', #208893, 0.1000000000000028644 ) ;
#63134=ORIENTED_EDGE ( 'NONE', *, *, #158554, .F. ) ;
#63136=AXIS2_PLACEMENT_3D ( 'NONE', #89016, #113417, #248098 ) ;
#63144=ORIENTED_EDGE ( 'NONE', *, *, #64454, .F. ) ;
#63151=DIRECTION ( 'NONE',  ( 0.000000000000000000, -0.000000000000000000, 1.000000000000000000 ) ) ;
#63170=ORIENTED_EDGE ( 'NONE', *, *, #57269, .T. ) ;
#63198=CARTESIAN_POINT ( 'NONE',  ( 20.95512820512820795, 10.62384868372303615, -112.7001620194244680 ) ) ;
#63220=CARTESIAN_POINT ( 'NONE',  ( -18.59999999999999787, -1.835859311432481045, -145.5044391687985694 ) ) ;
#63245=CIRCLE ( 'NONE', #209181, 2.000000000000001776 ) ;
#63247=DIRECTION ( 'NONE',  ( 1.000000000000000000, 3.265361837132813093E-16, -0.000000000000000000 ) ) ;
#63262=DIRECTION ( 'NONE',  ( 0.000000000000000000, -0.3738317757009345654, 0.9274965247785492695 ) ) ;
#63275=FACE_OUTER_BOUND ( 'NONE', #230283, .T. ) ;
#63283=DIRECTION ( 'NONE',  ( 0.000000000000000000, -0.7397360091702744889, 0.6728971962616842051 ) ) ;
#63353=CARTESIAN_POINT ( 'NONE',  ( 20.53930447208004040, 8.977148687536415039, -108.9425071415766553 ) ) ;
#63374=VERTEX_POINT ( 'NONE', #254690 ) ;
#63395=DIRECTION ( 'NONE',  ( 1.000000000000000000, -0.000000000000000000, -0.000000000000000000 ) ) ;
#63418=VECTOR ( 'NONE', #147465, 1000.000000000000000 ) ;
#63467=CARTESIAN_POINT ( 'NONE',  ( 18.59999999999999076, 6.650000000011155876, -121.7500000000000426 ) ) ;
#63473=CARTESIAN_POINT ( 'NONE',  ( -20.94999999999999929, -11.39257802169451672, -103.5739495798319751 ) ) ;
#63475=CARTESIAN_POINT ( 'NONE',  ( 21.07016717457010202, 1.116511100764040927E-11, -94.17905916189916127 ) ) ;
#63481=CIRCLE ( 'NONE', #184294, 0.09999999999999939493 ) ;
#63494=DIRECTION ( 'NONE',  ( 0.000000000000000000, 1.000000000000000000, 0.000000000000000000 ) ) ;
#63499=AXIS2_PLACEMENT_3D ( 'NONE', #161693, #145943, #182538 ) ;
#63530=ADVANCED_FACE ( 'NONE', ( #85052 ), #157629, .F. ) ;
#63533=B_SPLINE_CURVE_WITH_KNOTS ( 'NONE', 3,
 ( #44074, #123612, #203140, #85719, #183585, #165299, #4910, #89598, #71354, #206997, #249974, #68772, #150867, #208293, #107888, #8797 ),
 .UNSPECIFIED., .F., .F.,
 ( 4, 3, 3, 3, 3, 4 ),
 ( 0.000000000000000000, 2.209833635978075103E-05, 5.595056164119271205E-05, 8.979992002655367851E-05, 0.0001236482757198911655, 0.0001574984039362983660 ),
 .UNSPECIFIED. ) ;
#63571=DIRECTION ( 'NONE',  ( -0.000000000000000000, 1.000000000000000000, -1.224646799147352961E-16 ) ) ;
#63574=ADVANCED_FACE ( 'NONE', ( #2971 ), #15976, .T. ) ;
#63589=CARTESIAN_POINT ( 'NONE',  ( -18.54260524012593692, -9.624219390062691559, -140.7407730457707373 ) ) ;
#63649=ORIENTED_EDGE ( 'NONE', *, *, #30452, .F. ) ;
#63654=PLANE ( 'NONE',  #126114 ) ;
#63708=ORIENTED_EDGE ( 'NONE', *, *, #42807, .T. ) ;
#63709=CARTESIAN_POINT ( 'NONE',  ( -22.50000000000000000, 11.64976291804307884, -100.4111900236131021 ) ) ;
#63711=ADVANCED_FACE ( 'NONE', ( #128074 ), #248007, .T. ) ;
#63733=FACE_OUTER_BOUND ( 'NONE', #221030, .T. ) ;
#63737=CIRCLE ( 'NONE', #118077, 0.09999999999999939493 ) ;
#63829=ORIENTED_EDGE ( 'NONE', *, *, #191542, .F. ) ;
#63846=ORIENTED_EDGE ( 'NONE', *, *, #16732, .F. ) ;
#63858=CARTESIAN_POINT ( 'NONE',  ( 20.95512820512820440, 8.876151316299269567, -112.6500000000000341 ) ) ;
#63872=VERTEX_POINT ( 'NONE', #194486 ) ;
#63907=AXIS2_PLACEMENT_3D ( 'NONE', #64956, #124950, #204464 ) ;
#63926=CIRCLE ( 'NONE', #197181, 0.1000000000000008937 ) ;
#63947=AXIS2_PLACEMENT_3D ( 'NONE', #197110, #22362, #178885 ) ;
#63949=DIRECTION ( 'NONE',  ( 1.000000000000000000, 0.000000000000000000, 0.000000000000000000 ) ) ;
#63953=VECTOR ( 'NONE', #92681, 1000.000000000000000 ) ;
#63982=CARTESIAN_POINT ( 'NONE',  ( 18.59999999999999787, -9.321008403350148797, -107.7359382490778899 ) ) ;
#63989=ORIENTED_EDGE ( 'NONE', *, *, #176614, .T. ) ;
#64001=CARTESIAN_POINT ( 'NONE',  ( -20.64999999999999858, 4.350000000011156054, -112.8500000000000369 ) ) ;
#64015=VECTOR ( 'NONE', #13933, 1000.000000000000000 ) ;
#64031=FACE_OUTER_BOUND ( 'NONE', #53043, .T. ) ;
#64035=EDGE_CURVE ( 'NONE', #148820, #135828, #118508, .T. ) ;
#64038=ADVANCED_FACE ( 'NONE', ( #195488 ), #184235, .F. ) ;
#64046=DIRECTION ( 'NONE',  ( -1.000000000000000000, 0.000000000000000000, 0.000000000000000000 ) ) ;
#64097=VERTEX_POINT ( 'NONE', #183600 ) ;
#64102=CIRCLE ( 'NONE', #109874, 0.09999999999999892308 ) ;
#64109=DIRECTION ( 'NONE',  ( 1.000000000000000000, -0.000000000000000000, -0.000000000000000000 ) ) ;
#64140=ORIENTED_EDGE ( 'NONE', *, *, #228199, .F. ) ;
#64146=EDGE_LOOP ( 'NONE', ( #173372, #243648, #166532, #5946 ) ) ;
#64186=CARTESIAN_POINT ( 'NONE',  ( 21.05000000000000071, -1.736257131586239844, -112.0686523290175245 ) ) ;
#64197=AXIS2_PLACEMENT_3D ( 'NONE', #9757, #190996, #250923 ) ;
#64218=VERTEX_POINT ( 'NONE', #50471 ) ;
#64245=CARTESIAN_POINT ( 'NONE',  ( 22.49999999999999645, 0.04562336060752910510, -88.84949566144861421 ) ) ;
#64257=AXIS2_PLACEMENT_3D ( 'NONE', #167109, #169688, #69274 ) ;
#64267=DIRECTION ( 'NONE',  ( 0.000000000000000000, 0.000000000000000000, -1.000000000000000000 ) ) ;
#64299=DIRECTION ( 'NONE',  ( 1.000000000000000000, 2.952720810173289112E-16, -0.000000000000000000 ) ) ;
#64300=DIRECTION ( 'NONE',  ( 4.377807931758638789E-15, 0.2605042016806672911, 0.9654727137038716656 ) ) ;
#64324=ADVANCED_FACE ( 'NONE', ( #136423 ), #60249, .T. ) ;
#64329=B_SPLINE_CURVE_WITH_KNOTS ( 'NONE', 3,
 ( #168283, #127835, #7897, #108271, #69158, #114356, #207377, #153531, #133905, #246483, #213444, #28776, #106963, #126544, #105665, #148689 ),
 .UNSPECIFIED., .F., .F.,
 ( 4, 3, 3, 3, 3, 4 ),
 ( 0.000000000000000000, 2.372700795693552043E-05, 5.739057815866868386E-05, 9.073899019179277486E-05, 0.0001243544287365655867, 0.0001585386695601107032 ),
 .UNSPECIFIED. ) ;
#64331=CIRCLE ( 'NONE', #76793, 4.000000000000003553 ) ;
#64352=FACE_OUTER_BOUND ( 'NONE', #30165, .T. ) ;
#64356=CARTESIAN_POINT ( 'NONE',  ( -20.64999999999999858, 1.115600667400684642E-11, -100.5000000000000284 ) ) ;
#64357=CARTESIAN_POINT ( 'NONE',  ( 18.59999999999998721, 6.933893972137497030, -137.7856458343736108 ) ) ;
#64370=FACE_OUTER_BOUND ( 'NONE', #46262, .T. ) ;
#64377=VERTEX_POINT ( 'NONE', #153508 ) ;
#64407=DIRECTION ( 'NONE',  ( -0.000000000000000000, -0.000000000000000000, 1.000000000000000000 ) ) ;
#64419=ADVANCED_FACE ( 'NONE', ( #140281 ), #243243, .T. ) ;
#64429=ADVANCED_FACE ( 'NONE', ( #84123 ), #210301, .T. ) ;
#64431=DIRECTION ( 'NONE',  ( 0.7071067811865475727, 0.7071067811865475727, 0.000000000000000000 ) ) ;
#64437=DIRECTION ( 'NONE',  ( 0.000000000000000000, 1.000000000000000000, 0.000000000000000000 ) ) ;
#64440=CARTESIAN_POINT ( 'NONE',  ( -23.25000000000000000, -11.48912529306489994, -130.9000000000000341 ) ) ;
#64441=EDGE_CURVE ( 'NONE', #208598, #245837, #18742, .T. ) ;
#64454=EDGE_CURVE ( 'NONE', #217484, #60627, #214550, .T. ) ;
#64460=CARTESIAN_POINT ( 'NONE',  ( -23.15000000000000213, 4.150000000011156764, -112.8500000000000369 ) ) ;
#64505=DIRECTION ( 'NONE',  ( 0.000000000000000000, 0.1350103645451876666, 0.9908441862701600211 ) ) ;
#64506=ORIENTED_EDGE ( 'NONE', *, *, #13262, .F. ) ;
#64507=CARTESIAN_POINT ( 'NONE',  ( 20.96077737575349786, 11.62390063401585394, -127.1407919571063729 ) ) ;
#64522=DIRECTION ( 'NONE',  ( 1.000000000000000000, 0.000000000000000000, 0.000000000000000000 ) ) ;
#64569=DIRECTION ( 'NONE',  ( 0.000000000000000000, 1.000000000000000000, -0.000000000000000000 ) ) ;
#64582=CIRCLE ( 'NONE', #218697, 0.09999999999999693856 ) ;
#64595=ADVANCED_FACE ( 'NONE', ( #131976 ), #233661, .T. ) ;
#64600=CARTESIAN_POINT ( 'NONE',  ( 21.05000000000000071, 8.776282895303632259, -108.9880007215843989 ) ) ;
#64630=AXIS2_PLACEMENT_3D ( 'NONE', #417, #255983, #21314 ) ;
#64632=EDGE_CURVE ( 'NONE', #233320, #58778, #146694, .T. ) ;
#64640=CIRCLE ( 'NONE', #35656, 0.1000000000000028644 ) ;
#64662=CARTESIAN_POINT ( 'NONE',  ( -22.00411653962179770, 7.253442868381131170, -100.4009618941994404 ) ) ;
#64672=AXIS2_PLACEMENT_3D ( 'NONE', #113627, #233585, #173660 ) ;
#64687=VECTOR ( 'NONE', #115284, 1000.000000000000000 ) ;
#64689=CYLINDRICAL_SURFACE ( 'NONE', #96446, 0.09999999999999939493 ) ;
#64787=ORIENTED_EDGE ( 'NONE', *, *, #201848, .T. ) ;
#64866=EDGE_CURVE ( 'NONE', #159714, #161165, #202289, .T. ) ;
#64871=CARTESIAN_POINT ( 'NONE',  ( -18.50000000000000000, -9.480686695267820596, -140.9411151687578752 ) ) ;
#64883=DIRECTION ( 'NONE',  ( -0.000000000000000000, -1.000000000000000000, -0.000000000000000000 ) ) ;
#64891=AXIS2_PLACEMENT_3D ( 'NONE', #253382, #74791, #175184 ) ;
#64895=CARTESIAN_POINT ( 'NONE',  ( -20.54999999999999716, 7.150000000011155876, -112.7500000000000284 ) ) ;
#64909=EDGE_CURVE ( 'NONE', #201244, #246634, #189529, .T. ) ;
#64910=FACE_OUTER_BOUND ( 'NONE', #58140, .T. ) ;
#64912=EDGE_LOOP ( 'NONE', ( #245071, #192436, #243158, #56576, #76477, #245666, #22000, #181574, #142477, #57367, #189746, #139523, #132902, #28407, #66140, #155966 ) ) ;
#64923=ADVANCED_FACE ( 'NONE', ( #109530 ), #22812, .T. ) ;
#64956=CARTESIAN_POINT ( 'NONE',  ( 21.05000000000000071, 1.115600667400684642E-11, -134.0000000000000284 ) ) ;
#64964=ORIENTED_EDGE ( 'NONE', *, *, #206863, .F. ) ;
#64967=EDGE_CURVE ( 'NONE', #195862, #83522, #164680, .T. ) ;
#64972=ORIENTED_EDGE ( 'NONE', *, *, #150324, .F. ) ;
#64978=ORIENTED_EDGE ( 'NONE', *, *, #246478, .F. ) ;
#64992=DIRECTION ( 'NONE',  ( 0.000000000000000000, 0.000000000000000000, -1.000000000000000000 ) ) ;
#64997=VERTEX_POINT ( 'NONE', #59812 ) ;
#65008=FACE_OUTER_BOUND ( 'NONE', #190731, .T. ) ;
#65011=DIRECTION ( 'NONE',  ( 1.000000000000000000, 0.000000000000000000, -0.000000000000000000 ) ) ;
#65012=DIRECTION ( 'NONE',  ( -0.7071067811865389130, 8.659560562355038861E-17, -0.7071067811865561215 ) ) ;
#65031=EDGE_LOOP ( 'NONE', ( #176890, #95516, #171533, #243031 ) ) ;
#65033=CARTESIAN_POINT ( 'NONE',  ( 23.14999999999999858, 5.500000000011153745, -121.5947339810869465 ) ) ;
#65065=DIRECTION ( 'NONE',  ( 0.000000000000000000, 0.000000000000000000, 1.000000000000000000 ) ) ;
#65068=ORIENTED_EDGE ( 'NONE', *, *, #160864, .T. ) ;
#65115=CARTESIAN_POINT ( 'NONE',  ( -18.50000000000000000, -1.687074390080403941, -87.68542703345838163 ) ) ;
#65130=CARTESIAN_POINT ( 'NONE',  ( 21.04999999999999716, 8.871279686006799281, -112.6500000000000199 ) ) ;
#65134=DIRECTION ( 'NONE',  ( -1.000000000000000000, -3.265361837132813093E-16, 0.000000000000000000 ) ) ;
#65135=ADVANCED_FACE ( 'NONE', ( #44139 ), #110694, .T. ) ;
#65139=ORIENTED_EDGE ( 'NONE', *, *, #94095, .F. ) ;
#65155=CARTESIAN_POINT ( 'NONE',  ( -20.54999999999999716, 9.350000000011156942, -112.7500000000000284 ) ) ;
#65174=CIRCLE ( 'NONE', #136058, 11.64999999999999325 ) ;
#65198=ORIENTED_EDGE ( 'NONE', *, *, #13996, .T. ) ;
#65220=CARTESIAN_POINT ( 'NONE',  ( -20.00857864376270001, 9.150000000011157653, -121.7500000000000426 ) ) ;
#65259=CARTESIAN_POINT ( 'NONE',  ( 18.51565452909384746, -9.352859338825702196, -107.6949093212341353 ) ) ;
#65267=AXIS2_PLACEMENT_3D ( 'NONE', #222791, #44188, #243655 ) ;
#65273=ORIENTED_EDGE ( 'NONE', *, *, #26756, .F. ) ;
#65277=CARTESIAN_POINT ( 'NONE',  ( -21.00448002041558482, 11.75000000001147704, -107.3483408623108488 ) ) ;
#65286=DIRECTION ( 'NONE',  ( -1.000000000000000000, 0.000000000000000000, 0.000000000000000000 ) ) ;
#65287=DIRECTION ( 'NONE',  ( 0.000000000000000000, 1.000000000000000000, 0.000000000000000000 ) ) ;
#65305=CARTESIAN_POINT ( 'NONE',  ( -22.50014994444013894, 11.74971973190330843, -100.4169198432810788 ) ) ;
#65327=DIRECTION ( 'NONE',  ( 0.000000000000000000, 0.9908441862701596881, 0.1350103645451904977 ) ) ;
#65336=VECTOR ( 'NONE', #78096, 1000.000000000000000 ) ;
#65360=CARTESIAN_POINT ( 'NONE',  ( -23.15000000000000213, 1.910280373842936141, -113.1313678551989739 ) ) ;
#65400=DIRECTION ( 'NONE',  ( 0.000000000000000000, 0.000000000000000000, -1.000000000000000000 ) ) ;
#65410=AXIS2_PLACEMENT_3D ( 'NONE', #230492, #192653, #152261 ) ;
#65440=FACE_OUTER_BOUND ( 'NONE', #213876, .T. ) ;
#65462=ADVANCED_FACE ( 'NONE', ( #257667 ), #214751, .F. ) ;
#65505=ORIENTED_EDGE ( 'NONE', *, *, #132711, .F. ) ;
#65518=ORIENTED_EDGE ( 'NONE', *, *, #53008, .T. ) ;
#65538=DIRECTION ( 'NONE',  ( 1.000000000000000000, 0.000000000000000000, 0.000000000000000000 ) ) ;
#65543=CARTESIAN_POINT ( 'NONE',  ( -20.64999999999999858, 2.000000000011154189, -121.1753780772379230 ) ) ;
#65572=CARTESIAN_POINT ( 'NONE',  ( 20.94999999999999574, 1.835341550235569663, -112.0551512925630249 ) ) ;
#65580=AXIS2_PLACEMENT_3D ( 'NONE', #206336, #126790, #68101 ) ;
#65586=CARTESIAN_POINT ( 'NONE',  ( 21.08035267497491105, 6.331706839794169817, -100.4173113752239033 ) ) ;
#65589=VECTOR ( 'NONE', #20442, 1000.000000000000000 ) ;
#65627=CIRCLE ( 'NONE', #198899, 3.999999999999999112 ) ;
#65628=AXIS2_PLACEMENT_3D ( 'NONE', #201341, #124386, #202623 ) ;
#65630=ADVANCED_FACE ( 'NONE', ( #24278 ), #229191, .F. ) ;
#65666=ORIENTED_EDGE ( 'NONE', *, *, #208756, .F. ) ;
#65698=AXIS2_PLACEMENT_3D ( 'NONE', #42194, #198688, #60447 ) ;
#65716=EDGE_CURVE ( 'NONE', #227485, #84132, #48510, .T. ) ;
#65751=CARTESIAN_POINT ( 'NONE',  ( -20.64999999999999858, 2.000000000011154189, -113.2246219227621395 ) ) ;
#65777=ORIENTED_EDGE ( 'NONE', *, *, #207468, .F. ) ;
#65784=ORIENTED_EDGE ( 'NONE', *, *, #180532, .F. ) ;
#65787=CARTESIAN_POINT ( 'NONE',  ( -18.59999999999999787, 11.75000000001115197, -112.6500000000000341 ) ) ;
#65793=CARTESIAN_POINT ( 'NONE',  ( -18.49346865148320518, -9.443073798513779593, -107.6851962553148496 ) ) ;
#65845=DIRECTION ( 'NONE',  ( 0.000000000000000000, 0.000000000000000000, -1.000000000000000000 ) ) ;
#65981=FACE_OUTER_BOUND ( 'NONE', #93082, .T. ) ;
#65983=CARTESIAN_POINT ( 'NONE',  ( -21.05000000000000071, -11.39257802169451139, -130.9260504201681101 ) ) ;
#65995=CARTESIAN_POINT ( 'NONE',  ( -18.50000000000000000, 9.350000000011156942, -121.6500000000000341 ) ) ;
#66003=ORIENTED_EDGE ( 'NONE', *, *, #186700, .T. ) ;
#66017=FACE_OUTER_BOUND ( 'NONE', #47229, .T. ) ;
#66022=EDGE_CURVE ( 'NONE', #79682, #106008, #102846, .T. ) ;
#66045=DIRECTION ( 'NONE',  ( 0.000000000000000000, 0.000000000000000000, -1.000000000000000000 ) ) ;
#66076=CIRCLE ( 'NONE', #115995, 0.3999999999999975797 ) ;
#66097=DIRECTION ( 'NONE',  ( 0.000000000000000000, 0.000000000000000000, -1.000000000000000000 ) ) ;
#66130=CARTESIAN_POINT ( 'NONE',  ( 19.97071067811865674, 11.72071067812981759, -125.2085786437627206 ) ) ;
#66140=ORIENTED_EDGE ( 'NONE', *, *, #108909, .T. ) ;
#66142=EDGE_LOOP ( 'NONE', ( #92439, #223344, #163623, #134094, #228664 ) ) ;
#66160=ADVANCED_FACE ( 'NONE', ( #92899 ), #127825, .F. ) ;
#66163=CARTESIAN_POINT ( 'NONE',  ( -18.39999999999999503, -9.499999999988851584, -140.6001893912220737 ) ) ;
#66168=EDGE_CURVE ( 'NONE', #176862, #238954, #57045, .T. ) ;
#66252=DIRECTION ( 'NONE',  ( -1.000000000000000000, -7.304098846218134667E-16, 0.000000000000000000 ) ) ;
#66261=EDGE_CURVE ( 'NONE', #121101, #247064, #256935, .T. ) ;
#66262=CARTESIAN_POINT ( 'NONE',  ( -20.54999999999999716, 7.150000000011155876, -117.2500000000000284 ) ) ;
#66279=AXIS2_PLACEMENT_3D ( 'NONE', #147183, #230589, #228012 ) ;
#66280=CIRCLE ( 'NONE', #158086, 0.6000000000000015321 ) ;
#66292=CARTESIAN_POINT ( 'NONE',  ( -18.59999999999999787, 11.75000000001115197, -88.75000000000004263 ) ) ;
#66318=EDGE_CURVE ( 'NONE', #142934, #215339, #31974, .T. ) ;
#66337=DIRECTION ( 'NONE',  ( -0.000000000000000000, -0.000000000000000000, -1.000000000000000000 ) ) ;
#66353=CARTESIAN_POINT ( 'NONE',  ( 23.14999999999999858, 6.650000000011155876, -112.8500000000000369 ) ) ;
#66361=DIRECTION ( 'NONE',  ( 0.000000000000000000, 1.224646799142185182E-16, 1.000000000000000000 ) ) ;
#66380=DIRECTION ( 'NONE',  ( 0.000000000000000000, 0.8700118002898321601, -0.4930308989875230030 ) ) ;
#66386=CARTESIAN_POINT ( 'NONE',  ( 23.14999999999999503, 11.65000000001116298, -121.8500000000000369 ) ) ;
#66396=EDGE_CURVE ( 'NONE', #32589, #180521, #82169, .T. ) ;
#66416=DIRECTION ( 'NONE',  ( 0.7071067811865474617, 0.7071067811865474617, 0.000000000000000000 ) ) ;
#66417=EDGE_LOOP ( 'NONE', ( #174372, #245170, #125785, #205046 ) ) ;
#66432=DIRECTION ( 'NONE',  ( 0.000000000000000000, 1.000000000000000000, 0.000000000000000000 ) ) ;
#66485=DIRECTION ( 'NONE',  ( -0.000000000000000000, -0.000000000000000000, 1.000000000000000000 ) ) ;
#66491=ADVANCED_FACE ( 'NONE', ( #72758 ), #92275, .T. ) ;
#66511=ORIENTED_EDGE ( 'NONE', *, *, #122673, .T. ) ;
#66512=EDGE_LOOP ( 'NONE', ( #213045, #39497, #143182, #183205 ) ) ;
#66533=ORIENTED_EDGE ( 'NONE', *, *, #165099, .T. ) ;
#66554=CARTESIAN_POINT ( 'NONE',  ( 18.51997666896864914, -9.392332131508057458, -107.6434061874831656 ) ) ;
#66578=DIRECTION ( 'NONE',  ( 1.000000000000000000, -0.000000000000000000, -0.000000000000000000 ) ) ;
#66591=TOROIDAL_SURFACE ( 'NONE', #228891, 3.899999999999999467, 0.1000000000000000056 ) ;
#66600=ORIENTED_EDGE ( 'NONE', *, *, #7961, .T. ) ;
#66624=ADVANCED_FACE ( 'NONE', ( #197793 ), #255150, .F. ) ;
#66634=CARTESIAN_POINT ( 'NONE',  ( 22.14074124539698829, 7.390077851054901892, -100.4009471041559607 ) ) ;
#66651=CARTESIAN_POINT ( 'NONE',  ( 18.49999999999999289, 11.75000000001115907, -108.6000000000000227 ) ) ;
#66656=VECTOR ( 'NONE', #98294, 1000.000000000000000 ) ;
#66665=VERTEX_POINT ( 'NONE', #217344 ) ;
#66676=CARTESIAN_POINT ( 'NONE',  ( -18.59999999999999787, 1.115600667400684642E-11, -134.0000000000000284 ) ) ;
#66687=LINE ( 'NONE', #185345, #236244 ) ;
#66697=CARTESIAN_POINT ( 'NONE',  ( -21.14999999999999858, -11.64999999998884483, -100.5000000000000284 ) ) ;
#66706=CARTESIAN_POINT ( 'NONE',  ( -20.94999999999999929, 7.070967871809997973, -137.7465642218683399 ) ) ;
#66708=EDGE_LOOP ( 'NONE', ( #139568, #220243, #165130, #203225 ) ) ;
#66725=AXIS2_PLACEMENT_3D ( 'NONE', #248966, #109424, #212411 ) ;
#66768=ORIENTED_EDGE ( 'NONE', *, *, #198379, .F. ) ;
#66771=VERTEX_POINT ( 'NONE', #127252 ) ;
#66783=TOROIDAL_SURFACE ( 'NONE', #216795, 0.4000000000000005773, 0.1000000000000000056 ) ;
#66788=ORIENTED_EDGE ( 'NONE', *, *, #103968, .T. ) ;
#66802=ORIENTED_EDGE ( 'NONE', *, *, #125657, .F. ) ;
#66821=ORIENTED_EDGE ( 'NONE', *, *, #43945, .T. ) ;
#66841=FACE_OUTER_BOUND ( 'NONE', #7979, .T. ) ;
#66861=CIRCLE ( 'NONE', #216705, 0.1000000000000028644 ) ;
#66896=VERTEX_POINT ( 'NONE', #115377 ) ;
#66901=ORIENTED_EDGE ( 'NONE', *, *, #61188, .T. ) ;
#66906=ORIENTED_EDGE ( 'NONE', *, *, #66318, .F. ) ;
#66969=ORIENTED_EDGE ( 'NONE', *, *, #16266, .T. ) ;
#66994=DIRECTION ( 'NONE',  ( 0.000000000000000000, 0.8660254037844383745, -0.5000000000000003331 ) ) ;
#67038=EDGE_LOOP ( 'NONE', ( #180659, #8478, #75739, #79597 ) ) ;
#67044=DIRECTION ( 'NONE',  ( 0.000000000000000000, -0.9999176327611369874, 0.01283462868041987913 ) ) ;
#67045=EDGE_CURVE ( 'NONE', #59875, #41194, #215645, .T. ) ;
#67079=PLANE ( 'NONE',  #197762 ) ;
#67082=CARTESIAN_POINT ( 'NONE',  ( -18.40000000000000568, -9.499999999988851584, -107.4993620971801391 ) ) ;
#67084=ORIENTED_EDGE ( 'NONE', *, *, #224780, .F. ) ;
#67091=DIRECTION ( 'NONE',  ( 0.000000000000000000, 1.000000000000000000, 0.000000000000000000 ) ) ;
#67114=ORIENTED_EDGE ( 'NONE', *, *, #85000, .F. ) ;
#67147=DIRECTION ( 'NONE',  ( 1.000000000000000000, 0.000000000000000000, 0.000000000000000000 ) ) ;
#67173=DIRECTION ( 'NONE',  ( 0.000000000000000000, 0.000000000000000000, -1.000000000000000000 ) ) ;
#67204=ORIENTED_EDGE ( 'NONE', *, *, #133147, .T. ) ;
#67217=FACE_OUTER_BOUND ( 'NONE', #150777, .T. ) ;
#67219=DIRECTION ( 'NONE',  ( 0.000000000000000000, 0.000000000000000000, -1.000000000000000000 ) ) ;
#67221=FACE_OUTER_BOUND ( 'NONE', #55045, .T. ) ;
#67222=ORIENTED_EDGE ( 'NONE', *, *, #81045, .F. ) ;
#67239=VERTEX_POINT ( 'NONE', #137207 ) ;
#67247=DIRECTION ( 'NONE',  ( 1.000000000000000000, 0.000000000000000000, 0.000000000000000000 ) ) ;
#67261=CARTESIAN_POINT ( 'NONE',  ( 20.85000000000000142, -1.835859311432481045, -145.5044391687985694 ) ) ;
#67268=EDGE_LOOP ( 'NONE', ( #248085, #56773, #137537, #117115, #214952, #89605 ) ) ;
#67304=DIRECTION ( 'NONE',  ( -1.000000000000000000, 0.000000000000000000, 0.000000000000000000 ) ) ;
#67306=ORIENTED_EDGE ( 'NONE', *, *, #62339, .F. ) ;
#67360=EDGE_CURVE ( 'NONE', #230693, #117118, #84900, .T. ) ;
#67361=DIRECTION ( 'NONE',  ( -1.000000000000000000, -0.000000000000000000, -0.000000000000000000 ) ) ;
#67368=AXIS2_PLACEMENT_3D ( 'NONE', #133062, #107052, #109623 ) ;
#67372=ADVANCED_FACE ( 'NONE', ( #103198 ), #164493, .T. ) ;
#67388=ORIENTED_EDGE ( 'NONE', *, *, #194739, .F. ) ;
#67392=DIRECTION ( 'NONE',  ( 0.000000000000000000, 0.000000000000000000, -1.000000000000000000 ) ) ;
#67399=ORIENTED_EDGE ( 'NONE', *, *, #51077, .T. ) ;
#67407=FACE_OUTER_BOUND ( 'NONE', #214360, .T. ) ;
#67415=DIRECTION ( 'NONE',  ( -1.000000000000000000, -0.000000000000000000, -0.000000000000000000 ) ) ;
#67469=CIRCLE ( 'NONE', #811, 3.899999999999999467 ) ;
#67470=DIRECTION ( 'NONE',  ( 0.000000000000000000, 0.000000000000000000, -1.000000000000000000 ) ) ;
#67472=ORIENTED_EDGE ( 'NONE', *, *, #87882, .T. ) ;
#67475=CARTESIAN_POINT ( 'NONE',  ( -23.15000000000000213, -11.64999999998884483, -130.9000000000000341 ) ) ;
#67490=TOROIDAL_SURFACE ( 'NONE', #204855, 0.2000000000000000111, 0.1000000000000000056 ) ;
#67496=AXIS2_PLACEMENT_3D ( 'NONE', #140880, #220423, #53324 ) ;
#67499=AXIS2_PLACEMENT_3D ( 'NONE', #52401, #208926, #229772 ) ;
#67511=DIRECTION ( 'NONE',  ( -1.000000000000000000, -0.000000000000000000, -0.000000000000000000 ) ) ;
#67570=ORIENTED_EDGE ( 'NONE', *, *, #149762, .T. ) ;
#67577=ORIENTED_EDGE ( 'NONE', *, *, #114079, .T. ) ;
#67578=VERTEX_POINT ( 'NONE', #80127 ) ;
#67587=DIRECTION ( 'NONE',  ( 0.000000000000000000, 0.000000000000000000, -1.000000000000000000 ) ) ;
#67607=CARTESIAN_POINT ( 'NONE',  ( 21.87500000000000355, 9.750000000011153745, -121.6500000000000341 ) ) ;
#67647=CARTESIAN_POINT ( 'NONE',  ( 20.95035502843362707, 10.47763832678762164, -108.0762997087363999 ) ) ;
#67698=DIRECTION ( 'NONE',  ( -1.000000000000000000, 0.000000000000000000, 0.000000000000000000 ) ) ;
#67716=ORIENTED_EDGE ( 'NONE', *, *, #113155, .F. ) ;
#67721=ORIENTED_EDGE ( 'NONE', *, *, #84048, .T. ) ;
#67728=DIRECTION ( 'NONE',  ( 0.000000000000000000, 0.000000000000000000, 1.000000000000000000 ) ) ;
#67767=DIRECTION ( 'NONE',  ( 0.000000000000000000, 0.4999999999999956701, -0.8660254037844411501 ) ) ;
#67791=DIRECTION ( 'NONE',  ( 0.000000000000000000, 0.000000000000000000, 1.000000000000000000 ) ) ;
#67811=DIRECTION ( 'NONE',  ( 1.000000000000000000, 2.952720810173289112E-16, -0.000000000000000000 ) ) ;
#67823=DIRECTION ( 'NONE',  ( 0.000000000000000000, 0.000000000000000000, -1.000000000000000000 ) ) ;
#67843=ORIENTED_EDGE ( 'NONE', *, *, #233172, .T. ) ;
#67872=CARTESIAN_POINT ( 'NONE',  ( -22.48660254037843487, 11.65000000001115588, -100.4500000000000597 ) ) ;
#67888=CARTESIAN_POINT ( 'NONE',  ( -20.94999999999999929, -12.41227409413852811, -131.0000000000000284 ) ) ;
#67916=VECTOR ( 'NONE', #231004, 1000.000000000000000 ) ;
#67969=VERTEX_POINT ( 'NONE', #220671 ) ;
#67985=CARTESIAN_POINT ( 'NONE',  ( -23.25000000000000000, -1.164121893230052995, -141.9148480855716343 ) ) ;
#67998=DIRECTION ( 'NONE',  ( -0.000000000000000000, -0.000000000000000000, 1.000000000000000000 ) ) ;
#68013=EDGE_LOOP ( 'NONE', ( #18384, #218891, #133314, #101013 ) ) ;
#68036=DIRECTION ( 'NONE',  ( 0.000000000000000000, 0.000000000000000000, -1.000000000000000000 ) ) ;
#68039=AXIS2_PLACEMENT_3D ( 'NONE', #27628, #32763, #150125 ) ;
#68049=DIRECTION ( 'NONE',  ( -1.000000000000000000, -0.000000000000000000, -0.000000000000000000 ) ) ;
#68083=CIRCLE ( 'NONE', #134708, 6.258578643762696458 ) ;
#68101=DIRECTION ( 'NONE',  ( -1.000000000000000000, 0.000000000000000000, 0.000000000000000000 ) ) ;
#68112=CARTESIAN_POINT ( 'NONE',  ( -21.55000000000000426, 7.750000000011159074, -121.6500000000000341 ) ) ;
#68117=VERTEX_POINT ( 'NONE', #203671 ) ;
#68134=ORIENTED_EDGE ( 'NONE', *, *, #104928, .T. ) ;
#68157=DIRECTION ( 'NONE',  ( -1.000000000000000000, 0.000000000000000000, 0.000000000000000000 ) ) ;
#68164=EDGE_LOOP ( 'NONE', ( #174659, #40865, #237478, #170785 ) ) ;
#68166=CIRCLE ( 'NONE', #206110, 11.64999999999999325 ) ;
#68188=DIRECTION ( 'NONE',  ( 0.000000000000000000, 1.000000000000000000, 0.000000000000000000 ) ) ;
#68197=TOROIDAL_SURFACE ( 'NONE', #18128, 0.2000000000000000111, 0.1000000000000000056 ) ;
#68208=FACE_OUTER_BOUND ( 'NONE', #87782, .T. ) ;
#68221=CIRCLE ( 'NONE', #184723, 0.1000000000000002554 ) ;
#68247=VECTOR ( 'NONE', #106619, 1000.000000000000000 ) ;
#68265=AXIS2_PLACEMENT_3D ( 'NONE', #140594, #216278, #177199 ) ;
#68267=CARTESIAN_POINT ( 'NONE',  ( -20.64999999999999858, -8.999999999988846255, -110.3939691226524786 ) ) ;
#68298=CIRCLE ( 'NONE', #76651, 0.09999999999999939493 ) ;
#68299=EDGE_LOOP ( 'NONE', ( #184632, #65518, #88749 ) ) ;
#68358=AXIS2_PLACEMENT_3D ( 'NONE', #102396, #118145, #236794 ) ;
#68364=CARTESIAN_POINT ( 'NONE',  ( 20.87155475150661132, 11.75000000001115907, -127.0955865291576714 ) ) ;
#68390=CARTESIAN_POINT ( 'NONE',  ( -21.07946286933444924, 6.329037319018851804, -100.4233161567436525 ) ) ;
#68429=FACE_OUTER_BOUND ( 'NONE', #116846, .T. ) ;
#68469=CARTESIAN_POINT ( 'NONE',  ( -20.85000000000000142, 11.65000000001115232, -134.0000000000000284 ) ) ;
#68482=EDGE_CURVE ( 'NONE', #189704, #99810, #24758, .T. ) ;
#68510=CARTESIAN_POINT ( 'NONE',  ( 20.59588692710267921, 10.36872342117990975, -108.1390810945106864 ) ) ;
#68533=SURFACE_STYLE_USAGE ( .BOTH. , #8555 ) ;
#68550=CARTESIAN_POINT ( 'NONE',  ( -22.59080734064477625, 11.75000000001115907, -100.4692502919030090 ) ) ;
#68560=CARTESIAN_POINT ( 'NONE',  ( 21.97500000000000497, 9.750000000011153745, -121.6500000000000341 ) ) ;
#68587=CARTESIAN_POINT ( 'NONE',  ( -21.14999999999999858, -11.74999999998884448, -103.4000000000000341 ) ) ;
#68588=CARTESIAN_POINT ( 'NONE',  ( 18.59999999999999787, -1.835859311432481045, -145.5044391687985694 ) ) ;
#68590=CARTESIAN_POINT ( 'NONE',  ( -23.25000000000000000, 1.115600667400684642E-11, -100.5000000000000284 ) ) ;
#68595=VECTOR ( 'NONE', #66416, 1000.000000000000114 ) ;
#68615=EDGE_CURVE ( 'NONE', #5081, #66896, #233221, .T. ) ;
#68628=DIRECTION ( 'NONE',  ( 0.000000000000000000, 0.000000000000000000, -1.000000000000000000 ) ) ;
#68689=DIRECTION ( 'NONE',  ( 1.000000000000000000, 3.265361837132813093E-16, -0.000000000000000000 ) ) ;
#68715=DIRECTION ( 'NONE',  ( -1.000000000000000000, 0.000000000000000000, 0.000000000000000000 ) ) ;
#68743=ADVANCED_FACE ( 'NONE', ( #118392 ), #74868, .T. ) ;
#68748=ORIENTED_EDGE ( 'NONE', *, *, #17126, .T. ) ;
#68772=CARTESIAN_POINT ( 'NONE',  ( 22.49066049874202022, 0.05634325154338429287, -88.84998776248292529 ) ) ;
#68792=ADVANCED_FACE ( 'NONE', ( #81781 ), #156255, .T. ) ;
#68817=CARTESIAN_POINT ( 'NONE',  ( -23.25000000000000000, 1.115600667400684642E-11, -100.5000000000000284 ) ) ;
#68842=DIRECTION ( 'NONE',  ( -0.7071067811865474617, -0.7071067811865474617, -0.000000000000000000 ) ) ;
#68898=DIRECTION ( 'NONE',  ( 0.000000000000000000, 1.000000000000000000, 0.000000000000000000 ) ) ;
#68945=VERTEX_POINT ( 'NONE', #52951 ) ;
#68960=CARTESIAN_POINT ( 'NONE',  ( 23.14999999999999503, 11.65000000001116298, -126.9851942293460922 ) ) ;
#68970=DIRECTION ( 'NONE',  ( 1.000000000000000000, -0.000000000000000000, -0.000000000000000000 ) ) ;
#68974=CARTESIAN_POINT ( 'NONE',  ( -23.25000000000000000, 11.75000000001115552, -100.5000000000000284 ) ) ;
#68979=CIRCLE ( 'NONE', #2286, 0.5000000000000004441 ) ;
#68981=LINE ( 'NONE', #151067, #97006 ) ;
#68984=CARTESIAN_POINT ( 'NONE',  ( -20.54999999999999716, 7.150000000011155876, -121.6500000000000341 ) ) ;
#68988=EDGE_LOOP ( 'NONE', ( #248748, #148328, #51444, #30698 ) ) ;
#68990=EDGE_CURVE ( 'NONE', #169534, #142411, #249880, .T. ) ;
#68993=AXIS2_PLACEMENT_3D ( 'NONE', #59128, #199976, #176565 ) ;
#69041=ORIENTED_EDGE ( 'NONE', *, *, #223987, .F. ) ;
#69057=EDGE_CURVE ( 'NONE', #32249, #114550, #26728, .T. ) ;
#69068=ORIENTED_EDGE ( 'NONE', *, *, #82356, .F. ) ;
#69081=CIRCLE ( 'NONE', #60661, 0.09999999999999693856 ) ;
#69090=ORIENTED_EDGE ( 'NONE', *, *, #106455, .F. ) ;
#69102=ORIENTED_EDGE ( 'NONE', *, *, #160379, .T. ) ;
#69103=EDGE_CURVE ( 'NONE', #241932, #231975, #239100, .T. ) ;
#69116=AXIS2_PLACEMENT_3D ( 'NONE', #28755, #127812, #67823 ) ;
#69130=CARTESIAN_POINT ( 'NONE',  ( -20.94999999999999929, 11.60000000001115161, -107.4282032302755852 ) ) ;
#69140=FACE_OUTER_BOUND ( 'NONE', #137812, .T. ) ;
#69158=CARTESIAN_POINT ( 'NONE',  ( 21.05543885634738643, 8.775771046858691804, -112.6843844707147184 ) ) ;
#69160=ORIENTED_EDGE ( 'NONE', *, *, #22886, .F. ) ;
#69168=CARTESIAN_POINT ( 'NONE',  ( -23.25000000000000000, 1.115600667400684642E-11, -134.0000000000000284 ) ) ;
#69175=EDGE_CURVE ( 'NONE', #40759, #228873, #130759, .T. ) ;
#69177=CIRCLE ( 'NONE', #60743, 11.64999999999999325 ) ;
#69197=DIRECTION ( 'NONE',  ( 0.000000000000000000, 0.000000000000000000, -1.000000000000000000 ) ) ;
#69219=CARTESIAN_POINT ( 'NONE',  ( 20.12500000000000000, 9.750000000011153745, -121.7500000000000426 ) ) ;
#69220=AXIS2_PLACEMENT_3D ( 'NONE', #79068, #56928, #137767 ) ;
#69224=AXIS2_PLACEMENT_3D ( 'NONE', #74703, #177643, #96753 ) ;
#69249=ORIENTED_EDGE ( 'NONE', *, *, #40568, .F. ) ;
#69251=CARTESIAN_POINT ( 'NONE',  ( 20.94999999999999574, 5.900000000011102586, -110.7190997646564483 ) ) ;
#69270=CARTESIAN_POINT ( 'NONE',  ( -21.55000000000000071, 7.150000000011155876, -121.7500000000000426 ) ) ;
#69274=DIRECTION ( 'NONE',  ( 2.952720810173289112E-16, -1.000000000000000000, 0.000000000000000000 ) ) ;
#69386=ORIENTED_EDGE ( 'NONE', *, *, #141157, .F. ) ;
#69393=DIRECTION ( 'NONE',  ( 0.000000000000000000, -0.000000000000000000, 1.000000000000000000 ) ) ;
#69397=DIRECTION ( 'NONE',  ( 1.000000000000000000, 0.000000000000000000, 0.000000000000000000 ) ) ;
#69401=ORIENTED_EDGE ( 'NONE', *, *, #116113, .T. ) ;
#69485=CARTESIAN_POINT ( 'NONE',  ( -20.94999999999999929, -11.64999999998884483, -103.5000000000000426 ) ) ;
#69486=CARTESIAN_POINT ( 'NONE',  ( -23.25000000000000000, 4.150000000011156764, -121.7500000000000426 ) ) ;
#69513=DIRECTION ( 'NONE',  ( 0.000000000000000000, -0.000000000000000000, -1.000000000000000000 ) ) ;
#69519=EDGE_CURVE ( 'NONE', #169135, #194066, #185766, .T. ) ;
#69525=CIRCLE ( 'NONE', #132047, 2.000000000000001776 ) ;
#69575=DIRECTION ( 'NONE',  ( 0.000000000000000000, 0.000000000000000000, -1.000000000000000000 ) ) ;
#69593=ADVANCED_FACE ( 'NONE', ( #122602 ), #199582, .T. ) ;
#69597=CIRCLE ( 'NONE', #32183, 11.89999999999999858 ) ;
#69598=DIRECTION ( 'NONE',  ( 0.000000000000000000, 0.000000000000000000, -1.000000000000000000 ) ) ;
#69602=EDGE_CURVE ( 'NONE', #79411, #98538, #197569, .T. ) ;
#69630=AXIS2_PLACEMENT_3D ( 'NONE', #39790, #201388, #118003 ) ;
#69660=CARTESIAN_POINT ( 'NONE',  ( 20.85000000000000142, 11.75000000001115907, -127.2161343370219413 ) ) ;
#69662=AXIS2_PLACEMENT_3D ( 'NONE', #27998, #227437, #156624 ) ;
#69672=EDGE_LOOP ( 'NONE', ( #227161, #72180, #253255, #20654 ) ) ;
#69742=EDGE_CURVE ( 'NONE', #64377, #173790, #247466, .T. ) ;
#69745=DIRECTION ( 'NONE',  ( 0.000000000000000000, 0.000000000000000000, -1.000000000000000000 ) ) ;
#69754=LINE ( 'NONE', #134814, #89106 ) ;
#69768=AXIS2_PLACEMENT_3D ( 'NONE', #102904, #245007, #246299 ) ;
#69775=ORIENTED_EDGE ( 'NONE', *, *, #65716, .T. ) ;
#69780=CYLINDRICAL_SURFACE ( 'NONE', #102693, 0.09999999999999939493 ) ;
#69784=CARTESIAN_POINT ( 'NONE',  ( -23.25000000000000000, 11.75000000001115552, -126.9851942293460922 ) ) ;
#69792=ORIENTED_EDGE ( 'NONE', *, *, #77058, .F. ) ;
#69798=AXIS2_PLACEMENT_3D ( 'NONE', #113823, #31761, #151709 ) ;
#69817=VERTEX_POINT ( 'NONE', #174609 ) ;
#69826=DIRECTION ( 'NONE',  ( -1.000000000000000000, 0.000000000000000000, 0.000000000000000000 ) ) ;
#69829=CIRCLE ( 'NONE', #132172, 4.049999999999998046 ) ;
#69834=ORIENTED_EDGE ( 'NONE', *, *, #79182, .F. ) ;
#69841=CARTESIAN_POINT ( 'NONE',  ( -20.64999999999999858, -8.999999999988844479, -124.1060308773475924 ) ) ;
#69855=DIRECTION ( 'NONE',  ( -1.000000000000000000, 0.000000000000000000, 0.000000000000000000 ) ) ;
#69870=DIRECTION ( 'NONE',  ( 0.000000000000000000, 0.000000000000000000, 1.000000000000000000 ) ) ;
#69898=AXIS2_PLACEMENT_3D ( 'NONE', #103477, #162219, #83892 ) ;
#69915=CIRCLE ( 'NONE', #111588, 0.09999999999999820144 ) ;
#69921=EDGE_LOOP ( 'NONE', ( #38215, #46448, #150540, #60458, #19996 ) ) ;
#69924=DIRECTION ( 'NONE',  ( 1.000000000000000000, 0.000000000000000000, 0.000000000000000000 ) ) ;
#69928=CARTESIAN_POINT ( 'NONE',  ( 22.57320508075688537, 11.65000000001115588, -100.5000000000000284 ) ) ;
#69984=AXIS2_PLACEMENT_3D ( 'NONE', #903, #79175, #160042 ) ;
#70011=VERTEX_POINT ( 'NONE', #206945 ) ;
#70037=CARTESIAN_POINT ( 'NONE',  ( -20.64999999999999858, 4.250000000011156409, -121.6500000000000341 ) ) ;
#70038=CARTESIAN_POINT ( 'NONE',  ( 18.50000972452444969, 10.29326151435342851, -139.4592822510414862 ) ) ;
#70039=ORIENTED_EDGE ( 'NONE', *, *, #234793, .F. ) ;
#70068=LINE ( 'NONE', #105277, #238779 ) ;
#70078=DIRECTION ( 'NONE',  ( 1.000000000000000000, 0.000000000000000000, 0.000000000000000000 ) ) ;
#70086=SPHERICAL_SURFACE ( 'NONE', #88258, 0.1000000000000000056 ) ;
#70099=EDGE_CURVE ( 'NONE', #257642, #173164, #101876, .T. ) ;
#70101=CARTESIAN_POINT ( 'NONE',  ( 18.52928932188133970, 10.27928932189249878, -125.2085786437627206 ) ) ;
#70102=DIRECTION ( 'NONE',  ( -0.7071067811865388020, 0.7071067811865561215, 0.000000000000000000 ) ) ;
#70123=VERTEX_POINT ( 'NONE', #83100 ) ;
#70151=VERTEX_POINT ( 'NONE', #110398 ) ;
#70153=ORIENTED_EDGE ( 'NONE', *, *, #160574, .T. ) ;
#70176=DIRECTION ( 'NONE',  ( 1.000000000000000000, 3.265361837132813093E-16, -0.000000000000000000 ) ) ;
#70181=CARTESIAN_POINT ( 'NONE',  ( -18.39999999999999858, -9.499999999988849808, -107.4992856778388841 ) ) ;
#70187=DIRECTION ( 'NONE',  ( 0.000000000000000000, 0.000000000000000000, -1.000000000000000000 ) ) ;
#70217=CIRCLE ( 'NONE', #20121, 0.6000000000000015321 ) ;
#70246=CARTESIAN_POINT ( 'NONE',  ( 18.39999999999999858, -9.499999999988842703, -140.6001893912220737 ) ) ;
#70266=SPHERICAL_SURFACE ( 'NONE', #60330, 0.1000000000000000056 ) ;
#70295=ORIENTED_EDGE ( 'NONE', *, *, #70985, .T. ) ;
#70314=AXIS2_PLACEMENT_3D ( 'NONE', #185040, #68970, #27291 ) ;
#70376=AXIS2_PLACEMENT_3D ( 'NONE', #39384, #19804, #178899 ) ;
#70389=ORIENTED_EDGE ( 'NONE', *, *, #162242, .F. ) ;
#70421=ORIENTED_EDGE ( 'NONE', *, *, #204337, .T. ) ;
#70448=TOROIDAL_SURFACE ( 'NONE', #103689, 0.6000000000000006439, 0.1000000000000000056 ) ;
#70455=VERTEX_POINT ( 'NONE', #82784 ) ;
#70521=EDGE_CURVE ( 'NONE', #247339, #250368, #48835, .T. ) ;
#70531=DIRECTION ( 'NONE',  ( 1.000000000000000000, 0.000000000000000000, 0.000000000000000000 ) ) ;
#70535=DIRECTION ( 'NONE',  ( 0.000000000000000000, 0.1495327102803586661, -0.9887567792719350601 ) ) ;
#70536=EDGE_LOOP ( 'NONE', ( #152638, #144019, #152432, #61980 ) ) ;
#70559=DIRECTION ( 'NONE',  ( 0.000000000000000000, 0.000000000000000000, -1.000000000000000000 ) ) ;
#70586=DIRECTION ( 'NONE',  ( 0.000000000000000000, 0.000000000000000000, -1.000000000000000000 ) ) ;
#70587=AXIS2_PLACEMENT_3D ( 'NONE', #134031, #97450, #17936 ) ;
#70601=DIRECTION ( 'NONE',  ( -0.000000000000000000, -0.000000000000000000, 1.000000000000000000 ) ) ;
#70608=ORIENTED_EDGE ( 'NONE', *, *, #219147, .T. ) ;
#70623=EDGE_CURVE ( 'NONE', #28041, #146870, #23381, .T. ) ;
#70672=ORIENTED_EDGE ( 'NONE', *, *, #156874, .F. ) ;
#70686=ORIENTED_EDGE ( 'NONE', *, *, #7748, .F. ) ;
#70693=CARTESIAN_POINT ( 'NONE',  ( -18.59999999999999787, -1.835859311432481045, -145.5044391687985694 ) ) ;
#70719=DIRECTION ( 'NONE',  ( -2.561896900575096011E-15, -0.5907332058517279494, 0.8068669527897025517 ) ) ;
#70722=CARTESIAN_POINT ( 'NONE',  ( -23.25000000000000000, 1.115651490242849210E-11, -96.35000000000003695 ) ) ;
#70762=ORIENTED_EDGE ( 'NONE', *, *, #93294, .F. ) ;
#70778=EDGE_LOOP ( 'NONE', ( #122034, #38973, #207224, #24172 ) ) ;
#70781=CARTESIAN_POINT ( 'NONE',  ( 23.14999999999999503, 11.65000000001116298, -121.8500000000000369 ) ) ;
#70787=DIRECTION ( 'NONE',  ( -0.000000000000000000, -2.891205793294679805E-16, 1.000000000000000000 ) ) ;
#70813=DIRECTION ( 'NONE',  ( 1.000000000000000000, 0.000000000000000000, 0.000000000000000000 ) ) ;
#70863=CARTESIAN_POINT ( 'NONE',  ( -21.14999999999999858, 1.115600667400684642E-11, -94.24142135623733907 ) ) ;
#70871=DIRECTION ( 'NONE',  ( 0.000000000000000000, -0.1568667991644863147, -0.9876197685951252359 ) ) ;
#70942=ADVANCED_FACE ( 'NONE', ( #104200 ), #83336, .F. ) ;
#70956=ADVANCED_FACE ( 'NONE', ( #3838 ), #6396, .F. ) ;
#70967=EDGE_CURVE ( 'NONE', #257108, #190470, #215069, .T. ) ;
#70978=TOROIDAL_SURFACE ( 'NONE', #229176, 12.77500000000000036, 0.1000000000000000056 ) ;
#70981=FACE_OUTER_BOUND ( 'NONE', #174302, .T. ) ;
#70985=EDGE_CURVE ( 'NONE', #245055, #143179, #126344, .T. ) ;
#70989=ORIENTED_EDGE ( 'NONE', *, *, #107291, .F. ) ;
#71016=LINE ( 'NONE', #11017, #94431 ) ;
#71030=CARTESIAN_POINT ( 'NONE',  ( 20.94999999999999574, -1.162701749926853712, -108.5000000000000426 ) ) ;
#71031=ORIENTED_EDGE ( 'NONE', *, *, #60001, .F. ) ;
#71042=EDGE_CURVE ( 'NONE', #26109, #216892, #186335, .T. ) ;
#71062=EDGE_CURVE ( 'NONE', #198608, #177524, #44258, .T. ) ;
#71077=CIRCLE ( 'NONE', #54295, 0.09999999999999892308 ) ;
#71099=CIRCLE ( 'NONE', #100654, 0.1000000000000008937 ) ;
#71114=ORIENTED_EDGE ( 'NONE', *, *, #41052, .T. ) ;
#71122=CARTESIAN_POINT ( 'NONE',  ( -20.54999999999999716, 9.350000000011156942, -121.6500000000000341 ) ) ;
#71131=CARTESIAN_POINT ( 'NONE',  ( 18.59999999999997655, -1.164121893230052995, -141.9148480855716343 ) ) ;
#71132=CARTESIAN_POINT ( 'NONE',  ( -22.57320508075687115, 11.75000000001115552, -100.5000000000000284 ) ) ;
#71144=ORIENTED_EDGE ( 'NONE', *, *, #226009, .T. ) ;
#71151=EDGE_CURVE ( 'NONE', #64097, #163036, #182269, .T. ) ;
#71197=CARTESIAN_POINT ( 'NONE',  ( -20.94999999999999929, 7.021664781911246322, -137.8335654018973457 ) ) ;
#71260=CARTESIAN_POINT ( 'NONE',  ( 21.05000000000000071, 1.360870587203197646, -108.5729979270909951 ) ) ;
#71263=VECTOR ( 'NONE', #200510, 1000.000000000000000 ) ;
#71265=CARTESIAN_POINT ( 'NONE',  ( 23.25000000000000000, 6.550000000011156231, -112.8500000000000369 ) ) ;
#71296=DIRECTION ( 'NONE',  ( 1.000000000000000000, -7.304098846218134667E-16, 4.607487905232622991E-31 ) ) ;
#71300=CYLINDRICAL_SURFACE ( 'NONE', #128448, 0.09999999999999939493 ) ;
#71312=DIRECTION ( 'NONE',  ( 0.000000000000000000, 0.000000000000000000, -1.000000000000000000 ) ) ;
#71354=CARTESIAN_POINT ( 'NONE',  ( 22.47110162079220785, 0.02879741281384913879, -88.85006406331571327 ) ) ;
#71367=LINE ( 'NONE', #153503, #120890 ) ;
#71390=DIRECTION ( 'NONE',  ( -0.000000000000000000, -2.891205793294679805E-16, 1.000000000000000000 ) ) ;
#71450=EDGE_CURVE ( 'NONE', #211300, #233201, #176832, .T. ) ;
#71456=VERTEX_POINT ( 'NONE', #217200 ) ;
#71459=CARTESIAN_POINT ( 'NONE',  ( 23.15000000000000213, -11.64999999998884483, -100.5000000000000284 ) ) ;
#71477=VECTOR ( 'NONE', #130673, 1000.000000000000000 ) ;
#71481=CARTESIAN_POINT ( 'NONE',  ( -23.25000000000000000, -1.736705739456431807, -145.5174225876237699 ) ) ;
#71489=ORIENTED_EDGE ( 'NONE', *, *, #235357, .T. ) ;
#71507=ORIENTED_EDGE ( 'NONE', *, *, #148607, .T. ) ;
#71521=CARTESIAN_POINT ( 'NONE',  ( 21.08804281139618908, 10.62183430185229938, -112.8499999673788494 ) ) ;
#71552=TOROIDAL_SURFACE ( 'NONE', #200711, 0.2000000000000000111, 0.1000000000000000056 ) ;
#71553=CIRCLE ( 'NONE', #25739, 1.900000000000012790 ) ;
#71569=CARTESIAN_POINT ( 'NONE',  ( 21.05000000000000071, -0.09999999998884338825, -100.5000000000000284 ) ) ;
#71576=ORIENTED_EDGE ( 'NONE', *, *, #139490, .F. ) ;
#71587=VECTOR ( 'NONE', #144980, 1000.000000000000000 ) ;
#71590=EDGE_CURVE ( 'NONE', #60627, #177453, #71016, .T. ) ;
#71639=TOROIDAL_SURFACE ( 'NONE', #54853, 0.2000000000000000111, 0.1000000000000000056 ) ;
#71644=CIRCLE ( 'NONE', #50749, 0.1000000000000033223 ) ;
#71709=DIRECTION ( 'NONE',  ( -1.000000000000000000, 0.000000000000000000, 0.000000000000000000 ) ) ;
#71722=CARTESIAN_POINT ( 'NONE',  ( 18.47135592147663274, -9.471088613254405431, -140.6835949398439993 ) ) ;
#71743=LINE ( 'NONE', #109549, #161979 ) ;
#71746=ORIENTED_EDGE ( 'NONE', *, *, #19680, .F. ) ;
#71752=VECTOR ( 'NONE', #115595, 1000.000000000000000 ) ;
#71829=VECTOR ( 'NONE', #215058, 1000.000000000000000 ) ;
#71859=AXIS2_PLACEMENT_3D ( 'NONE', #179537, #19154, #2145 ) ;
#71870=ADVANCED_FACE ( 'NONE', ( #199947 ), #123680, .F. ) ;
#71874=DIRECTION ( 'NONE',  ( 0.000000000000000000, 1.000000000000000000, 0.000000000000000000 ) ) ;
#71881=FACE_OUTER_BOUND ( 'NONE', #97232, .T. ) ;
#71894=DIRECTION ( 'NONE',  ( 1.000000000000000000, 0.000000000000000000, 0.000000000000000000 ) ) ;
#71899=DIRECTION ( 'NONE',  ( -2.952720810173289112E-16, 1.000000000000000000, -0.000000000000000000 ) ) ;
#71922=LINE ( 'NONE', #156621, #67916 ) ;
#71934=FACE_OUTER_BOUND ( 'NONE', #86813, .T. ) ;
#71994=ADVANCED_FACE ( 'NONE', ( #190661 ), #136287, .F. ) ;
#72005=EDGE_CURVE ( 'NONE', #97978, #245888, #28017, .T. ) ;
#72014=ORIENTED_EDGE ( 'NONE', *, *, #121309, .F. ) ;
#72027=DIRECTION ( 'NONE',  ( 0.000000000000000000, 0.1298341882520022972, 0.9915357197604853789 ) ) ;
#72047=DIRECTION ( 'NONE',  ( -0.000000000000000000, -1.000000000000000000, -0.000000000000000000 ) ) ;
#72052=CARTESIAN_POINT ( 'NONE',  ( -22.50000000000000000, 0.1000000000111554016, -92.70922040162662370 ) ) ;
#72068=DIRECTION ( 'NONE',  ( -1.000000000000000000, 7.304098846218134667E-16, 4.217023435051625732E-16 ) ) ;
#72088=ORIENTED_EDGE ( 'NONE', *, *, #26997, .F. ) ;
#72097=AXIS2_PLACEMENT_3D ( 'NONE', #14696, #53788, #250697 ) ;
#72128=CARTESIAN_POINT ( 'NONE',  ( 21.05000000000000071, 5.850000000011156942, -123.8675027757221159 ) ) ;
#72141=ORIENTED_EDGE ( 'NONE', *, *, #145311, .F. ) ;
#72166=AXIS2_PLACEMENT_3D ( 'NONE', #187118, #64569, #145388 ) ;
#72180=ORIENTED_EDGE ( 'NONE', *, *, #220594, .F. ) ;
#72188=DIRECTION ( 'NONE',  ( -0.000000000000000000, 0.000000000000000000, -1.000000000000000000 ) ) ;
#72192=CARTESIAN_POINT ( 'NONE',  ( 18.59999999999999432, -9.480686695267811714, -140.9411151687579036 ) ) ;
#72199=EDGE_CURVE ( 'NONE', #127135, #139652, #94235, .T. ) ;
#72214=CARTESIAN_POINT ( 'NONE',  ( -20.94999999999999929, 5.850000000011105428, -110.6324972242780120 ) ) ;
#72224=EDGE_CURVE ( 'NONE', #237722, #106114, #257074, .T. ) ;
#72280=ORIENTED_EDGE ( 'NONE', *, *, #93887, .F. ) ;
#72286=EDGE_LOOP ( 'NONE', ( #83101, #257140, #213709, #163791 ) ) ;
#72307=VERTEX_POINT ( 'NONE', #12672 ) ;
#72317=EDGE_CURVE ( 'NONE', #60618, #197578, #231628, .T. ) ;
#72320=( BOUNDED_SURFACE ( )  B_SPLINE_SURFACE ( 3, 2, ( 
 ( #175444, #94587, #213248 ),
 ( #253654, #136262, #37211 ),
 ( #116726, #58013, #137556 ),
 ( #217088, #181848, #200127 ),
 ( #123160, #1898, #121885 ),
 ( #24080, #243095, #5745 ) ),
 .UNSPECIFIED., .F., .F., .F. ) 
 B_SPLINE_SURFACE_WITH_KNOTS ( ( 4, 2, 4 ),
 ( 3, 3 ),
 ( 0.0001300404313046710908, 0.0003183318589266752666, 0.0005066232865486794152 ),
 ( 0.000000000000000000, 1.000000000000000000 ),
 .UNSPECIFIED. ) 
 GEOMETRIC_REPRESENTATION_ITEM ( )  RATIONAL_B_SPLINE_SURFACE ( (
 ( 1.000000000000000000, 0.7071067811865475727, 1.000000000000000000),
 ( 1.000000000000000000, 0.7625113560543049784, 1.000000000000000000),
 ( 1.000000000000000000, 0.8126073484684088744, 1.000000000000000000),
 ( 1.000000000000000000, 0.8923049332736880945, 1.000000000000000000),
 ( 1.000000000000000000, 0.9231914937766396712, 1.000000000000000000),
 ( 1.000000000000000000, 0.9238795325112915124, 1.000000000000000000) ) ) 
 REPRESENTATION_ITEM ( '' )  SURFACE ( )  );
#72358=ADVANCED_FACE ( 'NONE', ( #253810 ), #32235, .F. ) ;
#72386=AXIS2_PLACEMENT_3D ( 'NONE', #176703, #217071, #99684 ) ;
#72387=VERTEX_POINT ( 'NONE', #213399 ) ;
#72391=CYLINDRICAL_SURFACE ( 'NONE', #110990, 2.000000000000001776 ) ;
#72411=CARTESIAN_POINT ( 'NONE',  ( -20.85000000000000142, 10.33248238083634440, -139.5948465439131780 ) ) ;
#72414=CARTESIAN_POINT ( 'NONE',  ( 20.84999999999999787, 11.75000000001116085, -127.0808527540413166 ) ) ;
#72461=EDGE_CURVE ( 'NONE', #231975, #28041, #195167, .T. ) ;
#72481=DIRECTION ( 'NONE',  ( 0.000000000000000000, 0.000000000000000000, -1.000000000000000000 ) ) ;
#72492=DIRECTION ( 'NONE',  ( 2.952720810173289112E-16, -1.000000000000000000, 0.000000000000000000 ) ) ;
#72527=DIRECTION ( 'NONE',  ( -1.000000000000000000, 0.000000000000000000, 0.000000000000000000 ) ) ;
#72533=DIRECTION ( 'NONE',  ( -3.469446951953635015E-14, 1.000000000000000000, 0.000000000000000000 ) ) ;
#72556=ORIENTED_EDGE ( 'NONE', *, *, #198648, .T. ) ;
#72573=CARTESIAN_POINT ( 'NONE',  ( -20.54999999999999716, 7.150000000011155876, -121.6500000000000341 ) ) ;
#72574=CARTESIAN_POINT ( 'NONE',  ( 21.04999999999999716, 8.894723818389232761, -108.9870843231514783 ) ) ;
#72606=DIRECTION ( 'NONE',  ( 1.000000000000000000, 0.000000000000000000, 0.000000000000000000 ) ) ;
#72613=CARTESIAN_POINT ( 'NONE',  ( -20.94999999999999929, 1.736257131608553550, -112.0686523290175245 ) ) ;
#72639=EDGE_CURVE ( 'NONE', #121457, #61914, #15822, .T. ) ;
#72689=CARTESIAN_POINT ( 'NONE',  ( 20.94999999999999574, 11.62071067812981795, -127.1315833476590740 ) ) ;
#72691=CIRCLE ( 'NONE', #39383, 0.09999999999998898659 ) ;
#72696=CARTESIAN_POINT ( 'NONE',  ( -18.50000000000000355, -9.419084502802135717, -140.8299078070255064 ) ) ;
#72697=DIRECTION ( 'NONE',  ( 2.694716079187272946E-16, -1.000000000000000000, 0.000000000000000000 ) ) ;
#72710=DIRECTION ( 'NONE',  ( 1.000000000000000000, -0.000000000000000000, -0.000000000000000000 ) ) ;
#72758=FACE_OUTER_BOUND ( 'NONE', #62696, .T. ) ;
#72795=CARTESIAN_POINT ( 'NONE',  ( -23.25000000000000000, 1.115600667400684642E-11, -100.5000000000000284 ) ) ;
#72799=DIRECTION ( 'NONE',  ( 0.000000000000000000, 0.000000000000000000, -1.000000000000000000 ) ) ;
#72803=AXIS2_PLACEMENT_3D ( 'NONE', #235165, #173953, #253423 ) ;
#72817=CARTESIAN_POINT ( 'NONE',  ( 20.94999999999999574, 10.47338541492405994, -108.0786544642485865 ) ) ;
#72823=CARTESIAN_POINT ( 'NONE',  ( -21.05000000000000071, 1.115600667400684642E-11, -134.0000000000000284 ) ) ;
#72850=EDGE_CURVE ( 'NONE', #76616, #34898, #118321, .T. ) ;
#72851=CARTESIAN_POINT ( 'NONE',  ( -20.54999999999999716, -8.999999999988844479, -124.5060308773475839 ) ) ;
#72864=ORIENTED_EDGE ( 'NONE', *, *, #179618, .F. ) ;
#72875=CIRCLE ( 'NONE', #97747, 0.09999999999998898659 ) ;
#72909=VERTEX_POINT ( 'NONE', #60440 ) ;
#72926=EDGE_CURVE ( 'NONE', #40304, #120532, #158311, .T. ) ;
#72936=EDGE_CURVE ( 'NONE', #163036, #223382, #256028, .T. ) ;
#72940=EDGE_LOOP ( 'NONE', ( #215392, #168128, #190308, #85780 ) ) ;
#72944=ORIENTED_EDGE ( 'NONE', *, *, #160425, .F. ) ;
#72953=DIRECTION ( 'NONE',  ( -1.000000000000000000, 0.000000000000000000, 0.000000000000000000 ) ) ;
#72966=LINE ( 'NONE', #131616, #93025 ) ;
#72968=DIRECTION ( 'NONE',  ( -1.000000000000000000, -2.952720810173289112E-16, 0.000000000000000000 ) ) ;
#72969=ORIENTED_EDGE ( 'NONE', *, *, #285, .F. ) ;
#72985=DIRECTION ( 'NONE',  ( 0.000000000000000000, -0.000000000000000000, 1.000000000000000000 ) ) ;
#72991=VECTOR ( 'NONE', #196839, 1000.000000000000000 ) ;
#73029=CARTESIAN_POINT ( 'NONE',  ( 18.54271179734065456, -9.624084290087184357, -140.7409648527008983 ) ) ;
#73053=DIRECTION ( 'NONE',  ( 1.000000000000000000, 0.000000000000000000, 0.000000000000000000 ) ) ;
#73062=CARTESIAN_POINT ( 'NONE',  ( 18.39999999999999858, -9.399999999988843058, -88.75000000000004263 ) ) ;
#73072=CYLINDRICAL_SURFACE ( 'NONE', #231295, 0.09999999999998898659 ) ;
#73081=CARTESIAN_POINT ( 'NONE',  ( -18.59999999999999787, 1.750000000011155743, -112.1695115579016857 ) ) ;
#73104=CARTESIAN_POINT ( 'NONE',  ( -23.25000000000000000, 11.75000000001115552, -112.6500000000000341 ) ) ;
#73107=LINE ( 'NONE', #53506, #250332 ) ;
#73137=CIRCLE ( 'NONE', #106390, 0.09999999999999949207 ) ;
#73195=CARTESIAN_POINT ( 'NONE',  ( -23.15000000000000213, 11.65000000001115588, -112.7500000000000284 ) ) ;
#73196=AXIS2_PLACEMENT_3D ( 'NONE', #42265, #121808, #57946 ) ;
#73209=DIRECTION ( 'NONE',  ( -1.000000000000000000, -0.000000000000000000, 0.000000000000000000 ) ) ;
#73211=ORIENTED_EDGE ( 'NONE', *, *, #146693, .F. ) ;
#73253=CARTESIAN_POINT ( 'NONE',  ( -23.25000000000000000, 6.933893972137497030, -137.7856458343736108 ) ) ;
#73262=EDGE_LOOP ( 'NONE', ( #46638, #191232, #255751, #5199 ) ) ;
#73275=ORIENTED_EDGE ( 'NONE', *, *, #88420, .T. ) ;
#73304=DIRECTION ( 'NONE',  ( 1.000000000000000000, 0.000000000000000000, 0.000000000000000000 ) ) ;
#73305=B_SPLINE_CURVE_WITH_KNOTS ( 'NONE', 3,
 ( #172177, #113436, #192986, #92574, #213821, #14367 ),
 .UNSPECIFIED., .F., .F.,
 ( 4, 2, 4 ),
 ( 1.138412281109779656E-18, 0.0001569047307838638433, 0.0003138094615677265481 ),
 .UNSPECIFIED. ) ;
#73342=CARTESIAN_POINT ( 'NONE',  ( -21.08621493067320429, 0.05619483948720407906, -94.15070570882809875 ) ) ;
#73346=ORIENTED_EDGE ( 'NONE', *, *, #45591, .T. ) ;
#73362=EDGE_CURVE ( 'NONE', #30919, #43391, #219684, .T. ) ;
#73394=( BOUNDED_SURFACE ( )  B_SPLINE_SURFACE ( 3, 2, ( 
 ( #41081, #179308, #163579 ),
 ( #219678, #203974, #61905 ),
 ( #239261, #244380, #123167 ),
 ( #184410, #612, #222231 ) ),
 .UNSPECIFIED., .F., .F., .T. ) 
 B_SPLINE_SURFACE_WITH_KNOTS ( ( 4, 4 ),
 ( 3, 3 ),
 ( 0.0006461284895274055275, 0.0007503702773986016886 ),
 ( 0.000000000000000000, 1.000000000000000000 ),
 .UNSPECIFIED. ) 
 GEOMETRIC_REPRESENTATION_ITEM ( )  RATIONAL_B_SPLINE_SURFACE ( (
 ( 1.000000000000000000, 0.7071067811865475727, 1.000000000000000000),
 ( 1.000000000000000000, 0.7076476444648701625, 1.000000000000000000),
 ( 1.000000000000000000, 0.7075727925191833689, 1.000000000000000000),
 ( 1.000000000000000000, 0.7071067811865475727, 1.000000000000000000) ) ) 
 REPRESENTATION_ITEM ( '' )  SURFACE ( )  );
#73397=DIRECTION ( 'NONE',  ( -1.000000000000000000, -3.265361837132813093E-16, 0.000000000000000000 ) ) ;
#73421=FACE_OUTER_BOUND ( 'NONE', #33506, .T. ) ;
#73434=CARTESIAN_POINT ( 'NONE',  ( -20.94999999999999929, -11.64999999998884483, -103.4000000000000341 ) ) ;
#73452=CARTESIAN_POINT ( 'NONE',  ( -18.56579813702275672, 10.33025634372637391, -139.5870929282639281 ) ) ;
#73456=EDGE_CURVE ( 'NONE', #218579, #92785, #148789, .T. ) ;
#73459=AXIS2_PLACEMENT_3D ( 'NONE', #45530, #125078, #46794 ) ;
#73468=EDGE_CURVE ( 'NONE', #74301, #128415, #232187, .T. ) ;
#73605=DIRECTION ( 'NONE',  ( 1.000000000000000000, -0.000000000000000000, -0.000000000000000000 ) ) ;
#73618=CYLINDRICAL_SURFACE ( 'NONE', #126316, 12.87499999999999822 ) ;
#73621=FACE_OUTER_BOUND ( 'NONE', #127484, .T. ) ;
#73639=DIRECTION ( 'NONE',  ( 1.000000000000000000, 2.952720810173289112E-16, -0.000000000000000000 ) ) ;
#73644=ORIENTED_EDGE ( 'NONE', *, *, #57623, .F. ) ;
#73655=CARTESIAN_POINT ( 'NONE',  ( 21.17356465864818915, 0.09891124102502621418, -94.07719687375829665 ) ) ;
#73668=CARTESIAN_POINT ( 'NONE',  ( 20.12481660106788084, 9.526343992285099205, -108.7261416690930815 ) ) ;
#73677=AXIS2_PLACEMENT_3D ( 'NONE', #133626, #213161, #167646 ) ;
#73690=SHAPE_REPRESENTATION_RELATIONSHIP ( 'NONE' , 'NONE' ,  #108449, #194461 ) ;
#73704=EDGE_LOOP ( 'NONE', ( #55029, #80829, #63989, #19236, #24849 ) ) ;
#73713=DIRECTION ( 'NONE',  ( 0.000000000000000000, 0.000000000000000000, -1.000000000000000000 ) ) ;
#73732=CARTESIAN_POINT ( 'NONE',  ( -21.44999999999999929, 7.150000000011155876, -112.7500000000000284 ) ) ;
#73748=DIRECTION ( 'NONE',  ( -0.000000000000000000, -1.000000000000000000, -0.000000000000000000 ) ) ;
#73759=AXIS2_PLACEMENT_3D ( 'NONE', #199727, #238832, #253242 ) ;
#73774=CIRCLE ( 'NONE', #36367, 0.09999999999999781286 ) ;
#73789=ORIENTED_EDGE ( 'NONE', *, *, #150359, .F. ) ;
#73827=AXIS2_PLACEMENT_3D ( 'NONE', #80641, #222727, #239748 ) ;
#73841=DIRECTION ( 'NONE',  ( 1.000000000000000000, 0.000000000000000000, -0.000000000000000000 ) ) ;
#73847=DIRECTION ( 'NONE',  ( 0.000000000000000000, 1.000000000000000000, 0.000000000000000000 ) ) ;
#73860=EDGE_CURVE ( 'NONE', #189704, #197589, #119956, .T. ) ;
#73867=DIRECTION ( 'NONE',  ( 1.000000000000000000, 0.000000000000000000, -0.000000000000000000 ) ) ;
#73880=CARTESIAN_POINT ( 'NONE',  ( -21.05000000000000071, 6.400000000011158541, -110.4304246300616086 ) ) ;
#73900=ORIENTED_EDGE ( 'NONE', *, *, #200496, .F. ) ;
#73923=EDGE_CURVE ( 'NONE', #114232, #220305, #174317, .T. ) ;
#73938=AXIS2_PLACEMENT_3D ( 'NONE', #257776, #218686, #41381 ) ;
#73963=EDGE_LOOP ( 'NONE', ( #256699, #247467, #166690, #65777 ) ) ;
#74001=DIRECTION ( 'NONE',  ( 0.000000000000000000, -0.9908441862701596881, -0.1350103645451904977 ) ) ;
#74024=ORIENTED_EDGE ( 'NONE', *, *, #95046, .F. ) ;
#74036=VERTEX_POINT ( 'NONE', #64357 ) ;
#74042=DIRECTION ( 'NONE',  ( 1.000000000000000000, 0.000000000000000000, 0.000000000000000000 ) ) ;
#74062=DIRECTION ( 'NONE',  ( 1.000000000000000000, 0.000000000000000000, 0.000000000000000000 ) ) ;
#74099=CARTESIAN_POINT ( 'NONE',  ( -18.59999999999999787, 11.65000000001115232, -112.7500000000000284 ) ) ;
#74140=FACE_OUTER_BOUND ( 'NONE', #231370, .T. ) ;
#74145=EDGE_CURVE ( 'NONE', #183734, #242007, #157561, .T. ) ;
#74162=LINE ( 'NONE', #254030, #59910 ) ;
#74171=CARTESIAN_POINT ( 'NONE',  ( 23.24999999999999645, 1.115600667400684642E-11, -134.0000000000000284 ) ) ;
#74179=AXIS2_PLACEMENT_3D ( 'NONE', #111138, #193253, #9465 ) ;
#74186=VECTOR ( 'NONE', #239384, 999.9999999999998863 ) ;
#74194=CIRCLE ( 'NONE', #103355, 0.5000000000000004441 ) ;
#74195=CARTESIAN_POINT ( 'NONE',  ( 20.04142135623731136, 11.75000000001116085, -125.2671572875254213 ) ) ;
#74247=B_SPLINE_CURVE_WITH_KNOTS ( 'NONE', 3,
 ( #153539, #34852, #131350, #13988, #169237, #111802, #192620, #148353, #72696, #113082 ),
 .UNSPECIFIED., .F., .F.,
 ( 4, 2, 2, 2, 4 ),
 ( 0.000000000000000000, 4.221631689688577077E-05, 8.443263379377154154E-05, 0.0001688652675874691676, 0.0003377305351749402868 ),
 .UNSPECIFIED. ) ;
#74301=VERTEX_POINT ( 'NONE', #164307 ) ;
#74309=CARTESIAN_POINT ( 'NONE',  ( 18.58725287972279361, -9.566626910681348406, -140.8225048057644244 ) ) ;
#74311=CARTESIAN_POINT ( 'NONE',  ( -18.50000000000000000, 1.835341550235567887, -112.0551512925630249 ) ) ;
#74313=EDGE_CURVE ( 'NONE', #156398, #151223, #120145, .T. ) ;
#74341=CARTESIAN_POINT ( 'NONE',  ( -22.48479450179659977, 0.04699158119804078271, -88.85000155374841313 ) ) ;
#74372=CIRCLE ( 'NONE', #15916, 0.1000000000000028644 ) ;
#74376=AXIS2_PLACEMENT_3D ( 'NONE', #185303, #6653, #44519 ) ;
#74386=ORIENTED_EDGE ( 'NONE', *, *, #137929, .F. ) ;
#74415=DIRECTION ( 'NONE',  ( -1.000000000000000000, -2.952720810173289112E-16, 0.000000000000000000 ) ) ;
#74440=ADVANCED_FACE ( 'NONE', ( #178439 ), #157764, .F. ) ;
#74448=ORIENTED_EDGE ( 'NONE', *, *, #171220, .T. ) ;
#74561=ORIENTED_EDGE ( 'NONE', *, *, #42676, .F. ) ;
#74611=DIRECTION ( 'NONE',  ( -0.000000000000000000, -0.000000000000000000, 1.000000000000000000 ) ) ;
#74637=CARTESIAN_POINT ( 'NONE',  ( -21.08078803292166725, 0.07918598716886154909, -94.16698703556289729 ) ) ;
#74648=FACE_OUTER_BOUND ( 'NONE', #250336, .T. ) ;
#74657=ORIENTED_EDGE ( 'NONE', *, *, #168579, .T. ) ;
#74676=VERTEX_POINT ( 'NONE', #169744 ) ;
#74679=ORIENTED_EDGE ( 'NONE', *, *, #257703, .F. ) ;
#74682=AXIS2_PLACEMENT_3D ( 'NONE', #182839, #175450, #83666 ) ;
#74697=ORIENTED_EDGE ( 'NONE', *, *, #108625, .F. ) ;
#74703=CARTESIAN_POINT ( 'NONE',  ( -21.05000000000000071, 1.115600667400684642E-11, -100.5000000000000284 ) ) ;
#74707=EDGE_CURVE ( 'NONE', #168971, #38731, #16259, .T. ) ;
#74719=EDGE_LOOP ( 'NONE', ( #49268, #190015, #117900, #238871 ) ) ;
#74743=DIRECTION ( 'NONE',  ( 0.000000000000000000, 0.000000000000000000, -1.000000000000000000 ) ) ;
#74747=DIRECTION ( 'NONE',  ( 0.000000000000000000, -0.6728971962616792091, 0.7397360091702790408 ) ) ;
#74786=VERTEX_POINT ( 'NONE', #196955 ) ;
#74791=DIRECTION ( 'NONE',  ( -1.000000000000000000, -2.952720810173289112E-16, 0.000000000000000000 ) ) ;
#74800=ADVANCED_FACE ( 'NONE', ( #39206 ), #232920, .F. ) ;
#74826=EDGE_CURVE ( 'NONE', #197596, #188850, #174691, .T. ) ;
#74868=TOROIDAL_SURFACE ( 'NONE', #95666, 0.2000000000000000111, 0.1000000000000000056 ) ;
#74875=DIRECTION ( 'NONE',  ( 0.000000000000000000, -1.776356839400188145E-15, 1.000000000000000000 ) ) ;
#74877=CARTESIAN_POINT ( 'NONE',  ( 18.59999999999999076, 1.835341550235567887, -112.1551512925630192 ) ) ;
#74892=VERTEX_POINT ( 'NONE', #165558 ) ;
#74903=DIRECTION ( 'NONE',  ( 0.000000000000000000, 0.000000000000000000, -1.000000000000000000 ) ) ;
#74932=ADVANCED_FACE ( 'NONE', ( #84680 ), #6462, .F. ) ;
#74941=EDGE_LOOP ( 'NONE', ( #164111, #43034, #111740, #29829 ) ) ;
#74961=VERTEX_POINT ( 'NONE', #28658 ) ;
#74984=CARTESIAN_POINT ( 'NONE',  ( -20.54999999999999716, -9.399999999988848387, -110.3939691226524786 ) ) ;
#75043=CARTESIAN_POINT ( 'NONE',  ( 20.94999999999999574, -11.64999999998883595, -103.4000000000000341 ) ) ;
#75046=AXIS2_PLACEMENT_3D ( 'NONE', #219585, #166083, #82619 ) ;
#75047=DIRECTION ( 'NONE',  ( 1.000000000000000000, 0.000000000000000000, 0.000000000000000000 ) ) ;
#75064=VERTEX_POINT ( 'NONE', #251489 ) ;
#75080=CARTESIAN_POINT ( 'NONE',  ( -20.85000000000000142, -1.135018845899022466, -141.7169768834323520 ) ) ;
#75100=ADVANCED_FACE ( 'NONE', ( #177123 ), #254051, .F. ) ;
#75117=VECTOR ( 'NONE', #132629, 1000.000000000000000 ) ;
#75136=ORIENTED_EDGE ( 'NONE', *, *, #233616, .F. ) ;
#75175=VECTOR ( 'NONE', #136298, 1000.000000000000000 ) ;
#75197=VERTEX_POINT ( 'NONE', #217483 ) ;
#75201=EDGE_CURVE ( 'NONE', #61667, #251571, #218768, .T. ) ;
#75214=DIRECTION ( 'NONE',  ( 1.000000000000000000, 0.000000000000000000, 0.000000000000000000 ) ) ;
#75266=CARTESIAN_POINT ( 'NONE',  ( -21.37071067811865532, 8.070710678129811910, -121.6500000000000341 ) ) ;
#75267=ORIENTED_EDGE ( 'NONE', *, *, #7197, .T. ) ;
#75273=ORIENTED_EDGE ( 'NONE', *, *, #105249, .F. ) ;
#75280=ORIENTED_EDGE ( 'NONE', *, *, #150665, .F. ) ;
#75299=EDGE_LOOP ( 'NONE', ( #237226, #92742, #89264, #4403 ) ) ;
#75371=CIRCLE ( 'NONE', #208640, 0.09999999999999939493 ) ;
#75372=VERTEX_POINT ( 'NONE', #127390 ) ;
#75393=LINE ( 'NONE', #16690, #7749 ) ;
#75394=CIRCLE ( 'NONE', #46127, 0.1000000000000001860 ) ;
#75419=DIRECTION ( 'NONE',  ( 4.026293107431335996E-15, -0.8700118002898359348, 0.4930308989875165082 ) ) ;
#75431=PRESENTATION_STYLE_ASSIGNMENT (( #94950 ) ) ;
#75449=ORIENTED_EDGE ( 'NONE', *, *, #169768, .F. ) ;
#75468=CARTESIAN_POINT ( 'NONE',  ( 19.75857864376268935, 11.75000000001115907, -125.3500000000000512 ) ) ;
#75491=CARTESIAN_POINT ( 'NONE',  ( -18.59999999999999787, -1.866714910046153308, -112.2526752462820525 ) ) ;
#75525=ORIENTED_EDGE ( 'NONE', *, *, #57623, .T. ) ;
#75539=PRODUCT_DEFINITION ( 'UNKNOWN', '', #44678, #180909 ) ;
#75540=ORIENTED_EDGE ( 'NONE', *, *, #62317, .F. ) ;
#75543=ORIENTED_EDGE ( 'NONE', *, *, #133988, .F. ) ;
#75560=DIRECTION ( 'NONE',  ( 0.000000000000000000, 2.891205793294679805E-16, -1.000000000000000000 ) ) ;
#75565=EDGE_LOOP ( 'NONE', ( #192912, #241981, #228467, #175000 ) ) ;
#75572=CARTESIAN_POINT ( 'NONE',  ( -21.05000000000000071, -11.48912529306489994, -131.0000000000000284 ) ) ;
#75580=CARTESIAN_POINT ( 'NONE',  ( -20.54999999999999716, 7.250000000011155521, -121.6500000000000341 ) ) ;
#75597=ORIENTED_EDGE ( 'NONE', *, *, #172474, .T. ) ;
#75598=ADVANCED_FACE ( 'NONE', ( #26397 ), #70978, .T. ) ;
#75604=DIRECTION ( 'NONE',  ( -1.000000000000000000, -0.000000000000000000, -0.000000000000000000 ) ) ;
#75616=CARTESIAN_POINT ( 'NONE',  ( -23.15000000000000213, 2.000000000011154189, -121.2753780772379315 ) ) ;
#75637=VECTOR ( 'NONE', #43537, 1000.000000000000000 ) ;
#75639=CARTESIAN_POINT ( 'NONE',  ( -20.64999999999999858, 7.150000000011155876, -121.6500000000000341 ) ) ;
#75697=AXIS2_PLACEMENT_3D ( 'NONE', #218363, #180554, #99691 ) ;
#75709=CARTESIAN_POINT ( 'NONE',  ( -23.15000000000000213, -11.64999999998884483, -131.0000000000000284 ) ) ;
#75739=ORIENTED_EDGE ( 'NONE', *, *, #61847, .F. ) ;
#75753=DIRECTION ( 'NONE',  ( 0.000000000000000000, 0.000000000000000000, 1.000000000000000000 ) ) ;
#75805=ORIENTED_EDGE ( 'NONE', *, *, #45902, .T. ) ;
#75880=AXIS2_PLACEMENT_3D ( 'NONE', #109268, #89705, #70187 ) ;
#75924=CARTESIAN_POINT ( 'NONE',  ( 21.14999999999999503, 1.115600667400684642E-11, -100.5000000000000284 ) ) ;
#75970=CARTESIAN_POINT ( 'NONE',  ( -20.85000000000000142, -11.64999999998884483, -131.1000000000000227 ) ) ;
#76003=AXIS2_PLACEMENT_3D ( 'NONE', #105363, #241088, #162834 ) ;
#76029=TOROIDAL_SURFACE ( 'NONE', #159437, 7.800000000000000711, 0.1000000000000000056 ) ;
#76048=ADVANCED_FACE ( 'NONE', ( #222982 ), #41938, .F. ) ;
#76090=CARTESIAN_POINT ( 'NONE',  ( 22.39999999999999858, 7.790779598384538929, -100.4000000000000341 ) ) ;
#76137=DIRECTION ( 'NONE',  ( 0.000000000000000000, 0.1350103645451876666, -0.9908441862701600211 ) ) ;
#76159=VECTOR ( 'NONE', #77954, 1000.000000000000000 ) ;
#76160=ORIENTED_EDGE ( 'NONE', *, *, #200336, .F. ) ;
#76164=CARTESIAN_POINT ( 'NONE',  ( -20.64999999999999858, 7.150000000011155876, -112.7500000000000284 ) ) ;
#76174=DIRECTION ( 'NONE',  ( 1.000000000000000000, 0.000000000000000000, 0.000000000000000000 ) ) ;
#76197=ORIENTED_EDGE ( 'NONE', *, *, #139490, .T. ) ;
#76199=FACE_OUTER_BOUND ( 'NONE', #185695, .T. ) ;
#76233=DIRECTION ( 'NONE',  ( -1.000000000000000000, 0.000000000000000000, 0.000000000000000000 ) ) ;
#76237=VECTOR ( 'NONE', #87689, 1000.000000000000000 ) ;
#76238=DIRECTION ( 'NONE',  ( -1.000000000000000000, 0.000000000000000000, -0.000000000000000000 ) ) ;
#76313=CIRCLE ( 'NONE', #192872, 0.09999999999999913125 ) ;
#76325=AXIS2_PLACEMENT_3D ( 'NONE', #8329, #164823, #64437 ) ;
#76342=AXIS2_PLACEMENT_3D ( 'NONE', #229187, #208352, #90942 ) ;
#76362=SPHERICAL_SURFACE ( 'NONE', #240160, 0.1000000000000000056 ) ;
#76371=ORIENTED_EDGE ( 'NONE', *, *, #245561, .F. ) ;
#76380=CARTESIAN_POINT ( 'NONE',  ( -20.85000000000000142, -1.835859311432481045, -145.6044391687985637 ) ) ;
#76389=DIRECTION ( 'NONE',  ( 0.000000000000000000, 0.000000000000000000, -1.000000000000000000 ) ) ;
#76409=CIRCLE ( 'NONE', #226228, 0.5000000000000004441 ) ;
#76477=ORIENTED_EDGE ( 'NONE', *, *, #35173, .T. ) ;
#76489=DIRECTION ( 'NONE',  ( 1.000000000000000000, -0.000000000000000000, -0.000000000000000000 ) ) ;
#76503=EDGE_CURVE ( 'NONE', #148589, #204523, #133669, .T. ) ;
#76514=CARTESIAN_POINT ( 'NONE',  ( -20.64999999999999858, 1.940186915899004161, -121.1708807889467039 ) ) ;
#76534=CARTESIAN_POINT ( 'NONE',  ( 20.94999999999999929, -1.835341550213257733, -112.0551512925630249 ) ) ;
#76535=CARTESIAN_POINT ( 'NONE',  ( 21.14999999999999858, 11.65000000001116298, -112.6500000000000341 ) ) ;
#76562=ORIENTED_EDGE ( 'NONE', *, *, #117024, .T. ) ;
#76592=DIRECTION ( 'NONE',  ( -1.000000000000000000, 0.000000000000000000, -0.000000000000000000 ) ) ;
#76598=ORIENTED_EDGE ( 'NONE', *, *, #89630, .F. ) ;
#76616=VERTEX_POINT ( 'NONE', #88271 ) ;
#76619=CARTESIAN_POINT ( 'NONE',  ( 20.94999999999999929, 5.400000000011154988, -121.5947339810869465 ) ) ;
#76651=AXIS2_PLACEMENT_3D ( 'NONE', #57772, #197292, #52640 ) ;
#76678=DIRECTION ( 'NONE',  ( 3.469446951953498700E-14, -0.7899159663865300551, -0.6132151058540831201 ) ) ;
#76693=AXIS2_PLACEMENT_3D ( 'NONE', #75266, #234299, #251292 ) ;
#76699=ORIENTED_EDGE ( 'NONE', *, *, #188174, .F. ) ;
#76741=VECTOR ( 'NONE', #66485, 1000.000000000000000 ) ;
#76769=AXIS2_PLACEMENT_3D ( 'NONE', #20947, #100423, #137007 ) ;
#76772=CARTESIAN_POINT ( 'NONE',  ( 21.06490991615909181, 10.72489134759826790, -112.7037113535331656 ) ) ;
#76789=FACE_OUTER_BOUND ( 'NONE', #100093, .T. ) ;
#76793=AXIS2_PLACEMENT_3D ( 'NONE', #230147, #210586, #48933 ) ;
#76816=LINE ( 'NONE', #38999, #107972 ) ;
#76820=EDGE_CURVE ( 'NONE', #245055, #142813, #233826, .T. ) ;
#76834=DIRECTION ( 'NONE',  ( -0.7071067811865475727, -0.7071067811865475727, 0.000000000000000000 ) ) ;
#76838=CARTESIAN_POINT ( 'NONE',  ( 20.94999999999999929, 7.120270961708750512, -137.6595630418393625 ) ) ;
#76840=AXIS2_PLACEMENT_3D ( 'NONE', #224645, #139959, #186831 ) ;
#76891=CARTESIAN_POINT ( 'NONE',  ( -22.37643362114956957, 0.09908137369253962323, -92.87421000604163623 ) ) ;
#76893=EDGE_LOOP ( 'NONE', ( #112055, #44521, #152469, #220782 ) ) ;
#76930=DIRECTION ( 'NONE',  ( 1.000000000000000000, 0.000000000000000000, -0.000000000000000000 ) ) ;
#76942=VERTEX_POINT ( 'NONE', #71030 ) ;
#77000=DIRECTION ( 'NONE',  ( -1.000000000000000000, 0.000000000000000000, 0.000000000000000000 ) ) ;
#77052=DIRECTION ( 'NONE',  ( -0.000000000000000000, 0.000000000000000000, -1.000000000000000000 ) ) ;
#77058=EDGE_CURVE ( 'NONE', #68117, #245768, #249994, .T. ) ;
#77067=ORIENTED_EDGE ( 'NONE', *, *, #11813, .F. ) ;
#77089=FACE_OUTER_BOUND ( 'NONE', #113145, .T. ) ;
#77099=CIRCLE ( 'NONE', #27261, 0.09999999999999939493 ) ;
#77154=CARTESIAN_POINT ( 'NONE',  ( -21.07928932188134041, 0.09889514566555068775, -94.17148334360673800 ) ) ;
#77155=CARTESIAN_POINT ( 'NONE',  ( -20.94999999999999929, -1.164121893230052995, -141.9148480855716343 ) ) ;
#77158=CIRCLE ( 'NONE', #256159, 0.8750000000000007772 ) ;
#77169=DIRECTION ( 'NONE',  ( 0.000000000000000000, 1.734723475976805517E-14, -1.000000000000000000 ) ) ;
#77182=LINE ( 'NONE', #34246, #249437 ) ;
#77201=CARTESIAN_POINT ( 'NONE',  ( -20.54999999999999716, 1.115600667400684642E-11, -134.0000000000000284 ) ) ;
#77205=CARTESIAN_POINT ( 'NONE',  ( 20.94999999999999929, 1.115600667400684642E-11, -138.0000000000000284 ) ) ;
#77219=DIRECTION ( 'NONE',  ( -1.000000000000000000, -0.000000000000000000, 0.000000000000000000 ) ) ;
#77243=EDGE_CURVE ( 'NONE', #4043, #17513, #25167, .T. ) ;
#77248=FACE_OUTER_BOUND ( 'NONE', #215557, .T. ) ;
#77268=LINE ( 'NONE', #236357, #160059 ) ;
#77281=FACE_OUTER_BOUND ( 'NONE', #158896, .T. ) ;
#77303=VERTEX_POINT ( 'NONE', #15567 ) ;
#77323=ORIENTED_EDGE ( 'NONE', *, *, #108625, .T. ) ;
#77325=CARTESIAN_POINT ( 'NONE',  ( -23.24999999999999645, -9.599999999988845900, -140.6001893912220737 ) ) ;
#77336=DIRECTION ( 'NONE',  ( 1.000000000000000000, 2.952720810173289112E-16, -0.000000000000000000 ) ) ;
#77339=ORIENTED_EDGE ( 'NONE', *, *, #142418, .F. ) ;
#77351=AXIS2_PLACEMENT_3D ( 'NONE', #69841, #67247, #206764 ) ;
#77385=ORIENTED_EDGE ( 'NONE', *, *, #132796, .T. ) ;
#77403=ORIENTED_EDGE ( 'NONE', *, *, #34401, .F. ) ;
#77412=VECTOR ( 'NONE', #24347, 1000.000000000000000 ) ;
#77417=DIRECTION ( 'NONE',  ( 1.000000000000000000, 2.952720810173289112E-16, -0.000000000000000000 ) ) ;
#77435=DIRECTION ( 'NONE',  ( 0.000000000000000000, 0.000000000000000000, -1.000000000000000000 ) ) ;
#77480=ADVANCED_FACE ( 'NONE', ( #76789 ), #122345, .F. ) ;
#77504=DIRECTION ( 'NONE',  ( 0.000000000000000000, 0.000000000000000000, 1.000000000000000000 ) ) ;
#77505=CARTESIAN_POINT ( 'NONE',  ( -20.64999999999999858, 1.925233644870972816, -113.2302435331261563 ) ) ;
#77515=EDGE_LOOP ( 'NONE', ( #163082, #181637, #122961, #219798 ) ) ;
#77524=CIRCLE ( 'NONE', #231696, 0.1000000000000000472 ) ;
#77553=CIRCLE ( 'NONE', #19134, 0.1000000000000028644 ) ;
#77557=CARTESIAN_POINT ( 'NONE',  ( -20.64999999999999858, 1.115600667400684642E-11, -134.0000000000000284 ) ) ;
#77639=CARTESIAN_POINT ( 'NONE',  ( 21.05000000000000071, 1.115600667400684642E-11, -131.1000000000000227 ) ) ;
#77662=VECTOR ( 'NONE', #115529, 1000.000000000000000 ) ;
#77665=DIRECTION ( 'NONE',  ( 0.000000000000000000, 0.000000000000000000, -1.000000000000000000 ) ) ;
#77676=VECTOR ( 'NONE', #197670, 1000.000000000000000 ) ;
#77697=LINE ( 'NONE', #161119, #177264 ) ;
#77715=LINE ( 'NONE', #99834, #74186 ) ;
#77763=SPHERICAL_SURFACE ( 'NONE', #81055, 0.1000000000000000056 ) ;
#77780=DIRECTION ( 'NONE',  ( 1.000000000000000000, -7.304098846218135653E-16, 0.000000000000000000 ) ) ;
#77781=CIRCLE ( 'NONE', #169427, 0.1000000000000096922 ) ;
#77796=CARTESIAN_POINT ( 'NONE',  ( -18.59999999999999787, -1.835859311432481045, -145.5044391687985694 ) ) ;
#77822=CARTESIAN_POINT ( 'NONE',  ( -21.59142135623730852, 7.850000000011158718, -121.6500000000000341 ) ) ;
#77823=AXIS2_PLACEMENT_3D ( 'NONE', #220819, #77435, #42199 ) ;
#77862=AXIS2_PLACEMENT_3D ( 'NONE', #249341, #9417, #29037 ) ;
#77880=EDGE_CURVE ( 'NONE', #182621, #146084, #192573, .T. ) ;
#77888=DIRECTION ( 'NONE',  ( 1.000000000000000000, 0.000000000000000000, 0.000000000000000000 ) ) ;
#77891=EDGE_CURVE ( 'NONE', #222832, #230693, #246726, .T. ) ;
#77900=CARTESIAN_POINT ( 'NONE',  ( 23.14999999999999503, 6.650000000011155876, -121.8500000000000369 ) ) ;
#77922=EDGE_CURVE ( 'NONE', #196436, #14418, #250990, .T. ) ;
#77948=CARTESIAN_POINT ( 'NONE',  ( -20.64999999999999858, 2.500000000011156409, -113.7246219227621395 ) ) ;
#77949=DIRECTION ( 'NONE',  ( 0.000000000000000000, 0.000000000000000000, -1.000000000000000000 ) ) ;
#77954=DIRECTION ( 'NONE',  ( -0.000000000000000000, -0.000000000000000000, 1.000000000000000000 ) ) ;
#77974=ADVANCED_FACE ( 'NONE', ( #197275 ), #199867, .T. ) ;
#77979=TOROIDAL_SURFACE ( 'NONE', #111328, 11.70000000000000107, 0.1000000000000000056 ) ;
#77994=CARTESIAN_POINT ( 'NONE',  ( 21.14999999999999503, -0.09999999998884338825, -88.85042919245522341 ) ) ;
#78029=DIRECTION ( 'NONE',  ( -0.000000000000000000, 1.000000000000000000, 1.734723475976807292E-15 ) ) ;
#78033=DIRECTION ( 'NONE',  ( 0.000000000000000000, 0.000000000000000000, 1.000000000000000000 ) ) ;
#78037=DIRECTION ( 'NONE',  ( 1.000000000000000000, -0.000000000000000000, -0.000000000000000000 ) ) ;
#78047=AXIS2_PLACEMENT_3D ( 'NONE', #139394, #1167, #218944 ) ;
#78056=DIRECTION ( 'NONE',  ( -1.836970198721029934E-16, 1.000000000000000000, 0.000000000000000000 ) ) ;
#78096=DIRECTION ( 'NONE',  ( -0.000000000000000000, -1.897661533703519897E-16, 1.000000000000000000 ) ) ;
#78104=DIRECTION ( 'NONE',  ( 1.000000000000000000, -0.000000000000000000, -0.000000000000000000 ) ) ;
#78105=EDGE_LOOP ( 'NONE', ( #184570, #11517, #180377, #12254 ) ) ;
#78178=DIRECTION ( 'NONE',  ( 0.000000000000000000, -6.308085367188393199E-16, -1.000000000000000000 ) ) ;
#78189=AXIS2_PLACEMENT_3D ( 'NONE', #114262, #176820, #63262 ) ;
#78242=DIRECTION ( 'NONE',  ( 1.000000000000000000, 0.000000000000000000, 0.000000000000000000 ) ) ;
#78256=ORIENTED_EDGE ( 'NONE', *, *, #84087, .F. ) ;
#78293=CARTESIAN_POINT ( 'NONE',  ( -22.60000000000094289, 0.1008583691096561347, -88.75043287651061519 ) ) ;
#78295=ORIENTED_EDGE ( 'NONE', *, *, #31383, .F. ) ;
#78320=CIRCLE ( 'NONE', #224068, 0.3999999999999975797 ) ;
#78330=DIRECTION ( 'NONE',  ( 0.000000000000000000, 0.000000000000000000, 1.000000000000000000 ) ) ;
#78377=ORIENTED_EDGE ( 'NONE', *, *, #217989, .F. ) ;
#78400=CARTESIAN_POINT ( 'NONE',  ( -23.15000000000000213, 1.115650265596050101E-11, -96.45000000000003126 ) ) ;
#78414=DIRECTION ( 'NONE',  ( 1.000000000000000000, -0.000000000000000000, -0.000000000000000000 ) ) ;
#78423=EDGE_CURVE ( 'NONE', #144728, #196043, #197016, .T. ) ;
#78443=LINE ( 'NONE', #198402, #237392 ) ;
#78447=DIRECTION ( 'NONE',  ( -0.000000000000000000, 0.000000000000000000, 1.000000000000000000 ) ) ;
#78449=ADVANCED_FACE ( 'NONE', ( #192012 ), #159623, .T. ) ;
#78459=CARTESIAN_POINT ( 'NONE',  ( 21.00000000000000000, 9.750000000011153745, -121.6500000000000341 ) ) ;
#78460=DIRECTION ( 'NONE',  ( 2.952720810173289112E-16, -1.000000000000000000, 0.000000000000000000 ) ) ;
#78518=AXIS2_PLACEMENT_3D ( 'NONE', #241290, #1356, #140894 ) ;
#78523=DIRECTION ( 'NONE',  ( -1.000000000000000000, -0.000000000000000000, -0.000000000000000000 ) ) ;
#78534=CARTESIAN_POINT ( 'NONE',  ( -18.50000000000000000, -1.866714910046153308, -112.2526752462820525 ) ) ;
#78541=CARTESIAN_POINT ( 'NONE',  ( -18.51024323315077424, 10.31104185824062469, -139.5204516983106089 ) ) ;
#78543=DIRECTION ( 'NONE',  ( 0.000000000000000000, 0.000000000000000000, 1.000000000000000000 ) ) ;
#78544=EDGE_CURVE ( 'NONE', #173746, #182849, #1574, .T. ) ;
#78561=ADVANCED_FACE ( 'NONE', ( #18491 ), #120196, .T. ) ;
#78564=CARTESIAN_POINT ( 'NONE',  ( -23.15000000000000213, -8.999999999988844479, -124.1060308773475924 ) ) ;
#78598=FACE_OUTER_BOUND ( 'NONE', #74941, .T. ) ;
#78625=ORIENTED_EDGE ( 'NONE', *, *, #245447, .F. ) ;
#78629=ORIENTED_EDGE ( 'NONE', *, *, #60875, .F. ) ;
#78712=ADVANCED_FACE ( 'NONE', ( #64031 ), #247803, .T. ) ;
#78715=DIRECTION ( 'NONE',  ( -0.000000000000000000, -0.000000000000000000, 1.000000000000000000 ) ) ;
#78762=CARTESIAN_POINT ( 'NONE',  ( 21.04999999999999716, -0.01759718699739741543, -94.05922910633762513 ) ) ;
#78774=VERTEX_POINT ( 'NONE', #13071 ) ;
#78823=ADVANCED_FACE ( 'NONE', ( #50860 ), #174740, .F. ) ;
#78835=CIRCLE ( 'NONE', #24727, 0.1000000000000028644 ) ;
#78841=DIRECTION ( 'NONE',  ( 0.000000000000000000, 0.000000000000000000, 1.000000000000000000 ) ) ;
#78865=AXIS2_PLACEMENT_3D ( 'NONE', #156743, #236241, #39361 ) ;
#78876=EDGE_CURVE ( 'NONE', #94985, #111525, #10488, .T. ) ;
#78882=FACE_OUTER_BOUND ( 'NONE', #35998, .T. ) ;
#78962=CARTESIAN_POINT ( 'NONE',  ( 21.14999999999999858, 6.540656951712399803, -100.5000000000000426 ) ) ;
#78963=AXIS2_PLACEMENT_3D ( 'NONE', #115484, #82432, #136306 ) ;
#78964=CARTESIAN_POINT ( 'NONE',  ( 18.59999999999996945, 10.33248238083634440, -139.5948465439131780 ) ) ;
#78970=LINE ( 'NONE', #137672, #42930 ) ;
#78971=CARTESIAN_POINT ( 'NONE',  ( -21.05000000000000071, 1.115600667400684642E-11, -108.4000000000000341 ) ) ;
#78977=CARTESIAN_POINT ( 'NONE',  ( -23.25000000000000000, -11.64999999998884483, -100.5000000000000284 ) ) ;
#78987=AXIS2_PLACEMENT_3D ( 'NONE', #122414, #42873, #85806 ) ;
#79009=CARTESIAN_POINT ( 'NONE',  ( 20.94999999999999929, 10.38178547073510316, -139.5078453638842291 ) ) ;
#79033=ORIENTED_EDGE ( 'NONE', *, *, #74707, .T. ) ;
#79068=CARTESIAN_POINT ( 'NONE',  ( 20.94999999999999574, 1.250000000011155299, -108.4000000000000341 ) ) ;
#79094=EDGE_LOOP ( 'NONE', ( #38178, #46581, #1415, #233774 ) ) ;
#79101=CARTESIAN_POINT ( 'NONE',  ( 20.94999999999999929, 5.000000000011153745, -112.9052660189131245 ) ) ;
#79103=ADVANCED_FACE ( 'NONE', ( #46385 ), #231507, .F. ) ;
#79108=ORIENTED_EDGE ( 'NONE', *, *, #100171, .T. ) ;
#79117=CARTESIAN_POINT ( 'NONE',  ( -20.94999999999999929, 7.031312794766356511, -137.6091509382273443 ) ) ;
#79122=DIRECTION ( 'NONE',  ( 0.000000000000000000, 0.000000000000000000, -1.000000000000000000 ) ) ;
#79123=DIRECTION ( 'NONE',  ( -1.000000000000000000, 0.000000000000000000, 0.000000000000000000 ) ) ;
#79165=CARTESIAN_POINT ( 'NONE',  ( -20.64999999999999858, 4.350000000011156054, -121.6500000000000341 ) ) ;
#79175=DIRECTION ( 'NONE',  ( 1.000000000000000000, 0.000000000000000000, 0.000000000000000000 ) ) ;
#79182=EDGE_CURVE ( 'NONE', #27184, #163802, #102645, .T. ) ;
#79184=CARTESIAN_POINT ( 'NONE',  ( -18.59999999999999787, 11.65000000001115232, -121.8500000000000369 ) ) ;
#79193=ORIENTED_EDGE ( 'NONE', *, *, #115097, .F. ) ;
#79298=AXIS2_PLACEMENT_3D ( 'NONE', #43080, #147303, #144724 ) ;
#79308=ORIENTED_EDGE ( 'NONE', *, *, #249001, .T. ) ;
#79333=ORIENTED_EDGE ( 'NONE', *, *, #108857, .F. ) ;
#79337=ORIENTED_EDGE ( 'NONE', *, *, #232448, .T. ) ;
#79410=ORIENTED_EDGE ( 'NONE', *, *, #54275, .F. ) ;
#79411=VERTEX_POINT ( 'NONE', #6964 ) ;
#79450=CARTESIAN_POINT ( 'NONE',  ( -21.76363531954647357, 0.09900187431060442078, -93.48706345212828239 ) ) ;
#79495=CARTESIAN_POINT ( 'NONE',  ( 20.94999999999999574, 1.115600667400684642E-11, -100.5000000000000284 ) ) ;
#79508=CARTESIAN_POINT ( 'NONE',  ( 18.59999999999999432, -1.162701749926853712, -108.6000000000000227 ) ) ;
#79513=EDGE_LOOP ( 'NONE', ( #117420, #116678, #89193, #56504 ) ) ;
#79530=TOROIDAL_SURFACE ( 'NONE', #133534, 7.800000000000000711, 0.1000000000000000056 ) ;
#79564=LINE ( 'NONE', #3901, #106469 ) ;
#79570=CARTESIAN_POINT ( 'NONE',  ( -22.50875500270928953, -0.1008579137641491541, -88.75043287260213276 ) ) ;
#79597=ORIENTED_EDGE ( 'NONE', *, *, #7762, .F. ) ;
#79608=CYLINDRICAL_SURFACE ( 'NONE', #232674, 0.5000000000000004441 ) ;
#79628=ORIENTED_EDGE ( 'NONE', *, *, #187651, .T. ) ;
#79634=AXIS2_PLACEMENT_3D ( 'NONE', #65995, #28190, #69870 ) ;
#79672=ORIENTED_EDGE ( 'NONE', *, *, #249001, .F. ) ;
#79681=ORIENTED_EDGE ( 'NONE', *, *, #158371, .F. ) ;
#79682=VERTEX_POINT ( 'NONE', #238 ) ;
#79711=DIRECTION ( 'NONE',  ( 0.000000000000000000, 0.9998779222360096863, -0.01562500000001061998 ) ) ;
#79778=DIRECTION ( 'NONE',  ( -0.000000000000000000, 0.8660254037844411501, 0.4999999999999956701 ) ) ;
#79784=EDGE_CURVE ( 'NONE', #198561, #192673, #161135, .T. ) ;
#79785=CARTESIAN_POINT ( 'NONE',  ( 20.95512820512820440, 8.876151316299271343, -112.6500000000000341 ) ) ;
#79786=CARTESIAN_POINT ( 'NONE',  ( -22.39999999999999858, 1.115600667400684642E-11, -92.70922040162662370 ) ) ;
#79789=DIRECTION ( 'NONE',  ( -0.000000000000000000, -0.000000000000000000, -1.000000000000000000 ) ) ;
#79800=DIRECTION ( 'NONE',  ( 1.000000000000000000, 0.000000000000000000, 0.000000000000000000 ) ) ;
#79805=FACE_OUTER_BOUND ( 'NONE', #245598, .T. ) ;
#79819=CIRCLE ( 'NONE', #4791, 11.75000000000000000 ) ;
#79840=EDGE_LOOP ( 'NONE', ( #218374, #5870, #59438, #157980 ) ) ;
#79861=ORIENTED_EDGE ( 'NONE', *, *, #209427, .T. ) ;
#79905=VERTEX_POINT ( 'NONE', #131747 ) ;
#79927=DIRECTION ( 'NONE',  ( -1.000000000000000000, -0.000000000000000000, -0.000000000000000000 ) ) ;
#79959=VERTEX_POINT ( 'NONE', #173505 ) ;
#79964=ORIENTED_EDGE ( 'NONE', *, *, #70099, .T. ) ;
#79971=ORIENTED_EDGE ( 'NONE', *, *, #200111, .F. ) ;
#79996=ADVANCED_FACE ( 'NONE', ( #1201 ), #97724, .F. ) ;
#80011=DIRECTION ( 'NONE',  ( 1.000000000000000000, -0.000000000000000000, -0.000000000000000000 ) ) ;
#80021=DIRECTION ( 'NONE',  ( 0.7071359030027419834, 0.000000000000000000, 0.7070776581709371511 ) ) ;
#80023=CARTESIAN_POINT ( 'NONE',  ( -20.95000000000000284, 11.65000000001115232, -126.9851942293460922 ) ) ;
#80045=DIRECTION ( 'NONE',  ( 0.7071359030027680737, 0.7070776581709111719, 0.000000000000000000 ) ) ;
#80069=ORIENTED_EDGE ( 'NONE', *, *, #144711, .T. ) ;
#80085=DIRECTION ( 'NONE',  ( 1.000000000000000000, -0.000000000000000000, -0.000000000000000000 ) ) ;
#80086=CARTESIAN_POINT ( 'NONE',  ( 23.24999999999999289, 11.65000000001116298, -121.8500000000000369 ) ) ;
#80087=FACE_OUTER_BOUND ( 'NONE', #48167, .T. ) ;
#80097=DIRECTION ( 'NONE',  ( 1.000000000000000000, 2.952720810173289112E-16, -0.000000000000000000 ) ) ;
#80102=CIRCLE ( 'NONE', #225857, 12.87499999999999822 ) ;
#80106=CARTESIAN_POINT ( 'NONE',  ( 21.05000000000000071, 1.115653327213047955E-11, -104.8000000000000540 ) ) ;
#80108=AXIS2_PLACEMENT_3D ( 'NONE', #113987, #77417, #175293 ) ;
#80120=CARTESIAN_POINT ( 'NONE',  ( 20.94999999999999574, 1.261786168576181755, -108.5864989635455089 ) ) ;
#80127=CARTESIAN_POINT ( 'NONE',  ( 18.49999999999999289, 11.65000000001115588, -134.0000000000000284 ) ) ;
#80147=AXIS2_PLACEMENT_3D ( 'NONE', #102052, #6831, #150212 ) ;
#80166=ORIENTED_EDGE ( 'NONE', *, *, #213918, .F. ) ;
#80177=CARTESIAN_POINT ( 'NONE',  ( 21.30000000000002558, 1.115600667400684642E-11, -104.5500000000000256 ) ) ;
#80191=EDGE_CURVE ( 'NONE', #198122, #223717, #252887, .T. ) ;
#80193=FACE_OUTER_BOUND ( 'NONE', #165003, .T. ) ;
#80218=DIRECTION ( 'NONE',  ( 0.000000000000000000, -0.5000000000000144329, -0.8660254037844302699 ) ) ;
#80264=EDGE_CURVE ( 'NONE', #205348, #107956, #90561, .T. ) ;
#80308=TOROIDAL_SURFACE ( 'NONE', #217701, 0.6000000000000015321, 0.1000000000000000056 ) ;
#80312=EDGE_LOOP ( 'NONE', ( #83792, #113413, #208108 ) ) ;
#80364=LINE ( 'NONE', #159959, #134418 ) ;
#80388=ORIENTED_EDGE ( 'NONE', *, *, #118809, .T. ) ;
#80403=VERTEX_POINT ( 'NONE', #97411 ) ;
#80408=TOROIDAL_SURFACE ( 'NONE', #134588, 11.65000000000000036, 0.1000000000000000056 ) ;
#80422=CARTESIAN_POINT ( 'NONE',  ( -18.50000000000000000, 1.115600667400684642E-11, -100.5000000000000284 ) ) ;
#80425=CARTESIAN_POINT ( 'NONE',  ( -23.15000000000000213, 11.65000000001115588, -121.8500000000000369 ) ) ;
#80464=AXIS2_PLACEMENT_3D ( 'NONE', #52455, #210280, #212846 ) ;
#80467=ORIENTED_EDGE ( 'NONE', *, *, #162827, .F. ) ;
#80481=DIRECTION ( 'NONE',  ( 0.000000000000000000, 0.000000000000000000, -1.000000000000000000 ) ) ;
#80502=ADVANCED_FACE ( 'NONE', ( #122156 ), #28253, .T. ) ;
#80535=CYLINDRICAL_SURFACE ( 'NONE', #135757, 0.09999999999999939493 ) ;
#80544=AXIS2_PLACEMENT_3D ( 'NONE', #133864, #187440, #49191 ) ;
#80553=ORIENTED_EDGE ( 'NONE', *, *, #253659, .F. ) ;
#80554=ADVANCED_FACE ( 'NONE', ( #146826 ), #157440, .T. ) ;
#80560=CARTESIAN_POINT ( 'NONE',  ( -18.59999999999999787, -9.480686695267820596, -140.9411151687578752 ) ) ;
#80570=ORIENTED_EDGE ( 'NONE', *, *, #141211, .F. ) ;
#80610=EDGE_CURVE ( 'NONE', #207792, #190717, #65627, .T. ) ;
#80636=EDGE_LOOP ( 'NONE', ( #133342, #138265, #87522, #223745 ) ) ;
#80641=CARTESIAN_POINT ( 'NONE',  ( -20.00857864376270001, 9.150000000011157653, -121.7500000000000426 ) ) ;
#80653=CARTESIAN_POINT ( 'NONE',  ( -18.59999999999999787, -1.362429037182155023, -141.8888812479212334 ) ) ;
#80658=DIRECTION ( 'NONE',  ( 1.000000000000000000, 0.000000000000000000, 0.000000000000000000 ) ) ;
#80677=ORIENTED_EDGE ( 'NONE', *, *, #213451, .T. ) ;
#80684=DIRECTION ( 'NONE',  ( 0.000000000000000000, 1.000000000000000000, 0.000000000000000000 ) ) ;
#80688=EDGE_LOOP ( 'NONE', ( #16770, #206802, #248070, #257280 ) ) ;
#80711=CARTESIAN_POINT ( 'NONE',  ( 23.15000000000000213, -8.999999999988844479, -110.3939691226524786 ) ) ;
#80719=AXIS2_PLACEMENT_3D ( 'NONE', #175909, #238422, #18083 ) ;
#80724=TOROIDAL_SURFACE ( 'NONE', #201534, 11.65000000000000036, 0.1000000000000000056 ) ;
#80795=TOROIDAL_SURFACE ( 'NONE', #226532, 0.2000000000000000111, 0.1000000000000000056 ) ;
#80797=CIRCLE ( 'NONE', #93285, 0.09999999999998898659 ) ;
#80809=EDGE_CURVE ( 'NONE', #150130, #113518, #45151, .T. ) ;
#80829=ORIENTED_EDGE ( 'NONE', *, *, #155397, .T. ) ;
#80842=CARTESIAN_POINT ( 'NONE',  ( 21.05000000000000071, 1.835341550235569663, -112.0551512925630249 ) ) ;
#80843=VERTEX_POINT ( 'NONE', #78534 ) ;
#80856=CARTESIAN_POINT ( 'NONE',  ( -22.50000000000094147, 0.1008583691097610646, -88.75043287651061519 ) ) ;
#80857=CARTESIAN_POINT ( 'NONE',  ( 20.94999999999999929, -1.162701749926853712, -108.4000000000000341 ) ) ;
#80872=ORIENTED_EDGE ( 'NONE', *, *, #144711, .F. ) ;
#80877=FACE_OUTER_BOUND ( 'NONE', #212364, .T. ) ;
#80893=DIRECTION ( 'NONE',  ( -3.469446951953635015E-14, -1.000000000000000000, 0.000000000000000000 ) ) ;
#80907=EDGE_CURVE ( 'NONE', #183616, #223717, #49689, .T. ) ;
#80931=CARTESIAN_POINT ( 'NONE',  ( 23.15000000000000213, -9.499999999988844479, -124.1060308773475924 ) ) ;
#80941=ORIENTED_EDGE ( 'NONE', *, *, #200160, .T. ) ;
#80943=AXIS2_PLACEMENT_3D ( 'NONE', #257836, #47489, #120978 ) ;
#80956=ORIENTED_EDGE ( 'NONE', *, *, #176246, .F. ) ;
#80976=CARTESIAN_POINT ( 'NONE',  ( -18.59999999999999787, 1.115600667400684642E-11, -134.0000000000000284 ) ) ;
#80987=CIRCLE ( 'NONE', #247598, 11.64999999999999325 ) ;
#80990=ORIENTED_EDGE ( 'NONE', *, *, #140611, .F. ) ;
#81014=DIRECTION ( 'NONE',  ( 1.000000000000000000, -0.000000000000000000, -0.000000000000000000 ) ) ;
#81040=CYLINDRICAL_SURFACE ( 'NONE', #142866, 0.1000000000000028644 ) ;
#81045=EDGE_CURVE ( 'NONE', #10935, #191177, #61911, .T. ) ;
#81055=AXIS2_PLACEMENT_3D ( 'NONE', #58199, #102443, #60773 ) ;
#81064=DIRECTION ( 'NONE',  ( 0.000000000000000000, 0.000000000000000000, -1.000000000000000000 ) ) ;
#81066=CARTESIAN_POINT ( 'NONE',  ( -18.50000000000000000, 1.162701749949165642, -108.6000000000000227 ) ) ;
#81096=ADVANCED_FACE ( 'NONE', ( #32738 ), #24507, .T. ) ;
#81099=CARTESIAN_POINT ( 'NONE',  ( -20.94999999999999929, 1.162701749949165642, -108.6000000000000227 ) ) ;
#81118=EDGE_CURVE ( 'NONE', #160208, #21528, #107687, .T. ) ;
#81120=PLANE ( 'NONE',  #50889 ) ;
#81162=DIRECTION ( 'NONE',  ( 0.000000000000000000, -1.000000000000000000, 0.000000000000000000 ) ) ;
#81193=AXIS2_PLACEMENT_3D ( 'NONE', #113257, #257843, #177111 ) ;
#81252=ORIENTED_EDGE ( 'NONE', *, *, #159300, .T. ) ;
#81295=VERTEX_POINT ( 'NONE', #149794 ) ;
#81302=DIRECTION ( 'NONE',  ( 0.000000000000000000, 1.000000000000000000, -6.308085367188393199E-16 ) ) ;
#81311=LINE ( 'NONE', #176617, #5791 ) ;
#81315=CARTESIAN_POINT ( 'NONE',  ( 21.04999999999999716, -0.01454569055747518061, -94.00298221356867145 ) ) ;
#81319=EDGE_CURVE ( 'NONE', #319, #144708, #182733, .T. ) ;
#81385=CIRCLE ( 'NONE', #85852, 0.1000000000000028644 ) ;
#81399=EDGE_CURVE ( 'NONE', #226312, #168568, #75393, .T. ) ;
#81407=AXIS2_PLACEMENT_3D ( 'NONE', #171841, #94822, #37444 ) ;
#81445=CARTESIAN_POINT ( 'NONE',  ( -18.50000000000000000, -1.164121893230052995, -141.9148480855716343 ) ) ;
#81452=CIRCLE ( 'NONE', #114813, 0.1000000000000028644 ) ;
#81460=CARTESIAN_POINT ( 'NONE',  ( 20.99749315643150638, 11.75000000001115907, -126.9851942312421045 ) ) ;
#81478=DIRECTION ( 'NONE',  ( 0.000000000000000000, 0.000000000000000000, -1.000000000000000000 ) ) ;
#81480=DIRECTION ( 'NONE',  ( 0.000000000000000000, 0.000000000000000000, -1.000000000000000000 ) ) ;
#81487=ADVANCED_FACE ( 'NONE', ( #81738 ), #201720, .F. ) ;
#81493=AXIS2_PLACEMENT_3D ( 'NONE', #243856, #27425, #44397 ) ;
#81507=CARTESIAN_POINT ( 'NONE',  ( -21.17356465864818205, 6.422803126252873973, -100.4010887589861625 ) ) ;
#81511=VERTEX_POINT ( 'NONE', #219999 ) ;
#81517=TOROIDAL_SURFACE ( 'NONE', #202182, 12.77499999999999858, 0.1000000000000000056 ) ;
#81520=CARTESIAN_POINT ( 'NONE',  ( 20.94999999999999929, -1.835859311432481045, -145.5044391687985694 ) ) ;
#81572=LINE ( 'NONE', #161157, #209096 ) ;
#81613=VECTOR ( 'NONE', #77000, 1000.000000000000000 ) ;
#81635=DIRECTION ( 'NONE',  ( 0.000000000000000000, 0.000000000000000000, 1.000000000000000000 ) ) ;
#81690=CARTESIAN_POINT ( 'NONE',  ( -18.59999999999999787, 1.162701749949165642, -108.5000000000000426 ) ) ;
#81696=ORIENTED_EDGE ( 'NONE', *, *, #24639, .T. ) ;
#81738=FACE_OUTER_BOUND ( 'NONE', #215034, .T. ) ;
#81781=FACE_OUTER_BOUND ( 'NONE', #9706, .T. ) ;
#81790=ORIENTED_EDGE ( 'NONE', *, *, #52488, .T. ) ;
#81908=FACE_OUTER_BOUND ( 'NONE', #193786, .T. ) ;
#81929=FACE_OUTER_BOUND ( 'NONE', #94512, .T. ) ;
#81964=VECTOR ( 'NONE', #40420, 1000.000000000000000 ) ;
#81990=AXIS2_PLACEMENT_3D ( 'NONE', #193308, #96732, #216708 ) ;
#82016=ADVANCED_FACE ( 'NONE', ( #215807 ), #235383, .T. ) ;
#82026=ADVANCED_FACE ( 'NONE', ( #214537, #35931 ), #195006, .T. ) ;
#82080=VECTOR ( 'NONE', #23529, 1000.000000000000000 ) ;
#82093=CARTESIAN_POINT ( 'NONE',  ( 18.49999999999998934, 19.85039924724470950, -102.7803030578013903 ) ) ;
#82143=CARTESIAN_POINT ( 'NONE',  ( -20.94999999999999574, 11.62071067812980907, -127.1315833476590740 ) ) ;
#82169=CIRCLE ( 'NONE', #28066, 0.2000000000000057288 ) ;
#82171=CIRCLE ( 'NONE', #227961, 0.09999999999999939493 ) ;
#82206=DIRECTION ( 'NONE',  ( -1.000000000000000000, 0.000000000000000000, 0.000000000000000000 ) ) ;
#82235=DIRECTION ( 'NONE',  ( 1.000000000000000000, -0.000000000000000000, -0.000000000000000000 ) ) ;
#82280=EDGE_CURVE ( 'NONE', #59875, #53618, #94291, .T. ) ;
#82281=CARTESIAN_POINT ( 'NONE',  ( -21.13422380239045850, 1.115526128501326264E-11, -94.00667348519432664 ) ) ;
#82326=FACE_OUTER_BOUND ( 'NONE', #154322, .T. ) ;
#82344=DIRECTION ( 'NONE',  ( -1.000000000000000000, 0.000000000000000000, 0.000000000000000000 ) ) ;
#82346=ADVANCED_FACE ( 'NONE', ( #18620 ), #139834, .T. ) ;
#82356=EDGE_CURVE ( 'NONE', #79411, #183734, #254631, .T. ) ;
#82413=TOROIDAL_SURFACE ( 'NONE', #69798, 3.899999999999999467, 0.1000000000000000056 ) ;
#82426=EDGE_CURVE ( 'NONE', #162338, #16939, #154327, .T. ) ;
#82432=DIRECTION ( 'NONE',  ( -2.812466655313719426E-14, 0.1350103645451904977, 0.9908441862701596881 ) ) ;
#82437=ORIENTED_EDGE ( 'NONE', *, *, #35616, .T. ) ;
#82454=DIRECTION ( 'NONE',  ( -1.000000000000000000, 0.000000000000000000, 0.000000000000000000 ) ) ;
#82458=AXIS2_PLACEMENT_3D ( 'NONE', #34295, #91666, #33029 ) ;
#82469=DIRECTION ( 'NONE',  ( 0.000000000000000000, 0.000000000000000000, -1.000000000000000000 ) ) ;
#82489=AXIS2_PLACEMENT_3D ( 'NONE', #71459, #148414, #130113 ) ;
#82497=ORIENTED_EDGE ( 'NONE', *, *, #174472, .T. ) ;
#82528=EDGE_CURVE ( 'NONE', #50377, #116815, #83681, .T. ) ;
#82536=ADVANCED_FACE ( 'NONE', ( #65440 ), #121603, .T. ) ;
#82547=CARTESIAN_POINT ( 'NONE',  ( 21.07928932188134397, 6.328516656404459262, -100.4011048543456468 ) ) ;
#82591=AXIS2_PLACEMENT_3D ( 'NONE', #171708, #183865, #251189 ) ;
#82619=DIRECTION ( 'NONE',  ( 0.000000000000000000, 0.1495327102803586661, -0.9887567792719350601 ) ) ;
#82631=EDGE_CURVE ( 'NONE', #8209, #242007, #191854, .T. ) ;
#82642=ADVANCED_FACE ( 'NONE', ( #71881 ), #195930, .F. ) ;
#82644=ORIENTED_EDGE ( 'NONE', *, *, #186812, .T. ) ;
#82658=EDGE_LOOP ( 'NONE', ( #157362, #80388, #3262, #127878 ) ) ;
#82685=CARTESIAN_POINT ( 'NONE',  ( -21.05000000000000071, 1.835341550235569663, -112.0551512925630249 ) ) ;
#82714=CARTESIAN_POINT ( 'NONE',  ( -18.39999999999999858, -9.599999999988849453, -140.6001893912220737 ) ) ;
#82726=EDGE_CURVE ( 'NONE', #256518, #231259, #208414, .T. ) ;
#82728=CARTESIAN_POINT ( 'NONE',  ( -21.51976009735018991, 6.910458441670358276, -100.5000000000000284 ) ) ;
#82763=ORIENTED_EDGE ( 'NONE', *, *, #76820, .T. ) ;
#82784=CARTESIAN_POINT ( 'NONE',  ( 21.05000000000000071, 10.42338541492406279, -107.9920519238701218 ) ) ;
#82812=ORIENTED_EDGE ( 'NONE', *, *, #80191, .T. ) ;
#82814=CIRCLE ( 'NONE', #228624, 12.87499999999999822 ) ;
#82893=CARTESIAN_POINT ( 'NONE',  ( 20.58091095332318332, 9.018470153363605135, -108.9186501821586006 ) ) ;
#82896=AXIS2_PLACEMENT_3D ( 'NONE', #213134, #79711, #159290 ) ;
#82918=FACE_OUTER_BOUND ( 'NONE', #95646, .T. ) ;
#82927=DIRECTION ( 'NONE',  ( -4.408576920032448588E-17, 0.1350103645451876666, 0.9908441862701600211 ) ) ;
#82980=DIRECTION ( 'NONE',  ( 0.000000000000000000, 0.000000000000000000, 1.000000000000000000 ) ) ;
#83015=CARTESIAN_POINT ( 'NONE',  ( 21.53752568622133978, 0.09897446127743518562, -93.71319212545147082 ) ) ;
#83017=VECTOR ( 'NONE', #149029, 1000.000000000000000 ) ;
#83029=DIRECTION ( 'NONE',  ( -0.000000000000000000, -1.000000000000000000, 6.308085367188393199E-16 ) ) ;
#83035=SPHERICAL_SURFACE ( 'NONE', #121311, 0.1000000000000000056 ) ;
#83096=CARTESIAN_POINT ( 'NONE',  ( 23.14999999999999858, 1.115649653272650466E-11, -130.0000000000000284 ) ) ;
#83100=CARTESIAN_POINT ( 'NONE',  ( 23.24999999999999645, 3.900000000011155432, -134.0000000000000284 ) ) ;
#83101=ORIENTED_EDGE ( 'NONE', *, *, #199471, .T. ) ;
#83114=CARTESIAN_POINT ( 'NONE',  ( -18.48408745364672967, -9.664322258652003228, -140.6830785333283416 ) ) ;
#83217=DIRECTION ( 'NONE',  ( 0.000000000000000000, 1.000000000000000000, 0.000000000000000000 ) ) ;
#83225=EDGE_CURVE ( 'NONE', #221499, #190980, #33828, .T. ) ;
#83241=DIRECTION ( 'NONE',  ( 0.000000000000000000, 0.000000000000000000, 1.000000000000000000 ) ) ;
#83242=DIRECTION ( 'NONE',  ( -1.000000000000000000, 0.000000000000000000, 0.000000000000000000 ) ) ;
#83268=DIRECTION ( 'NONE',  ( 1.000000000000000000, 0.000000000000000000, 0.000000000000000000 ) ) ;
#83286=ADVANCED_FACE ( 'NONE', ( #233853 ), #108606, .T. ) ;
#83290=CARTESIAN_POINT ( 'NONE',  ( -18.39999999999999858, -9.499999999988849808, -140.6001893912220737 ) ) ;
#83303=ORIENTED_EDGE ( 'NONE', *, *, #86451, .T. ) ;
#83324=CARTESIAN_POINT ( 'NONE',  ( 18.49999999999999289, 10.34378108836433263, -125.3284452778770373 ) ) ;
#83336=PLANE ( 'NONE',  #94262 ) ;
#83346=ADVANCED_FACE ( 'NONE', ( #51325 ), #31829, .F. ) ;
#83351=ORIENTED_EDGE ( 'NONE', *, *, #72926, .F. ) ;
#83378=CARTESIAN_POINT ( 'NONE',  ( 21.05000000000000071, 8.776282895303632259, -112.6500000000000341 ) ) ;
#83397=EDGE_CURVE ( 'NONE', #111333, #204479, #162405, .T. ) ;
#83412=CARTESIAN_POINT ( 'NONE',  ( -22.40000000000000213, 1.115486932051692071E-11, -88.74956710754142364 ) ) ;
#83456=CIRCLE ( 'NONE', #146019, 0.1000000000000028644 ) ;
#83495=VERTEX_POINT ( 'NONE', #115187 ) ;
#83498=ADVANCED_FACE ( 'NONE', ( #254655 ), #16111, .T. ) ;
#83507=CARTESIAN_POINT ( 'NONE',  ( 18.43579564894463374, -9.519327535281719932, -107.4729766438598944 ) ) ;
#83513=VERTEX_POINT ( 'NONE', #95613 ) ;
#83520=EDGE_CURVE ( 'NONE', #208327, #237460, #18653, .T. ) ;
#83522=VERTEX_POINT ( 'NONE', #119046 ) ;
#83523=CARTESIAN_POINT ( 'NONE',  ( -21.14999999999999858, 11.65000000001115588, -100.5000000000000284 ) ) ;
#83534=DIRECTION ( 'NONE',  ( 1.000000000000000000, 0.000000000000000000, -0.000000000000000000 ) ) ;
#83543=AXIS2_PLACEMENT_3D ( 'NONE', #156447, #171195, #151614 ) ;
#83551=CARTESIAN_POINT ( 'NONE',  ( -18.59999999999999787, -1.164121893230052995, -141.9148480855716343 ) ) ;
#83562=CARTESIAN_POINT ( 'NONE',  ( -21.05000000000000071, -0.09999999998884476216, -93.95934304829879125 ) ) ;
#83574=DIRECTION ( 'NONE',  ( 0.000000000000000000, 0.000000000000000000, 1.000000000000000000 ) ) ;
#83613=CARTESIAN_POINT ( 'NONE',  ( -21.05000000000000071, 5.850000000011108092, -110.6324972242780120 ) ) ;
#83621=DIRECTION ( 'NONE',  ( -1.000000000000000000, -0.000000000000000000, -0.000000000000000000 ) ) ;
#83633=DIRECTION ( 'NONE',  ( 0.000000000000000000, 0.5000000000000004441, 0.8660254037844384856 ) ) ;
#83666=DIRECTION ( 'NONE',  ( 0.000000000000000000, 0.000000000000000000, -1.000000000000000000 ) ) ;
#83681=LINE ( 'NONE', #242789, #187571 ) ;
#83690=EDGE_LOOP ( 'NONE', ( #121296, #92404, #201202 ) ) ;
#83715=DIRECTION ( 'NONE',  ( 0.000000000000000000, 0.4999999999999608646, 0.8660254037844612451 ) ) ;
#83736=ORIENTED_EDGE ( 'NONE', *, *, #138619, .F. ) ;
#83737=CARTESIAN_POINT ( 'NONE',  ( -20.94999999999999929, 11.75000000001115552, -107.5148057706540357 ) ) ;
#83757=DIRECTION ( 'NONE',  ( 0.000000000000000000, -0.8700118002898359348, 0.4930308989875165082 ) ) ;
#83791=ORIENTED_EDGE ( 'NONE', *, *, #42790, .T. ) ;
#83792=ORIENTED_EDGE ( 'NONE', *, *, #93633, .T. ) ;
#83816=CARTESIAN_POINT ( 'NONE',  ( -21.05000000000000071, 11.75000000001115197, -127.1583993101029790 ) ) ;
#83857=LINE ( 'NONE', #222100, #179025 ) ;
#83860=DIRECTION ( 'NONE',  ( 0.000000000000000000, -0.000000000000000000, -1.000000000000000000 ) ) ;
#83869=CIRCLE ( 'NONE', #108851, 0.1000000000000028644 ) ;
#83872=ORIENTED_EDGE ( 'NONE', *, *, #99311, .F. ) ;
#83886=AXIS2_PLACEMENT_3D ( 'NONE', #105434, #203293, #139448 ) ;
#83892=DIRECTION ( 'NONE',  ( 0.000000000000000000, -0.9915357197604971473, 0.1298341882519111479 ) ) ;
#84006=CARTESIAN_POINT ( 'NONE',  ( -21.05000000000000071, -1.249999999988843369, -108.5000000000000426 ) ) ;
#84009=FACE_OUTER_BOUND ( 'NONE', #112651, .T. ) ;
#84010=CARTESIAN_POINT ( 'NONE',  ( 21.08489834409762054, 10.62232389474667293, -112.8500000000000369 ) ) ;
#84018=CARTESIAN_POINT ( 'NONE',  ( -18.48550754432008958, -9.463399778548764019, -107.5487897524156580 ) ) ;
#84034=DIRECTION ( 'NONE',  ( 0.000000000000000000, -0.8777080977375715243, 0.4791956752370512551 ) ) ;
#84038=AXIS2_PLACEMENT_3D ( 'NONE', #225156, #186059, #47807 ) ;
#84048=EDGE_CURVE ( 'NONE', #196016, #243821, #242529, .T. ) ;
#84087=EDGE_CURVE ( 'NONE', #132946, #8700, #145817, .T. ) ;
#84112=CARTESIAN_POINT ( 'NONE',  ( 21.05000000000000071, 10.62950747927179229, -108.1279793999968035 ) ) ;
#84117=EDGE_CURVE ( 'NONE', #67578, #173670, #129438, .T. ) ;
#84123=FACE_OUTER_BOUND ( 'NONE', #158077, .T. ) ;
#84132=VERTEX_POINT ( 'NONE', #9055 ) ;
#84179=CARTESIAN_POINT ( 'NONE',  ( 20.94999999999999929, 1.115600667400684642E-11, -113.4750000000000369 ) ) ;
#84230=ADVANCED_FACE ( 'NONE', ( #58422 ), #79530, .T. ) ;
#84253=ADVANCED_FACE ( 'NONE', ( #157597 ), #37626, .F. ) ;
#84287=CYLINDRICAL_SURFACE ( 'NONE', #164914, 12.87499999999999822 ) ;
#84300=ORIENTED_EDGE ( 'NONE', *, *, #171145, .F. ) ;
#84327=EDGE_CURVE ( 'NONE', #191177, #142271, #92016, .T. ) ;
#84332=CARTESIAN_POINT ( 'NONE',  ( 20.46382478191414833, 8.901379558713770734, -109.0457280948831453 ) ) ;
#84339=AXIS2_PLACEMENT_3D ( 'NONE', #186193, #166658, #149649 ) ;
#84341=VERTEX_POINT ( 'NONE', #25743 ) ;
#84348=CARTESIAN_POINT ( 'NONE',  ( 21.05000000000000071, 5.000000000011153745, -121.9947339810869380 ) ) ;
#84357=CARTESIAN_POINT ( 'NONE',  ( 20.85000000000000142, 6.846123162363745074, -137.7377262668498759 ) ) ;
#84385=CARTESIAN_POINT ( 'NONE',  ( -18.37151313414693732, -9.571014125767270286, -140.8166629092384596 ) ) ;
#84431=AXIS2_PLACEMENT_3D ( 'NONE', #122225, #120963, #124794 ) ;
#84449=EDGE_CURVE ( 'NONE', #111732, #185160, #61005, .T. ) ;
#84458=CARTESIAN_POINT ( 'NONE',  ( -20.94999999999999929, -1.261786168553869603, -108.5864989635455089 ) ) ;
#84459=AXIS2_PLACEMENT_3D ( 'NONE', #50038, #128308, #51293 ) ;
#84473=ORIENTED_EDGE ( 'NONE', *, *, #69742, .T. ) ;
#84486=EDGE_CURVE ( 'NONE', #167915, #45115, #25408, .T. ) ;
#84509=DIRECTION ( 'NONE',  ( 1.000000000000000000, -0.000000000000000000, -0.000000000000000000 ) ) ;
#84511=LINE ( 'NONE', #66292, #216398 ) ;
#84521=LINE ( 'NONE', #243644, #204132 ) ;
#84529=CARTESIAN_POINT ( 'NONE',  ( -20.93284271247462058, 11.75000000001115019, -126.9851942293460922 ) ) ;
#84536=AXIS2_PLACEMENT_3D ( 'NONE', #146494, #203918, #226017 ) ;
#84548=ADVANCED_FACE ( 'NONE', ( #188658 ), #55213, .F. ) ;
#84561=DIRECTION ( 'NONE',  ( -1.000000000000000000, -3.265361837132813093E-16, 0.000000000000000000 ) ) ;
#84613=DIRECTION ( 'NONE',  ( 0.000000000000000000, 1.000000000000000000, 0.000000000000000000 ) ) ;
#84615=LINE ( 'NONE', #68974, #206483 ) ;
#84642=DIRECTION ( 'NONE',  ( 0.000000000000000000, 0.000000000000000000, -1.000000000000000000 ) ) ;
#84655=CYLINDRICAL_SURFACE ( 'NONE', #113412, 0.1000000000000000472 ) ;
#84673=CARTESIAN_POINT ( 'NONE',  ( 21.05000000000000071, 5.500000000011153745, -121.5947339810869465 ) ) ;
#84680=FACE_OUTER_BOUND ( 'NONE', #198920, .T. ) ;
#84681=ORIENTED_EDGE ( 'NONE', *, *, #1587, .F. ) ;
#84686=LINE ( 'NONE', #65155, #52981 ) ;
#84688=ORIENTED_EDGE ( 'NONE', *, *, #124270, .T. ) ;
#84698=AXIS2_PLACEMENT_3D ( 'NONE', #60189, #138424, #98011 ) ;
#84704=CARTESIAN_POINT ( 'NONE',  ( -18.50000000000000000, 11.65000000001115232, -88.75000000000004263 ) ) ;
#84788=CARTESIAN_POINT ( 'NONE',  ( 18.50000000000000000, -9.399999999988823518, -107.7972597596632909 ) ) ;
#84814=SPHERICAL_SURFACE ( 'NONE', #103518, 0.1000000000000000056 ) ;
#84828=CARTESIAN_POINT ( 'NONE',  ( -18.50000000000000000, 11.65000000001115588, -134.0000000000000284 ) ) ;
#84829=DIRECTION ( 'NONE',  ( 0.000000000000000000, 0.000000000000000000, -1.000000000000000000 ) ) ;
#84844=CARTESIAN_POINT ( 'NONE',  ( 22.39999999999999503, 1.115600667400684642E-11, -88.85042919245522341 ) ) ;
#84865=CARTESIAN_POINT ( 'NONE',  ( 21.53551880898956838, 6.784797761427480367, -100.4010302654283606 ) ) ;
#84886=ORIENTED_EDGE ( 'NONE', *, *, #148616, .T. ) ;
#84897=VECTOR ( 'NONE', #159475, 1000.000000000000000 ) ;
#84900=LINE ( 'NONE', #83613, #170098 ) ;
#84911=DIRECTION ( 'NONE',  ( -1.000000000000000000, 0.000000000000000000, 0.000000000000000000 ) ) ;
#84946=AXIS2_PLACEMENT_3D ( 'NONE', #122386, #242319, #147061 ) ;
#84949=AXIS2_PLACEMENT_3D ( 'NONE', #213232, #34636, #253637 ) ;
#84976=CARTESIAN_POINT ( 'NONE',  ( 19.75857864376268935, 11.75000000001115907, -125.3500000000000512 ) ) ;
#85000=EDGE_CURVE ( 'NONE', #225371, #79959, #129802, .T. ) ;
#85015=CARTESIAN_POINT ( 'NONE',  ( 18.59999999999999432, -1.299733671219632791, -90.52812952286942050 ) ) ;
#85047=EDGE_LOOP ( 'NONE', ( #179211, #2941, #32339 ) ) ;
#85052=FACE_OUTER_BOUND ( 'NONE', #200497, .T. ) ;
#85085=EDGE_LOOP ( 'NONE', ( #157150, #128204, #141123, #12459, #180342 ) ) ;
#85095=ORIENTED_EDGE ( 'NONE', *, *, #27775, .T. ) ;
#85106=CARTESIAN_POINT ( 'NONE',  ( -20.96077737575350142, 11.62390063401584861, -127.1407919571063729 ) ) ;
#85112=CARTESIAN_POINT ( 'NONE',  ( 21.11927991906888025, 6.448493118502572230, -100.4909163205261393 ) ) ;
#85120=VECTOR ( 'NONE', #103633, 1000.000000000000000 ) ;
#85144=AXIS2_PLACEMENT_3D ( 'NONE', #197199, #280, #257128 ) ;
#85187=ORIENTED_EDGE ( 'NONE', *, *, #47699, .F. ) ;
#85189=CARTESIAN_POINT ( 'NONE',  ( -21.14999999999999858, 11.65000000001115588, -100.6000000000000369 ) ) ;
#85209=EDGE_CURVE ( 'NONE', #7281, #40759, #17388, .T. ) ;
#85242=CARTESIAN_POINT ( 'NONE',  ( 22.59999999999999432, 11.74987124438766273, -100.4345704089863602 ) ) ;
#85249=ORIENTED_EDGE ( 'NONE', *, *, #131215, .F. ) ;
#85250=AXIS2_PLACEMENT_3D ( 'NONE', #228814, #204086, #149290 ) ;
#85288=FACE_OUTER_BOUND ( 'NONE', #52109, .T. ) ;
#85319=CARTESIAN_POINT ( 'NONE',  ( 20.99551997958415583, 11.75000000001125144, -127.1516591376888954 ) ) ;
#85324=EDGE_CURVE ( 'NONE', #92189, #237605, #4867, .T. ) ;
#85328=CARTESIAN_POINT ( 'NONE',  ( -18.40000000000000213, -9.499999999988851584, -107.5320693966996970 ) ) ;
#85360=ADVANCED_FACE ( 'NONE', ( #64910 ), #70086, .T. ) ;
#85365=VERTEX_POINT ( 'NONE', #128758 ) ;
#85377=VERTEX_POINT ( 'NONE', #183591 ) ;
#85396=EDGE_CURVE ( 'NONE', #173670, #232908, #28405, .T. ) ;
#85428=AXIS2_PLACEMENT_3D ( 'NONE', #133435, #212970, #176435 ) ;
#85437=ORIENTED_EDGE ( 'NONE', *, *, #105061, .F. ) ;
#85468=VERTEX_POINT ( 'NONE', #149619 ) ;
#85474=AXIS2_PLACEMENT_3D ( 'NONE', #124801, #6109, #25696 ) ;
#85484=LINE ( 'NONE', #244590, #11807 ) ;
#85492=CARTESIAN_POINT ( 'NONE',  ( -20.87600722750343252, 10.33112638556969465, -139.5901228926975080 ) ) ;
#85500=VECTOR ( 'NONE', #84509, 1000.000000000000000 ) ;
#85505=EDGE_CURVE ( 'NONE', #118818, #177703, #253812, .T. ) ;
#85547=EDGE_LOOP ( 'NONE', ( #40298, #257852, #138003 ) ) ;
#85582=TOROIDAL_SURFACE ( 'NONE', #231387, 0.4000000000000003553, 0.1000000000000000056 ) ;
#85586=EDGE_CURVE ( 'NONE', #59875, #170174, #113429, .T. ) ;
#85625=ORIENTED_EDGE ( 'NONE', *, *, #38278, .T. ) ;
#85652=VERTEX_POINT ( 'NONE', #215965 ) ;
#85676=AXIS2_PLACEMENT_3D ( 'NONE', #105671, #223069, #242630 ) ;
#85706=ORIENTED_EDGE ( 'NONE', *, *, #102861, .F. ) ;
#85711=EDGE_CURVE ( 'NONE', #44449, #159674, #5057, .T. ) ;
#85713=EDGE_LOOP ( 'NONE', ( #155647, #29939, #128097, #9629 ) ) ;
#85719=CARTESIAN_POINT ( 'NONE',  ( 22.42196299218230493, 0.002441673998456600492, -88.85038829735056254 ) ) ;
#85720=DIRECTION ( 'NONE',  ( 1.000000000000000000, 0.000000000000000000, 0.000000000000000000 ) ) ;
#85724=EDGE_CURVE ( 'NONE', #25027, #205348, #81572, .T. ) ;
#85730=EDGE_CURVE ( 'NONE', #111333, #12223, #257614, .T. ) ;
#85737=CARTESIAN_POINT ( 'NONE',  ( 21.07016717456946253, 6.320940838111409832, -100.5000000000000568 ) ) ;
#85780=ORIENTED_EDGE ( 'NONE', *, *, #221028, .F. ) ;
#85782=ORIENTED_EDGE ( 'NONE', *, *, #243223, .T. ) ;
#85800=DIRECTION ( 'NONE',  ( 1.000000000000000000, 0.000000000000000000, 0.000000000000000000 ) ) ;
#85806=DIRECTION ( 'NONE',  ( 0.000000000000000000, 0.000000000000000000, -1.000000000000000000 ) ) ;
#85852=AXIS2_PLACEMENT_3D ( 'NONE', #166878, #145981, #125158 ) ;
#85854=VECTOR ( 'NONE', #66380, 1000.000000000000227 ) ;
#85855=ORIENTED_EDGE ( 'NONE', *, *, #22204, .T. ) ;
#85902=AXIS2_PLACEMENT_3D ( 'NONE', #90633, #171503, #249727 ) ;
#85949=DIRECTION ( 'NONE',  ( 0.000000000000000000, -0.9908441862701596881, -0.1350103645451904977 ) ) ;
#85977=CARTESIAN_POINT ( 'NONE',  ( -20.54999999999999716, 1.115624548013267999E-11, -132.1000000000000227 ) ) ;
#86020=EDGE_LOOP ( 'NONE', ( #142968, #144915, #239728, #185844 ) ) ;
#86051=VECTOR ( 'NONE', #172489, 1000.000000000000000 ) ;
#86084=AXIS2_PLACEMENT_3D ( 'NONE', #75924, #35544, #32990 ) ;
#86092=CARTESIAN_POINT ( 'NONE',  ( -21.00219873199057119, 11.60538868788778899, -107.4126474282948180 ) ) ;
#86096=DIRECTION ( 'NONE',  ( 1.000000000000000000, 0.000000000000000000, 0.000000000000000000 ) ) ;
#86108=EDGE_LOOP ( 'NONE', ( #228594, #66003, #142309, #126425 ) ) ;
#86123=FACE_OUTER_BOUND ( 'NONE', #118952, .T. ) ;
#86143=CARTESIAN_POINT ( 'NONE',  ( -18.59999999999999787, 9.350000000011156942, -112.8500000000000369 ) ) ;
#86197=ORIENTED_EDGE ( 'NONE', *, *, #239164, .F. ) ;
#86205=CARTESIAN_POINT ( 'NONE',  ( 18.59999999999999787, -1.362429037182151470, -141.8888812479212334 ) ) ;
#86245=CIRCLE ( 'NONE', #198693, 7.800000000000001599 ) ;
#86248=CARTESIAN_POINT ( 'NONE',  ( -23.25000000000000000, 1.115600667400684642E-11, -134.0000000000000284 ) ) ;
#86295=CYLINDRICAL_SURFACE ( 'NONE', #196014, 0.09999999999999939493 ) ;
#86306=CARTESIAN_POINT ( 'NONE',  ( 18.59999999999999787, 5.900000000011102586, -110.7190997646564483 ) ) ;
#86312=ORIENTED_EDGE ( 'NONE', *, *, #89291, .T. ) ;
#86359=LINE ( 'NONE', #146350, #199300 ) ;
#86377=ORIENTED_EDGE ( 'NONE', *, *, #223023, .F. ) ;
#86394=DIRECTION ( 'NONE',  ( -1.000000000000000000, -0.000000000000000000, 0.000000000000000000 ) ) ;
#86407=DIRECTION ( 'NONE',  ( -7.304098846218134667E-16, 1.000000000000000000, -0.000000000000000000 ) ) ;
#86438=VERTEX_POINT ( 'NONE', #100210 ) ;
#86451=EDGE_CURVE ( 'NONE', #79411, #222495, #9543, .T. ) ;
#86470=ORIENTED_EDGE ( 'NONE', *, *, #120594, .F. ) ;
#86473=CIRCLE ( 'NONE', #240622, 0.09999999999998898659 ) ;
#86504=DIRECTION ( 'NONE',  ( 0.000000000000000000, 0.000000000000000000, -1.000000000000000000 ) ) ;
#86543=TOROIDAL_SURFACE ( 'NONE', #28350, 0.2000000000000000111, 0.1000000000000000056 ) ;
#86575=CARTESIAN_POINT ( 'NONE',  ( -18.59999999999999787, 1.162701749949165642, -108.6000000000000227 ) ) ;
#86576=EDGE_CURVE ( 'NONE', #68945, #115014, #122170, .T. ) ;
#86594=EDGE_CURVE ( 'NONE', #162687, #141245, #10133, .T. ) ;
#86606=CARTESIAN_POINT ( 'NONE',  ( 20.85000000106584750, 11.75000000001115907, -127.1555046564734113 ) ) ;
#86607=CARTESIAN_POINT ( 'NONE',  ( 20.95512820512820440, 10.62384868372303615, -112.6500000000000341 ) ) ;
#86614=CARTESIAN_POINT ( 'NONE',  ( -21.05000000000000071, 6.257814610487270279, -100.4022097086912311 ) ) ;
#86626=CARTESIAN_POINT ( 'NONE',  ( -21.09610168723073542, 6.378955715235941071, -100.4664104931085262 ) ) ;
#86637=ADVANCED_FACE ( 'NONE', ( #110504 ), #138864, .F. ) ;
#86657=( BOUNDED_SURFACE ( )  B_SPLINE_SURFACE ( 3, 2, ( 
 ( #124021, #122749, #139698 ),
 ( #40667, #143570, #4054 ),
 ( #58869, #160599, #219244 ),
 ( #2758, #120197, #101849 ),
 ( #82281, #180146, #199718 ),
 ( #21086, #161877, #83562 ) ),
 .UNSPECIFIED., .F., .F., .F. ) 
 B_SPLINE_SURFACE_WITH_KNOTS ( ( 4, 2, 4 ),
 ( 3, 3 ),
 ( 0.0001792624049599542612, 0.0003686986002124735670, 0.0005581347954649928727 ),
 ( 0.000000000000000000, 1.000000000000000000 ),
 .UNSPECIFIED. ) 
 GEOMETRIC_REPRESENTATION_ITEM ( )  RATIONAL_B_SPLINE_SURFACE ( (
 ( 1.000000000000000000, 0.9238795325112985068, 1.000000000000000000),
 ( 1.000000000000000000, 0.9229318695241288673, 1.000000000000000000),
 ( 1.000000000000000000, 0.8926288119226872819, 1.000000000000000000),
 ( 1.000000000000000000, 0.8123777807275367469, 1.000000000000000000),
 ( 1.000000000000000000, 0.7629087100928569898, 1.000000000000000000),
 ( 1.000000000000000000, 0.7071067811865475727, 1.000000000000000000) ) ) 
 REPRESENTATION_ITEM ( '' )  SURFACE ( )  );
#86667=CARTESIAN_POINT ( 'NONE',  ( -18.59999999999999787, 11.75000000001115197, -88.75000000000004263 ) ) ;
#86672=ORIENTED_EDGE ( 'NONE', *, *, #252273, .T. ) ;
#86686=DIRECTION ( 'NONE',  ( 0.000000000000000000, 0.000000000000000000, 1.000000000000000000 ) ) ;
#86707=FACE_OUTER_BOUND ( 'NONE', #31142, .T. ) ;
#86749=DIRECTION ( 'NONE',  ( -1.836970198721029934E-16, 1.000000000000000000, 0.000000000000000000 ) ) ;
#86755=DIRECTION ( 'NONE',  ( -0.000000000000000000, -1.000000000000000000, 6.308085367188393199E-16 ) ) ;
#86760=DIRECTION ( 'NONE',  ( -1.000000000000000000, -0.000000000000000000, 0.000000000000000000 ) ) ;
#86767=EDGE_LOOP ( 'NONE', ( #144970, #172197, #240699, #1909 ) ) ;
#86781=AXIS2_PLACEMENT_3D ( 'NONE', #51376, #189648, #249630 ) ;
#86784=VECTOR ( 'NONE', #92483, 1000.000000000000000 ) ;
#86795=FACE_OUTER_BOUND ( 'NONE', #194797, .T. ) ;
#86799=DIRECTION ( 'NONE',  ( 0.000000000000000000, 1.000000000000000000, 0.000000000000000000 ) ) ;
#86813=EDGE_LOOP ( 'NONE', ( #146921, #105022, #181129, #90215 ) ) ;
#86857=DIRECTION ( 'NONE',  ( 1.000000000000000000, 0.000000000000000000, 0.000000000000000000 ) ) ;
#86871=DIRECTION ( 'NONE',  ( 1.000000000000000000, -7.304098846218133681E-16, 0.000000000000000000 ) ) ;
#86881=CIRCLE ( 'NONE', #70376, 4.150000000000001243 ) ;
#86909=CARTESIAN_POINT ( 'NONE',  ( -21.05000000000000071, 1.250000000011155299, -108.5000000000000426 ) ) ;
#86916=CARTESIAN_POINT ( 'NONE',  ( 20.94999999999999574, 1.835341550235567887, -112.0551512925630249 ) ) ;
#86934=ORIENTED_EDGE ( 'NONE', *, *, #92875, .T. ) ;
#86983=EDGE_CURVE ( 'NONE', #87387, #193635, #143169, .T. ) ;
#86999=VECTOR ( 'NONE', #83621, 1000.000000000000000 ) ;
#87003=LINE ( 'NONE', #64895, #216700 ) ;
#87018=CIRCLE ( 'NONE', #24530, 11.64999999999999325 ) ;
#87028=ORIENTED_EDGE ( 'NONE', *, *, #241275, .F. ) ;
#87090=CARTESIAN_POINT ( 'NONE',  ( 18.59999999999999787, -1.263275465206102233, -141.9018646667464338 ) ) ;
#87100=CIRCLE ( 'NONE', #16398, 0.09999999999999939493 ) ;
#87103=ADVANCED_FACE ( 'NONE', ( #214426 ), #155693, .F. ) ;
#87119=ORIENTED_EDGE ( 'NONE', *, *, #239870, .T. ) ;
#87148=AXIS2_PLACEMENT_3D ( 'NONE', #64356, #128180, #104716 ) ;
#87206=AXIS2_PLACEMENT_3D ( 'NONE', #62497, #239852, #221531 ) ;
#87213=ADVANCED_FACE ( 'NONE', ( #193598 ), #14970, .T. ) ;
#87249=TOROIDAL_SURFACE ( 'NONE', #49847, 0.4000000000000012990, 0.1000000000000000056 ) ;
#87252=DIRECTION ( 'NONE',  ( -1.000000000000000000, 0.000000000000000000, 0.000000000000000000 ) ) ;
#87254=EDGE_CURVE ( 'NONE', #95552, #190717, #81311, .T. ) ;
#87257=ORIENTED_EDGE ( 'NONE', *, *, #196047, .F. ) ;
#87263=EDGE_LOOP ( 'NONE', ( #28167, #104527, #244080, #148897 ) ) ;
#87278=EDGE_CURVE ( 'NONE', #37616, #30650, #101836, .T. ) ;
#87348=ORIENTED_EDGE ( 'NONE', *, *, #128349, .T. ) ;
#87377=ORIENTED_EDGE ( 'NONE', *, *, #143768, .T. ) ;
#87378=ADVANCED_FACE ( 'NONE', ( #163458 ), #168555, .F. ) ;
#87387=VERTEX_POINT ( 'NONE', #207740 ) ;
#87413=EDGE_CURVE ( 'NONE', #165636, #5450, #242980, .T. ) ;
#87454=CIRCLE ( 'NONE', #95809, 0.1000000000000028644 ) ;
#87464=ORIENTED_EDGE ( 'NONE', *, *, #200912, .F. ) ;
#87468=VECTOR ( 'NONE', #53479, 1000.000000000000000 ) ;
#87472=CIRCLE ( 'NONE', #50067, 0.1000000000000028644 ) ;
#87522=ORIENTED_EDGE ( 'NONE', *, *, #194495, .F. ) ;
#87581=FACE_OUTER_BOUND ( 'NONE', #79094, .T. ) ;
#87602=EDGE_LOOP ( 'NONE', ( #233732, #148659, #116362, #139460, #188482, #225935, #199639, #149033, #29799, #174093, #123065, #95039, #191473, #157104, #114325, #130082, #33469, #159351 ) ) ;
#87608=DIRECTION ( 'NONE',  ( -1.000000000000000000, 0.000000000000000000, 0.000000000000000000 ) ) ;
#87644=ORIENTED_EDGE ( 'NONE', *, *, #230383, .F. ) ;
#87658=EDGE_LOOP ( 'NONE', ( #10740, #108781, #40130 ) ) ;
#87678=CYLINDRICAL_SURFACE ( 'NONE', #94033, 0.1000000000000028644 ) ;
#87689=DIRECTION ( 'NONE',  ( 0.000000000000000000, -0.000000000000000000, 1.000000000000000000 ) ) ;
#87732=ORIENTED_EDGE ( 'NONE', *, *, #70967, .F. ) ;
#87782=EDGE_LOOP ( 'NONE', ( #32832, #228140, #30054, #111504 ) ) ;
#87842=CARTESIAN_POINT ( 'NONE',  ( -22.39999999999999858, 11.65000000001115588, -100.6000000000000369 ) ) ;
#87849=ORIENTED_EDGE ( 'NONE', *, *, #238980, .F. ) ;
#87852=CARTESIAN_POINT ( 'NONE',  ( 21.05000000000000071, 6.650000000011155876, -110.3438220896831581 ) ) ;
#87882=EDGE_CURVE ( 'NONE', #109044, #12223, #99072, .T. ) ;
#87883=ORIENTED_EDGE ( 'NONE', *, *, #192106, .F. ) ;
#87909=DIRECTION ( 'NONE',  ( 1.000000000000000000, 0.000000000000000000, -0.000000000000000000 ) ) ;
#87913=AXIS2_PLACEMENT_3D ( 'NONE', #26680, #125744, #7084 ) ;
#87915=AXIS2_PLACEMENT_3D ( 'NONE', #94843, #206642, #48844 ) ;
#87928=ORIENTED_EDGE ( 'NONE', *, *, #207935, .F. ) ;
#87935=ORIENTED_EDGE ( 'NONE', *, *, #196211, .T. ) ;
#87948=DIRECTION ( 'NONE',  ( -0.000000000000000000, -0.000000000000000000, -1.000000000000000000 ) ) ;
#87957=ORIENTED_EDGE ( 'NONE', *, *, #45902, .F. ) ;
#87965=ORIENTED_EDGE ( 'NONE', *, *, #100054, .T. ) ;
#87981=CIRCLE ( 'NONE', #104723, 12.87499999999999822 ) ;
#88004=AXIS2_PLACEMENT_3D ( 'NONE', #79184, #252690, #233173 ) ;
#88027=EDGE_CURVE ( 'NONE', #94061, #214758, #231453, .T. ) ;
#88030=LINE ( 'NONE', #250966, #116533 ) ;
#88037=DIRECTION ( 'NONE',  ( -1.000000000000000000, -0.000000000000000000, -0.000000000000000000 ) ) ;
#88045=VERTEX_POINT ( 'NONE', #226314 ) ;
#88055=AXIS2_PLACEMENT_3D ( 'NONE', #186866, #185561, #162170 ) ;
#88073=DIRECTION ( 'NONE',  ( 0.000000000000000000, -1.000000000000000000, -2.891205793294679805E-16 ) ) ;
#88079=ORIENTED_EDGE ( 'NONE', *, *, #154436, .T. ) ;
#88085=ORIENTED_EDGE ( 'NONE', *, *, #125863, .F. ) ;
#88095=CARTESIAN_POINT ( 'NONE',  ( 21.05000000000000071, -9.399999999988846611, -110.3939691226524786 ) ) ;
#88103=ORIENTED_EDGE ( 'NONE', *, *, #120714, .F. ) ;
#88130=DIRECTION ( 'NONE',  ( -1.000000000000000000, -2.952720810173289112E-16, 0.000000000000000000 ) ) ;
#88155=CARTESIAN_POINT ( 'NONE',  ( 18.59999999999999076, -1.851617760457748618, -145.6031897196037050 ) ) ;
#88158=AXIS2_PLACEMENT_3D ( 'NONE', #84357, #2291, #221335 ) ;
#88159=CARTESIAN_POINT ( 'NONE',  ( -20.00857864376270001, 9.150000000011157653, -112.8500000000000369 ) ) ;
#88164=CARTESIAN_POINT ( 'NONE',  ( -23.15000000000000213, -11.48912529306489994, -130.9000000000000341 ) ) ;
#88169=EDGE_CURVE ( 'NONE', #168409, #74676, #193639, .T. ) ;
#88170=CARTESIAN_POINT ( 'NONE',  ( -20.64999999999999858, -8.730841121484171907, -110.0980747189843640 ) ) ;
#88171=ORIENTED_EDGE ( 'NONE', *, *, #86576, .T. ) ;
#88206=EDGE_CURVE ( 'NONE', #12223, #173371, #235966, .T. ) ;
#88220=EDGE_CURVE ( 'NONE', #319, #208145, #175386, .T. ) ;
#88233=ADVANCED_FACE ( 'NONE', ( #174118 ), #131089, .F. ) ;
#88258=AXIS2_PLACEMENT_3D ( 'NONE', #244831, #204417, #225253 ) ;
#88271=CARTESIAN_POINT ( 'NONE',  ( 18.50000000000000000, -9.399999999988843058, -107.7972597596633193 ) ) ;
#88314=VERTEX_POINT ( 'NONE', #1830 ) ;
#88336=ORIENTED_EDGE ( 'NONE', *, *, #211550, .F. ) ;
#88337=DIRECTION ( 'NONE',  ( 1.000000000000000000, 0.000000000000000000, 0.000000000000000000 ) ) ;
#88380=CARTESIAN_POINT ( 'NONE',  ( 20.94999999999999929, 8.776282895303628706, -109.0586289951409924 ) ) ;
#88389=DIRECTION ( 'NONE',  ( 0.000000000000000000, 1.000000000000000000, -0.000000000000000000 ) ) ;
#88420=EDGE_CURVE ( 'NONE', #19526, #74676, #173681, .T. ) ;
#88453=ORIENTED_EDGE ( 'NONE', *, *, #160687, .T. ) ;
#88495=ORIENTED_EDGE ( 'NONE', *, *, #145357, .F. ) ;
#88532=CIRCLE ( 'NONE', #200808, 0.09999999999999939493 ) ;
#88537=AXIS2_PLACEMENT_3D ( 'NONE', #198058, #83217, #80658 ) ;
#88546=ADVANCED_FACE ( 'NONE', ( #253290 ), #134615, .F. ) ;
#88548=CIRCLE ( 'NONE', #138592, 0.09999999999998807065 ) ;
#88634=CARTESIAN_POINT ( 'NONE',  ( 23.15000000000000213, -8.999999999988842703, -124.1060308773475924 ) ) ;
#88641=ORIENTED_EDGE ( 'NONE', *, *, #206696, .F. ) ;
#88689=EDGE_CURVE ( 'NONE', #18989, #72387, #199773, .T. ) ;
#88690=FACE_OUTER_BOUND ( 'NONE', #143241, .T. ) ;
#88695=CARTESIAN_POINT ( 'NONE',  ( -22.49533356619864577, 11.65000000631534149, -100.4348774196772638 ) ) ;
#88700=CARTESIAN_POINT ( 'NONE',  ( 18.49999999999999645, 1.866714910068465239, -112.2526752462820525 ) ) ;
#88717=EDGE_LOOP ( 'NONE', ( #13428, #229931, #251410, #61116 ) ) ;
#88727=CARTESIAN_POINT ( 'NONE',  ( -20.85000000000000142, 1.115600667400684642E-11, -141.9000000000000341 ) ) ;
#88728=CARTESIAN_POINT ( 'NONE',  ( 20.94999999999999929, 10.29270135741298731, -139.4573618871519614 ) ) ;
#88734=EDGE_CURVE ( 'NONE', #109895, #84132, #115346, .T. ) ;
#88740=VECTOR ( 'NONE', #40527, 1000.000000000000000 ) ;
#88749=ORIENTED_EDGE ( 'NONE', *, *, #134778, .F. ) ;
#88775=FACE_OUTER_BOUND ( 'NONE', #151068, .T. ) ;
#88824=CARTESIAN_POINT ( 'NONE',  ( -21.44999999999999929, 7.250000000011155521, -112.8500000000000369 ) ) ;
#88827=FACE_OUTER_BOUND ( 'NONE', #66708, .T. ) ;
#88843=TOROIDAL_SURFACE ( 'NONE', #172118, 11.65000000000000036, 0.1000000000000000056 ) ;
#88851=EDGE_LOOP ( 'NONE', ( #31652, #59568, #12976, #227685 ) ) ;
#88854=DIRECTION ( 'NONE',  ( 0.000000000000000000, 1.000000000000000000, 0.000000000000000000 ) ) ;
#88878=FACE_OUTER_BOUND ( 'NONE', #103938, .T. ) ;
#88894=CIRCLE ( 'NONE', #234665, 0.1999999999999996503 ) ;
#88896=LINE ( 'NONE', #145022, #26337 ) ;
#88899=ORIENTED_EDGE ( 'NONE', *, *, #228999, .T. ) ;
#88903=CIRCLE ( 'NONE', #155415, 0.3999999999999975797 ) ;
#88948=CYLINDRICAL_SURFACE ( 'NONE', #257204, 0.5000000000000004441 ) ;
#88953=EDGE_LOOP ( 'NONE', ( #114255, #130269, #225090, #133829 ) ) ;
#88962=DIRECTION ( 'NONE',  ( 0.000000000000000000, 0.000000000000000000, -1.000000000000000000 ) ) ;
#88968=AXIS2_PLACEMENT_3D ( 'NONE', #155653, #197299, #137319 ) ;
#88969=ORIENTED_EDGE ( 'NONE', *, *, #131215, .T. ) ;
#89004=FACE_OUTER_BOUND ( 'NONE', #131892, .T. ) ;
#89010=DIRECTION ( 'NONE',  ( 0.7071067811865388020, -0.7071067811865561215, 0.000000000000000000 ) ) ;
#89016=CARTESIAN_POINT ( 'NONE',  ( -20.54999999999999716, 2.000000000011154189, -120.7753780772379315 ) ) ;
#89017=DIRECTION ( 'NONE',  ( 1.000000000000000000, 0.000000000000000000, 0.000000000000000000 ) ) ;
#89035=AXIS2_PLACEMENT_3D ( 'NONE', #96475, #236002, #57350 ) ;
#89036=CARTESIAN_POINT ( 'NONE',  ( -22.50000000000000000, 0.1000000000111554016, -100.5000000000000284 ) ) ;
#89050=ORIENTED_EDGE ( 'NONE', *, *, #46727, .F. ) ;
#89080=DIRECTION ( 'NONE',  ( 0.000000000000000000, 0.000000000000000000, 1.000000000000000000 ) ) ;
#89099=CIRCLE ( 'NONE', #68265, 6.258578643762710669 ) ;
#89103=CARTESIAN_POINT ( 'NONE',  ( 21.05000000000000071, 5.000000000011153745, -121.5947339810869465 ) ) ;
#89106=VECTOR ( 'NONE', #50155, 1000.000000000000000 ) ;
#89144=CARTESIAN_POINT ( 'NONE',  ( 23.14999999999999858, -2.099999999988846344, -134.0000000000000284 ) ) ;
#89148=EDGE_LOOP ( 'NONE', ( #118620, #103613, #140634, #203866 ) ) ;
#89153=DIRECTION ( 'NONE',  ( 1.000000000000000000, 7.304098846218134667E-16, 0.000000000000000000 ) ) ;
#89179=EDGE_LOOP ( 'NONE', ( #249663, #203783, #245090, #31756 ) ) ;
#89186=CARTESIAN_POINT ( 'NONE',  ( -20.64999999999999858, -9.499999999988846255, -124.1060308773475924 ) ) ;
#89193=ORIENTED_EDGE ( 'NONE', *, *, #201740, .T. ) ;
#89194=CARTESIAN_POINT ( 'NONE',  ( 20.04142135623730070, 11.75000000001115907, -125.1500000000000341 ) ) ;
#89223=LINE ( 'NONE', #47516, #85120 ) ;
#89264=ORIENTED_EDGE ( 'NONE', *, *, #239262, .T. ) ;
#89291=EDGE_CURVE ( 'NONE', #234652, #142813, #9975, .T. ) ;
#89294=CARTESIAN_POINT ( 'NONE',  ( -18.43707690579159930, -9.682403433465241349, -140.6568433774128266 ) ) ;
#89296=FACE_OUTER_BOUND ( 'NONE', #202506, .T. ) ;
#89300=AXIS2_PLACEMENT_3D ( 'NONE', #92841, #236208, #254460 ) ;
#89310=EDGE_LOOP ( 'NONE', ( #71489, #43315, #219266, #109218 ) ) ;
#89337=CARTESIAN_POINT ( 'NONE',  ( 20.94999999999999574, 1.736257131608553550, -112.0686523290175245 ) ) ;
#89375=CARTESIAN_POINT ( 'NONE',  ( -20.85000000000000142, -11.64999999998884483, -134.0000000000000284 ) ) ;
#89380=ORIENTED_EDGE ( 'NONE', *, *, #113272, .F. ) ;
#89420=ORIENTED_EDGE ( 'NONE', *, *, #166125, .T. ) ;
#89429=CARTESIAN_POINT ( 'NONE',  ( 21.05000000000000071, 11.65000000001115943, -100.6000000000000369 ) ) ;
#89438=DIRECTION ( 'NONE',  ( 0.000000000000000000, 0.000000000000000000, -1.000000000000000000 ) ) ;
#89448=CARTESIAN_POINT ( 'NONE',  ( 20.84999999999999432, -1.164121893230052995, -141.9148480855716343 ) ) ;
#89489=UNCERTAINTY_MEASURE_WITH_UNIT (LENGTH_MEASURE( 1.000000000000000082E-05 ), #53275, 'distance_accuracy_value', 'NONE');
#89494=DIRECTION ( 'NONE',  ( -1.000000000000000000, 0.000000000000000000, -0.000000000000000000 ) ) ;
#89496=ORIENTED_EDGE ( 'NONE', *, *, #188211, .T. ) ;
#89500=CARTESIAN_POINT ( 'NONE',  ( 20.95443524775735256, 8.878554263883966513, -109.0337222756001836 ) ) ;
#89567=ORIENTED_EDGE ( 'NONE', *, *, #171773, .T. ) ;
#89583=DIRECTION ( 'NONE',  ( 1.000000000000000000, 0.000000000000000000, 0.000000000000000000 ) ) ;
#89586=DIRECTION ( 'NONE',  ( 0.000000000000000000, 0.000000000000000000, -1.000000000000000000 ) ) ;
#89595=CARTESIAN_POINT ( 'NONE',  ( -21.05000000000000071, 1.835341550235567887, -112.0551512925630249 ) ) ;
#89598=CARTESIAN_POINT ( 'NONE',  ( 22.46250603428203618, 0.02114417614996233138, -88.85013690265994057 ) ) ;
#89605=ORIENTED_EDGE ( 'NONE', *, *, #161349, .T. ) ;
#89630=EDGE_CURVE ( 'NONE', #46680, #150422, #26943, .T. ) ;
#89646=DIRECTION ( 'NONE',  ( -1.000000000000000000, -0.000000000000000000, -0.000000000000000000 ) ) ;
#89656=ORIENTED_EDGE ( 'NONE', *, *, #231633, .F. ) ;
#89678=ORIENTED_EDGE ( 'NONE', *, *, #181020, .F. ) ;
#89690=ADVANCED_FACE ( 'NONE', ( #237655 ), #39421, .T. ) ;
#89705=DIRECTION ( 'NONE',  ( 1.000000000000000000, -0.000000000000000000, 0.000000000000000000 ) ) ;
#89721=EDGE_CURVE ( 'NONE', #148820, #110439, #185138, .T. ) ;
#89775=ORIENTED_EDGE ( 'NONE', *, *, #238215, .T. ) ;
#89864=DIRECTION ( 'NONE',  ( 0.000000000000000000, 1.000000000000000000, -6.308085367188393199E-16 ) ) ;
#89900=ORIENTED_EDGE ( 'NONE', *, *, #169046, .F. ) ;
#89918=ORIENTED_EDGE ( 'NONE', *, *, #38795, .F. ) ;
#89928=CIRCLE ( 'NONE', #164944, 0.09999999999999982514 ) ;
#89939=EDGE_LOOP ( 'NONE', ( #137729, #154297, #140017, #93819 ) ) ;
#89943=DIRECTION ( 'NONE',  ( 1.000000000000000000, 0.000000000000000000, -0.000000000000000000 ) ) ;
#89953=CARTESIAN_POINT ( 'NONE',  ( 21.05000000000000071, -11.48912529306489994, -130.9000000000000341 ) ) ;
#89954=CARTESIAN_POINT ( 'NONE',  ( -20.64999999999999858, 2.400000000011155432, -120.7753780772379315 ) ) ;
#89968=CARTESIAN_POINT ( 'NONE',  ( -21.05000000000000071, 6.258316057343176197, -100.4342983896779344 ) ) ;
#89974=DIRECTION ( 'NONE',  ( -1.000000000000000000, -0.000000000000000000, 0.000000000000000000 ) ) ;
#89986=VERTEX_POINT ( 'NONE', #230949 ) ;
#89994=EDGE_LOOP ( 'NONE', ( #76197, #199857, #178080, #191702 ) ) ;
#89996=CARTESIAN_POINT ( 'NONE',  ( -22.59999999999999787, 11.74956712350054566, -100.3991416309013260 ) ) ;
#89999=CARTESIAN_POINT ( 'NONE',  ( -22.49917693094574389, 0.08522996423282762357, -88.85020421546937541 ) ) ;
#90000=EDGE_CURVE ( 'NONE', #213681, #185072, #10369, .T. ) ;
#90007=EDGE_LOOP ( 'NONE', ( #108939, #214679, #179115, #112909 ) ) ;
#90024=CARTESIAN_POINT ( 'NONE',  ( 20.84999999999998721, 10.33248238083634440, -139.5948465439131780 ) ) ;
#90041=CARTESIAN_POINT ( 'NONE',  ( 21.05000000000000071, 1.115600667400684642E-11, -138.1000000000000227 ) ) ;
#90074=AXIS2_PLACEMENT_3D ( 'NONE', #16338, #73748, #254862 ) ;
#90107=CYLINDRICAL_SURFACE ( 'NONE', #144789, 11.75000000000001066 ) ;
#90110=DIRECTION ( 'NONE',  ( 1.000000000000000000, 0.000000000000000000, 0.000000000000000000 ) ) ;
#90126=DIRECTION ( 'NONE',  ( -1.000000000000000000, -2.952720810173289112E-16, 0.000000000000000000 ) ) ;
#90200=ORIENTED_EDGE ( 'NONE', *, *, #201423, .T. ) ;
#90215=ORIENTED_EDGE ( 'NONE', *, *, #1497, .T. ) ;
#90224=EDGE_CURVE ( 'NONE', #208604, #220305, #100819, .T. ) ;
#90248=VERTEX_POINT ( 'NONE', #142080 ) ;
#90254=LINE ( 'NONE', #207673, #76237 ) ;
#90280=AXIS2_PLACEMENT_3D ( 'NONE', #127681, #108115, #187670 ) ;
#90291=EDGE_CURVE ( 'NONE', #153129, #26109, #44288, .T. ) ;
#90320=LINE ( 'NONE', #149047, #197786 ) ;
#90321=CARTESIAN_POINT ( 'NONE',  ( -20.54999999999999716, -11.74999999998884448, -121.6500000000000341 ) ) ;
#90352=CARTESIAN_POINT ( 'NONE',  ( 20.94999999999999574, -11.48912529306490349, -103.4000000000000341 ) ) ;
#90386=CIRCLE ( 'NONE', #48878, 0.1000000000000028644 ) ;
#90394=DIRECTION ( 'NONE',  ( 1.000000000000000000, 0.000000000000000000, 0.000000000000000000 ) ) ;
#90433=PLANE ( 'NONE',  #151408 ) ;
#90464=ADVANCED_FACE ( 'NONE', ( #187660 ), #118378, .T. ) ;
#90501=CARTESIAN_POINT ( 'NONE',  ( -20.54999999999999716, -9.399999999988846611, -124.1060308773475924 ) ) ;
#90503=DIRECTION ( 'NONE',  ( 0.000000000000000000, 1.000000000000000000, 0.000000000000000000 ) ) ;
#90515=AXIS2_PLACEMENT_3D ( 'NONE', #24638, #44183, #100265 ) ;
#90516=AXIS2_PLACEMENT_3D ( 'NONE', #140354, #219904, #221173 ) ;
#90527=DIRECTION ( 'NONE',  ( 1.000000000000000000, 1.836970198721029934E-16, -0.000000000000000000 ) ) ;
#90545=VERTEX_POINT ( 'NONE', #152392 ) ;
#90561=CIRCLE ( 'NONE', #123910, 0.09999999999999939493 ) ;
#90580=CARTESIAN_POINT ( 'NONE',  ( 18.49505832270840955, -9.438028062771739002, -107.6984731748938771 ) ) ;
#90595=CYLINDRICAL_SURFACE ( 'NONE', #107924, 0.1000000000000098310 ) ;
#90605=DIRECTION ( 'NONE',  ( 1.000000000000000000, -0.000000000000000000, -0.000000000000000000 ) ) ;
#90610=EDGE_CURVE ( 'NONE', #49667, #179995, #4807, .T. ) ;
#90616=CARTESIAN_POINT ( 'NONE',  ( 20.97250901189795513, 10.62456803371303593, -108.1645457169670266 ) ) ;
#90620=CIRCLE ( 'NONE', #190615, 11.74999999999999645 ) ;
#90624=AXIS2_PLACEMENT_3D ( 'NONE', #234139, #111634, #72527 ) ;
#90633=CARTESIAN_POINT ( 'NONE',  ( -23.15000000000000213, 2.600000000011156054, -113.7246219227621395 ) ) ;
#90643=CIRCLE ( 'NONE', #232339, 7.791421356237338003 ) ;
#90722=DIRECTION ( 'NONE',  ( 1.000000000000000000, 0.000000000000000000, 0.000000000000000000 ) ) ;
#90735=DIRECTION ( 'NONE',  ( 0.000000000000000000, -0.9908441862701596881, -0.1350103645451901924 ) ) ;
#90743=AXIS2_PLACEMENT_3D ( 'NONE', #46426, #28195, #187252 ) ;
#90745=ORIENTED_EDGE ( 'NONE', *, *, #147994, .T. ) ;
#90775=CARTESIAN_POINT ( 'NONE',  ( -21.55000000000000426, 7.708578643773852157, -121.6500000000000341 ) ) ;
#90793=FACE_OUTER_BOUND ( 'NONE', #228456, .T. ) ;
#90798=DIRECTION ( 'NONE',  ( 0.000000000000000000, 0.000000000000000000, 1.000000000000000000 ) ) ;
#90810=CARTESIAN_POINT ( 'NONE',  ( -23.15000000000000213, 4.350000000011156054, -112.8500000000000369 ) ) ;
#90817=CARTESIAN_POINT ( 'NONE',  ( 21.05000000000000071, 8.872080675389215187, -109.0210474188294114 ) ) ;
#90860=EDGE_CURVE ( 'NONE', #185160, #162338, #32128, .T. ) ;
#90884=CIRCLE ( 'NONE', #170059, 0.1000000000000002692 ) ;
#90891=CIRCLE ( 'NONE', #116051, 11.64999999999999325 ) ;
#90892=DIRECTION ( 'NONE',  ( 0.000000000000000000, -1.000000000000000000, 6.308085367188393199E-16 ) ) ;
#90910=VERTEX_POINT ( 'NONE', #80177 ) ;
#90942=DIRECTION ( 'NONE',  ( 0.000000000000000000, 0.000000000000000000, -1.000000000000000000 ) ) ;
#90970=DIRECTION ( 'NONE',  ( 1.000000000000000000, 3.265361837132813093E-16, -0.000000000000000000 ) ) ;
#90993=DIRECTION ( 'NONE',  ( -0.000000000000000000, 1.000000000000000000, 0.000000000000000000 ) ) ;
#91002=ORIENTED_EDGE ( 'NONE', *, *, #177946, .T. ) ;
#91004=FACE_OUTER_BOUND ( 'NONE', #119525, .T. ) ;
#91011=DIRECTION ( 'NONE',  ( -1.000000000000000000, 0.000000000000000000, 0.000000000000000000 ) ) ;
#91082=ADVANCED_FACE ( 'NONE', ( #4518 ), #10963, .F. ) ;
#91105=CARTESIAN_POINT ( 'NONE',  ( 21.05000000000000071, -8.999999999988844479, -110.3939691226524786 ) ) ;
#91119=LINE ( 'NONE', #247626, #47443 ) ;
#91122=DIRECTION ( 'NONE',  ( 1.224646799147353207E-16, 1.000000000000000000, 0.000000000000000000 ) ) ;
#91157=DIRECTION ( 'NONE',  ( 0.000000000000000000, -0.5907332058517320572, 0.8068669527896995541 ) ) ;
#91165=ADVANCED_FACE ( 'NONE', ( #185743, #147912 ), #67079, .F. ) ;
#91219=CIRCLE ( 'NONE', #149494, 0.09999999999998898659 ) ;
#91232=CARTESIAN_POINT ( 'NONE',  ( 18.59999999999999076, 6.650000000011155876, -121.6500000000000341 ) ) ;
#91273=CARTESIAN_POINT ( 'NONE',  ( -21.14999999999999858, 6.540656951712397138, -100.5000000000000284 ) ) ;
#91287=AXIS2_PLACEMENT_3D ( 'NONE', #215319, #231059, #133220 ) ;
#91331=CARTESIAN_POINT ( 'NONE',  ( 20.90851465518105812, 10.32532329027886320, -139.5699343018359855 ) ) ;
#91342=CARTESIAN_POINT ( 'NONE',  ( -21.29999999999995808, 1.115650265596050101E-11, -96.45000000000003126 ) ) ;
#91358=ORIENTED_EDGE ( 'NONE', *, *, #151039, .T. ) ;
#91370=CARTESIAN_POINT ( 'NONE',  ( 23.24999999999999289, 5.950000000011163692, -123.6942976949652149 ) ) ;
#91435=EDGE_CURVE ( 'NONE', #75064, #148589, #118867, .T. ) ;
#91442=EDGE_LOOP ( 'NONE', ( #108862, #101505, #44419, #252996 ) ) ;
#91445=AXIS2_PLACEMENT_3D ( 'NONE', #88159, #225112, #247252 ) ;
#91456=DIRECTION ( 'NONE',  ( 0.000000000000000000, -0.8700118002898321601, 0.4930308989875230030 ) ) ;
#91467=EDGE_LOOP ( 'NONE', ( #24138, #77385, #5532, #118181 ) ) ;
#91482=DIRECTION ( 'NONE',  ( 0.000000000000000000, 1.000000000000000000, 0.000000000000000000 ) ) ;
#91520=EDGE_LOOP ( 'NONE', ( #193417, #208605, #28951, #206323 ) ) ;
#91528=FACE_OUTER_BOUND ( 'NONE', #68013, .T. ) ;
#91533=B_SPLINE_CURVE_WITH_KNOTS ( 'NONE', 3,
 ( #116457, #176442, #60308, #139844, #180278, #255899, #156887 ),
 .UNSPECIFIED., .F., .F.,
 ( 4, 3, 4 ),
 ( 0.000000000000000000, 0.0007844235214594269838, 0.001767853679404345069 ),
 .UNSPECIFIED. ) ;
#91543=ORIENTED_EDGE ( 'NONE', *, *, #209895, .F. ) ;
#91592=CARTESIAN_POINT ( 'NONE',  ( -23.25000000000000000, 10.33248238083634440, -139.5948465439131780 ) ) ;
#91596=ORIENTED_EDGE ( 'NONE', *, *, #79182, .T. ) ;
#91620=CARTESIAN_POINT ( 'NONE',  ( -18.59999999999999787, -1.835859311432481045, -145.5044391687985694 ) ) ;
#91622=DIRECTION ( 'NONE',  ( 4.239556034732056743E-17, -0.1298341882520022972, -0.9915357197604853789 ) ) ;
#91666=DIRECTION ( 'NONE',  ( 1.000000000000000000, -7.304098846218133681E-16, -2.111765289898285610E-31 ) ) ;
#91670=CARTESIAN_POINT ( 'NONE',  ( -21.05000000000000071, 1.835341550235567887, -112.0551512925630249 ) ) ;
#91697=PLANE ( 'NONE',  #121901 ) ;
#91748=LINE ( 'NONE', #189574, #6847 ) ;
#91751=ORIENTED_EDGE ( 'NONE', *, *, #14430, .T. ) ;
#91761=CIRCLE ( 'NONE', #145910, 0.1000000000000096922 ) ;
#91773=DIRECTION ( 'NONE',  ( 1.000000000000000000, 0.000000000000000000, -0.000000000000000000 ) ) ;
#91818=LINE ( 'NONE', #12306, #132042 ) ;
#91875=CARTESIAN_POINT ( 'NONE',  ( 18.44364597020195262, -9.490487317151105273, -107.5579778896838974 ) ) ;
#91951=LINE ( 'NONE', #129793, #4362 ) ;
#91963=VERTEX_POINT ( 'NONE', #72573 ) ;
#91976=CIRCLE ( 'NONE', #16995, 0.1000000000000010186 ) ;
#92014=CARTESIAN_POINT ( 'NONE',  ( 21.14999999999999503, 1.115600667400684642E-11, -100.5000000000000284 ) ) ;
#92016=CIRCLE ( 'NONE', #237771, 0.1000000000000028644 ) ;
#92051=CARTESIAN_POINT ( 'NONE',  ( -22.50000000000000000, 1.115600667400684642E-11, -88.85042919245522341 ) ) ;
#92062=DIRECTION ( 'NONE',  ( 0.000000000000000000, 0.9999631594459056361, -0.008583690987128059571 ) ) ;
#92103=EDGE_CURVE ( 'NONE', #76616, #8107, #156662, .T. ) ;
#92113=ORIENTED_EDGE ( 'NONE', *, *, #29611, .T. ) ;
#92117=CARTESIAN_POINT ( 'NONE',  ( -20.94999999999999929, -11.48912529306490349, -103.6000000000000369 ) ) ;
#92133=CYLINDRICAL_SURFACE ( 'NONE', #82591, 0.1000000000000028644 ) ;
#92151=EDGE_CURVE ( 'NONE', #221229, #256826, #20300, .T. ) ;
#92189=VERTEX_POINT ( 'NONE', #206621 ) ;
#92208=EDGE_LOOP ( 'NONE', ( #239490, #198725, #174218, #244110, #79681, #203323, #103142, #130398, #75267, #120888, #60380, #6197 ) ) ;
#92209=DIRECTION ( 'NONE',  ( 1.000000000000000000, 0.000000000000000000, 0.000000000000000000 ) ) ;
#92213=AXIS2_PLACEMENT_3D ( 'NONE', #8449, #145374, #164945 ) ;
#92215=EDGE_CURVE ( 'NONE', #24871, #62504, #127085, .T. ) ;
#92275=SPHERICAL_SURFACE ( 'NONE', #11493, 0.1000000000000000056 ) ;
#92289=ORIENTED_EDGE ( 'NONE', *, *, #168579, .F. ) ;
#92308=EDGE_CURVE ( 'NONE', #208145, #226146, #219148, .T. ) ;
#92316=DIRECTION ( 'NONE',  ( 1.000000000000000000, -0.000000000000000000, -0.000000000000000000 ) ) ;
#92337=CARTESIAN_POINT ( 'NONE',  ( 20.95512820512820440, 10.62384868372303259, -112.6500000000000341 ) ) ;
#92341=CARTESIAN_POINT ( 'NONE',  ( 23.15000000000000213, -11.48912529306489816, -130.9000000000000341 ) ) ;
#92403=CARTESIAN_POINT ( 'NONE',  ( -23.25000000000000000, 4.350000000011156054, -112.6500000000000483 ) ) ;
#92404=ORIENTED_EDGE ( 'NONE', *, *, #230383, .T. ) ;
#92417=CARTESIAN_POINT ( 'NONE',  ( -18.59999999999999787, 1.835341550235567887, -112.0551512925630249 ) ) ;
#92418=DIRECTION ( 'NONE',  ( 0.000000000000000000, 0.000000000000000000, 1.000000000000000000 ) ) ;
#92435=ORIENTED_EDGE ( 'NONE', *, *, #197179, .F. ) ;
#92439=ORIENTED_EDGE ( 'NONE', *, *, #239413, .T. ) ;
#92451=DIRECTION ( 'NONE',  ( 9.044546369203339308E-15, -0.7397360091702694929, -0.6728971962616898672 ) ) ;
#92452=DIRECTION ( 'NONE',  ( 0.000000000000000000, 0.8660254037844411501, 0.4999999999999956701 ) ) ;
#92463=DIRECTION ( 'NONE',  ( 0.000000000000000000, -0.000000000000000000, 1.000000000000000000 ) ) ;
#92483=DIRECTION ( 'NONE',  ( -0.000000000000000000, -0.000000000000000000, -1.000000000000000000 ) ) ;
#92494=CARTESIAN_POINT ( 'NONE',  ( 20.94999999999999574, 1.835341550235567887, -112.1551512925630192 ) ) ;
#92506=ORIENTED_EDGE ( 'NONE', *, *, #255543, .F. ) ;
#92537=CARTESIAN_POINT ( 'NONE',  ( 18.39999999999999858, -9.499999999988844479, -140.9221498493304239 ) ) ;
#92574=CARTESIAN_POINT ( 'NONE',  ( 22.50497660315937054, -0.07871793021434785043, -88.75020449510458320 ) ) ;
#92609=CARTESIAN_POINT ( 'NONE',  ( 21.05000000000000071, 1.115600667400684642E-11, -100.5000000000000284 ) ) ;
#92615=EDGE_CURVE ( 'NONE', #72387, #61667, #19449, .T. ) ;
#92624=ORIENTED_EDGE ( 'NONE', *, *, #107684, .F. ) ;
#92681=DIRECTION ( 'NONE',  ( 0.000000000000000000, 0.000000000000000000, 1.000000000000000000 ) ) ;
#92687=DIRECTION ( 'NONE',  ( -1.000000000000000000, -0.000000000000000000, -0.000000000000000000 ) ) ;
#92713=DIRECTION ( 'NONE',  ( 1.000000000000000000, -0.000000000000000000, -0.000000000000000000 ) ) ;
#92742=ORIENTED_EDGE ( 'NONE', *, *, #216837, .T. ) ;
#92777=CARTESIAN_POINT ( 'NONE',  ( 21.05000000000000071, 1.115600667400684642E-11, -100.5000000000000284 ) ) ;
#92785=VERTEX_POINT ( 'NONE', #117274 ) ;
#92820=AXIS2_PLACEMENT_3D ( 'NONE', #34559, #154527, #119225 ) ;
#92841=CARTESIAN_POINT ( 'NONE',  ( -20.94999999999999929, 1.115600667400684642E-11, -134.0000000000000284 ) ) ;
#92856=CIRCLE ( 'NONE', #201194, 0.3999999999999975797 ) ;
#92860=EDGE_CURVE ( 'NONE', #165636, #224344, #152931, .T. ) ;
#92875=EDGE_CURVE ( 'NONE', #121457, #143803, #52926, .T. ) ;
#92879=EDGE_CURVE ( 'NONE', #74786, #78774, #69525, .T. ) ;
#92883=VERTEX_POINT ( 'NONE', #144511 ) ;
#92899=FACE_OUTER_BOUND ( 'NONE', #205357, .T. ) ;
#92914=EDGE_CURVE ( 'NONE', #31301, #173746, #123695, .T. ) ;
#92929=AXIS2_PLACEMENT_3D ( 'NONE', #245489, #48554, #188075 ) ;
#92966=CARTESIAN_POINT ( 'NONE',  ( -21.65000000000000213, 7.708578643773852157, -121.6500000000000341 ) ) ;
#92984=PLANE ( 'NONE',  #38425 ) ;
#92991=AXIS2_PLACEMENT_3D ( 'NONE', #138370, #220515, #221755 ) ;
#92999=DIRECTION ( 'NONE',  ( 0.000000000000000000, 0.000000000000000000, 1.000000000000000000 ) ) ;
#93011=EDGE_LOOP ( 'NONE', ( #238371, #134220, #108056, #38164 ) ) ;
#93013=DIRECTION ( 'NONE',  ( 7.304098846218134667E-16, -1.000000000000000000, 0.000000000000000000 ) ) ;
#93016=PLANE ( 'NONE',  #84459 ) ;
#93025=VECTOR ( 'NONE', #230737, 1000.000000000000000 ) ;
#93036=ORIENTED_EDGE ( 'NONE', *, *, #169192, .T. ) ;
#93045=ORIENTED_EDGE ( 'NONE', *, *, #105249, .T. ) ;
#93064=EDGE_LOOP ( 'NONE', ( #12605, #107184, #152121, #60493 ) ) ;
#93082=EDGE_LOOP ( 'NONE', ( #224657, #26165, #247006 ) ) ;
#93107=CARTESIAN_POINT ( 'NONE',  ( 20.94999999999999929, -11.29603075032412995, -103.5478991596638991 ) ) ;
#93129=DIRECTION ( 'NONE',  ( 0.000000000000000000, 0.000000000000000000, -1.000000000000000000 ) ) ;
#93130=CIRCLE ( 'NONE', #109696, 11.80000000000000426 ) ;
#93140=EDGE_CURVE ( 'NONE', #182294, #256518, #190324, .T. ) ;
#93148=EDGE_CURVE ( 'NONE', #161835, #197578, #211153, .T. ) ;
#93163=DIRECTION ( 'NONE',  ( 0.000000000000000000, 0.000000000000000000, -1.000000000000000000 ) ) ;
#93193=CARTESIAN_POINT ( 'NONE',  ( 21.14999999999999858, 11.65000000001115943, -100.6000000000000369 ) ) ;
#93214=AXIS2_PLACEMENT_3D ( 'NONE', #233862, #77336, #216851 ) ;
#93220=DIRECTION ( 'NONE',  ( 0.000000000000000000, 0.000000000000000000, 1.000000000000000000 ) ) ;
#93260=EDGE_CURVE ( 'NONE', #163802, #54193, #11445, .T. ) ;
#93267=CARTESIAN_POINT ( 'NONE',  ( 21.05000000000000426, 0.06570161033324353750, -94.24168394266798998 ) ) ;
#93278=EDGE_CURVE ( 'NONE', #88045, #26647, #115468, .T. ) ;
#93282=CARTESIAN_POINT ( 'NONE',  ( -20.64999999999999858, 2.000000000011154189, -120.7753780772379315 ) ) ;
#93283=CIRCLE ( 'NONE', #247219, 0.09999999999999939493 ) ;
#93285=AXIS2_PLACEMENT_3D ( 'NONE', #157571, #21872, #137941 ) ;
#93294=EDGE_CURVE ( 'NONE', #248313, #243146, #236898, .T. ) ;
#93306=ORIENTED_EDGE ( 'NONE', *, *, #115668, .F. ) ;
#93329=DIRECTION ( 'NONE',  ( 0.000000000000000000, -1.000000000000000000, 0.000000000000000000 ) ) ;
#93335=AXIS2_PLACEMENT_3D ( 'NONE', #217143, #58071, #136316 ) ;
#93357=VERTEX_POINT ( 'NONE', #245896 ) ;
#93369=FACE_OUTER_BOUND ( 'NONE', #69672, .T. ) ;
#93373=ORIENTED_EDGE ( 'NONE', *, *, #75201, .F. ) ;
#93425=DIRECTION ( 'NONE',  ( 1.000000000000000000, -0.000000000000000000, -0.000000000000000000 ) ) ;
#93446=FACE_OUTER_BOUND ( 'NONE', #186397, .T. ) ;
#93465=ORIENTED_EDGE ( 'NONE', *, *, #132373, .F. ) ;
#93467=EDGE_CURVE ( 'NONE', #239014, #63872, #182071, .T. ) ;
#93470=AXIS2_PLACEMENT_3D ( 'NONE', #46066, #166052, #124336 ) ;
#93490=EDGE_CURVE ( 'NONE', #248313, #43405, #215432, .T. ) ;
#93501=EDGE_LOOP ( 'NONE', ( #212336, #231076, #192294, #54613 ) ) ;
#93515=ORIENTED_EDGE ( 'NONE', *, *, #216977, .T. ) ;
#93521=DIRECTION ( 'NONE',  ( -0.7070776581709311559, 0.000000000000000000, 0.7071359030027479786 ) ) ;
#93554=AXIS2_PLACEMENT_3D ( 'NONE', #80023, #95753, #39682 ) ;
#93556=CARTESIAN_POINT ( 'NONE',  ( -21.65000000000000213, 7.708578643773852157, -112.7500000000000284 ) ) ;
#93558=ORIENTED_EDGE ( 'NONE', *, *, #218623, .T. ) ;
#93562=DIRECTION ( 'NONE',  ( -0.000000000000000000, -0.000000000000000000, 1.000000000000000000 ) ) ;
#93614=DIRECTION ( 'NONE',  ( 0.000000000000000000, 0.000000000000000000, -1.000000000000000000 ) ) ;
#93633=EDGE_CURVE ( 'NONE', #253865, #137271, #207442, .T. ) ;
#93637=DIRECTION ( 'NONE',  ( 0.000000000000000000, 2.664535259100315349E-15, 1.000000000000000000 ) ) ;
#93699=ORIENTED_EDGE ( 'NONE', *, *, #81319, .T. ) ;
#93712=DIRECTION ( 'NONE',  ( 0.000000000000000000, 0.000000000000000000, -1.000000000000000000 ) ) ;
#93731=EDGE_CURVE ( 'NONE', #43405, #7066, #119980, .T. ) ;
#93765=CARTESIAN_POINT ( 'NONE',  ( 21.07888907270776002, 10.72506921352637654, -112.7211935868332375 ) ) ;
#93768=EDGE_CURVE ( 'NONE', #185160, #33839, #15924, .T. ) ;
#93802=CARTESIAN_POINT ( 'NONE',  ( 20.94999999999999929, -11.39257802169451317, -130.9260504201681101 ) ) ;
#93810=CIRCLE ( 'NONE', #218695, 0.09999999999999864553 ) ;
#93819=ORIENTED_EDGE ( 'NONE', *, *, #90860, .F. ) ;
#93851=EDGE_LOOP ( 'NONE', ( #23173, #91358, #118953, #55254 ) ) ;
#93864=DIRECTION ( 'NONE',  ( -1.000000000000000000, 0.000000000000000000, 0.000000000000000000 ) ) ;
#93887=EDGE_CURVE ( 'NONE', #62504, #29706, #32499, .T. ) ;
#93909=CARTESIAN_POINT ( 'NONE',  ( 20.94999999999999574, 1.851028230152016674, -112.1539132694225316 ) ) ;
#93956=ORIENTED_EDGE ( 'NONE', *, *, #40616, .F. ) ;
#93973=CYLINDRICAL_SURFACE ( 'NONE', #114183, 0.09999999999999939493 ) ;
#94026=EDGE_CURVE ( 'NONE', #186401, #240710, #237580, .T. ) ;
#94033=AXIS2_PLACEMENT_3D ( 'NONE', #22609, #104653, #45995 ) ;
#94034=CARTESIAN_POINT ( 'NONE',  ( 18.49999999999998934, 10.25000000001115552, -125.1500000000000341 ) ) ;
#94040=DIRECTION ( 'NONE',  ( 0.000000000000000000, 0.000000000000000000, -1.000000000000000000 ) ) ;
#94041=ORIENTED_EDGE ( 'NONE', *, *, #153169, .T. ) ;
#94044=ORIENTED_EDGE ( 'NONE', *, *, #37868, .F. ) ;
#94054=ORIENTED_EDGE ( 'NONE', *, *, #22074, .F. ) ;
#94061=VERTEX_POINT ( 'NONE', #221829 ) ;
#94062=EDGE_LOOP ( 'NONE', ( #87257, #116175, #39298, #109397 ) ) ;
#94071=AXIS2_PLACEMENT_3D ( 'NONE', #142771, #63247, #22876 ) ;
#94082=ORIENTED_EDGE ( 'NONE', *, *, #34362, .F. ) ;
#94095=EDGE_CURVE ( 'NONE', #124703, #219174, #103350, .T. ) ;
#94100=DIRECTION ( 'NONE',  ( 0.000000000000000000, 4.440892098500631684E-15, -1.000000000000000000 ) ) ;
#94128=FACE_BOUND ( 'NONE', #121378, .T. ) ;
#94141=EDGE_LOOP ( 'NONE', ( #165232, #71144, #244504 ) ) ;
#94190=ORIENTED_EDGE ( 'NONE', *, *, #2633, .F. ) ;
#94204=ORIENTED_EDGE ( 'NONE', *, *, #77880, .F. ) ;
#94235=CIRCLE ( 'NONE', #223791, 0.09999999999999939493 ) ;
#94238=EDGE_CURVE ( 'NONE', #31259, #51418, #122628, .T. ) ;
#94241=DIRECTION ( 'NONE',  ( -1.836970198721029934E-16, 1.000000000000000000, 0.000000000000000000 ) ) ;
#94249=DIRECTION ( 'NONE',  ( -1.000000000000000000, -2.952720810173289112E-16, 0.000000000000000000 ) ) ;
#94262=AXIS2_PLACEMENT_3D ( 'NONE', #162932, #183760, #42968 ) ;
#94291=LINE ( 'NONE', #190870, #137440 ) ;
#94320=CARTESIAN_POINT ( 'NONE',  ( 18.60000000000000497, 1.115600667400684642E-11, -100.5000000000000284 ) ) ;
#94329=CARTESIAN_POINT ( 'NONE',  ( -23.15000000000000213, -8.999999999988844479, -124.1060308773475924 ) ) ;
#94352=CIRCLE ( 'NONE', #106829, 0.09999999999999939493 ) ;
#94364=ORIENTED_EDGE ( 'NONE', *, *, #109479, .T. ) ;
#94381=CIRCLE ( 'NONE', #90280, 0.2000000000000057288 ) ;
#94385=ORIENTED_EDGE ( 'NONE', *, *, #208756, .T. ) ;
#94431=VECTOR ( 'NONE', #209208, 1000.000000000000000 ) ;
#94440=EDGE_CURVE ( 'NONE', #140362, #61948, #195160, .T. ) ;
#94450=CYLINDRICAL_SURFACE ( 'NONE', #210935, 0.1000000000000028644 ) ;
#94494=CARTESIAN_POINT ( 'NONE',  ( 18.59999999999997655, 11.75000000001115552, -134.0000000000000284 ) ) ;
#94512=EDGE_LOOP ( 'NONE', ( #39185, #28891, #155075, #215590 ) ) ;
#94547=TOROIDAL_SURFACE ( 'NONE', #15474, 2.100000000000002309, 0.1000000000000000056 ) ;
#94548=EDGE_CURVE ( 'NONE', #190980, #124703, #253612, .T. ) ;
#94569=DIRECTION ( 'NONE',  ( 1.000000000000000000, -0.000000000000000000, 0.000000000000000000 ) ) ;
#94587=CARTESIAN_POINT ( 'NONE',  ( -21.05000000000000071, 6.540656951712399803, -100.5000000000000142 ) ) ;
#94595=DIRECTION ( 'NONE',  ( 0.000000000000000000, -1.000000000000000000, 0.000000000000000000 ) ) ;
#94675=VECTOR ( 'NONE', #68036, 1000.000000000000000 ) ;
#94688=ADVANCED_FACE ( 'NONE', ( #159677 ), #39751, .T. ) ;
#94690=ORIENTED_EDGE ( 'NONE', *, *, #228510, .F. ) ;
#94693=DIRECTION ( 'NONE',  ( 0.000000000000000000, 0.000000000000000000, -1.000000000000000000 ) ) ;
#94696=DIRECTION ( 'NONE',  ( -1.000000000000000000, 0.000000000000000000, 0.000000000000000000 ) ) ;
#94776=FACE_OUTER_BOUND ( 'NONE', #93851, .T. ) ;
#94786=AXIS2_PLACEMENT_3D ( 'NONE', #31340, #249084, #109536 ) ;
#94795=ORIENTED_EDGE ( 'NONE', *, *, #81319, .F. ) ;
#94812=ORIENTED_EDGE ( 'NONE', *, *, #202823, .F. ) ;
#94822=DIRECTION ( 'NONE',  ( -2.827886303505249259E-16, 0.8660254037844412611, 0.4999999999999956701 ) ) ;
#94843=CARTESIAN_POINT ( 'NONE',  ( -18.59999999999999787, 1.115600667400684642E-11, -134.0000000000000284 ) ) ;
#94850=AXIS2_PLACEMENT_3D ( 'NONE', #201680, #206820, #145549 ) ;
#94902=CARTESIAN_POINT ( 'NONE',  ( 20.95566103547454517, 10.61824765095822087, -108.1318401929806186 ) ) ;
#94911=CYLINDRICAL_SURFACE ( 'NONE', #8063, 0.09999999999999939493 ) ;
#94942=DIRECTION ( 'NONE',  ( 0.000000000000000000, -0.000000000000000000, 1.000000000000000000 ) ) ;
#94950=SURFACE_STYLE_USAGE ( .BOTH. , #171978 ) ;
#94960=CARTESIAN_POINT ( 'NONE',  ( -18.59999999999999787, -9.399999999988787991, -107.7972597596633193 ) ) ;
#94976=ORIENTED_EDGE ( 'NONE', *, *, #200971, .T. ) ;
#94980=DIRECTION ( 'NONE',  ( 0.000000000000000000, 0.000000000000000000, -1.000000000000000000 ) ) ;
#94985=VERTEX_POINT ( 'NONE', #154284 ) ;
#95021=DIRECTION ( 'NONE',  ( -3.265361837132813093E-16, 1.000000000000000000, 0.000000000000000000 ) ) ;
#95022=ADVANCED_FACE ( 'NONE', ( #130810 ), #30448, .F. ) ;
#95030=ORIENTED_EDGE ( 'NONE', *, *, #22922, .F. ) ;
#95038=EDGE_CURVE ( 'NONE', #70123, #208162, #153281, .T. ) ;
#95039=ORIENTED_EDGE ( 'NONE', *, *, #189400, .F. ) ;
#95040=ORIENTED_EDGE ( 'NONE', *, *, #38117, .T. ) ;
#95046=EDGE_CURVE ( 'NONE', #250368, #198727, #195946, .T. ) ;
#95049=EDGE_LOOP ( 'NONE', ( #244137, #199588, #51304, #196452 ) ) ;
#95050=AXIS2_PLACEMENT_3D ( 'NONE', #89103, #226016, #207804 ) ;
#95053=CARTESIAN_POINT ( 'NONE',  ( 21.05563370358598263, 10.72423035585766549, -112.6830908159630980 ) ) ;
#95068=CARTESIAN_POINT ( 'NONE',  ( 21.46681500593265213, 6.857511159395767386, -100.5000000000000426 ) ) ;
#95090=ADVANCED_FACE ( 'NONE', ( #120280 ), #190880, .F. ) ;
#95104=ORIENTED_EDGE ( 'NONE', *, *, #212973, .T. ) ;
#95115=CARTESIAN_POINT ( 'NONE',  ( -23.15000000000000213, 11.75000000001115552, -112.6500000000000341 ) ) ;
#95119=CARTESIAN_POINT ( 'NONE',  ( 18.44206774312976904, -9.491027357528897923, -140.6262275046982779 ) ) ;
#95137=CARTESIAN_POINT ( 'NONE',  ( -18.59999999999999787, -9.480686695267820596, -140.9411151687578752 ) ) ;
#95138=CARTESIAN_POINT ( 'NONE',  ( -18.49499033040907037, -9.438148771733516185, -107.6981532259234484 ) ) ;
#95142=CARTESIAN_POINT ( 'NONE',  ( -22.48660254037843487, 11.65000000001115588, -100.4500000000000597 ) ) ;
#95144=DIRECTION ( 'NONE',  ( 0.000000000000000000, 0.000000000000000000, -1.000000000000000000 ) ) ;
#95247=CARTESIAN_POINT ( 'NONE',  ( 20.85000000000000142, 1.115600667400684642E-11, -134.0000000000000284 ) ) ;
#95280=CARTESIAN_POINT ( 'NONE',  ( 21.13461538461539035, 8.885417037985600786, -112.7500000000000142 ) ) ;
#95287=ORIENTED_EDGE ( 'NONE', *, *, #173587, .F. ) ;
#95313=CARTESIAN_POINT ( 'NONE',  ( -20.54999999999999716, 2.000000000011154189, -120.7753780772379315 ) ) ;
#95316=VERTEX_POINT ( 'NONE', #150097 ) ;
#95335=AXIS2_PLACEMENT_3D ( 'NONE', #122492, #181188, #185017 ) ;
#95355=CARTESIAN_POINT ( 'NONE',  ( 18.54116936837188589, -9.463564198361288149, -107.5485424908882948 ) ) ;
#95375=ORIENTED_EDGE ( 'NONE', *, *, #190809, .T. ) ;
#95376=EDGE_CURVE ( 'NONE', #27558, #150130, #31447, .T. ) ;
#95379=ORIENTED_EDGE ( 'NONE', *, *, #216170, .F. ) ;
#95402=ORIENTED_EDGE ( 'NONE', *, *, #84486, .F. ) ;
#95424=CARTESIAN_POINT ( 'NONE',  ( -23.15000000000000213, -9.599999999988844124, -88.75000000000004263 ) ) ;
#95430=VECTOR ( 'NONE', #180614, 1000.000000000000000 ) ;
#95431=CARTESIAN_POINT ( 'NONE',  ( -23.15000000000000213, 4.350000000011156054, -121.7500000000000426 ) ) ;
#95457=CARTESIAN_POINT ( 'NONE',  ( 23.14999999999999503, 11.65000000001116298, -126.9851942293460922 ) ) ;
#95468=DIRECTION ( 'NONE',  ( -1.000000000000000000, -0.000000000000000000, 0.000000000000000000 ) ) ;
#95473=ORIENTED_EDGE ( 'NONE', *, *, #135493, .T. ) ;
#95502=CARTESIAN_POINT ( 'NONE',  ( 20.94999999999999929, 1.115650877919449575E-11, -129.9000000000000341 ) ) ;
#95510=ORIENTED_EDGE ( 'NONE', *, *, #43528, .F. ) ;
#95516=ORIENTED_EDGE ( 'NONE', *, *, #161459, .F. ) ;
#95534=FACE_OUTER_BOUND ( 'NONE', #106637, .T. ) ;
#95539=ORIENTED_EDGE ( 'NONE', *, *, #80907, .F. ) ;
#95544=DIRECTION ( 'NONE',  ( -0.000000000000000000, 0.7397360091702694929, 0.6728971962616898672 ) ) ;
#95552=VERTEX_POINT ( 'NONE', #114800 ) ;
#95589=DIRECTION ( 'NONE',  ( -0.000000000000000000, -0.000000000000000000, 1.000000000000000000 ) ) ;
#95591=AXIS2_PLACEMENT_3D ( 'NONE', #229505, #234629, #190391 ) ;
#95603=EDGE_CURVE ( 'NONE', #238064, #222495, #61850, .T. ) ;
#95613=CARTESIAN_POINT ( 'NONE',  ( -23.25000000000000000, 1.910280373842930812, -121.3686321448010972 ) ) ;
#95646=EDGE_LOOP ( 'NONE', ( #81696, #21699, #246152, #79672 ) ) ;
#95666=AXIS2_PLACEMENT_3D ( 'NONE', #217456, #137922, #135359 ) ;
#95681=VERTEX_POINT ( 'NONE', #123790 ) ;
#95733=CARTESIAN_POINT ( 'NONE',  ( 20.94999999999999929, 1.115600667400684642E-11, -134.0000000000000284 ) ) ;
#95753=DIRECTION ( 'NONE',  ( -1.000000000000000000, 7.304098846218133681E-16, -4.217023435051677994E-16 ) ) ;
#95803=ORIENTED_EDGE ( 'NONE', *, *, #126515, .T. ) ;
#95809=AXIS2_PLACEMENT_3D ( 'NONE', #173234, #170672, #110640 ) ;
#95850=CYLINDRICAL_SURFACE ( 'NONE', #42530, 0.09999999999999939493 ) ;
#95852=ADVANCED_FACE ( 'NONE', ( #128928 ), #70448, .T. ) ;
#95853=DIRECTION ( 'NONE',  ( -1.000000000000000000, 0.000000000000000000, 0.000000000000000000 ) ) ;
#95864=DIRECTION ( 'NONE',  ( 0.000000000000000000, 1.000000000000000000, 0.000000000000000000 ) ) ;
#95874=DIRECTION ( 'NONE',  ( 1.000000000000000000, 2.952720810173289112E-16, -0.000000000000000000 ) ) ;
#95892=ADVANCED_FACE ( 'NONE', ( #196581 ), #94911, .T. ) ;
#95926=DIRECTION ( 'NONE',  ( 1.000000000000000000, 0.000000000000000000, 0.000000000000000000 ) ) ;
#95969=DIRECTION ( 'NONE',  ( 1.000000000000000000, 0.000000000000000000, 0.000000000000000000 ) ) ;
#96035=AXIS2_PLACEMENT_3D ( 'NONE', #37042, #179127, #237784 ) ;
#96045=LINE ( 'NONE', #111785, #124995 ) ;
#96056=ORIENTED_EDGE ( 'NONE', *, *, #15655, .T. ) ;
#96075=DIRECTION ( 'NONE',  ( 1.000000000000000000, -0.000000000000000000, 0.000000000000000000 ) ) ;
#96082=AXIS2_PLACEMENT_3D ( 'NONE', #178226, #40007, #179505 ) ;
#96088=DIRECTION ( 'NONE',  ( 0.000000000000000000, -0.9908441862701596881, 0.1350103645451899148 ) ) ;
#96125=ADVANCED_FACE ( 'NONE', ( #107751 ), #166475, .F. ) ;
#96150=CARTESIAN_POINT ( 'NONE',  ( 19.97071067811864609, 11.72071067812981404, -125.2500000000000284 ) ) ;
#96177=CYLINDRICAL_SURFACE ( 'NONE', #243518, 0.09999999999999939493 ) ;
#96179=DIRECTION ( 'NONE',  ( -4.801466763864313332E-15, -0.2605042016806672911, -0.9654727137038716656 ) ) ;
#96206=CARTESIAN_POINT ( 'NONE',  ( -18.59999999999999787, 9.150000000011157653, -88.75000000000004263 ) ) ;
#96223=DIRECTION ( 'NONE',  ( 0.000000000000000000, -0.4930308989874653269, -0.8700118002898649117 ) ) ;
#96224=DIRECTION ( 'NONE',  ( 0.000000000000000000, 1.000000000000000000, 1.265107689135680095E-16 ) ) ;
#96254=AXIS2_PLACEMENT_3D ( 'NONE', #59509, #139041, #81635 ) ;
#96259=ORIENTED_EDGE ( 'NONE', *, *, #245510, .F. ) ;
#96301=AXIS2_PLACEMENT_3D ( 'NONE', #4731, #242072, #205512 ) ;
#96305=ORIENTED_EDGE ( 'NONE', *, *, #139293, .T. ) ;
#96344=VERTEX_POINT ( 'NONE', #95137 ) ;
#96373=AXIS2_PLACEMENT_3D ( 'NONE', #75043, #55405, #150263 ) ;
#96393=AXIS2_PLACEMENT_3D ( 'NONE', #199153, #20536, #189857 ) ;
#96408=ORIENTED_EDGE ( 'NONE', *, *, #35616, .F. ) ;
#96424=DIRECTION ( 'NONE',  ( 0.000000000000000000, 0.000000000000000000, 1.000000000000000000 ) ) ;
#96436=EDGE_CURVE ( 'NONE', #227912, #94985, #162190, .T. ) ;
#96442=EDGE_CURVE ( 'NONE', #109044, #212285, #248101, .T. ) ;
#96444=DIRECTION ( 'NONE',  ( 0.000000000000000000, 0.9908441862701596881, 0.1350103645451904977 ) ) ;
#96446=AXIS2_PLACEMENT_3D ( 'NONE', #89375, #205476, #125935 ) ;
#96455=EDGE_LOOP ( 'NONE', ( #179539, #46400, #198734, #85437 ) ) ;
#96459=VERTEX_POINT ( 'NONE', #255439 ) ;
#96475=CARTESIAN_POINT ( 'NONE',  ( -20.64999999999999858, -8.999999999988844479, -124.5060308773475839 ) ) ;
#96491=EDGE_LOOP ( 'NONE', ( #236663, #113674, #69834, #30266, #128411 ) ) ;
#96500=CARTESIAN_POINT ( 'NONE',  ( -21.05000000000000071, 0.09779029131994770863, -94.24218538952392521 ) ) ;
#96503=EDGE_CURVE ( 'NONE', #254324, #28381, #49917, .T. ) ;
#96556=EDGE_CURVE ( 'NONE', #183119, #40953, #238719, .T. ) ;
#96594=CARTESIAN_POINT ( 'NONE',  ( -20.54999999999999716, -8.999999999988844479, -124.1060308773475924 ) ) ;
#96603=LINE ( 'NONE', #116222, #44518 ) ;
#96634=VECTOR ( 'NONE', #158605, 1000.000000000000227 ) ;
#96639=ORIENTED_EDGE ( 'NONE', *, *, #60201, .F. ) ;
#96697=CIRCLE ( 'NONE', #179950, 0.1000000000000028644 ) ;
#96698=AXIS2_PLACEMENT_3D ( 'NONE', #51104, #227200, #30305 ) ;
#96712=EDGE_CURVE ( 'NONE', #164082, #253301, #245141, .T. ) ;
#96732=DIRECTION ( 'NONE',  ( 1.000000000000000000, 0.000000000000000000, 0.000000000000000000 ) ) ;
#96753=DIRECTION ( 'NONE',  ( 0.000000000000000000, 0.000000000000000000, -1.000000000000000000 ) ) ;
#96763=CIRCLE ( 'NONE', #17672, 0.1000000000000028644 ) ;
#96781=DIRECTION ( 'NONE',  ( -1.836970198721029934E-16, 1.000000000000000000, 0.000000000000000000 ) ) ;
#96791=DIRECTION ( 'NONE',  ( -0.000000000000000000, 1.000000000000000000, -0.000000000000000000 ) ) ;
#96800=ORIENTED_EDGE ( 'NONE', *, *, #67360, .F. ) ;
#96812=AXIS2_PLACEMENT_3D ( 'NONE', #230493, #90970, #170573 ) ;
#96875=ORIENTED_EDGE ( 'NONE', *, *, #164308, .T. ) ;
#96912=LINE ( 'NONE', #55223, #123678 ) ;
#96941=ORIENTED_EDGE ( 'NONE', *, *, #10692, .T. ) ;
#96949=ADVANCED_FACE ( 'NONE', ( #242245 ), #177186, .F. ) ;
#96992=EDGE_LOOP ( 'NONE', ( #194986, #129027, #162775, #199206 ) ) ;
#97006=VECTOR ( 'NONE', #128940, 1000.000000000000000 ) ;
#97017=EDGE_CURVE ( 'NONE', #19526, #135831, #87003, .T. ) ;
#97018=CARTESIAN_POINT ( 'NONE',  ( 21.04999999999999361, 0.01471785653522959120, -94.15527659591015208 ) ) ;
#97043=DIRECTION ( 'NONE',  ( 0.000000000000000000, 0.000000000000000000, -1.000000000000000000 ) ) ;
#97064=CARTESIAN_POINT ( 'NONE',  ( -23.25000000000000000, -11.64999999998884483, -131.0000000000000284 ) ) ;
#97101=AXIS2_PLACEMENT_3D ( 'NONE', #126148, #23247, #223967 ) ;
#97105=FACE_OUTER_BOUND ( 'NONE', #86020, .T. ) ;
#97113=DIRECTION ( 'NONE',  ( 0.000000000000000000, 0.000000000000000000, -1.000000000000000000 ) ) ;
#97163=ORIENTED_EDGE ( 'NONE', *, *, #193060, .T. ) ;
#97170=VERTEX_POINT ( 'NONE', #209553 ) ;
#97181=AXIS2_PLACEMENT_3D ( 'NONE', #34373, #67361, #113877 ) ;
#97229=CARTESIAN_POINT ( 'NONE',  ( 21.05000000000021743, 6.344359042054673381, -100.4851443651061942 ) ) ;
#97230=CIRCLE ( 'NONE', #255456, 0.09999999999999939493 ) ;
#97232=EDGE_LOOP ( 'NONE', ( #146059, #33932, #197314, #48298 ) ) ;
#97245=CIRCLE ( 'NONE', #151490, 0.1000000000000000472 ) ;
#97284=EDGE_LOOP ( 'NONE', ( #86934, #107995, #79410, #20449 ) ) ;
#97291=EDGE_LOOP ( 'NONE', ( #70762, #12854, #210408, #15862 ) ) ;
#97352=DIRECTION ( 'NONE',  ( 1.000000000000000000, 7.304098846218134667E-16, -0.000000000000000000 ) ) ;
#97376=ORIENTED_EDGE ( 'NONE', *, *, #49259, .F. ) ;
#97411=CARTESIAN_POINT ( 'NONE',  ( 20.94999999999999929, -11.64999999998883595, -131.1000000000000227 ) ) ;
#97413=ADVANCED_FACE ( 'NONE', ( #147674 ), #231083, .F. ) ;
#97418=CARTESIAN_POINT ( 'NONE',  ( 23.14999999999999147, 1.115600667400684642E-11, -100.5000000000000284 ) ) ;
#97431=EDGE_CURVE ( 'NONE', #63374, #101017, #250656, .T. ) ;
#97444=DIRECTION ( 'NONE',  ( 0.000000000000000000, 0.000000000000000000, -1.000000000000000000 ) ) ;
#97450=DIRECTION ( 'NONE',  ( -1.000000000000000000, -3.265361837132813093E-16, 0.000000000000000000 ) ) ;
#97465=ADVANCED_FACE ( 'NONE', ( #177543 ), #242466, .F. ) ;
#97475=AXIS2_PLACEMENT_3D ( 'NONE', #33223, #151874, #192271 ) ;
#97505=FACE_OUTER_BOUND ( 'NONE', #187029, .T. ) ;
#97508=DIRECTION ( 'NONE',  ( 0.000000000000000000, -1.000000000000000000, 0.000000000000000000 ) ) ;
#97540=DIRECTION ( 'NONE',  ( 1.000000000000000000, -7.304098846218134667E-16, 0.000000000000000000 ) ) ;
#97548=EDGE_LOOP ( 'NONE', ( #93373, #113524, #129088, #119186, #40844, #209100, #213318, #248592 ) ) ;
#97550=CIRCLE ( 'NONE', #51764, 0.1000000000000028644 ) ;
#97565=LINE ( 'NONE', #117169, #31138 ) ;
#97582=ORIENTED_EDGE ( 'NONE', *, *, #231860, .T. ) ;
#97643=CARTESIAN_POINT ( 'NONE',  ( 23.14999999999999858, 5.500000000011153745, -121.5947339810869465 ) ) ;
#97675=CARTESIAN_POINT ( 'NONE',  ( -18.41353343127310893, -9.499999999988851584, -107.5320693966996970 ) ) ;
#97718=FACE_OUTER_BOUND ( 'NONE', #42351, .T. ) ;
#97722=DIRECTION ( 'NONE',  ( -4.408576920032448588E-17, 0.1350103645451876944, 0.9908441862701601321 ) ) ;
#97724=PLANE ( 'NONE',  #115505 ) ;
#97725=CIRCLE ( 'NONE', #60329, 0.3999999999999975797 ) ;
#97747=AXIS2_PLACEMENT_3D ( 'NONE', #103868, #186000, #68628 ) ;
#97756=LINE ( 'NONE', #118660, #156862 ) ;
#97757=ADVANCED_FACE ( 'NONE', ( #170832 ), #46824, .T. ) ;
#97763=CARTESIAN_POINT ( 'NONE',  ( 21.05000000000000071, 4.813084112160680661, -112.4415177565238650 ) ) ;
#97764=ORIENTED_EDGE ( 'NONE', *, *, #137020, .F. ) ;
#97776=VERTEX_POINT ( 'NONE', #69130 ) ;
#97815=CARTESIAN_POINT ( 'NONE',  ( 21.08804582317318577, 8.878166167103049844, -112.8499998294053910 ) ) ;
#97831=DIRECTION ( 'NONE',  ( 0.000000000000000000, 0.000000000000000000, -1.000000000000000000 ) ) ;
#97855=LINE ( 'NONE', #177460, #88740 ) ;
#97873=LINE ( 'NONE', #120073, #199156 ) ;
#97893=CARTESIAN_POINT ( 'NONE',  ( -18.50000000000000000, 11.65000000001115232, -88.75000000000004263 ) ) ;
#97918=DIRECTION ( 'NONE',  ( 0.000000000000000000, -1.000000000000000000, -1.897661533703519897E-16 ) ) ;
#97941=VERTEX_POINT ( 'NONE', #251596 ) ;
#97947=B_SPLINE_CURVE_WITH_KNOTS ( 'NONE', 3,
 ( #49602, #10485, #89999, #169600, #215094, #252926, #74341, #153894, #133007, #216371, #117285, #177287, #195557, #152591, #114712, #32651 ),
 .UNSPECIFIED., .F., .F.,
 ( 4, 3, 3, 3, 3, 4 ),
 ( 0.000000000000000000, 2.209075297430721397E-05, 5.594258369009613512E-05, 8.979524372342007066E-05, 0.0001236472815274586030, 0.0001574990747609554737 ),
 .UNSPECIFIED. ) ;
#97953=LINE ( 'NONE', #211516, #141873 ) ;
#97956=DIRECTION ( 'NONE',  ( 0.000000000000000000, -0.000000000000000000, -1.000000000000000000 ) ) ;
#97978=VERTEX_POINT ( 'NONE', #114653 ) ;
#97980=CARTESIAN_POINT ( 'NONE',  ( -21.10320863425827298, 0.02502225123826237740, -94.09972261354079137 ) ) ;
#98005=SPHERICAL_SURFACE ( 'NONE', #205767, 0.1000000000000000056 ) ;
#98011=DIRECTION ( 'NONE',  ( 0.000000000000000000, 0.000000000000000000, -1.000000000000000000 ) ) ;
#98013=AXIS2_PLACEMENT_3D ( 'NONE', #238477, #100221, #58538 ) ;
#98053=CYLINDRICAL_SURFACE ( 'NONE', #166184, 0.09999999999999939493 ) ;
#98121=DIRECTION ( 'NONE',  ( 2.952720810173289112E-16, -1.000000000000000000, 0.000000000000000000 ) ) ;
#98125=ADVANCED_FACE ( 'NONE', ( #241029 ), #63654, .T. ) ;
#98160=ADVANCED_FACE ( 'NONE', ( #139326 ), #104043, .F. ) ;
#98178=VECTOR ( 'NONE', #19839, 1000.000000000000000 ) ;
#98217=ORIENTED_EDGE ( 'NONE', *, *, #107906, .T. ) ;
#98248=CARTESIAN_POINT ( 'NONE',  ( 22.50000000000000000, 1.115600667400684642E-11, -100.5000000000000284 ) ) ;
#98278=CIRCLE ( 'NONE', #256672, 0.09999999999998898659 ) ;
#98294=DIRECTION ( 'NONE',  ( 0.000000000000000000, 0.1350103645451876666, -0.9908441862701600211 ) ) ;
#98298=DIRECTION ( 'NONE',  ( -1.000000000000000000, -2.952720810173289112E-16, 0.000000000000000000 ) ) ;
#98308=ORIENTED_EDGE ( 'NONE', *, *, #80264, .T. ) ;
#98361=EDGE_CURVE ( 'NONE', #167562, #126637, #234274, .T. ) ;
#98362=FACE_OUTER_BOUND ( 'NONE', #178454, .T. ) ;
#98365=CARTESIAN_POINT ( 'NONE',  ( 19.75857864376268935, 11.65000000001115943, -125.3500000000000512 ) ) ;
#98381=CIRCLE ( 'NONE', #119100, 0.1000000000000028644 ) ;
#98421=CARTESIAN_POINT ( 'NONE',  ( 21.05000000000000071, 1.115600667400684642E-11, -136.0000000000000284 ) ) ;
#98429=ORIENTED_EDGE ( 'NONE', *, *, #182284, .T. ) ;
#98437=LINE ( 'NONE', #114196, #8346 ) ;
#98447=DIRECTION ( 'NONE',  ( 1.000000000000000000, 2.952720810173289112E-16, -0.000000000000000000 ) ) ;
#98508=CARTESIAN_POINT ( 'NONE',  ( 21.05000000000000071, 6.258847123090201414, -100.4682416469448469 ) ) ;
#98513=ORIENTED_EDGE ( 'NONE', *, *, #233844, .F. ) ;
#98516=DIRECTION ( 'NONE',  ( 3.469446951953635015E-14, -0.000000000000000000, 1.000000000000000000 ) ) ;
#98538=VERTEX_POINT ( 'NONE', #217264 ) ;
#98571=CARTESIAN_POINT ( 'NONE',  ( 23.15000000000000213, -11.64999999998883595, -131.0000000000000284 ) ) ;
#98577=ORIENTED_EDGE ( 'NONE', *, *, #189774, .F. ) ;
#98582=CARTESIAN_POINT ( 'NONE',  ( -20.85000000000000142, 7.021664781911246322, -137.8335654018973457 ) ) ;
#98589=AXIS2_PLACEMENT_3D ( 'NONE', #15996, #138450, #18538 ) ;
#98609=DIRECTION ( 'NONE',  ( 0.000000000000000000, -1.000000000000000000, 0.000000000000000000 ) ) ;
#98624=ORIENTED_EDGE ( 'NONE', *, *, #59349, .F. ) ;
#98627=DIRECTION ( 'NONE',  ( 0.000000000000000000, 0.4930308989875313852, 0.8700118002898274971 ) ) ;
#98696=DIRECTION ( 'NONE',  ( 0.000000000000000000, -0.000000000000000000, -1.000000000000000000 ) ) ;
#98705=DIRECTION ( 'NONE',  ( 0.000000000000000000, -1.000000000000000000, -2.891205793294679805E-16 ) ) ;
#98715=CARTESIAN_POINT ( 'NONE',  ( 20.94999999999999929, -1.164121893230052995, -141.9148480855716343 ) ) ;
#98724=DIRECTION ( 'NONE',  ( -1.000000000000000000, -0.000000000000000000, 0.000000000000000000 ) ) ;
#98751=ORIENTED_EDGE ( 'NONE', *, *, #106662, .T. ) ;
#98760=EDGE_CURVE ( 'NONE', #88314, #225371, #71553, .T. ) ;
#98782=FACE_OUTER_BOUND ( 'NONE', #34475, .T. ) ;
#98814=CARTESIAN_POINT ( 'NONE',  ( -21.05000000000000071, 1.115600667400684642E-11, -100.5000000000000284 ) ) ;
#98833=AXIS2_PLACEMENT_3D ( 'NONE', #74311, #155132, #237207 ) ;
#98859=DIRECTION ( 'NONE',  ( -7.304098846218201720E-16, 1.000000000000000000, 0.000000000000000000 ) ) ;
#98914=ADVANCED_FACE ( 'NONE', ( #107302 ), #171511, .T. ) ;
#98941=DIRECTION ( 'NONE',  ( 0.000000000000000000, 0.7397360091702777085, -0.6728971962616808744 ) ) ;
#98948=AXIS2_PLACEMENT_3D ( 'NONE', #134291, #252962, #96444 ) ;
#98949=EDGE_LOOP ( 'NONE', ( #98217, #73644, #118498, #100579 ) ) ;
#99003=CARTESIAN_POINT ( 'NONE',  ( 22.50000000000000000, 11.64957080755595520, -100.4000000000000483 ) ) ;
#99022=ORIENTED_EDGE ( 'NONE', *, *, #71450, .T. ) ;
#99035=ORIENTED_EDGE ( 'NONE', *, *, #124392, .F. ) ;
#99038=CARTESIAN_POINT ( 'NONE',  ( 23.14999999999998437, 1.115600667400684642E-11, -100.5000000000000284 ) ) ;
#99052=DIRECTION ( 'NONE',  ( -1.000000000000000000, 0.000000000000000000, 0.000000000000000000 ) ) ;
#99066=VECTOR ( 'NONE', #7610, 1000.000000000000000 ) ;
#99072=B_SPLINE_CURVE_WITH_KNOTS ( 'NONE', 3,
 ( #90024, #152612, #153918, #148742, #32679, #49625, #9214, #91331, #187875, #33966, #130443, #129171, #208722, #228277, #113450, #110884, #189138, #173486, #88728 ),
 .UNSPECIFIED., .F., .F.,
 ( 4, 3, 3, 3, 3, 3, 4 ),
 ( 1.387778780781445676E-17, 2.646747978908746686E-05, 5.271166642129237432E-05, 9.008788829885646201E-05, 0.0001426648776561085163, 0.0001897378458660004691, 0.0001917382627806451167 ),
 .UNSPECIFIED. ) ;
#99091=PLANE ( 'NONE',  #112014 ) ;
#99099=EDGE_CURVE ( 'NONE', #130606, #113797, #4853, .T. ) ;
#99115=ORIENTED_EDGE ( 'NONE', *, *, #121370, .T. ) ;
#99128=DIRECTION ( 'NONE',  ( 0.000000000000000000, 0.000000000000000000, -1.000000000000000000 ) ) ;
#99182=ORIENTED_EDGE ( 'NONE', *, *, #223541, .F. ) ;
#99289=DIRECTION ( 'NONE',  ( -0.7071067811865475727, -0.7071067811865475727, 0.000000000000000000 ) ) ;
#99311=EDGE_CURVE ( 'NONE', #106114, #123284, #209637, .T. ) ;
#99317=SPHERICAL_SURFACE ( 'NONE', #22309, 0.1000000000000000056 ) ;
#99335=ORIENTED_EDGE ( 'NONE', *, *, #158321, .T. ) ;
#99407=CARTESIAN_POINT ( 'NONE',  ( -23.15000000000000213, 11.75000000001115552, -126.9851942293460922 ) ) ;
#99417=DIRECTION ( 'NONE',  ( 0.000000000000000000, -0.000000000000000000, -1.000000000000000000 ) ) ;
#99479=CARTESIAN_POINT ( 'NONE',  ( -21.05000000000000071, 1.750000000011155743, -112.1695115579016857 ) ) ;
#99484=CARTESIAN_POINT ( 'NONE',  ( 22.39999999999999503, 11.75000000001116263, -100.4000000000000483 ) ) ;
#99491=EDGE_LOOP ( 'NONE', ( #58807, #203179, #216631, #101018 ) ) ;
#99494=ORIENTED_EDGE ( 'NONE', *, *, #14823, .T. ) ;
#99538=CARTESIAN_POINT ( 'NONE',  ( 23.14999999999999858, 1.115600667400684642E-11, -134.0000000000000284 ) ) ;
#99546=CARTESIAN_POINT ( 'NONE',  ( 21.07971444708685738, 6.329792081637704015, -100.4121765636821380 ) ) ;
#99556=CONICAL_SURFACE ( 'NONE', #203817, 7.750000000000020428, 0.7853981633974531640 ) ;
#99598=CARTESIAN_POINT ( 'NONE',  ( 21.05000000000046256, 0.05148288189289713934, -94.19982018208359875 ) ) ;
#99657=LINE ( 'NONE', #121835, #158751 ) ;
#99663=DIRECTION ( 'NONE',  ( 1.000000000000000000, 0.000000000000000000, 0.000000000000000000 ) ) ;
#99677=EDGE_CURVE ( 'NONE', #12292, #154382, #54568, .T. ) ;
#99679=CARTESIAN_POINT ( 'NONE',  ( -22.59999999999999787, 0.1008583691098682150, -88.75043287651064361 ) ) ;
#99684=DIRECTION ( 'NONE',  ( 0.000000000000000000, 0.000000000000000000, -1.000000000000000000 ) ) ;
#99691=DIRECTION ( 'NONE',  ( 1.000000000000000000, 0.000000000000000000, 0.000000000000000000 ) ) ;
#99765=DIRECTION ( 'NONE',  ( 0.000000000000000000, 0.000000000000000000, 1.000000000000000000 ) ) ;
#99792=CARTESIAN_POINT ( 'NONE',  ( -22.24259225415828567, 7.491937870576586889, -100.4009341165472051 ) ) ;
#99810=VERTEX_POINT ( 'NONE', #244589 ) ;
#99816=DIRECTION ( 'NONE',  ( -0.000000000000000000, 1.000000000000000000, 0.000000000000000000 ) ) ;
#99834=CARTESIAN_POINT ( 'NONE',  ( -18.59999999999999787, 14.05000000001115623, -106.0136950707610310 ) ) ;
#99876=TOROIDAL_SURFACE ( 'NONE', #216624, 11.70000000000000462, 0.1000000000000000056 ) ;
#99901=ORIENTED_EDGE ( 'NONE', *, *, #9622, .F. ) ;
#99906=DIRECTION ( 'NONE',  ( -0.000000000000000000, -1.000000000000000000, -0.000000000000000000 ) ) ;
#99918=AXIS2_PLACEMENT_3D ( 'NONE', #133115, #67044, #53574 ) ;
#99953=CARTESIAN_POINT ( 'NONE',  ( -21.05000000000000071, 11.65000000001115588, -126.9851942293460922 ) ) ;
#100007=FACE_OUTER_BOUND ( 'NONE', #124968, .T. ) ;
#100013=FACE_OUTER_BOUND ( 'NONE', #217429, .T. ) ;
#100017=ADVANCED_FACE ( 'NONE', ( #61809 ), #3090, .T. ) ;
#100043=VERTEX_POINT ( 'NONE', #21423 ) ;
#100054=EDGE_CURVE ( 'NONE', #15812, #31301, #241725, .T. ) ;
#100080=ORIENTED_EDGE ( 'NONE', *, *, #239870, .F. ) ;
#100093=EDGE_LOOP ( 'NONE', ( #43785, #69041, #51751, #164924 ) ) ;
#100118=DIRECTION ( 'NONE',  ( -1.000000000000000000, -0.000000000000000000, -0.000000000000000000 ) ) ;
#100149=ORIENTED_EDGE ( 'NONE', *, *, #85396, .F. ) ;
#100152=DIRECTION ( 'NONE',  ( 1.000000000000000000, 0.000000000000000000, 0.000000000000000000 ) ) ;
#100171=EDGE_CURVE ( 'NONE', #24921, #219174, #117311, .T. ) ;
#100175=CARTESIAN_POINT ( 'NONE',  ( 22.39999999999999858, 7.790779598384538041, -100.5000000000000426 ) ) ;
#100210=CARTESIAN_POINT ( 'NONE',  ( -23.25000000000000000, -11.64999999998884483, -130.9000000000000341 ) ) ;
#100221=DIRECTION ( 'NONE',  ( 1.000000000000000000, 0.000000000000000000, 0.000000000000000000 ) ) ;
#100265=DIRECTION ( 'NONE',  ( -1.000000000000000000, 0.000000000000000000, 0.000000000000000000 ) ) ;
#100288=VECTOR ( 'NONE', #60946, 1000.000000000000000 ) ;
#100295=DIRECTION ( 'NONE',  ( 1.000000000000000000, 0.000000000000000000, -0.000000000000000000 ) ) ;
#100301=DIRECTION ( 'NONE',  ( 0.000000000000000000, 1.000000000000000000, -6.308085367188393199E-16 ) ) ;
#100304=VERTEX_POINT ( 'NONE', #91370 ) ;
#100327=EDGE_CURVE ( 'NONE', #163036, #63872, #154931, .T. ) ;
#100360=ORIENTED_EDGE ( 'NONE', *, *, #34401, .T. ) ;
#100383=CARTESIAN_POINT ( 'NONE',  ( 18.50000000000000000, -9.499999999988842703, -140.6001893912220737 ) ) ;
#100394=CIRCLE ( 'NONE', #17239, 0.5000000000000004441 ) ;
#100397=EDGE_CURVE ( 'NONE', #208145, #255700, #171499, .T. ) ;
#100414=CARTESIAN_POINT ( 'NONE',  ( -22.39999999999999858, -0.1008583690875575894, -88.75043287651062940 ) ) ;
#100423=DIRECTION ( 'NONE',  ( 0.000000000000000000, 1.000000000000000000, 0.000000000000000000 ) ) ;
#100469=ORIENTED_EDGE ( 'NONE', *, *, #195233, .T. ) ;
#100488=CARTESIAN_POINT ( 'NONE',  ( 21.05000000000000071, -11.64999999998883595, -100.5000000000000284 ) ) ;
#100539=CARTESIAN_POINT ( 'NONE',  ( 20.94999999999999574, 1.250000000011155299, -108.5000000000000426 ) ) ;
#100579=ORIENTED_EDGE ( 'NONE', *, *, #37310, .F. ) ;
#100580=EDGE_CURVE ( 'NONE', #96459, #54193, #159063, .T. ) ;
#100594=EDGE_LOOP ( 'NONE', ( #740, #181913, #139053, #220532 ) ) ;
#100611=AXIS2_PLACEMENT_3D ( 'NONE', #10536, #48362, #127913 ) ;
#100622=CARTESIAN_POINT ( 'NONE',  ( 20.94999999999999929, 10.72371710471867701, -121.7500000000000426 ) ) ;
#100644=DIRECTION ( 'NONE',  ( 0.000000000000000000, 1.000000000000000000, 0.000000000000000000 ) ) ;
#100649=DIRECTION ( 'NONE',  ( -4.391705002472929091E-16, 1.000000000000000000, 0.000000000000000000 ) ) ;
#100654=AXIS2_PLACEMENT_3D ( 'NONE', #135000, #49403, #17639 ) ;
#100676=VERTEX_POINT ( 'NONE', #89429 ) ;
#100706=EDGE_CURVE ( 'NONE', #5450, #16939, #192495, .T. ) ;
#100753=EDGE_CURVE ( 'NONE', #228873, #142411, #63481, .T. ) ;
#100819=B_SPLINE_CURVE_WITH_KNOTS ( 'NONE', 3,
 ( #123822, #241209, #61273, #101643 ),
 .UNSPECIFIED., .F., .F.,
 ( 4, 4 ),
 ( 0.000000000000000000, 0.001767853679387133359 ),
 .UNSPECIFIED. ) ;
#100884=DIRECTION ( 'NONE',  ( 0.7070776581709139474, -0.7071359030027652981, -2.453168425935592377E-14 ) ) ;
#100895=ORIENTED_EDGE ( 'NONE', *, *, #257353, .T. ) ;
#100918=DIRECTION ( 'NONE',  ( -2.557131231893036985E-16, 0.8660254037844384856, -0.5000000000000002220 ) ) ;
#100955=CARTESIAN_POINT ( 'NONE',  ( 20.95462737510932882, 10.55678195165489441, -108.0699500565623339 ) ) ;
#100999=VERTEX_POINT ( 'NONE', #188241 ) ;
#101006=CARTESIAN_POINT ( 'NONE',  ( 21.05000000000000071, 11.60000000001116049, -127.0717967697245427 ) ) ;
#101013=ORIENTED_EDGE ( 'NONE', *, *, #230473, .F. ) ;
#101017=VERTEX_POINT ( 'NONE', #33071 ) ;
#101018=ORIENTED_EDGE ( 'NONE', *, *, #196211, .F. ) ;
#101037=VERTEX_POINT ( 'NONE', #153004 ) ;
#101067=ORIENTED_EDGE ( 'NONE', *, *, #74707, .F. ) ;
#101083=ORIENTED_EDGE ( 'NONE', *, *, #94548, .T. ) ;
#101117=CIRCLE ( 'NONE', #176216, 0.5000000000000004441 ) ;
#101157=CARTESIAN_POINT ( 'NONE',  ( 20.97438252431638972, 8.925423506087151182, -108.9723706890108446 ) ) ;
#101177=CARTESIAN_POINT ( 'NONE',  ( -22.39999999999999858, 7.790779598384559357, -100.5000000000000426 ) ) ;
#101203=CARTESIAN_POINT ( 'NONE',  ( 20.94999999999999929, -11.48912529306489994, -131.1000000000000227 ) ) ;
#101258=DIRECTION ( 'NONE',  ( 0.000000000000000000, 1.000000000000000000, 0.000000000000000000 ) ) ;
#101269=PLANE ( 'NONE',  #111223 ) ;
#101300=AXIS2_PLACEMENT_3D ( 'NONE', #107546, #207964, #244491 ) ;
#101302=CIRCLE ( 'NONE', #92991, 0.09999999999998898659 ) ;
#101310=DIRECTION ( 'NONE',  ( -0.000000000000000000, -0.000000000000000000, 1.000000000000000000 ) ) ;
#101323=CARTESIAN_POINT ( 'NONE',  ( 20.95159278453404283, 8.907896337960206523, -108.9847201851092819 ) ) ;
#101344=CIRCLE ( 'NONE', #213839, 0.1000000000000043493 ) ;
#101345=EDGE_CURVE ( 'NONE', #85652, #198608, #26300, .T. ) ;
#101348=LINE ( 'NONE', #45283, #198261 ) ;
#101356=CARTESIAN_POINT ( 'NONE',  ( 21.05000000000000071, 5.500000000011153745, -112.9052660189131245 ) ) ;
#101357=CARTESIAN_POINT ( 'NONE',  ( 18.49999999999999645, 1.115600667400684642E-11, -134.0000000000000284 ) ) ;
#101370=ORIENTED_EDGE ( 'NONE', *, *, #131970, .F. ) ;
#101373=DIRECTION ( 'NONE',  ( -1.000000000000000000, -0.000000000000000000, 0.000000000000000000 ) ) ;
#101385=CARTESIAN_POINT ( 'NONE',  ( -18.36527282682067863, -9.500000599987966865, -140.9221489645001668 ) ) ;
#101413=EDGE_CURVE ( 'NONE', #129536, #14749, #76313, .T. ) ;
#101487=EDGE_CURVE ( 'NONE', #110634, #2822, #116109, .T. ) ;
#101505=ORIENTED_EDGE ( 'NONE', *, *, #152095, .F. ) ;
#101529=CARTESIAN_POINT ( 'NONE',  ( 20.94999999999999929, 1.115600667400684642E-11, -138.1000000000000227 ) ) ;
#101532=AXIS2_PLACEMENT_3D ( 'NONE', #242004, #67219, #25543 ) ;
#101568=DIRECTION ( 'NONE',  ( -0.000000000000000000, 0.000000000000000000, -1.000000000000000000 ) ) ;
#101594=DIRECTION ( 'NONE',  ( 0.000000000000000000, 0.5000000000000144329, 0.8660254037844302699 ) ) ;
#101620=ADVANCED_FACE ( 'NONE', ( #53559 ), #201228, .T. ) ;
#101635=ORIENTED_EDGE ( 'NONE', *, *, #25419, .F. ) ;
#101643=CARTESIAN_POINT ( 'NONE',  ( -22.39999999999999858, 1.115600667400684642E-11, -92.70922040162662370 ) ) ;
#101649=DIRECTION ( 'NONE',  ( -2.827886303505248766E-16, 0.8660254037844411501, 0.4999999999999956146 ) ) ;
#101684=DIRECTION ( 'NONE',  ( 3.265361837132813093E-16, -1.000000000000000000, -0.000000000000000000 ) ) ;
#101732=DIRECTION ( 'NONE',  ( 1.000000000000000000, -0.000000000000000000, -0.000000000000000000 ) ) ;
#101736=AXIS2_PLACEMENT_3D ( 'NONE', #189540, #50014, #209089 ) ;
#101739=CARTESIAN_POINT ( 'NONE',  ( -20.00857864376270001, 9.350000000011156942, -112.8500000000000369 ) ) ;
#101741=DIRECTION ( 'NONE',  ( 0.000000000000000000, -0.1455152366551721865, -0.9893560106964475187 ) ) ;
#101750=FACE_OUTER_BOUND ( 'NONE', #222207, .T. ) ;
#101758=ORIENTED_EDGE ( 'NONE', *, *, #191577, .F. ) ;
#101770=ADVANCED_FACE ( 'NONE', ( #208492 ), #159732, .T. ) ;
#101780=ADVANCED_FACE ( 'NONE', ( #250169 ), #131495, .F. ) ;
#101787=ORIENTED_EDGE ( 'NONE', *, *, #10472, .T. ) ;
#101803=LINE ( 'NONE', #138367, #229386 ) ;
#101836=CIRCLE ( 'NONE', #176709, 0.2000000000000057288 ) ;
#101844=LINE ( 'NONE', #204806, #166411 ) ;
#101849=CARTESIAN_POINT ( 'NONE',  ( -21.05000000000000071, -0.08579911626291911175, -94.08602111851160998 ) ) ;
#101857=CYLINDRICAL_SURFACE ( 'NONE', #179189, 12.87499999999999822 ) ;
#101876=CIRCLE ( 'NONE', #247652, 11.64999999999999325 ) ;
#101881=DIRECTION ( 'NONE',  ( 1.000000000000000000, 0.000000000000000000, 0.000000000000000000 ) ) ;
#101905=DIRECTION ( 'NONE',  ( 0.000000000000000000, 0.9915357197604972583, -0.1298341882519109536 ) ) ;
#101914=CARTESIAN_POINT ( 'NONE',  ( -18.59999999999999787, 11.65000000001115232, -107.5148057706540357 ) ) ;
#101940=EDGE_CURVE ( 'NONE', #236931, #254860, #207202, .T. ) ;
#101984=CARTESIAN_POINT ( 'NONE',  ( -20.94999999999999929, 1.115600667400684642E-11, -100.5000000000000284 ) ) ;
#101987=LINE ( 'NONE', #142425, #71587 ) ;
#101989=DIRECTION ( 'NONE',  ( 0.000000000000000000, -0.4930308989874718772, -0.8700118002898612479 ) ) ;
#102052=CARTESIAN_POINT ( 'NONE',  ( -22.39999999999999858, 11.75000000001115552, -100.4000000000000483 ) ) ;
#102101=AXIS2_PLACEMENT_3D ( 'NONE', #234941, #253202, #232389 ) ;
#102109=CARTESIAN_POINT ( 'NONE',  ( -20.99749315643150638, 11.75000000001115197, -126.9851942312421045 ) ) ;
#102111=DIRECTION ( 'NONE',  ( -1.000000000000000000, -7.304098846218134667E-16, 4.217023435051678980E-16 ) ) ;
#102114=CARTESIAN_POINT ( 'NONE',  ( 21.08621493067296271, 6.349294291182824068, -100.4438051605239224 ) ) ;
#102151=CARTESIAN_POINT ( 'NONE',  ( -18.59999999999999787, 10.33248238083634440, -139.5948465439131780 ) ) ;
#102208=TOROIDAL_SURFACE ( 'NONE', #10504, 11.90000000000000213, 0.1000000000000000056 ) ;
#102213=CARTESIAN_POINT ( 'NONE',  ( 18.49999999999999289, 7.120270961708750512, -137.6595630418393625 ) ) ;
#102261=ORIENTED_EDGE ( 'NONE', *, *, #193584, .T. ) ;
#102264=DIRECTION ( 'NONE',  ( 0.000000000000000000, 0.000000000000000000, -1.000000000000000000 ) ) ;
#102275=CARTESIAN_POINT ( 'NONE',  ( 20.94999999999999929, 5.500000000011153745, -121.5947339810869465 ) ) ;
#102276=DIRECTION ( 'NONE',  ( 0.000000000000000000, 0.000000000000000000, -1.000000000000000000 ) ) ;
#102282=ORIENTED_EDGE ( 'NONE', *, *, #64909, .T. ) ;
#102360=VECTOR ( 'NONE', #56433, 1000.000000000000000 ) ;
#102365=CARTESIAN_POINT ( 'NONE',  ( -21.05000000000000071, -11.74999999998884448, -131.0000000000000284 ) ) ;
#102373=CARTESIAN_POINT ( 'NONE',  ( 21.05000000000000071, 6.257814610487288043, -100.4022097086912311 ) ) ;
#102396=CARTESIAN_POINT ( 'NONE',  ( -23.15000000000000213, 4.350000000011156054, -112.8500000000000369 ) ) ;
#102443=DIRECTION ( 'NONE',  ( 0.000000000000000000, 1.000000000000000000, 0.000000000000000000 ) ) ;
#102448=EDGE_CURVE ( 'NONE', #141039, #50377, #201770, .T. ) ;
#102457=CARTESIAN_POINT ( 'NONE',  ( 20.75572585718142093, 8.882316728412554596, -108.9972583987020442 ) ) ;
#102466=VERTEX_POINT ( 'NONE', #146267 ) ;
#102503=DIRECTION ( 'NONE',  ( -1.000000000000000000, -3.265361837132813093E-16, 0.000000000000000000 ) ) ;
#102539=ADVANCED_FACE ( 'NONE', ( #10628 ), #226719, .T. ) ;
#102559=DIRECTION ( 'NONE',  ( -1.000000000000000000, -0.000000000000000000, 0.000000000000000000 ) ) ;
#102560=FACE_OUTER_BOUND ( 'NONE', #195172, .T. ) ;
#102574=CARTESIAN_POINT ( 'NONE',  ( -18.50000000000000000, 9.350000000011156942, -121.8500000000000369 ) ) ;
#102584=AXIS2_PLACEMENT_3D ( 'NONE', #111752, #188712, #75214 ) ;
#102610=ORIENTED_EDGE ( 'NONE', *, *, #210505, .F. ) ;
#102643=VERTEX_POINT ( 'NONE', #73195 ) ;
#102645=CIRCLE ( 'NONE', #235955, 11.80000000000000426 ) ;
#102684=LINE ( 'NONE', #182264, #113481 ) ;
#102685=( BOUNDED_SURFACE ( )  B_SPLINE_SURFACE ( 3, 2, ( 
 ( #206691, #243232, #28083 ),
 ( #207995, #84112, #29380 ),
 ( #108870, #241956, #183278 ),
 ( #142831, #43763, #202831 ),
 ( #24220, #103707, #54031 ),
 ( #31931, #30645, #11057 ) ),
 .UNSPECIFIED., .F., .F., .F. ) 
 B_SPLINE_SURFACE_WITH_KNOTS ( ( 4, 2, 4 ),
 ( 3, 3 ),
 ( 6.719893378901017553E-05, 0.0002757154632485521472, 0.0004842319927080941189 ),
 ( 0.000000000000000000, 1.000000000000000000 ),
 .UNSPECIFIED. ) 
 GEOMETRIC_REPRESENTATION_ITEM ( )  RATIONAL_B_SPLINE_SURFACE ( (
 ( 1.000000000000000000, 0.7250110520819756932, 1.000000000000000000),
 ( 1.000000000000000000, 0.7277932058368639101, 1.000000000000000000),
 ( 1.000000000000000000, 0.7278452872604711521, 1.000000000000000000),
 ( 1.000000000000000000, 0.7221445671562100044, 1.000000000000000000),
 ( 1.000000000000000000, 0.7163662143769800039, 1.000000000000000000),
 ( 1.000000000000000000, 0.7071067811865475727, 1.000000000000000000) ) ) 
 REPRESENTATION_ITEM ( '' )  SURFACE ( )  );
#102689=ORIENTED_EDGE ( 'NONE', *, *, #193021, .F. ) ;
#102691=DIRECTION ( 'NONE',  ( 0.000000000000000000, 0.000000000000000000, 1.000000000000000000 ) ) ;
#102693=AXIS2_PLACEMENT_3D ( 'NONE', #132295, #228844, #34511 ) ;
#102709=CARTESIAN_POINT ( 'NONE',  ( -21.05000000000000071, 1.115600667400684642E-11, -100.5000000000000284 ) ) ;
#102721=LINE ( 'NONE', #165293, #1265 ) ;
#102757=LINE ( 'NONE', #1089, #11355 ) ;
#102774=VECTOR ( 'NONE', #155738, 1000.000000000000000 ) ;
#102837=DIRECTION ( 'NONE',  ( 0.000000000000000000, 0.000000000000000000, 1.000000000000000000 ) ) ;
#102840=CYLINDRICAL_SURFACE ( 'NONE', #20668, 0.09999999999998898659 ) ;
#102846=CIRCLE ( 'NONE', #161136, 0.9750000000000036415 ) ;
#102861=EDGE_CURVE ( 'NONE', #257618, #15694, #64582, .T. ) ;
#102869=CIRCLE ( 'NONE', #48721, 0.1000000000000028644 ) ;
#102876=DIRECTION ( 'NONE',  ( 1.000000000000000000, -0.000000000000000000, -0.000000000000000000 ) ) ;
#102884=DIRECTION ( 'NONE',  ( -1.000000000000000000, -0.000000000000000000, -0.000000000000000000 ) ) ;
#102899=AXIS2_PLACEMENT_3D ( 'NONE', #87842, #145257, #147857 ) ;
#102904=CARTESIAN_POINT ( 'NONE',  ( 20.94999999999999929, 1.115600667400684642E-11, -134.0000000000000284 ) ) ;
#102945=CARTESIAN_POINT ( 'NONE',  ( -21.55000000000000071, 7.350000000011155166, -121.6500000000000341 ) ) ;
#103006=VERTEX_POINT ( 'NONE', #92403 ) ;
#103017=DIRECTION ( 'NONE',  ( 0.000000000000000000, 0.9908441862701596881, -0.1350103645451904977 ) ) ;
#103031=AXIS2_PLACEMENT_3D ( 'NONE', #196510, #19162, #178271 ) ;
#103072=ORIENTED_EDGE ( 'NONE', *, *, #218763, .F. ) ;
#103073=ORIENTED_EDGE ( 'NONE', *, *, #212820, .T. ) ;
#103085=AXIS2_PLACEMENT_3D ( 'NONE', #14474, #70601, #90110 ) ;
#103091=AXIS2_PLACEMENT_3D ( 'NONE', #21835, #24424, #162633 ) ;
#103104=DIRECTION ( 'NONE',  ( 0.000000000000000000, 0.000000000000000000, 1.000000000000000000 ) ) ;
#103131=ORIENTED_EDGE ( 'NONE', *, *, #34362, .T. ) ;
#103142=ORIENTED_EDGE ( 'NONE', *, *, #177165, .T. ) ;
#103169=AXIS2_PLACEMENT_3D ( 'NONE', #137472, #100884, #80045 ) ;
#103175=VECTOR ( 'NONE', #234265, 1000.000000000000000 ) ;
#103185=EDGE_CURVE ( 'NONE', #207918, #13818, #252202, .T. ) ;
#103198=FACE_OUTER_BOUND ( 'NONE', #89939, .T. ) ;
#103212=CIRCLE ( 'NONE', #90743, 11.75000000000000000 ) ;
#103221=DIRECTION ( 'NONE',  ( 0.000000000000000000, 0.000000000000000000, -1.000000000000000000 ) ) ;
#103294=CARTESIAN_POINT ( 'NONE',  ( -23.25000000000000000, 1.115600667400684642E-11, -134.0000000000000284 ) ) ;
#103298=DIRECTION ( 'NONE',  ( -3.265361837132813093E-16, 1.000000000000000000, 0.000000000000000000 ) ) ;
#103317=ORIENTED_EDGE ( 'NONE', *, *, #16060, .T. ) ;
#103323=ORIENTED_EDGE ( 'NONE', *, *, #42807, .F. ) ;
#103348=CARTESIAN_POINT ( 'NONE',  ( 22.40000000000010516, 1.020945751984553285E-11, -88.85042919245492499 ) ) ;
#103350=CIRCLE ( 'NONE', #74376, 0.09999999999999939493 ) ;
#103355=AXIS2_PLACEMENT_3D ( 'NONE', #94329, #214295, #175215 ) ;
#103359=ORIENTED_EDGE ( 'NONE', *, *, #202456, .F. ) ;
#103377=EDGE_LOOP ( 'NONE', ( #27138, #58346, #129063, #136511 ) ) ;
#103381=ORIENTED_EDGE ( 'NONE', *, *, #68990, .T. ) ;
#103398=FACE_OUTER_BOUND ( 'NONE', #86108, .T. ) ;
#103477=CARTESIAN_POINT ( 'NONE',  ( 20.85000000000000142, -1.362429037182151470, -141.8888812479212334 ) ) ;
#103488=CARTESIAN_POINT ( 'NONE',  ( 21.00000000000000000, 9.750000000011153745, -112.7500000000000284 ) ) ;
#103518=AXIS2_PLACEMENT_3D ( 'NONE', #164399, #65287, #224357 ) ;
#103548=DIRECTION ( 'NONE',  ( 1.000000000000000000, 0.000000000000000000, 0.000000000000000000 ) ) ;
#103607=CARTESIAN_POINT ( 'NONE',  ( -18.58693740092133240, -9.406432150242029167, -107.6248164565011081 ) ) ;
#103610=CARTESIAN_POINT ( 'NONE',  ( -23.25000000000000000, -11.74999999998884448, -130.9000000000000341 ) ) ;
#103613=ORIENTED_EDGE ( 'NONE', *, *, #57050, .F. ) ;
#103633=DIRECTION ( 'NONE',  ( 1.000000000000000000, -0.000000000000000000, -0.000000000000000000 ) ) ;
#103656=CIRCLE ( 'NONE', #170369, 0.1000000000000028644 ) ;
#103689=AXIS2_PLACEMENT_3D ( 'NONE', #50642, #231893, #130186 ) ;
#103707=CARTESIAN_POINT ( 'NONE',  ( 21.04999999999999716, 10.50253167713731628, -108.0588298170750647 ) ) ;
#103734=CARTESIAN_POINT ( 'NONE',  ( 20.01093837587850288, 11.75000000001116263, -125.2543974345976778 ) ) ;
#103746=AXIS2_PLACEMENT_3D ( 'NONE', #64001, #208670, #86096 ) ;
#103790=EDGE_CURVE ( 'NONE', #109188, #6219, #233500, .T. ) ;
#103814=DIRECTION ( 'NONE',  ( -1.000000000000000000, -0.000000000000000000, 0.000000000000000000 ) ) ;
#103856=CARTESIAN_POINT ( 'NONE',  ( 23.15000000000000213, -9.499999999988844479, -124.1060308773475924 ) ) ;
#103866=CYLINDRICAL_SURFACE ( 'NONE', #73938, 0.5000000000000004441 ) ;
#103868=CARTESIAN_POINT ( 'NONE',  ( 20.84999999999999432, 7.021664781911246322, -137.8335654018973457 ) ) ;
#103885=ADVANCED_FACE ( 'NONE', ( #171379 ), #213022, .T. ) ;
#103934=AXIS2_PLACEMENT_3D ( 'NONE', #246927, #143974, #223506 ) ;
#103938=EDGE_LOOP ( 'NONE', ( #124409, #156827, #88495, #212921 ) ) ;
#103963=DIRECTION ( 'NONE',  ( -1.000000000000000000, -0.000000000000000000, -0.000000000000000000 ) ) ;
#103964=EDGE_LOOP ( 'NONE', ( #133749, #242281, #119068, #166179, #178126 ) ) ;
#103968=EDGE_CURVE ( 'NONE', #232908, #173371, #201962, .T. ) ;
#103974=DIRECTION ( 'NONE',  ( -1.000000000000000000, -0.000000000000000000, -0.000000000000000000 ) ) ;
#104040=CARTESIAN_POINT ( 'NONE',  ( 22.39999999999999503, 7.790779598384535376, -100.5000000000000284 ) ) ;
#104043=SPHERICAL_SURFACE ( 'NONE', #184565, 0.1000000000000000056 ) ;
#104055=ORIENTED_EDGE ( 'NONE', *, *, #107422, .T. ) ;
#104070=DIRECTION ( 'NONE',  ( -0.000000000000000000, -0.2605042016806452532, -0.9654727137038777718 ) ) ;
#104079=CIRCLE ( 'NONE', #237384, 0.1000000000000028644 ) ;
#104105=ORIENTED_EDGE ( 'NONE', *, *, #153866, .T. ) ;
#104150=CIRCLE ( 'NONE', #220697, 0.09999999999999939493 ) ;
#104181=ORIENTED_EDGE ( 'NONE', *, *, #115449, .T. ) ;
#104183=CARTESIAN_POINT ( 'NONE',  ( 21.05000000000000071, 1.115623935689868526E-11, -132.1000000000000227 ) ) ;
#104200=FACE_OUTER_BOUND ( 'NONE', #15711, .T. ) ;
#104232=CARTESIAN_POINT ( 'NONE',  ( -22.50000000000000000, 1.115600667400684642E-11, -94.25000000000002842 ) ) ;
#104233=CARTESIAN_POINT ( 'NONE',  ( 18.49999999999999289, 6.650000000011155876, -121.8500000000000369 ) ) ;
#104267=LINE ( 'NONE', #27367, #111668 ) ;
#104287=CARTESIAN_POINT ( 'NONE',  ( 20.94999999999999574, -11.74999999998883560, -103.6000000000000369 ) ) ;
#104293=EDGE_LOOP ( 'NONE', ( #164706, #157946, #128780, #60717 ) ) ;
#104317=VERTEX_POINT ( 'NONE', #140247 ) ;
#104318=DIRECTION ( 'NONE',  ( 0.000000000000000000, 0.000000000000000000, 1.000000000000000000 ) ) ;
#104360=ADVANCED_FACE ( 'NONE', ( #137679 ), #256295, .F. ) ;
#104364=CARTESIAN_POINT ( 'NONE',  ( 18.43473516226073983, -9.494942282747041773, -107.5458986833495203 ) ) ;
#104378=CARTESIAN_POINT ( 'NONE',  ( -21.05439746398122836, 11.75000000001115197, -107.4899164874846065 ) ) ;
#104386=FACE_OUTER_BOUND ( 'NONE', #217115, .T. ) ;
#104400=LINE ( 'NONE', #100539, #136869 ) ;
#104435=CARTESIAN_POINT ( 'NONE',  ( -23.25000000000000000, 5.950000000011163692, -123.6942976949652149 ) ) ;
#104437=EDGE_LOOP ( 'NONE', ( #82763, #185559, #112859, #144982 ) ) ;
#104441=EDGE_CURVE ( 'NONE', #66665, #5506, #118946, .T. ) ;
#104450=CIRCLE ( 'NONE', #129421, 0.1000000000000028644 ) ;
#104453=AXIS2_PLACEMENT_3D ( 'NONE', #7746, #91122, #87252 ) ;
#104475=EDGE_LOOP ( 'NONE', ( #89420, #46973, #221647, #117514 ) ) ;
#104507=ORIENTED_EDGE ( 'NONE', *, *, #80809, .T. ) ;
#104513=CARTESIAN_POINT ( 'NONE',  ( -23.15000000000000213, -11.39257802169451139, -130.9260504201681101 ) ) ;
#104514=CARTESIAN_POINT ( 'NONE',  ( 21.05000000000000071, -8.999999999988842703, -124.1060308773475924 ) ) ;
#104527=ORIENTED_EDGE ( 'NONE', *, *, #93467, .F. ) ;
#104530=ORIENTED_EDGE ( 'NONE', *, *, #88027, .T. ) ;
#104569=DIRECTION ( 'NONE',  ( 1.000000000000000000, 0.000000000000000000, -0.000000000000000000 ) ) ;
#104570=AXIS2_PLACEMENT_3D ( 'NONE', #146183, #47072, #57961 ) ;
#104604=ORIENTED_EDGE ( 'NONE', *, *, #190695, .T. ) ;
#104612=ADVANCED_FACE ( 'NONE', ( #199961 ), #137387, .F. ) ;
#104653=DIRECTION ( 'NONE',  ( 1.000000000000000000, 0.000000000000000000, 0.000000000000000000 ) ) ;
#104657=CIRCLE ( 'NONE', #87915, 11.74999999999999645 ) ;
#104669=CARTESIAN_POINT ( 'NONE',  ( -20.94999999999999574, 11.75000000001114842, -127.2161343370219555 ) ) ;
#104695=ORIENTED_EDGE ( 'NONE', *, *, #179841, .T. ) ;
#104716=DIRECTION ( 'NONE',  ( 0.000000000000000000, 0.000000000000000000, -1.000000000000000000 ) ) ;
#104723=AXIS2_PLACEMENT_3D ( 'NONE', #208547, #11632, #9042 ) ;
#104735=VERTEX_POINT ( 'NONE', #105953 ) ;
#104748=DIRECTION ( 'NONE',  ( 0.000000000000000000, 0.9274965247785529332, -0.3738317757009255171 ) ) ;
#104786=AXIS2_PLACEMENT_3D ( 'NONE', #164762, #126920, #186916 ) ;
#104831=CARTESIAN_POINT ( 'NONE',  ( 20.85000000000000142, 1.115600667400684642E-11, -134.0000000000000284 ) ) ;
#104835=FACE_OUTER_BOUND ( 'NONE', #27207, .T. ) ;
#104842=CIRCLE ( 'NONE', #179721, 0.5000000000000004441 ) ;
#104851=VERTEX_POINT ( 'NONE', #4294 ) ;
#104866=CARTESIAN_POINT ( 'NONE',  ( 19.99999999999998934, 11.75000000001115907, -125.3500000000000512 ) ) ;
#104871=DIRECTION ( 'NONE',  ( 0.000000000000000000, 0.000000000000000000, 1.000000000000000000 ) ) ;
#104883=AXIS2_PLACEMENT_3D ( 'NONE', #43256, #203608, #224446 ) ;
#104884=AXIS2_PLACEMENT_3D ( 'NONE', #134502, #17167, #137093 ) ;
#104888=CIRCLE ( 'NONE', #250663, 0.1000000000000028644 ) ;
#104908=CARTESIAN_POINT ( 'NONE',  ( -20.94999999999999929, -11.64999999998884306, -130.9000000000000341 ) ) ;
#104919=AXIS2_PLACEMENT_3D ( 'NONE', #80422, #219972, #204250 ) ;
#104925=DIRECTION ( 'NONE',  ( 0.000000000000000000, 0.000000000000000000, 1.000000000000000000 ) ) ;
#104928=EDGE_CURVE ( 'NONE', #189415, #204479, #10784, .T. ) ;
#104948=CYLINDRICAL_SURFACE ( 'NONE', #101300, 0.09999999999999939493 ) ;
#104953=ORIENTED_EDGE ( 'NONE', *, *, #136102, .F. ) ;
#104969=VERTEX_POINT ( 'NONE', #237486 ) ;
#104982=CARTESIAN_POINT ( 'NONE',  ( 20.94999999999999929, 1.115600667400684642E-11, -134.0000000000000284 ) ) ;
#104990=ORIENTED_EDGE ( 'NONE', *, *, #175765, .F. ) ;
#104992=EDGE_LOOP ( 'NONE', ( #149200, #125609, #36268, #178683 ) ) ;
#105004=VERTEX_POINT ( 'NONE', #19732 ) ;
#105022=ORIENTED_EDGE ( 'NONE', *, *, #201833, .T. ) ;
#105029=CARTESIAN_POINT ( 'NONE',  ( -21.93340585971646561, 7.324147022868593204, -100.5000000000000426 ) ) ;
#105058=CARTESIAN_POINT ( 'NONE',  ( -18.50000000000000000, 9.250000000011157297, -112.8500000000000369 ) ) ;
#105061=EDGE_CURVE ( 'NONE', #38481, #144465, #134506, .T. ) ;
#105066=CARTESIAN_POINT ( 'NONE',  ( 20.12500000000000355, 10.24195072709382970, -108.3602037270861587 ) ) ;
#105107=CARTESIAN_POINT ( 'NONE',  ( 18.49999999999999289, 10.49142135624846439, -125.3500000000000512 ) ) ;
#105128=DIRECTION ( 'NONE',  ( 1.000000000000000000, 0.000000000000000000, 0.000000000000000000 ) ) ;
#105131=CARTESIAN_POINT ( 'NONE',  ( 20.85000000000000142, -11.64999999998883595, -134.0000000000000284 ) ) ;
#105150=EDGE_LOOP ( 'NONE', ( #184455, #138138, #208060, #47154 ) ) ;
#105160=ADVANCED_FACE ( 'NONE', ( #44430 ), #214673, .T. ) ;
#105173=CARTESIAN_POINT ( 'NONE',  ( 20.85000000000000142, 11.75000000001115907, -127.2161343370219413 ) ) ;
#105192=AXIS2_PLACEMENT_3D ( 'NONE', #219345, #40756, #253335 ) ;
#105193=B_SPLINE_CURVE_WITH_KNOTS ( 'NONE', 3,
 ( #131077, #210618, #68550, #71132 ),
 .UNSPECIFIED., .F., .F.,
 ( 4, 4 ),
 ( 0.000000000000000000, 0.0001048066582182451801 ),
 .UNSPECIFIED. ) ;
#105249=EDGE_CURVE ( 'NONE', #106008, #237605, #7876, .T. ) ;
#105254=CARTESIAN_POINT ( 'NONE',  ( -18.59999999999999787, 5.900000000011102586, -110.7190997646564483 ) ) ;
#105265=DIRECTION ( 'NONE',  ( 1.000000000000000000, 0.000000000000000000, 0.000000000000000000 ) ) ;
#105277=CARTESIAN_POINT ( 'NONE',  ( 23.14999999999999503, 14.05000000001115623, -128.4863049292391395 ) ) ;
#105322=CARTESIAN_POINT ( 'NONE',  ( -18.59999999999999787, 7.021664781911246322, -137.7335654018973514 ) ) ;
#105330=LINE ( 'NONE', #147050, #198775 ) ;
#105349=EDGE_LOOP ( 'NONE', ( #152119, #144959, #4543, #257043 ) ) ;
#105363=CARTESIAN_POINT ( 'NONE',  ( -21.14999999999999858, 11.65000000001115588, -100.6000000000000369 ) ) ;
#105368=CARTESIAN_POINT ( 'NONE',  ( -22.49436431346200038, 11.64995094766461392, -100.4330964702777749 ) ) ;
#105381=EDGE_CURVE ( 'NONE', #79682, #233201, #198578, .T. ) ;
#105388=FACE_OUTER_BOUND ( 'NONE', #199054, .T. ) ;
#105399=DIRECTION ( 'NONE',  ( -1.000000000000000000, 0.000000000000000000, 0.000000000000000000 ) ) ;
#105415=LINE ( 'NONE', #184996, #156591 ) ;
#105426=CIRCLE ( 'NONE', #134664, 0.09999999999999967248 ) ;
#105434=CARTESIAN_POINT ( 'NONE',  ( -18.50000000000000000, 11.75000000001115197, -88.75000000000004263 ) ) ;
#105494=DIRECTION ( 'NONE',  ( 0.000000000000000000, -0.1350103645451876666, 0.9908441862701600211 ) ) ;
#105513=CARTESIAN_POINT ( 'NONE',  ( 21.05000000000000071, -11.48912529306490349, -103.4000000000000341 ) ) ;
#105521=AXIS2_PLACEMENT_3D ( 'NONE', #172664, #228751, #252137 ) ;
#105547=CIRCLE ( 'NONE', #131088, 2.000000000000002665 ) ;
#105644=CARTESIAN_POINT ( 'NONE',  ( 18.45036689428353682, -9.490184143317748067, -107.5126958274858708 ) ) ;
#105665=CARTESIAN_POINT ( 'NONE',  ( 21.13920837816993270, 8.783247050131068434, -112.7500000000000284 ) ) ;
#105671=CARTESIAN_POINT ( 'NONE',  ( -20.85000000000000142, -1.362429037182151470, -141.8888812479212334 ) ) ;
#105676=CIRCLE ( 'NONE', #97475, 2.099999999999990763 ) ;
#105683=DIRECTION ( 'NONE',  ( 0.000000000000000000, 0.000000000000000000, 1.000000000000000000 ) ) ;
#105689=CARTESIAN_POINT ( 'NONE',  ( -21.05000000000000071, 1.115600667400684642E-11, -100.5000000000000284 ) ) ;
#105707=ADVANCED_FACE ( 'NONE', ( #129733 ), #69780, .T. ) ;
#105766=LINE ( 'NONE', #204877, #173739 ) ;
#105782=DIRECTION ( 'NONE',  ( 1.000000000000000000, -0.000000000000000000, -0.000000000000000000 ) ) ;
#105785=DIRECTION ( 'NONE',  ( 0.000000000000000000, -1.000000000000000000, 0.000000000000000000 ) ) ;
#105799=DIRECTION ( 'NONE',  ( 1.000000000000000000, -0.000000000000000000, -0.000000000000000000 ) ) ;
#105830=ORIENTED_EDGE ( 'NONE', *, *, #159300, .F. ) ;
#105900=EDGE_CURVE ( 'NONE', #100999, #79411, #223378, .T. ) ;
#105953=CARTESIAN_POINT ( 'NONE',  ( 21.05000000000000071, -8.663551401857999323, -124.4758988819327215 ) ) ;
#106008=VERTEX_POINT ( 'NONE', #129433 ) ;
#106011=TOROIDAL_SURFACE ( 'NONE', #14496, 1.900000000000002576, 0.1000000000000000056 ) ;
#106023=ORIENTED_EDGE ( 'NONE', *, *, #84087, .T. ) ;
#106089=DIRECTION ( 'NONE',  ( 1.000000000000000000, 0.000000000000000000, 0.000000000000000000 ) ) ;
#106111=ADVANCED_FACE ( 'NONE', ( #89004 ), #229812, .T. ) ;
#106114=VERTEX_POINT ( 'NONE', #112455 ) ;
#106120=TOROIDAL_SURFACE ( 'NONE', #164422, 0.2000000000000000111, 0.1000000000000000056 ) ;
#106175=CARTESIAN_POINT ( 'NONE',  ( 20.97224591636398472, 10.62515341617478271, -112.7499259046635984 ) ) ;
#106180=AXIS2_PLACEMENT_3D ( 'NONE', #151907, #132309, #157034 ) ;
#106239=DIRECTION ( 'NONE',  ( 1.000000000000000000, 0.000000000000000000, 0.000000000000000000 ) ) ;
#106320=CARTESIAN_POINT ( 'NONE',  ( -21.05000000000000071, 1.115600667400684642E-11, -134.0000000000000284 ) ) ;
#106385=CARTESIAN_POINT ( 'NONE',  ( -21.05000000000000071, 6.540656951712397138, -100.6000000000000369 ) ) ;
#106390=AXIS2_PLACEMENT_3D ( 'NONE', #168772, #27954, #146558 ) ;
#106394=ORIENTED_EDGE ( 'NONE', *, *, #21573, .F. ) ;
#106399=DIRECTION ( 'NONE',  ( 0.000000000000000000, 0.000000000000000000, 1.000000000000000000 ) ) ;
#106403=DIRECTION ( 'NONE',  ( 0.000000000000000000, 0.4999999999999949485, -0.8660254037844415942 ) ) ;
#106425=DIRECTION ( 'NONE',  ( 0.000000000000000000, 0.1575844902526835067, 0.9875055080513738259 ) ) ;
#106427=ORIENTED_EDGE ( 'NONE', *, *, #250212, .T. ) ;
#106455=EDGE_CURVE ( 'NONE', #243325, #79959, #36490, .T. ) ;
#106464=CARTESIAN_POINT ( 'NONE',  ( -20.64999999999999858, 4.250000000011156409, -112.8500000000000369 ) ) ;
#106466=CARTESIAN_POINT ( 'NONE',  ( 22.50000000000000000, 0.1000000000111554016, -88.85042919245522341 ) ) ;
#106468=VECTOR ( 'NONE', #198226, 1000.000000000000000 ) ;
#106469=VECTOR ( 'NONE', #97831, 1000.000000000000000 ) ;
#106476=CARTESIAN_POINT ( 'NONE',  ( 23.25000000000000000, -9.599999999988845900, -110.3939691226524786 ) ) ;
#106480=LINE ( 'NONE', #9982, #139172 ) ;
#106485=DIRECTION ( 'NONE',  ( 1.000000000000000000, 0.000000000000000000, 0.000000000000000000 ) ) ;
#106543=DIRECTION ( 'NONE',  ( 1.000000000000000000, 0.000000000000000000, 0.000000000000000000 ) ) ;
#106546=ORIENTED_EDGE ( 'NONE', *, *, #49886, .T. ) ;
#106550=CARTESIAN_POINT ( 'NONE',  ( -18.41817142474042157, -9.498703066590927335, -140.6039654876370264 ) ) ;
#106577=ORIENTED_EDGE ( 'NONE', *, *, #23406, .T. ) ;
#106585=DIRECTION ( 'NONE',  ( 0.000000000000000000, 0.000000000000000000, -1.000000000000000000 ) ) ;
#106595=FACE_OUTER_BOUND ( 'NONE', #68299, .T. ) ;
#106598=ORIENTED_EDGE ( 'NONE', *, *, #184834, .F. ) ;
#106617=DIRECTION ( 'NONE',  ( 0.000000000000000000, 8.881784197002011602E-16, -1.000000000000000000 ) ) ;
#106618=CARTESIAN_POINT ( 'NONE',  ( 19.58285714285715073, 10.38499851036257837, -108.1296846673899950 ) ) ;
#106619=DIRECTION ( 'NONE',  ( -0.000000000000000000, -0.000000000000000000, 1.000000000000000000 ) ) ;
#106633=AXIS2_PLACEMENT_3D ( 'NONE', #140591, #243547, #106585 ) ;
#106637=EDGE_LOOP ( 'NONE', ( #141593, #73346, #156391, #232641 ) ) ;
#106642=ORIENTED_EDGE ( 'NONE', *, *, #85000, .T. ) ;
#106662=EDGE_CURVE ( 'NONE', #145162, #68945, #149086, .T. ) ;
#106669=CARTESIAN_POINT ( 'NONE',  ( -22.49231231312463208, 11.64998490368843953, -100.4389471123986652 ) ) ;
#106670=ORIENTED_EDGE ( 'NONE', *, *, #14697, .T. ) ;
#106700=CARTESIAN_POINT ( 'NONE',  ( -21.05000000000000071, 14.05000000001115623, -106.0136950707610310 ) ) ;
#106716=AXIS2_PLACEMENT_3D ( 'NONE', #182492, #144610, #5082 ) ;
#106721=AXIS2_PLACEMENT_3D ( 'NONE', #247017, #227457, #209184 ) ;
#106732=LINE ( 'NONE', #186301, #255087 ) ;
#106815=CARTESIAN_POINT ( 'NONE',  ( 20.94999999999999929, 1.115600667400684642E-11, -100.5000000000000284 ) ) ;
#106827=EDGE_CURVE ( 'NONE', #110428, #18469, #78320, .T. ) ;
#106829=AXIS2_PLACEMENT_3D ( 'NONE', #68469, #188403, #9764 ) ;
#106864=AXIS2_PLACEMENT_3D ( 'NONE', #38544, #180621, #81478 ) ;
#106881=CARTESIAN_POINT ( 'NONE',  ( -23.25000000000000000, -1.835859311432481045, -145.5044391687985694 ) ) ;
#106902=VECTOR ( 'NONE', #137661, 1000.000000000000000 ) ;
#106963=CARTESIAN_POINT ( 'NONE',  ( 21.11747605621531321, 8.778708005504054057, -112.7445631697898136 ) ) ;
#106994=CARTESIAN_POINT ( 'NONE',  ( 23.15000000000000213, -11.64999999998883595, -88.75000000000004263 ) ) ;
#107026=VECTOR ( 'NONE', #134324, 1000.000000000000114 ) ;
#107029=CIRCLE ( 'NONE', #27973, 0.1999999999999987899 ) ;
#107030=CARTESIAN_POINT ( 'NONE',  ( -21.05000000000000071, -0.09999999998884338825, -93.95934304829879125 ) ) ;
#107052=DIRECTION ( 'NONE',  ( 0.000000000000000000, -1.000000000000000000, 0.000000000000000000 ) ) ;
#107073=DIRECTION ( 'NONE',  ( 0.000000000000000000, 0.000000000000000000, -1.000000000000000000 ) ) ;
#107074=CYLINDRICAL_SURFACE ( 'NONE', #245159, 7.899999999999990585 ) ;
#107079=ADVANCED_FACE ( 'NONE', ( #86795 ), #206767, .F. ) ;
#107103=DIRECTION ( 'NONE',  ( 0.000000000000000000, -1.000000000000000000, -2.891205793294679805E-16 ) ) ;
#107108=DIRECTION ( 'NONE',  ( 0.000000000000000000, 0.000000000000000000, 1.000000000000000000 ) ) ;
#107109=CYLINDRICAL_SURFACE ( 'NONE', #119158, 0.09999999999998898659 ) ;
#107184=ORIENTED_EDGE ( 'NONE', *, *, #154440, .F. ) ;
#107194=VERTEX_POINT ( 'NONE', #74984 ) ;
#107201=ORIENTED_EDGE ( 'NONE', *, *, #237402, .T. ) ;
#107204=ORIENTED_EDGE ( 'NONE', *, *, #255543, .T. ) ;
#107218=EDGE_LOOP ( 'NONE', ( #178398, #223298, #174185, #145068 ) ) ;
#107242=DIRECTION ( 'NONE',  ( 0.000000000000000000, 0.000000000000000000, -1.000000000000000000 ) ) ;
#107251=ORIENTED_EDGE ( 'NONE', *, *, #132529, .T. ) ;
#107274=CARTESIAN_POINT ( 'NONE',  ( 18.59999999999999076, 6.450000000011156587, -110.5170271704400591 ) ) ;
#107291=EDGE_CURVE ( 'NONE', #144467, #18904, #129487, .T. ) ;
#107302=FACE_OUTER_BOUND ( 'NONE', #96491, .T. ) ;
#107330=( BOUNDED_CURVE ( )  B_SPLINE_CURVE ( 3, ( #251005, #72414, #167666, #48972 ),
 .UNSPECIFIED., .F., .T. ) 
 B_SPLINE_CURVE_WITH_KNOTS ( ( 4, 4 ),
 ( 4.712388980384690562, 6.283185307179586232 ),
 .UNSPECIFIED. ) 
 CURVE ( )  GEOMETRIC_REPRESENTATION_ITEM ( )  RATIONAL_B_SPLINE_CURVE ( ( 1.000000000000000000, 0.8047378541243652705, 0.8047378541243652705, 1.000000000000000000 ) ) 
 REPRESENTATION_ITEM ( '' )  );
#107408=EDGE_CURVE ( 'NONE', #177703, #104317, #117176, .T. ) ;
#107422=EDGE_CURVE ( 'NONE', #258105, #74301, #238393, .T. ) ;
#107444=CYLINDRICAL_SURFACE ( 'NONE', #43017, 0.1000000000000028644 ) ;
#107465=AXIS2_PLACEMENT_3D ( 'NONE', #110440, #170475, #249959 ) ;
#107472=EDGE_LOOP ( 'NONE', ( #209711, #237899, #101370, #146168 ) ) ;
#107483=DIRECTION ( 'NONE',  ( 0.7071067811865475727, -0.7071067811865475727, 0.000000000000000000 ) ) ;
#107513=CARTESIAN_POINT ( 'NONE',  ( 18.59999999999999076, 14.05000000001116689, -106.0136950707610168 ) ) ;
#107532=CARTESIAN_POINT ( 'NONE',  ( 21.05000000000000071, -9.399999999988844834, -124.1060308773475924 ) ) ;
#107538=CARTESIAN_POINT ( 'NONE',  ( 21.14999999999999858, 11.65000000001116298, -112.6500000000000341 ) ) ;
#107539=AXIS2_PLACEMENT_3D ( 'NONE', #216362, #75604, #217625 ) ;
#107546=CARTESIAN_POINT ( 'NONE',  ( 18.59999999999999787, -11.74999999998883737, -125.3500000000000512 ) ) ;
#107557=DIRECTION ( 'NONE',  ( -0.000000000000000000, -0.1350103645451876666, -0.9908441862701600211 ) ) ;
#107602=ORIENTED_EDGE ( 'NONE', *, *, #251064, .F. ) ;
#107611=CARTESIAN_POINT ( 'NONE',  ( 21.40925344232283223, 0.09895018863080314031, -93.84148114060958790 ) ) ;
#107633=EDGE_CURVE ( 'NONE', #177703, #114911, #104450, .T. ) ;
#107647=SURFACE_STYLE_FILL_AREA ( #167647 ) ;
#107659=CARTESIAN_POINT ( 'NONE',  ( -20.94999675878240808, 10.29307482169071442, -139.4586421466940465 ) ) ;
#107660=ORIENTED_EDGE ( 'NONE', *, *, #237921, .F. ) ;
#107663=FACE_OUTER_BOUND ( 'NONE', #9011, .T. ) ;
#107677=DIRECTION ( 'NONE',  ( 0.000000000000000000, 0.000000000000000000, 1.000000000000000000 ) ) ;
#107684=EDGE_CURVE ( 'NONE', #26109, #188180, #37869, .T. ) ;
#107687=CIRCLE ( 'NONE', #232619, 0.09999999999999939493 ) ;
#107713=EDGE_CURVE ( 'NONE', #195772, #12292, #254304, .T. ) ;
#107751=FACE_OUTER_BOUND ( 'NONE', #119721, .T. ) ;
#107807=CARTESIAN_POINT ( 'NONE',  ( -18.59999999999999787, -1.835341550213255957, -112.0551512925630107 ) ) ;
#107834=ORIENTED_EDGE ( 'NONE', *, *, #121390, .T. ) ;
#107836=CARTESIAN_POINT ( 'NONE',  ( 18.59999999999999076, 6.400000000011158541, -110.4304246300616086 ) ) ;
#107853=DIRECTION ( 'NONE',  ( 1.000000000000000000, -0.000000000000000000, -0.000000000000000000 ) ) ;
#107861=ADVANCED_FACE ( 'NONE', ( #218585 ), #115661, .T. ) ;
#107879=EDGE_CURVE ( 'NONE', #90248, #242007, #234, .T. ) ;
#107886=DIRECTION ( 'NONE',  ( 1.000000000000000000, -0.000000000000000000, -0.000000000000000000 ) ) ;
#107888=CARTESIAN_POINT ( 'NONE',  ( 22.49999999999999645, 0.08880997639808875521, -88.85023708196810333 ) ) ;
#107906=EDGE_CURVE ( 'NONE', #119449, #27184, #98278, .T. ) ;
#107910=CYLINDRICAL_SURFACE ( 'NONE', #165576, 0.09999999999999892308 ) ;
#107924=AXIS2_PLACEMENT_3D ( 'NONE', #29395, #228848, #108886 ) ;
#107927=SPHERICAL_SURFACE ( 'NONE', #3473, 0.1000000000000000056 ) ;
#107933=CARTESIAN_POINT ( 'NONE',  ( -20.64999999999999858, 2.000000000011154189, -113.7246219227621395 ) ) ;
#107940=CARTESIAN_POINT ( 'NONE',  ( -21.05000000000000071, -11.74999999998884448, -130.9000000000000341 ) ) ;
#107956=VERTEX_POINT ( 'NONE', #205449 ) ;
#107962=ORIENTED_EDGE ( 'NONE', *, *, #15436, .T. ) ;
#107969=CIRCLE ( 'NONE', #66279, 0.09999999999998898659 ) ;
#107972=VECTOR ( 'NONE', #139339, 1000.000000000000000 ) ;
#107995=ORIENTED_EDGE ( 'NONE', *, *, #225315, .F. ) ;
#107998=ORIENTED_EDGE ( 'NONE', *, *, #92879, .F. ) ;
#108045=EDGE_CURVE ( 'NONE', #8209, #90248, #215030, .T. ) ;
#108056=ORIENTED_EDGE ( 'NONE', *, *, #30896, .F. ) ;
#108059=ADVANCED_FACE ( 'NONE', ( #150627 ), #72391, .F. ) ;
#108094=AXIS2_PLACEMENT_3D ( 'NONE', #124800, #25695, #66097 ) ;
#108096=DIRECTION ( 'NONE',  ( -0.000000000000000000, -1.000000000000000000, 6.308085367188393199E-16 ) ) ;
#108112=DIRECTION ( 'NONE',  ( 0.000000000000000000, -1.000000000000000000, 0.000000000000000000 ) ) ;
#108115=DIRECTION ( 'NONE',  ( 1.000000000000000000, 0.000000000000000000, 0.000000000000000000 ) ) ;
#108146=AXIS2_PLACEMENT_3D ( 'NONE', #216488, #133112, #117393 ) ;
#108166=AXIS2_PLACEMENT_3D ( 'NONE', #20583, #136641, #218741 ) ;
#108218=ORIENTED_EDGE ( 'NONE', *, *, #222807, .F. ) ;
#108220=CARTESIAN_POINT ( 'NONE',  ( 18.49999999999999645, -1.135018845899022466, -141.7169768834323520 ) ) ;
#108251=DIRECTION ( 'NONE',  ( 1.000000000000000000, 0.000000000000000000, 0.000000000000000000 ) ) ;
#108270=CARTESIAN_POINT ( 'NONE',  ( -21.14999999999999858, 11.75000000001115197, -107.2838656629781724 ) ) ;
#108271=CARTESIAN_POINT ( 'NONE',  ( 21.05281448260627641, 8.776010158548784190, -112.6735579118114572 ) ) ;
#108299=DIRECTION ( 'NONE',  ( 1.000000000000000000, -0.000000000000000000, -0.000000000000000000 ) ) ;
#108326=CARTESIAN_POINT ( 'NONE',  ( -21.05000000000000071, 1.115600667400684642E-11, -100.5000000000000284 ) ) ;
#108345=AXIS2_PLACEMENT_3D ( 'NONE', #108601, #228566, #6930 ) ;
#108368=ADVANCED_FACE ( 'NONE', ( #64370 ), #47346, .F. ) ;
#108411=CARTESIAN_POINT ( 'NONE',  ( 20.85000000000000142, -1.736705739456431807, -145.5174225876237699 ) ) ;
#108421=CARTESIAN_POINT ( 'NONE',  ( -23.25000000000000000, -11.64999999998884483, -130.9000000000000341 ) ) ;
#108423=CARTESIAN_POINT ( 'NONE',  ( -23.15000000000000213, 1.115600667400684642E-11, -100.5000000000000284 ) ) ;
#108449=SHAPE_REPRESENTATION ( 'Injection Molded Chain Links 4', ( #2425 ), #119141 ) ;
#108490=AXIS2_PLACEMENT_3D ( 'NONE', #252414, #116771, #133762 ) ;
#108506=VERTEX_POINT ( 'NONE', #152922 ) ;
#108557=ADVANCED_FACE ( 'NONE', ( #63733 ), #241114, .F. ) ;
#108587=ORIENTED_EDGE ( 'NONE', *, *, #5710, .T. ) ;
#108594=CARTESIAN_POINT ( 'NONE',  ( 20.94999999999999929, 8.776282895303632259, -121.7500000000000426 ) ) ;
#108601=CARTESIAN_POINT ( 'NONE',  ( -23.15000000000000213, 1.115600667400684642E-11, -134.0000000000000284 ) ) ;
#108606=TOROIDAL_SURFACE ( 'NONE', #175285, 0.2000000000000000111, 0.1000000000000000056 ) ;
#108612=DIRECTION ( 'NONE',  ( 0.000000000000000000, 0.9915357197604971473, -0.1298341882519111479 ) ) ;
#108620=TOROIDAL_SURFACE ( 'NONE', #254344, 0.2000000000000000111, 0.1000000000000000056 ) ;
#108625=EDGE_CURVE ( 'NONE', #169627, #26411, #48800, .T. ) ;
#108647=ORIENTED_EDGE ( 'NONE', *, *, #85586, .T. ) ;
#108651=EDGE_LOOP ( 'NONE', ( #94041, #159866, #178187, #236872 ) ) ;
#108655=DIRECTION ( 'NONE',  ( 0.000000000000000000, 1.000000000000000000, 0.000000000000000000 ) ) ;
#108671=DIRECTION ( 'NONE',  ( 0.000000000000000000, 0.000000000000000000, -1.000000000000000000 ) ) ;
#108708=AXIS2_PLACEMENT_3D ( 'NONE', #189782, #69855, #47680 ) ;
#108728=FACE_OUTER_BOUND ( 'NONE', #198447, .T. ) ;
#108781=ORIENTED_EDGE ( 'NONE', *, *, #170342, .F. ) ;
#108793=DIRECTION ( 'NONE',  ( -0.000000000000000000, -1.265107689135680095E-16, 1.000000000000000000 ) ) ;
#108801=DIRECTION ( 'NONE',  ( 0.000000000000000000, 0.000000000000000000, 1.000000000000000000 ) ) ;
#108842=DIRECTION ( 'NONE',  ( 1.000000000000000000, -0.000000000000000000, -0.000000000000000000 ) ) ;
#108843=AXIS2_PLACEMENT_3D ( 'NONE', #108594, #9486, #89017 ) ;
#108851=AXIS2_PLACEMENT_3D ( 'NONE', #226800, #48160, #93712 ) ;
#108857=EDGE_CURVE ( 'NONE', #102466, #43391, #73774, .T. ) ;
#108861=FACE_OUTER_BOUND ( 'NONE', #97291, .T. ) ;
#108862=ORIENTED_EDGE ( 'NONE', *, *, #226884, .T. ) ;
#108870=CARTESIAN_POINT ( 'NONE',  ( 21.05000000000000071, 10.68429367439823352, -108.0266739386370887 ) ) ;
#108886=DIRECTION ( 'NONE',  ( 0.000000000000000000, 0.4999999999999478195, 0.8660254037844686836 ) ) ;
#108906=CARTESIAN_POINT ( 'NONE',  ( 20.19326291201235790, 10.15606098791279877, -108.2618618076038786 ) ) ;
#108907=DIRECTION ( 'NONE',  ( 0.000000000000000000, 0.000000000000000000, 1.000000000000000000 ) ) ;
#108909=EDGE_CURVE ( 'NONE', #242555, #135846, #157435, .T. ) ;
#108926=ORIENTED_EDGE ( 'NONE', *, *, #72317, .T. ) ;
#108939=ORIENTED_EDGE ( 'NONE', *, *, #208248, .T. ) ;
#108949=DIRECTION ( 'NONE',  ( 0.000000000000000000, -1.000000000000000000, -0.000000000000000000 ) ) ;
#108964=ADVANCED_FACE ( 'NONE', ( #17872 ), #21747, .T. ) ;
#108999=AXIS2_PLACEMENT_3D ( 'NONE', #163160, #24945, #183990 ) ;
#109044=VERTEX_POINT ( 'NONE', #163822 ) ;
#109048=CARTESIAN_POINT ( 'NONE',  ( 20.94999999999999929, 10.72371710471868056, -112.6500000000000341 ) ) ;
#109095=CARTESIAN_POINT ( 'NONE',  ( 21.14999999999999858, 1.115600667400684642E-11, -93.95934304829877703 ) ) ;
#109104=ORIENTED_EDGE ( 'NONE', *, *, #129343, .F. ) ;
#109119=EDGE_LOOP ( 'NONE', ( #917, #204766, #134376 ) ) ;
#109123=CARTESIAN_POINT ( 'NONE',  ( 18.50211644919734866, 10.30207779525984435, -139.4895520716783039 ) ) ;
#109188=VERTEX_POINT ( 'NONE', #35873 ) ;
#109216=DIRECTION ( 'NONE',  ( -1.000000000000000000, 0.000000000000000000, 0.000000000000000000 ) ) ;
#109218=ORIENTED_EDGE ( 'NONE', *, *, #72936, .T. ) ;
#109232=AXIS2_PLACEMENT_3D ( 'NONE', #208139, #86857, #89438 ) ;
#109243=DIRECTION ( 'NONE',  ( 1.000000000000000000, -0.000000000000000000, -0.000000000000000000 ) ) ;
#109254=CARTESIAN_POINT ( 'NONE',  ( 18.49999999999999289, 10.25000000001115552, -121.8500000000000369 ) ) ;
#109268=CARTESIAN_POINT ( 'NONE',  ( 18.39999999999999858, -9.599999999988845900, -140.6001893912220737 ) ) ;
#109270=DIRECTION ( 'NONE',  ( 0.000000000000000000, 0.4999999999999956701, -0.8660254037844411501 ) ) ;
#109294=DIRECTION ( 'NONE',  ( 1.000000000000000000, 0.000000000000000000, 0.000000000000000000 ) ) ;
#109313=ORIENTED_EDGE ( 'NONE', *, *, #17126, .F. ) ;
#109321=AXIS2_PLACEMENT_3D ( 'NONE', #128678, #152105, #249898 ) ;
#109324=TOROIDAL_SURFACE ( 'NONE', #25970, 0.2000000000000000111, 0.1000000000000000056 ) ;
#109377=TOROIDAL_SURFACE ( 'NONE', #55188, 4.149999999999999467, 0.1000000000000000056 ) ;
#109385=EDGE_CURVE ( 'NONE', #138314, #7281, #21450, .T. ) ;
#109387=AXIS2_PLACEMENT_3D ( 'NONE', #110215, #93220, #230168 ) ;
#109392=ORIENTED_EDGE ( 'NONE', *, *, #88169, .T. ) ;
#109397=ORIENTED_EDGE ( 'NONE', *, *, #150679, .F. ) ;
#109403=LINE ( 'NONE', #48154, #155491 ) ;
#109409=DIRECTION ( 'NONE',  ( 0.000000000000000000, -1.084202172485473353E-14, 1.000000000000000000 ) ) ;
#109424=DIRECTION ( 'NONE',  ( -0.000000000000000000, 0.9876197685951276783, 0.1568667991644721316 ) ) ;
#109465=ORIENTED_EDGE ( 'NONE', *, *, #208248, .F. ) ;
#109474=AXIS2_PLACEMENT_3D ( 'NONE', #170710, #113246, #130229 ) ;
#109479=EDGE_CURVE ( 'NONE', #6436, #14418, #244308, .T. ) ;
#109483=ORIENTED_EDGE ( 'NONE', *, *, #15830, .F. ) ;
#109525=ADVANCED_FACE ( 'NONE', ( #73421 ), #212904, .T. ) ;
#109530=FACE_OUTER_BOUND ( 'NONE', #212534, .T. ) ;
#109536=DIRECTION ( 'NONE',  ( 0.7071067811865388020, -0.7071067811865561215, 0.000000000000000000 ) ) ;
#109542=ORIENTED_EDGE ( 'NONE', *, *, #157491, .T. ) ;
#109544=CIRCLE ( 'NONE', #218242, 0.1000000000000008937 ) ;
#109549=CARTESIAN_POINT ( 'NONE',  ( -21.05000000000000071, 1.115600667400684642E-11, -104.7999999999999972 ) ) ;
#109569=FACE_OUTER_BOUND ( 'NONE', #231950, .T. ) ;
#109586=CARTESIAN_POINT ( 'NONE',  ( 18.49999999999999289, 10.20857864377385127, -121.8500000000000369 ) ) ;
#109620=SHAPE_DEFINITION_REPRESENTATION ( #145016, #108449 ) ;
#109623=DIRECTION ( 'NONE',  ( 0.000000000000000000, 0.000000000000000000, -1.000000000000000000 ) ) ;
#109665=PLANE ( 'NONE',  #197805 ) ;
#109683=FACE_OUTER_BOUND ( 'NONE', #157831, .T. ) ;
#109696=AXIS2_PLACEMENT_3D ( 'NONE', #241469, #78523, #177672 ) ;
#109737=CARTESIAN_POINT ( 'NONE',  ( -20.64999999999999858, 7.150000000011155876, -112.8500000000000369 ) ) ;
#109746=CARTESIAN_POINT ( 'NONE',  ( 23.15000000000000213, -11.48912529306489994, -131.0000000000000284 ) ) ;
#109765=EDGE_LOOP ( 'NONE', ( #207630, #40285 ) ) ;
#109806=EDGE_LOOP ( 'NONE', ( #247802, #79193, #121629, #161705 ) ) ;
#109833=DIRECTION ( 'NONE',  ( 0.000000000000000000, -3.339342691255721203E-13, 1.000000000000000000 ) ) ;
#109844=AXIS2_PLACEMENT_3D ( 'NONE', #57168, #78033, #237120 ) ;
#109846=DIRECTION ( 'NONE',  ( 0.000000000000000000, -1.000000000000000000, 0.000000000000000000 ) ) ;
#109874=AXIS2_PLACEMENT_3D ( 'NONE', #182865, #26340, #42061 ) ;
#109877=CARTESIAN_POINT ( 'NONE',  ( 18.49999999999999289, 6.450000000011156587, -121.6500000000000341 ) ) ;
#109895=VERTEX_POINT ( 'NONE', #164494 ) ;
#109900=VECTOR ( 'NONE', #105494, 1000.000000000000114 ) ;
#109912=CARTESIAN_POINT ( 'NONE',  ( -21.05000000000000071, 1.835341550235567887, -112.1551512925630192 ) ) ;
#109932=AXIS2_PLACEMENT_3D ( 'NONE', #233285, #92451, #214972 ) ;
#109956=VERTEX_POINT ( 'NONE', #110924 ) ;
#109959=CARTESIAN_POINT ( 'NONE',  ( -18.50000000000000000, 9.350000000011156942, -112.8500000000000369 ) ) ;
#109972=CIRCLE ( 'NONE', #93214, 0.5000000000000013323 ) ;
#110008=FACE_OUTER_BOUND ( 'NONE', #233450, .T. ) ;
#110017=VECTOR ( 'NONE', #228449, 1000.000000000000000 ) ;
#110047=CARTESIAN_POINT ( 'NONE',  ( 20.94999999999999929, 10.72371710471867701, -108.1649135690876449 ) ) ;
#110054=CARTESIAN_POINT ( 'NONE',  ( -20.54999999999999716, -9.399999999988846611, -124.1060308773475924 ) ) ;
#110087=AXIS2_PLACEMENT_3D ( 'NONE', #180006, #216544, #37935 ) ;
#110100=CARTESIAN_POINT ( 'NONE',  ( 23.14999999999999858, 1.115600667400684642E-11, -134.0000000000000284 ) ) ;
#110109=AXIS2_PLACEMENT_3D ( 'NONE', #139819, #58980, #72492 ) ;
#110199=EDGE_CURVE ( 'NONE', #185811, #250368, #124562, .T. ) ;
#110215=CARTESIAN_POINT ( 'NONE',  ( 20.94999999999999929, 8.776282895303632259, -112.6500000000000341 ) ) ;
#110223=CARTESIAN_POINT ( 'NONE',  ( -20.94403535211772294, 10.30632246271647467, -139.5041836778896140 ) ) ;
#110233=ORIENTED_EDGE ( 'NONE', *, *, #29611, .F. ) ;
#110235=DIRECTION ( 'NONE',  ( 1.000000000000000000, 0.000000000000000000, 0.000000000000000000 ) ) ;
#110241=TOROIDAL_SURFACE ( 'NONE', #255943, 11.90000000000000213, 0.1000000000000000056 ) ;
#110250=TOROIDAL_SURFACE ( 'NONE', #143580, 0.2000000000000000111, 0.1000000000000000056 ) ;
#110268=ORIENTED_EDGE ( 'NONE', *, *, #246560, .F. ) ;
#110304=DIRECTION ( 'NONE',  ( 0.000000000000000000, 0.000000000000000000, -1.000000000000000000 ) ) ;
#110384=EDGE_CURVE ( 'NONE', #242360, #71456, #82814, .T. ) ;
#110398=CARTESIAN_POINT ( 'NONE',  ( 23.14999999999998437, 1.115650265596050101E-11, -96.45000000000003126 ) ) ;
#110406=ORIENTED_EDGE ( 'NONE', *, *, #226891, .T. ) ;
#110417=CARTESIAN_POINT ( 'NONE',  ( 18.52643265882457868, 10.31973158071402885, -139.5505334713354841 ) ) ;
#110424=AXIS2_PLACEMENT_3D ( 'NONE', #4764, #86871, #127310 ) ;
#110428=VERTEX_POINT ( 'NONE', #179285 ) ;
#110436=ORIENTED_EDGE ( 'NONE', *, *, #26997, .T. ) ;
#110439=VERTEX_POINT ( 'NONE', #82685 ) ;
#110440=CARTESIAN_POINT ( 'NONE',  ( 21.05000000000000071, -1.162701749926853712, -108.6000000000000227 ) ) ;
#110493=EDGE_LOOP ( 'NONE', ( #89496, #114494, #106598, #166808 ) ) ;
#110504=FACE_OUTER_BOUND ( 'NONE', #185146, .T. ) ;
#110559=ADVANCED_FACE ( 'NONE', ( #145250 ), #26627, .T. ) ;
#110564=VERTEX_POINT ( 'NONE', #226051 ) ;
#110587=CARTESIAN_POINT ( 'NONE',  ( -20.85000000000000142, -1.249999999988843369, -141.8004807544151333 ) ) ;
#110608=DIRECTION ( 'NONE',  ( 1.000000000000000000, 2.952720810173289112E-16, -0.000000000000000000 ) ) ;
#110634=VERTEX_POINT ( 'NONE', #140988 ) ;
#110640=DIRECTION ( 'NONE',  ( 0.000000000000000000, 0.000000000000000000, 1.000000000000000000 ) ) ;
#110644=EDGE_LOOP ( 'NONE', ( #240123, #254965, #257647, #90745 ) ) ;
#110650=ORIENTED_EDGE ( 'NONE', *, *, #212973, .F. ) ;
#110676=SURFACE_STYLE_FILL_AREA ( #111977 ) ;
#110679=CARTESIAN_POINT ( 'NONE',  ( -20.54999999999999716, -8.999999999988846255, -109.8939691226524786 ) ) ;
#110694=TOROIDAL_SURFACE ( 'NONE', #185716, 0.2000000000000000111, 0.1000000000000000056 ) ;
#110730=ORIENTED_EDGE ( 'NONE', *, *, #177385, .F. ) ;
#110781=EDGE_CURVE ( 'NONE', #157888, #203753, #137204, .T. ) ;
#110815=VERTEX_POINT ( 'NONE', #204780 ) ;
#110821=CARTESIAN_POINT ( 'NONE',  ( -21.05000000000000071, 6.540656951712397138, -100.6000000000000369 ) ) ;
#110830=VECTOR ( 'NONE', #62529, 1000.000000000000000 ) ;
#110847=CARTESIAN_POINT ( 'NONE',  ( 21.05000000000000071, -1.849084418615859926, -112.1560105214471577 ) ) ;
#110852=CARTESIAN_POINT ( 'NONE',  ( -22.50000000000000000, 11.64987090377453960, -100.4174801091271121 ) ) ;
#110855=EDGE_LOOP ( 'NONE', ( #11083, #228880, #14520, #241495 ) ) ;
#110861=CARTESIAN_POINT ( 'NONE',  ( 23.14999999999999858, -11.74999999998883560, -88.75000000000004263 ) ) ;
#110866=DIRECTION ( 'NONE',  ( 1.000000000000000000, 0.000000000000000000, -0.000000000000000000 ) ) ;
#110869=CIRCLE ( 'NONE', #35872, 0.09999999999999939493 ) ;
#110884=CARTESIAN_POINT ( 'NONE',  ( 20.94999027547553894, 10.29326151435327219, -139.4592822510415147 ) ) ;
#110919=EDGE_CURVE ( 'NONE', #141245, #45367, #128447, .T. ) ;
#110924=CARTESIAN_POINT ( 'NONE',  ( -22.50000000000000000, 0.1000000000111554016, -88.85042919245522341 ) ) ;
#110929=CARTESIAN_POINT ( 'NONE',  ( -23.15000000000000213, 1.115626384983466744E-11, -131.9000000000000341 ) ) ;
#110931=DIRECTION ( 'NONE',  ( -0.000000000000000000, 0.000000000000000000, 1.000000000000000000 ) ) ;
#110933=CIRCLE ( 'NONE', #219261, 11.80000000000000426 ) ;
#110950=ORIENTED_EDGE ( 'NONE', *, *, #73468, .F. ) ;
#110957=VERTEX_POINT ( 'NONE', #95431 ) ;
#110972=TOROIDAL_SURFACE ( 'NONE', #106864, 11.65000000000000036, 0.1000000000000000056 ) ;
#110987=CIRCLE ( 'NONE', #173583, 0.5000000000000013323 ) ;
#110990=AXIS2_PLACEMENT_3D ( 'NONE', #189750, #69826, #34549 ) ;
#111031=( BOUNDED_SURFACE ( )  B_SPLINE_SURFACE ( 3, 2, ( 
 ( #159613, #116625, #141326 ),
 ( #196160, #81315, #177901 ),
 ( #158361, #78762, #59175 ),
 ( #17512, #97018, #138713 ),
 ( #218270, #99598, #39689 ),
 ( #20106, #239145, #140016 ) ),
 .UNSPECIFIED., .F., .F., .F. ) 
 B_SPLINE_SURFACE_WITH_KNOTS ( ( 4, 2, 4 ),
 ( 3, 3 ),
 ( 0.0001300404313046571046, 0.0003183318589266614972, 0.0005066232865486658627 ),
 ( 0.000000000000000000, 1.000000000000000000 ),
 .UNSPECIFIED. ) 
 GEOMETRIC_REPRESENTATION_ITEM ( )  RATIONAL_B_SPLINE_SURFACE ( (
 ( 1.000000000000000000, 0.7071067811865475727, 1.000000000000000000),
 ( 1.000000000000000000, 0.7625113560542592372, 1.000000000000000000),
 ( 1.000000000000000000, 0.8126073484685066850, 1.000000000000000000),
 ( 1.000000000000000000, 0.8923049332735827344, 1.000000000000000000),
 ( 1.000000000000000000, 0.9231914937766932949, 1.000000000000000000),
 ( 1.000000000000000000, 0.9238795325112901802, 1.000000000000000000) ) ) 
 REPRESENTATION_ITEM ( '' )  SURFACE ( )  );
#111060=EDGE_LOOP ( 'NONE', ( #124797, #169226, #118188, #198739 ) ) ;
#111113=DIRECTION ( 'NONE',  ( 0.000000000000000000, 0.000000000000000000, -1.000000000000000000 ) ) ;
#111125=LINE ( 'NONE', #173720, #150873 ) ;
#111128=CIRCLE ( 'NONE', #40440, 0.09999999999998898659 ) ;
#111138=CARTESIAN_POINT ( 'NONE',  ( -21.05000000000000071, -12.41227409413852811, -131.1000000000000227 ) ) ;
#111154=TOROIDAL_SURFACE ( 'NONE', #69662, 11.65000000000000036, 0.1000000000000000056 ) ;
#111155=CIRCLE ( 'NONE', #161242, 0.1000000000000000472 ) ;
#111207=ORIENTED_EDGE ( 'NONE', *, *, #203750, .F. ) ;
#111223=AXIS2_PLACEMENT_3D ( 'NONE', #58321, #234407, #199148 ) ;
#111250=VECTOR ( 'NONE', #62773, 1000.000000000000000 ) ;
#111274=FACE_OUTER_BOUND ( 'NONE', #204787, .T. ) ;
#111279=EDGE_CURVE ( 'NONE', #5875, #34079, #257750, .T. ) ;
#111312=ORIENTED_EDGE ( 'NONE', *, *, #43296, .T. ) ;
#111320=AXIS2_PLACEMENT_3D ( 'NONE', #241730, #63083, #142609 ) ;
#111328=AXIS2_PLACEMENT_3D ( 'NONE', #204190, #248469, #127237 ) ;
#111333=VERTEX_POINT ( 'NONE', #76838 ) ;
#111334=CARTESIAN_POINT ( 'NONE',  ( 21.12230431290519661, 0.005209851700161530035, -94.04243334670701415 ) ) ;
#111336=ORIENTED_EDGE ( 'NONE', *, *, #176082, .F. ) ;
#111353=AXIS2_PLACEMENT_3D ( 'NONE', #160301, #102837, #23363 ) ;
#111361=DIRECTION ( 'NONE',  ( 0.000000000000000000, -0.4930308989874729320, -0.8700118002898605818 ) ) ;
#111390=DIRECTION ( 'NONE',  ( 1.000000000000000000, 0.000000000000000000, 0.000000000000000000 ) ) ;
#111391=ORIENTED_EDGE ( 'NONE', *, *, #16732, .T. ) ;
#111409=EDGE_LOOP ( 'NONE', ( #65784, #243609, #174591, #42967 ) ) ;
#111417=CARTESIAN_POINT ( 'NONE',  ( -18.50000000000000000, 5.341242990002803559, -90.69334979351201298 ) ) ;
#111426=VERTEX_POINT ( 'NONE', #131685 ) ;
#111442=CARTESIAN_POINT ( 'NONE',  ( 18.45068634130097252, -9.486506073331604227, -107.5687784311681412 ) ) ;
#111452=CARTESIAN_POINT ( 'NONE',  ( -23.25000000000000000, -0.09999999998884338825, -88.85042919245522341 ) ) ;
#111469=EDGE_CURVE ( 'NONE', #231259, #256518, #199388, .T. ) ;
#111504=ORIENTED_EDGE ( 'NONE', *, *, #87413, .F. ) ;
#111510=AXIS2_PLACEMENT_3D ( 'NONE', #247431, #71390, #131336 ) ;
#111525=VERTEX_POINT ( 'NONE', #44144 ) ;
#111558=EDGE_CURVE ( 'NONE', #154355, #169627, #178550, .T. ) ;
#111570=DIRECTION ( 'NONE',  ( 0.000000000000000000, 0.000000000000000000, -1.000000000000000000 ) ) ;
#111588=AXIS2_PLACEMENT_3D ( 'NONE', #69928, #149463, #228984 ) ;
#111593=DIRECTION ( 'NONE',  ( 0.000000000000000000, -1.000000000000000000, 0.000000000000000000 ) ) ;
#111615=ORIENTED_EDGE ( 'NONE', *, *, #255216, .T. ) ;
#111634=DIRECTION ( 'NONE',  ( -0.000000000000000000, -0.000000000000000000, 1.000000000000000000 ) ) ;
#111637=CARTESIAN_POINT ( 'NONE',  ( 20.85000000000000142, -1.749999999988843813, -145.6189500386223017 ) ) ;
#111652=AXIS2_PLACEMENT_3D ( 'NONE', #23416, #226703, #122497 ) ;
#111668=VECTOR ( 'NONE', #101684, 1000.000000000000000 ) ;
#111676=EDGE_LOOP ( 'NONE', ( #19421, #70608, #228752, #242432 ) ) ;
#111681=ORIENTED_EDGE ( 'NONE', *, *, #133605, .F. ) ;
#111714=ORIENTED_EDGE ( 'NONE', *, *, #171773, .F. ) ;
#111719=DIRECTION ( 'NONE',  ( -1.000000000000000000, 0.000000000000000000, 0.000000000000000000 ) ) ;
#111722=ORIENTED_EDGE ( 'NONE', *, *, #90291, .T. ) ;
#111732=VERTEX_POINT ( 'NONE', #87090 ) ;
#111740=ORIENTED_EDGE ( 'NONE', *, *, #115390, .F. ) ;
#111752=CARTESIAN_POINT ( 'NONE',  ( 22.39999999999999858, 0.1000000000111554016, -92.70922040162665212 ) ) ;
#111756=ORIENTED_EDGE ( 'NONE', *, *, #3196, .F. ) ;
#111785=CARTESIAN_POINT ( 'NONE',  ( -18.50000000000000000, 9.150000000011157653, -88.75000000000004263 ) ) ;
#111787=DIRECTION ( 'NONE',  ( 1.000000000000000000, -0.000000000000000000, -0.000000000000000000 ) ) ;
#111802=CARTESIAN_POINT ( 'NONE',  ( -18.46907102845854354, -9.473727364752946301, -140.6760347387365471 ) ) ;
#111803=EDGE_CURVE ( 'NONE', #44449, #140474, #66280, .T. ) ;
#111873=ADVANCED_FACE ( 'NONE', ( #23963 ), #99556, .T. ) ;
#111914=ADVANCED_FACE ( 'NONE', ( #68208 ), #126898, .T. ) ;
#111924=DIRECTION ( 'NONE',  ( 0.000000000000000000, 0.000000000000000000, -1.000000000000000000 ) ) ;
#111925=EDGE_CURVE ( 'NONE', #58429, #61278, #87100, .T. ) ;
#111935=CARTESIAN_POINT ( 'NONE',  ( 18.60000000000000142, -9.321008403350125704, -107.7359382490779325 ) ) ;
#111944=AXIS2_PLACEMENT_3D ( 'NONE', #106320, #125897, #108907 ) ;
#111952=VECTOR ( 'NONE', #102876, 1000.000000000000000 ) ;
#111964=DIRECTION ( 'NONE',  ( -1.000000000000000000, 0.000000000000000000, 0.000000000000000000 ) ) ;
#111977=FILL_AREA_STYLE ('',( #191528 ) ) ;
#112010=CIRCLE ( 'NONE', #232635, 0.1000000000000028644 ) ;
#112014=AXIS2_PLACEMENT_3D ( 'NONE', #104232, #108112, #126383 ) ;
#112055=ORIENTED_EDGE ( 'NONE', *, *, #4249, .T. ) ;
#112063=AXIS2_PLACEMENT_3D ( 'NONE', #178642, #59920, #20846 ) ;
#112064=CARTESIAN_POINT ( 'NONE',  ( 18.49999999999999289, 6.846123162363745074, -137.7377262668498759 ) ) ;
#112077=CIRCLE ( 'NONE', #41356, 0.1999999999999987899 ) ;
#112120=ORIENTED_EDGE ( 'NONE', *, *, #238980, .T. ) ;
#112151=EDGE_LOOP ( 'NONE', ( #38132, #100080, #29308 ) ) ;
#112155=EDGE_LOOP ( 'NONE', ( #80872, #27916, #218861, #40571, #6575 ) ) ;
#112159=DIRECTION ( 'NONE',  ( 0.000000000000000000, 1.000000000000000000, -1.224646799147353207E-16 ) ) ;
#112201=DIRECTION ( 'NONE',  ( 0.000000000000000000, -1.000000000000000000, 0.000000000000000000 ) ) ;
#112248=AXIS2_PLACEMENT_3D ( 'NONE', #204925, #124139, #125417 ) ;
#112294=CARTESIAN_POINT ( 'NONE',  ( 21.05000000000000071, -11.64999999998883595, -103.4000000000000341 ) ) ;
#112306=ORIENTED_EDGE ( 'NONE', *, *, #150359, .T. ) ;
#112351=FACE_OUTER_BOUND ( 'NONE', #201174, .T. ) ;
#112363=CARTESIAN_POINT ( 'NONE',  ( 18.58685178364169843, -9.406733083793096029, -107.6244204690877524 ) ) ;
#112371=AXIS2_PLACEMENT_3D ( 'NONE', #256426, #21754, #179554 ) ;
#112396=ORIENTED_EDGE ( 'NONE', *, *, #96712, .F. ) ;
#112406=ORIENTED_EDGE ( 'NONE', *, *, #43702, .T. ) ;
#112411=CARTESIAN_POINT ( 'NONE',  ( 20.94999999999999929, 1.115600667400684642E-11, -134.0000000000000284 ) ) ;
#112414=LINE ( 'NONE', #191969, #129707 ) ;
#112418=AXIS2_PLACEMENT_3D ( 'NONE', #160402, #61274, #140813 ) ;
#112449=VERTEX_POINT ( 'NONE', #152610 ) ;
#112451=CIRCLE ( 'NONE', #29090, 0.1000000000000028644 ) ;
#112455=CARTESIAN_POINT ( 'NONE',  ( 21.05000000000000071, 1.115600667400684642E-11, -113.3750000000000284 ) ) ;
#112484=DIRECTION ( 'NONE',  ( 0.000000000000000000, 0.9915357197604792727, -0.1298341882520475943 ) ) ;
#112526=ORIENTED_EDGE ( 'NONE', *, *, #227037, .T. ) ;
#112538=DIRECTION ( 'NONE',  ( 1.000000000000000000, 0.000000000000000000, 0.000000000000000000 ) ) ;
#112556=CARTESIAN_POINT ( 'NONE',  ( -20.54999999999999716, 1.115600667400684642E-11, -134.0000000000000284 ) ) ;
#112567=EDGE_CURVE ( 'NONE', #188180, #75064, #255472, .T. ) ;
#112579=CARTESIAN_POINT ( 'NONE',  ( 20.94999999999999574, -1.835341550213255957, -112.0551512925630107 ) ) ;
#112589=DIRECTION ( 'NONE',  ( 1.000000000000000000, 0.000000000000000000, 0.000000000000000000 ) ) ;
#112607=CARTESIAN_POINT ( 'NONE',  ( -18.59999999999999787, 1.866714910068465239, -112.2526752462820525 ) ) ;
#112649=AXIS2_PLACEMENT_3D ( 'NONE', #118477, #78037, #157630 ) ;
#112651=EDGE_LOOP ( 'NONE', ( #127569, #160590, #251325, #30923 ) ) ;
#112652=AXIS2_PLACEMENT_3D ( 'NONE', #141985, #42903, #105399 ) ;
#112676=VECTOR ( 'NONE', #256734, 1000.000000000000000 ) ;
#112690=CARTESIAN_POINT ( 'NONE',  ( -21.14999999999999858, 0.09779029131994770863, -94.24218538952392521 ) ) ;
#112763=CARTESIAN_POINT ( 'NONE',  ( 23.14999999999999147, 4.150000000011154988, -100.5000000000000284 ) ) ;
#112771=AXIS2_PLACEMENT_3D ( 'NONE', #169061, #9944, #52914 ) ;
#112813=DIRECTION ( 'NONE',  ( 0.000000000000000000, 0.000000000000000000, -1.000000000000000000 ) ) ;
#112836=ORIENTED_EDGE ( 'NONE', *, *, #194001, .F. ) ;
#112838=CARTESIAN_POINT ( 'NONE',  ( 20.94999999999999929, -9.499999999988844479, -124.1060308773475924 ) ) ;
#112859=ORIENTED_EDGE ( 'NONE', *, *, #4878, .F. ) ;
#112898=AXIS2_PLACEMENT_3D ( 'NONE', #92966, #249494, #69575 ) ;
#112909=ORIENTED_EDGE ( 'NONE', *, *, #139765, .F. ) ;
#112921=DIRECTION ( 'NONE',  ( 0.000000000000000000, -1.000000000000000000, 0.000000000000000000 ) ) ;
#112965=CARTESIAN_POINT ( 'NONE',  ( 21.05000000000000071, 5.000000000011153745, -121.5947339810869465 ) ) ;
#112972=CARTESIAN_POINT ( 'NONE',  ( 20.95512820512820440, 8.876151316299273120, -109.0586289951409924 ) ) ;
#112993=EDGE_CURVE ( 'NONE', #191177, #10935, #142011, .T. ) ;
#113029=CARTESIAN_POINT ( 'NONE',  ( -20.94999999999999929, 1.115600667400684642E-11, -134.0000000000000284 ) ) ;
#113057=EDGE_LOOP ( 'NONE', ( #69249, #114212, #56268 ) ) ;
#113068=ORIENTED_EDGE ( 'NONE', *, *, #190695, .F. ) ;
#113082=CARTESIAN_POINT ( 'NONE',  ( -18.50000000000000000, -9.399999999988850163, -140.8820418481727188 ) ) ;
#113117=ORIENTED_EDGE ( 'NONE', *, *, #188275, .T. ) ;
#113123=AXIS2_PLACEMENT_3D ( 'NONE', #104908, #42409, #241886 ) ;
#113145=EDGE_LOOP ( 'NONE', ( #133912, #181969, #164520, #171623 ) ) ;
#113155=EDGE_CURVE ( 'NONE', #172714, #162071, #42086, .T. ) ;
#113239=DIRECTION ( 'NONE',  ( 0.000000000000000000, 1.776356839400308446E-15, -1.000000000000000000 ) ) ;
#113246=DIRECTION ( 'NONE',  ( 0.000000000000000000, -1.000000000000000000, 0.000000000000000000 ) ) ;
#113257=CARTESIAN_POINT ( 'NONE',  ( -20.64999999999999858, -9.399999999988846611, -124.1060308773475924 ) ) ;
#113272=EDGE_CURVE ( 'NONE', #210115, #240059, #177947, .T. ) ;
#113315=ADVANCED_FACE ( 'NONE', ( #225693 ), #179243, .F. ) ;
#113318=DIRECTION ( 'NONE',  ( 1.000000000000000000, 0.000000000000000000, -0.000000000000000000 ) ) ;
#113328=DIRECTION ( 'NONE',  ( -0.000000000000000000, -0.000000000000000000, 1.000000000000000000 ) ) ;
#113338=LINE ( 'NONE', #192887, #86784 ) ;
#113357=ORIENTED_EDGE ( 'NONE', *, *, #183609, .T. ) ;
#113403=CARTESIAN_POINT ( 'NONE',  ( 18.39999999999999858, -9.682403433465237796, -140.6568433774128266 ) ) ;
#113412=AXIS2_PLACEMENT_3D ( 'NONE', #242480, #202086, #85949 ) ;
#113413=ORIENTED_EDGE ( 'NONE', *, *, #35793, .T. ) ;
#113414=EDGE_LOOP ( 'NONE', ( #168980, #230651, #190042, #103131 ) ) ;
#113417=DIRECTION ( 'NONE',  ( -1.000000000000000000, -0.000000000000000000, -0.000000000000000000 ) ) ;
#113427=FACE_OUTER_BOUND ( 'NONE', #47924, .T. ) ;
#113429=CIRCLE ( 'NONE', #46769, 0.1000000000000028644 ) ;
#113436=CARTESIAN_POINT ( 'NONE',  ( 22.60000000000000142, 0.04781839071596408891, -88.74997758095283018 ) ) ;
#113450=CARTESIAN_POINT ( 'NONE',  ( 20.94983749550516450, 10.29766095125282810, -139.4743663933276139 ) ) ;
#113452=ORIENTED_EDGE ( 'NONE', *, *, #200336, .T. ) ;
#113456=ADVANCED_FACE ( 'NONE', ( #211305 ), #130474, .T. ) ;
#113481=VECTOR ( 'NONE', #100118, 1000.000000000000000 ) ;
#113483=AXIS2_PLACEMENT_3D ( 'NONE', #257931, #78056, #119787 ) ;
#113491=ORIENTED_EDGE ( 'NONE', *, *, #85724, .T. ) ;
#113514=CARTESIAN_POINT ( 'NONE',  ( -23.25000000000000000, -1.851617760457748618, -145.6031897196037050 ) ) ;
#113518=VERTEX_POINT ( 'NONE', #178626 ) ;
#113524=ORIENTED_EDGE ( 'NONE', *, *, #183003, .T. ) ;
#113531=CARTESIAN_POINT ( 'NONE',  ( 23.25000000000000000, -9.599999999988849453, -88.75000000000004263 ) ) ;
#113561=CARTESIAN_POINT ( 'NONE',  ( 21.15000000000000213, 8.786607556611267356, -112.7500000000000284 ) ) ;
#113577=ADVANCED_FACE ( 'NONE', ( #3811 ), #143310, .F. ) ;
#113592=CARTESIAN_POINT ( 'NONE',  ( -23.25000000000000000, -1.851617760457748618, -145.6031897196037050 ) ) ;
#113599=CARTESIAN_POINT ( 'NONE',  ( -23.25000000000000000, -1.835859311432481045, -145.5044391687985694 ) ) ;
#113620=EDGE_LOOP ( 'NONE', ( #185572, #29612, #15584, #242517 ) ) ;
#113625=CIRCLE ( 'NONE', #146916, 0.09999999999998898659 ) ;
#113627=CARTESIAN_POINT ( 'NONE',  ( 21.05000000000000071, 1.115600667400684642E-11, -100.5000000000000284 ) ) ;
#113653=SPHERICAL_SURFACE ( 'NONE', #38281, 0.1000000000000000056 ) ;
#113674=ORIENTED_EDGE ( 'NONE', *, *, #93260, .F. ) ;
#113698=PLANE ( 'NONE',  #89300 ) ;
#113705=CYLINDRICAL_SURFACE ( 'NONE', #74179, 0.09999999999998898659 ) ;
#113747=EDGE_CURVE ( 'NONE', #7281, #142411, #196540, .T. ) ;
#113797=VERTEX_POINT ( 'NONE', #169344 ) ;
#113823=CARTESIAN_POINT ( 'NONE',  ( 23.14999999999999858, 1.115600667400684642E-11, -134.0000000000000284 ) ) ;
#113863=CARTESIAN_POINT ( 'NONE',  ( -21.65000000000000213, 7.750000000011155521, -112.8500000000000369 ) ) ;
#113868=AXIS2_PLACEMENT_3D ( 'NONE', #77201, #254534, #116354 ) ;
#113877=DIRECTION ( 'NONE',  ( 0.000000000000000000, -4.336808689942494997E-15, -1.000000000000000000 ) ) ;
#113885=ORIENTED_EDGE ( 'NONE', *, *, #42449, .T. ) ;
#113891=ADVANCED_FACE ( 'NONE', ( #217390 ), #115743, .F. ) ;
#113899=DIRECTION ( 'NONE',  ( -1.000000000000000000, 0.000000000000000000, 0.000000000000000000 ) ) ;
#113901=CARTESIAN_POINT ( 'NONE',  ( -23.15000000000000213, 1.115600667400684642E-11, -122.2000000000000313 ) ) ;
#113908=EDGE_CURVE ( 'NONE', #246634, #6219, #125799, .T. ) ;
#113940=DIRECTION ( 'NONE',  ( -3.265361837132813093E-16, 1.000000000000000000, -0.000000000000000000 ) ) ;
#113974=CARTESIAN_POINT ( 'NONE',  ( 22.50000000000000000, 1.115600667400684642E-11, -100.5000000000000284 ) ) ;
#113978=CIRCLE ( 'NONE', #230532, 4.049999999999998934 ) ;
#113987=CARTESIAN_POINT ( 'NONE',  ( 23.14999999999999858, 1.115600667400684642E-11, -134.0000000000000284 ) ) ;
#114015=FACE_OUTER_BOUND ( 'NONE', #191491, .T. ) ;
#114018=DIRECTION ( 'NONE',  ( 0.000000000000000000, 0.000000000000000000, -1.000000000000000000 ) ) ;
#114055=EDGE_CURVE ( 'NONE', #188850, #109895, #121738, .T. ) ;
#114064=DIRECTION ( 'NONE',  ( -1.000000000000000000, -0.000000000000000000, -0.000000000000000000 ) ) ;
#114076=VERTEX_POINT ( 'NONE', #140425 ) ;
#114079=EDGE_CURVE ( 'NONE', #80843, #16782, #217376, .T. ) ;
#114122=FACE_OUTER_BOUND ( 'NONE', #243247, .T. ) ;
#114128=DIRECTION ( 'NONE',  ( -0.000000000000000000, -0.1298341882519737922, -0.9915357197604890427 ) ) ;
#114165=EDGE_LOOP ( 'NONE', ( #201794, #200303, #43439, #34211 ) ) ;
#114167=DIRECTION ( 'NONE',  ( 0.000000000000000000, 0.000000000000000000, -1.000000000000000000 ) ) ;
#114183=AXIS2_PLACEMENT_3D ( 'NONE', #108421, #247915, #71874 ) ;
#114191=ADVANCED_FACE ( 'NONE', ( #6047 ), #188548, .T. ) ;
#114193=ORIENTED_EDGE ( 'NONE', *, *, #216837, .F. ) ;
#114196=CARTESIAN_POINT ( 'NONE',  ( 20.94999999999999929, -1.349153571964892606, -141.7874973355899328 ) ) ;
#114212=ORIENTED_EDGE ( 'NONE', *, *, #161341, .T. ) ;
#114228=CARTESIAN_POINT ( 'NONE',  ( -20.64999999999999858, 4.350000000011156054, -121.6500000000000341 ) ) ;
#114232=VERTEX_POINT ( 'NONE', #225084 ) ;
#114236=ORIENTED_EDGE ( 'NONE', *, *, #6621, .T. ) ;
#114238=VECTOR ( 'NONE', #172737, 1000.000000000000000 ) ;
#114249=DIRECTION ( 'NONE',  ( -1.000000000000000000, -0.000000000000000000, -0.000000000000000000 ) ) ;
#114255=ORIENTED_EDGE ( 'NONE', *, *, #228199, .T. ) ;
#114258=CIRCLE ( 'NONE', #35197, 0.09999999999999939493 ) ;
#114262=CARTESIAN_POINT ( 'NONE',  ( 21.05000000000000071, 4.850467289730772791, -112.5342674090017141 ) ) ;
#114290=CARTESIAN_POINT ( 'NONE',  ( -21.05000000000000071, 1.851028230152016674, -112.1539132694225316 ) ) ;
#114307=CIRCLE ( 'NONE', #222044, 0.1000000000000028644 ) ;
#114312=EDGE_CURVE ( 'NONE', #190717, #167341, #188353, .T. ) ;
#114325=ORIENTED_EDGE ( 'NONE', *, *, #67360, .T. ) ;
#114354=CARTESIAN_POINT ( 'NONE',  ( -20.64999999999999858, 1.115600667400684642E-11, -134.0000000000000284 ) ) ;
#114356=CARTESIAN_POINT ( 'NONE',  ( 21.05995757104869526, 8.775389244732430427, -112.6949051229912442 ) ) ;
#114374=EDGE_LOOP ( 'NONE', ( #215801, #108587, #85706, #46099 ) ) ;
#114453=CARTESIAN_POINT ( 'NONE',  ( 21.30000000000002558, 1.115650265596050101E-11, -96.45000000000003126 ) ) ;
#114494=ORIENTED_EDGE ( 'NONE', *, *, #77880, .T. ) ;
#114529=ORIENTED_EDGE ( 'NONE', *, *, #158121, .F. ) ;
#114550=VERTEX_POINT ( 'NONE', #251824 ) ;
#114597=DIRECTION ( 'NONE',  ( -6.938893903907224433E-15, 1.000000000000000000, 0.000000000000000000 ) ) ;
#114609=AXIS2_PLACEMENT_3D ( 'NONE', #82714, #183153, #21516 ) ;
#114613=FACE_OUTER_BOUND ( 'NONE', #162120, .T. ) ;
#114615=EDGE_CURVE ( 'NONE', #72909, #168030, #71922, .T. ) ;
#114653=CARTESIAN_POINT ( 'NONE',  ( -20.94999999999999929, -1.362429037182149694, -141.8888812479212334 ) ) ;
#114658=DIRECTION ( 'NONE',  ( 0.000000000000000000, -1.000000000000000000, -0.000000000000000000 ) ) ;
#114672=CIRCLE ( 'NONE', #73196, 0.1000000000000002554 ) ;
#114682=ORIENTED_EDGE ( 'NONE', *, *, #172152, .T. ) ;
#114683=CARTESIAN_POINT ( 'NONE',  ( 18.33996824403501691, -9.569639859420098205, -140.8190656375171272 ) ) ;
#114689=CARTESIAN_POINT ( 'NONE',  ( -23.15000000000000213, 11.65000000001115588, -112.6500000000000341 ) ) ;
#114693=EDGE_LOOP ( 'NONE', ( #1022, #12387, #94812, #232950 ) ) ;
#114712=CARTESIAN_POINT ( 'NONE',  ( -22.41119224318417125, 1.115600667400684642E-11, -88.85042919245522341 ) ) ;
#114720=CARTESIAN_POINT ( 'NONE',  ( -21.05000000000000071, -11.48912529306490349, -103.4000000000000341 ) ) ;
#114734=EDGE_CURVE ( 'NONE', #240059, #119449, #97855, .T. ) ;
#114749=DIRECTION ( 'NONE',  ( -1.000000000000000000, 7.304098846218135653E-16, 0.000000000000000000 ) ) ;
#114752=DIRECTION ( 'NONE',  ( 1.000000000000000000, 0.000000000000000000, -0.000000000000000000 ) ) ;
#114762=FACE_OUTER_BOUND ( 'NONE', #47445, .T. ) ;
#114797=ORIENTED_EDGE ( 'NONE', *, *, #139284, .T. ) ;
#114800=CARTESIAN_POINT ( 'NONE',  ( 21.05000000000000071, 1.115649653272650466E-11, -130.0000000000000284 ) ) ;
#114813=AXIS2_PLACEMENT_3D ( 'NONE', #118897, #39374, #155479 ) ;
#114820=CARTESIAN_POINT ( 'NONE',  ( -23.25000000000000000, 1.115600667400684642E-11, -137.9000000000000341 ) ) ;
#114842=EDGE_LOOP ( 'NONE', ( #96639, #219454, #88085, #253581 ) ) ;
#114902=DIRECTION ( 'NONE',  ( 0.000000000000000000, 0.000000000000000000, -1.000000000000000000 ) ) ;
#114911=VERTEX_POINT ( 'NONE', #104287 ) ;
#114945=ORIENTED_EDGE ( 'NONE', *, *, #135893, .F. ) ;
#114983=ORIENTED_EDGE ( 'NONE', *, *, #60201, .T. ) ;
#115001=CARTESIAN_POINT ( 'NONE',  ( -21.08134388332232589, 0.07581891751813445157, -94.16531941948205997 ) ) ;
#115008=ORIENTED_EDGE ( 'NONE', *, *, #32053, .F. ) ;
#115014=VERTEX_POINT ( 'NONE', #212413 ) ;
#115018=CARTESIAN_POINT ( 'NONE',  ( 21.05000000000000071, -1.162701749926853712, -108.4000000000000341 ) ) ;
#115021=CARTESIAN_POINT ( 'NONE',  ( 18.39999999999999858, -9.599999999988845900, -140.6001893912220737 ) ) ;
#115027=SPHERICAL_SURFACE ( 'NONE', #35731, 0.1000000000000000056 ) ;
#115052=EDGE_CURVE ( 'NONE', #135846, #198608, #126364, .T. ) ;
#115058=ORIENTED_EDGE ( 'NONE', *, *, #9540, .F. ) ;
#115060=VECTOR ( 'NONE', #56799, 1000.000000000000227 ) ;
#115069=PLANE ( 'NONE',  #98589 ) ;
#115096=DIRECTION ( 'NONE',  ( 1.000000000000000000, -0.000000000000000000, -0.000000000000000000 ) ) ;
#115097=EDGE_CURVE ( 'NONE', #78774, #74786, #197087, .T. ) ;
#115104=CARTESIAN_POINT ( 'NONE',  ( 18.59999999999999432, -1.835859311432481045, -145.5044391687985694 ) ) ;
#115106=CARTESIAN_POINT ( 'NONE',  ( -21.44999999999999929, 7.350000000011155166, -121.6500000000000341 ) ) ;
#115118=DIRECTION ( 'NONE',  ( -0.000000000000000000, 0.000000000000000000, 1.000000000000000000 ) ) ;
#115167=CIRCLE ( 'NONE', #198547, 0.2000000000000057288 ) ;
#115187=CARTESIAN_POINT ( 'NONE',  ( -22.59999999999999787, 0.1008583691098682150, -88.75043287651064361 ) ) ;
#115261=CIRCLE ( 'NONE', #215226, 0.2000000000000005107 ) ;
#115272=DIRECTION ( 'NONE',  ( 7.304098846218134667E-16, -1.000000000000000000, 0.000000000000000000 ) ) ;
#115280=VECTOR ( 'NONE', #53969, 999.9999999999998863 ) ;
#115282=CARTESIAN_POINT ( 'NONE',  ( 23.14999999999999858, 5.000000000011153745, -121.5947339810869465 ) ) ;
#115284=DIRECTION ( 'NONE',  ( -1.000000000000000000, -0.000000000000000000, -0.000000000000000000 ) ) ;
#115346=CIRCLE ( 'NONE', #148699, 0.5000000000000004441 ) ;
#115377=CARTESIAN_POINT ( 'NONE',  ( -23.15000000000000213, -8.999999999988846255, -109.8939691226524786 ) ) ;
#115390=EDGE_CURVE ( 'NONE', #38731, #224903, #39089, .T. ) ;
#115394=ORIENTED_EDGE ( 'NONE', *, *, #92308, .T. ) ;
#115443=ADVANCED_FACE ( 'NONE', ( #1680 ), #192625, .F. ) ;
#115449=EDGE_CURVE ( 'NONE', #129536, #243362, #30712, .T. ) ;
#115468=CIRCLE ( 'NONE', #236279, 4.300000000000025580 ) ;
#115476=CARTESIAN_POINT ( 'NONE',  ( -20.54999999999999716, 2.000000000011154189, -113.2246219227621395 ) ) ;
#115484=CARTESIAN_POINT ( 'NONE',  ( -20.94999999999999929, -1.835341550213255957, -112.0551512925630107 ) ) ;
#115505=AXIS2_PLACEMENT_3D ( 'NONE', #198138, #78178, #100301 ) ;
#115524=CARTESIAN_POINT ( 'NONE',  ( 18.59999999999999076, 11.65000000001115943, -88.75000000000004263 ) ) ;
#115529=DIRECTION ( 'NONE',  ( -1.000000000000000000, -0.000000000000000000, -0.000000000000000000 ) ) ;
#115530=DIRECTION ( 'NONE',  ( 1.000000000000000000, 0.000000000000000000, 0.000000000000000000 ) ) ;
#115582=CIRCLE ( 'NONE', #223724, 0.09999999999999892308 ) ;
#115595=DIRECTION ( 'NONE',  ( 1.000000000000000000, 1.836970198721029934E-16, 3.186635328391151676E-31 ) ) ;
#115611=ADVANCED_FACE ( 'NONE', ( #17128 ), #117611, .F. ) ;
#115641=AXIS2_PLACEMENT_3D ( 'NONE', #209955, #187828, #206090 ) ;
#115658=ORIENTED_EDGE ( 'NONE', *, *, #47715, .F. ) ;
#115661=CYLINDRICAL_SURFACE ( 'NONE', #96082, 4.000000000000003553 ) ;
#115668=EDGE_CURVE ( 'NONE', #161835, #186134, #251854, .T. ) ;
#115692=DIRECTION ( 'NONE',  ( 0.000000000000000000, 5.329070518200686707E-15, 1.000000000000000000 ) ) ;
#115697=ORIENTED_EDGE ( 'NONE', *, *, #239012, .F. ) ;
#115698=CARTESIAN_POINT ( 'NONE',  ( 18.49999999999999645, -1.866714910046153308, -112.2526752462820525 ) ) ;
#115731=CIRCLE ( 'NONE', #207323, 0.09999999999999939493 ) ;
#115743=CYLINDRICAL_SURFACE ( 'NONE', #46688, 0.09999999999998898659 ) ;
#115754=DIRECTION ( 'NONE',  ( 0.000000000000000000, -1.000000000000000000, 0.000000000000000000 ) ) ;
#115761=EDGE_CURVE ( 'NONE', #224344, #253301, #88548, .T. ) ;
#115762=DIRECTION ( 'NONE',  ( 0.000000000000000000, 0.9654727137038715545, -0.2605042016806676242 ) ) ;
#115784=CARTESIAN_POINT ( 'NONE',  ( 21.05000000000000071, -8.999999999988844479, -110.3939691226524786 ) ) ;
#115792=ORIENTED_EDGE ( 'NONE', *, *, #35118, .F. ) ;
#115816=TOROIDAL_SURFACE ( 'NONE', #3349, 6.258578643762700899, 0.1000000000000000056 ) ;
#115820=DIRECTION ( 'NONE',  ( 0.000000000000000000, -0.8660254037844411501, -0.4999999999999956146 ) ) ;
#115822=ADVANCED_FACE ( 'NONE', ( #159205 ), #200874, .F. ) ;
#115834=EDGE_CURVE ( 'NONE', #185932, #8739, #21935, .T. ) ;
#115838=EDGE_LOOP ( 'NONE', ( #173975, #93558, #57745, #149194 ) ) ;
#115855=FACE_OUTER_BOUND ( 'NONE', #114374, .T. ) ;
#115882=CARTESIAN_POINT ( 'NONE',  ( 18.59999999999999076, -1.164121893230052995, -141.9148480855716343 ) ) ;
#115935=CARTESIAN_POINT ( 'NONE',  ( 23.25000000000000000, -11.48912529306489994, -130.9000000000000341 ) ) ;
#115938=CIRCLE ( 'NONE', #111652, 0.09999999999998807065 ) ;
#115973=ADVANCED_FACE ( 'NONE', ( #114613 ), #52050, .T. ) ;
#115991=TOROIDAL_SURFACE ( 'NONE', #178353, 0.2000000000000000111, 0.1000000000000000056 ) ;
#115995=AXIS2_PLACEMENT_3D ( 'NONE', #153966, #11861, #70559 ) ;
#116001=CARTESIAN_POINT ( 'NONE',  ( 23.15000000000000213, -11.64999999998883595, -130.9000000000000341 ) ) ;
#116002=CARTESIAN_POINT ( 'NONE',  ( -18.50000000000000000, -9.399999999988850163, -107.7972597596633193 ) ) ;
#116010=EDGE_CURVE ( 'NONE', #172714, #17513, #180330, .T. ) ;
#116036=VECTOR ( 'NONE', #190510, 1000.000000000000000 ) ;
#116046=CARTESIAN_POINT ( 'NONE',  ( -21.64999999999999858, 7.350000000011155166, -121.7500000000000426 ) ) ;
#116051=AXIS2_PLACEMENT_3D ( 'NONE', #59383, #219766, #104925 ) ;
#116109=LINE ( 'NONE', #195658, #18066 ) ;
#116113=EDGE_CURVE ( 'NONE', #97776, #117118, #33445, .T. ) ;
#116126=EDGE_CURVE ( 'NONE', #246420, #100043, #1430, .T. ) ;
#116165=DIRECTION ( 'NONE',  ( 1.000000000000000000, 0.000000000000000000, -0.000000000000000000 ) ) ;
#116175=ORIENTED_EDGE ( 'NONE', *, *, #131018, .F. ) ;
#116179=ADVANCED_FACE ( 'NONE', ( #20665 ), #143136, .T. ) ;
#116219=ADVANCED_FACE ( 'NONE', ( #187433 ), #127449, .T. ) ;
#116222=CARTESIAN_POINT ( 'NONE',  ( 20.94999999999999929, 1.115600667400684642E-11, -131.1000000000000227 ) ) ;
#116261=ORIENTED_EDGE ( 'NONE', *, *, #132217, .T. ) ;
#116265=EDGE_CURVE ( 'NONE', #40869, #231259, #205686, .T. ) ;
#116280=CARTESIAN_POINT ( 'NONE',  ( 20.85000000000000142, -11.74999999998883560, -131.1000000000000227 ) ) ;
#116303=ORIENTED_EDGE ( 'NONE', *, *, #78876, .F. ) ;
#116306=DIRECTION ( 'NONE',  ( -1.000000000000000000, 0.000000000000000000, 0.000000000000000000 ) ) ;
#116315=EDGE_CURVE ( 'NONE', #50700, #237460, #70068, .T. ) ;
#116327=DIRECTION ( 'NONE',  ( 1.000000000000000000, 0.000000000000000000, 0.000000000000000000 ) ) ;
#116339=DIRECTION ( 'NONE',  ( 0.000000000000000000, -1.000000000000000000, 0.000000000000000000 ) ) ;
#116354=DIRECTION ( 'NONE',  ( 0.000000000000000000, 0.000000000000000000, 1.000000000000000000 ) ) ;
#116362=ORIENTED_EDGE ( 'NONE', *, *, #228510, .T. ) ;
#116383=CARTESIAN_POINT ( 'NONE',  ( 20.97239005616515684, 8.874843841361279573, -112.7501528021532238 ) ) ;
#116385=DIRECTION ( 'NONE',  ( 1.000000000000000000, 0.000000000000000000, 0.000000000000000000 ) ) ;
#116397=ORIENTED_EDGE ( 'NONE', *, *, #13208, .F. ) ;
#116399=DIRECTION ( 'NONE',  ( 1.000000000000000000, 2.952720810173289112E-16, -0.000000000000000000 ) ) ;
#116456=CIRCLE ( 'NONE', #212321, 0.09999999999999939493 ) ;
#116457=CARTESIAN_POINT ( 'NONE',  ( 21.14999999999999858, 6.540656951712400691, -100.5000000000000284 ) ) ;
#116471=DIRECTION ( 'NONE',  ( 2.715809747126116508E-16, -1.000000000000000000, 0.000000000000000000 ) ) ;
#116531=CIRCLE ( 'NONE', #229137, 0.09999999999998898659 ) ;
#116533=VECTOR ( 'NONE', #86755, 1000.000000000000000 ) ;
#116563=VECTOR ( 'NONE', #28705, 1000.000000000000000 ) ;
#116567=DIRECTION ( 'NONE',  ( 1.000000000000000000, -0.000000000000000000, -0.000000000000000000 ) ) ;
#116606=EDGE_CURVE ( 'NONE', #241144, #173164, #222172, .T. ) ;
#116609=LINE ( 'NONE', #176605, #33550 ) ;
#116625=CARTESIAN_POINT ( 'NONE',  ( 21.05000000000000071, 1.115486826172573664E-11, -93.95934304829879125 ) ) ;
#116635=ORIENTED_EDGE ( 'NONE', *, *, #154094, .T. ) ;
#116653=FACE_OUTER_BOUND ( 'NONE', #28682, .T. ) ;
#116677=SPHERICAL_SURFACE ( 'NONE', #254548, 0.1000000000000000056 ) ;
#116678=ORIENTED_EDGE ( 'NONE', *, *, #165988, .T. ) ;
#116683=DIRECTION ( 'NONE',  ( -1.000000000000000000, -2.952720810173289112E-16, 0.000000000000000000 ) ) ;
#116689=VECTOR ( 'NONE', #159648, 1000.000000000000000 ) ;
#116720=ORIENTED_EDGE ( 'NONE', *, *, #68615, .T. ) ;
#116726=CARTESIAN_POINT ( 'NONE',  ( -21.11825140030088122, 6.445407565431050756, -100.4927963793672205 ) ) ;
#116742=CIRCLE ( 'NONE', #112652, 0.09999999999999939493 ) ;
#116747=CARTESIAN_POINT ( 'NONE',  ( -20.94999999999999929, 7.120270961708750512, -137.6595630418393625 ) ) ;
#116768=FACE_OUTER_BOUND ( 'NONE', #3614, .T. ) ;
#116771=DIRECTION ( 'NONE',  ( 1.000000000000000000, 3.265361837132813093E-16, -0.000000000000000000 ) ) ;
#116795=AXIS2_PLACEMENT_3D ( 'NONE', #204938, #185395, #6755 ) ;
#116810=EDGE_CURVE ( 'NONE', #83522, #151223, #69754, .T. ) ;
#116815=VERTEX_POINT ( 'NONE', #13617 ) ;
#116822=EDGE_CURVE ( 'NONE', #8739, #17513, #12354, .T. ) ;
#116835=DIRECTION ( 'NONE',  ( 1.000000000000000000, -0.000000000000000000, -0.000000000000000000 ) ) ;
#116846=EDGE_LOOP ( 'NONE', ( #10729, #75136, #137492, #128493 ) ) ;
#116896=VERTEX_POINT ( 'NONE', #232679 ) ;
#116909=LINE ( 'NONE', #131334, #75117 ) ;
#116933=ORIENTED_EDGE ( 'NONE', *, *, #223325, .F. ) ;
#116934=EDGE_LOOP ( 'NONE', ( #24453, #5011, #123285, #190029 ) ) ;
#116993=DIRECTION ( 'NONE',  ( 1.000000000000000000, -0.000000000000000000, -0.000000000000000000 ) ) ;
#117010=LINE ( 'NONE', #218658, #77412 ) ;
#117020=FACE_OUTER_BOUND ( 'NONE', #202430, .T. ) ;
#117024=EDGE_CURVE ( 'NONE', #111426, #26411, #142221, .T. ) ;
#117032=CYLINDRICAL_SURFACE ( 'NONE', #237975, 0.1000000000000028644 ) ;
#117052=DIRECTION ( 'NONE',  ( 0.000000000000000000, 3.552713678800446104E-15, -1.000000000000000000 ) ) ;
#117061=VECTOR ( 'NONE', #143710, 1000.000000000000000 ) ;
#117064=DIRECTION ( 'NONE',  ( 0.000000000000000000, 0.000000000000000000, -1.000000000000000000 ) ) ;
#117079=VECTOR ( 'NONE', #245301, 1000.000000000000000 ) ;
#117115=ORIENTED_EDGE ( 'NONE', *, *, #92615, .T. ) ;
#117118=VERTEX_POINT ( 'NONE', #127810 ) ;
#117169=CARTESIAN_POINT ( 'NONE',  ( -21.64999999999999858, 7.250000000011148416, -121.7500000000000426 ) ) ;
#117176=LINE ( 'NONE', #201836, #125162 ) ;
#117194=CARTESIAN_POINT ( 'NONE',  ( 21.05933563467872460, 10.72452471209247626, -112.6936477489559820 ) ) ;
#117196=DIRECTION ( 'NONE',  ( 1.000000000000000000, 0.000000000000000000, 0.000000000000000000 ) ) ;
#117200=ORIENTED_EDGE ( 'NONE', *, *, #257494, .T. ) ;
#117238=DIRECTION ( 'NONE',  ( 0.000000000000000000, 0.000000000000000000, -1.000000000000000000 ) ) ;
#117274=CARTESIAN_POINT ( 'NONE',  ( -20.94999999999999929, 1.115600667400684642E-11, -129.9000000000000341 ) ) ;
#117285=CARTESIAN_POINT ( 'NONE',  ( -22.45372860728439690, 0.01492061955964464268, -88.85020286529615419 ) ) ;
#117298=FACE_OUTER_BOUND ( 'NONE', #12547, .T. ) ;
#117311=CIRCLE ( 'NONE', #104786, 0.5999999999999998668 ) ;
#117323=FACE_OUTER_BOUND ( 'NONE', #87263, .T. ) ;
#117357=FACE_OUTER_BOUND ( 'NONE', #74719, .T. ) ;
#117367=ORIENTED_EDGE ( 'NONE', *, *, #42305, .T. ) ;
#117378=TOROIDAL_SURFACE ( 'NONE', #13327, 11.65000000000000036, 0.1000000000000000056 ) ;
#117393=DIRECTION ( 'NONE',  ( 0.000000000000000000, 0.000000000000000000, -1.000000000000000000 ) ) ;
#117420=ORIENTED_EDGE ( 'NONE', *, *, #83520, .T. ) ;
#117430=ORIENTED_EDGE ( 'NONE', *, *, #74826, .T. ) ;
#117440=CARTESIAN_POINT ( 'NONE',  ( 20.94999999999999574, -11.48912529306490349, -103.6000000000000369 ) ) ;
#117450=AXIS2_PLACEMENT_3D ( 'NONE', #66353, #110608, #166769 ) ;
#117498=CARTESIAN_POINT ( 'NONE',  ( -20.94999999999999929, 7.021664781911246322, -137.6335654018973287 ) ) ;
#117514=ORIENTED_EDGE ( 'NONE', *, *, #164212, .F. ) ;
#117520=CARTESIAN_POINT ( 'NONE',  ( -22.50000000000000000, 1.115600667400684642E-11, -100.5000000000000284 ) ) ;
#117542=EDGE_LOOP ( 'NONE', ( #168850, #99901, #63134, #177144 ) ) ;
#117546=ORIENTED_EDGE ( 'NONE', *, *, #170538, .F. ) ;
#117550=DIRECTION ( 'NONE',  ( -1.000000000000000000, 0.000000000000000000, 0.000000000000000000 ) ) ;
#117564=ORIENTED_EDGE ( 'NONE', *, *, #207992, .T. ) ;
#117569=CARTESIAN_POINT ( 'NONE',  ( -21.14999999999999858, 1.115600667400684642E-11, -93.95934304829879125 ) ) ;
#117611=TOROIDAL_SURFACE ( 'NONE', #5148, 12.97499999999999787, 0.1000000000000000056 ) ;
#117618=LINE ( 'NONE', #197141, #247029 ) ;
#117630=ORIENTED_EDGE ( 'NONE', *, *, #201740, .F. ) ;
#117648=ADVANCED_FACE ( 'NONE', ( #173084 ), #233030, .T. ) ;
#117662=EDGE_LOOP ( 'NONE', ( #199270, #209312, #245656, #116261, #161813, #234391, #241555, #82497, #242694, #104507 ) ) ;
#117671=EDGE_CURVE ( 'NONE', #236424, #189704, #116909, .T. ) ;
#117675=DIRECTION ( 'NONE',  ( 1.000000000000000000, 0.000000000000000000, -0.000000000000000000 ) ) ;
#117676=EDGE_CURVE ( 'NONE', #172714, #185932, #96045, .T. ) ;
#117679=CARTESIAN_POINT ( 'NONE',  ( -18.55121869061588669, 10.32747123227773045, -139.5774032850249569 ) ) ;
#117694=CARTESIAN_POINT ( 'NONE',  ( -18.50000000000000000, -9.499999999988849808, -88.75000000000004263 ) ) ;
#117716=LINE ( 'NONE', #214259, #188940 ) ;
#117723=CIRCLE ( 'NONE', #109321, 0.09999999999998898659 ) ;
#117744=DIRECTION ( 'NONE',  ( -2.940209281316621509E-16, 1.000000000000000000, 1.176083712526648603E-15 ) ) ;
#117751=CARTESIAN_POINT ( 'NONE',  ( -23.25000000000000000, 11.65000000001115588, -121.7500000000000426 ) ) ;
#117761=TOROIDAL_SURFACE ( 'NONE', #113483, 0.2000000000000000111, 0.1000000000000000056 ) ;
#117780=AXIS2_PLACEMENT_3D ( 'NONE', #234556, #113328, #72953 ) ;
#117817=CARTESIAN_POINT ( 'NONE',  ( 23.24999999999999645, 1.115600667400684642E-11, -134.0000000000000284 ) ) ;
#117831=LINE ( 'NONE', #197367, #193815 ) ;
#117880=DIRECTION ( 'NONE',  ( 0.000000000000000000, 3.552713678800509607E-15, 1.000000000000000000 ) ) ;
#117900=ORIENTED_EDGE ( 'NONE', *, *, #69057, .F. ) ;
#117903=ORIENTED_EDGE ( 'NONE', *, *, #126515, .F. ) ;
#117928=ORIENTED_EDGE ( 'NONE', *, *, #27920, .F. ) ;
#117946=DIRECTION ( 'NONE',  ( 0.000000000000000000, 1.000000000000000000, 2.891205793294679805E-16 ) ) ;
#117992=VECTOR ( 'NONE', #253797, 1000.000000000000000 ) ;
#118003=DIRECTION ( 'NONE',  ( 0.000000000000000000, 1.224646799142185182E-16, 1.000000000000000000 ) ) ;
#118018=CARTESIAN_POINT ( 'NONE',  ( 23.14999999999998437, 1.115600667400684642E-11, -100.5000000000000284 ) ) ;
#118074=ADVANCED_FACE ( 'NONE', ( #88878 ), #225815, .T. ) ;
#118077=AXIS2_PLACEMENT_3D ( 'NONE', #152775, #94040, #190603 ) ;
#118081=CIRCLE ( 'NONE', #89035, 0.1000000000000028644 ) ;
#118092=DIRECTION ( 'NONE',  ( -0.000000000000000000, 0.000000000000000000, 1.000000000000000000 ) ) ;
#118105=FACE_OUTER_BOUND ( 'NONE', #522, .T. ) ;
#118109=ORIENTED_EDGE ( 'NONE', *, *, #153006, .F. ) ;
#118117=DIRECTION ( 'NONE',  ( 0.000000000000000000, -1.000000000000000000, 0.000000000000000000 ) ) ;
#118124=CARTESIAN_POINT ( 'NONE',  ( 21.05000000000000071, 6.413978881499639684, -100.5857991162744867 ) ) ;
#118133=DIRECTION ( 'NONE',  ( -0.000000000000000000, -0.000000000000000000, 1.000000000000000000 ) ) ;
#118145=DIRECTION ( 'NONE',  ( 1.000000000000000000, 0.000000000000000000, -0.000000000000000000 ) ) ;
#118171=DIRECTION ( 'NONE',  ( -0.000000000000000000, -0.000000000000000000, 1.000000000000000000 ) ) ;
#118173=ORIENTED_EDGE ( 'NONE', *, *, #27920, .T. ) ;
#118181=ORIENTED_EDGE ( 'NONE', *, *, #9014, .F. ) ;
#118188=ORIENTED_EDGE ( 'NONE', *, *, #38892, .F. ) ;
#118241=CARTESIAN_POINT ( 'NONE',  ( 20.94999999999999929, 5.000000000011153745, -122.0947339810869465 ) ) ;
#118242=CARTESIAN_POINT ( 'NONE',  ( -20.54999999999999716, 7.150000000011155876, -112.8500000000000369 ) ) ;
#118268=AXIS2_PLACEMENT_3D ( 'NONE', #180028, #176182, #1355 ) ;
#118306=VECTOR ( 'NONE', #101310, 1000.000000000000000 ) ;
#118321=B_SPLINE_CURVE_WITH_KNOTS ( 'NONE', 3,
 ( #232692, #31934, #90580, #250933, #52742, #111442, #91875, #168891, #12369, #248389 ),
 .UNSPECIFIED., .F., .F.,
 ( 4, 2, 2, 2, 4 ),
 ( 0.000000000000000000, 0.0001584437871625036642, 0.0002376656807437575833, 0.0002772766275343837433, 0.0003168875743250099304 ),
 .UNSPECIFIED. ) ;
#118327=CIRCLE ( 'NONE', #5861, 12.87500000000000000 ) ;
#118378=PLANE ( 'NONE',  #147329 ) ;
#118392=FACE_OUTER_BOUND ( 'NONE', #67038, .T. ) ;
#118393=CARTESIAN_POINT ( 'NONE',  ( -23.15000000000000213, 11.75000000001115552, -88.75000000000004263 ) ) ;
#118424=LINE ( 'NONE', #135391, #13031 ) ;
#118425=AXIS2_PLACEMENT_3D ( 'NONE', #31511, #207563, #91456 ) ;
#118434=EDGE_LOOP ( 'NONE', ( #95375, #198696, #101787, #41875 ) ) ;
#118450=ORIENTED_EDGE ( 'NONE', *, *, #239262, .F. ) ;
#118477=CARTESIAN_POINT ( 'NONE',  ( 20.94999999999999929, 1.115600667400684642E-11, -134.0000000000000284 ) ) ;
#118479=CARTESIAN_POINT ( 'NONE',  ( -1.739115166359751801E-14, 11.65000000001114699, -125.3500000000000512 ) ) ;
#118498=ORIENTED_EDGE ( 'NONE', *, *, #64866, .F. ) ;
#118506=ORIENTED_EDGE ( 'NONE', *, *, #137583, .T. ) ;
#118508=LINE ( 'NONE', #59767, #168649 ) ;
#118541=DIRECTION ( 'NONE',  ( 0.000000000000000000, 0.000000000000000000, -1.000000000000000000 ) ) ;
#118582=CARTESIAN_POINT ( 'NONE',  ( -23.15000000000000213, -11.48912529306489994, -131.0000000000000284 ) ) ;
#118620=ORIENTED_EDGE ( 'NONE', *, *, #191215, .T. ) ;
#118656=CIRCLE ( 'NONE', #31195, 0.1000000000000000472 ) ;
#118660=CARTESIAN_POINT ( 'NONE',  ( 18.50000000000000000, -10.35479209691423996, -127.7565409830737906 ) ) ;
#118661=CARTESIAN_POINT ( 'NONE',  ( 18.52928932304149967, 10.27928932305266407, -125.1762534328032217 ) ) ;
#118675=CARTESIAN_POINT ( 'NONE',  ( -20.64999999999999858, -8.999999999988846255, -110.3939691226524786 ) ) ;
#118717=CARTESIAN_POINT ( 'NONE',  ( 21.13461538461538680, 8.885417037985614996, -112.8500000000000369 ) ) ;
#118729=AXIS2_PLACEMENT_3D ( 'NONE', #190531, #28913, #170990 ) ;
#118739=CARTESIAN_POINT ( 'NONE',  ( -22.39999999999999858, 1.115486826172573664E-11, -88.85042919245522341 ) ) ;
#118747=DIRECTION ( 'NONE',  ( -1.000000000000000000, -0.000000000000000000, -0.000000000000000000 ) ) ;
#118808=EDGE_LOOP ( 'NONE', ( #66788, #193507, #44476, #109104 ) ) ;
#118809=EDGE_CURVE ( 'NONE', #188954, #124743, #33412, .T. ) ;
#118818=VERTEX_POINT ( 'NONE', #69485 ) ;
#118859=CIRCLE ( 'NONE', #60378, 0.09999999999998898659 ) ;
#118867=CIRCLE ( 'NONE', #218590, 0.1000000000000028644 ) ;
#118897=CARTESIAN_POINT ( 'NONE',  ( -20.94999999999999929, -11.48912529306490349, -103.4000000000000341 ) ) ;
#118946=CIRCLE ( 'NONE', #214593, 0.09999999999998898659 ) ;
#118952=EDGE_LOOP ( 'NONE', ( #118450, #217518, #41462, #148645 ) ) ;
#118953=ORIENTED_EDGE ( 'NONE', *, *, #257703, .T. ) ;
#118973=ORIENTED_EDGE ( 'NONE', *, *, #72199, .T. ) ;
#118995=AXIS2_PLACEMENT_3D ( 'NONE', #10620, #90126, #169728 ) ;
#119018=AXIS2_PLACEMENT_3D ( 'NONE', #79508, #3845, #42979 ) ;
#119020=FACE_OUTER_BOUND ( 'NONE', #205232, .T. ) ;
#119025=EDGE_CURVE ( 'NONE', #134210, #142111, #78443, .T. ) ;
#119031=DIRECTION ( 'NONE',  ( 2.840903330521633255E-16, -0.8700118002898322711, 0.4930308989875231696 ) ) ;
#119036=DIRECTION ( 'NONE',  ( 0.000000000000000000, 0.000000000000000000, -1.000000000000000000 ) ) ;
#119045=FACE_OUTER_BOUND ( 'NONE', #9407, .T. ) ;
#119046=CARTESIAN_POINT ( 'NONE',  ( -20.94999999999999929, -1.736257131586239844, -112.0686523290175245 ) ) ;
#119068=ORIENTED_EDGE ( 'NONE', *, *, #204131, .T. ) ;
#119073=AXIS2_PLACEMENT_3D ( 'NONE', #73062, #31366, #254205 ) ;
#119081=FACE_OUTER_BOUND ( 'NONE', #118434, .T. ) ;
#119100=AXIS2_PLACEMENT_3D ( 'NONE', #17624, #24091, #146557 ) ;
#119108=ORIENTED_EDGE ( 'NONE', *, *, #203726, .T. ) ;
#119114=CARTESIAN_POINT ( 'NONE',  ( -20.85000000000000142, 7.021664781911246322, -137.6335654018973287 ) ) ;
#119141=( GEOMETRIC_REPRESENTATION_CONTEXT ( 3 ) GLOBAL_UNCERTAINTY_ASSIGNED_CONTEXT ( ( #173258 ) ) GLOBAL_UNIT_ASSIGNED_CONTEXT ( ( #7251, #166378, #245884 ) ) REPRESENTATION_CONTEXT ( 'NONE', 'WORKASPACE' ) );
#119158=AXIS2_PLACEMENT_3D ( 'NONE', #67985, #105799, #47114 ) ;
#119186=ORIENTED_EDGE ( 'NONE', *, *, #158121, .T. ) ;
#119200=CARTESIAN_POINT ( 'NONE',  ( -20.94999999999999929, 7.021664781911246322, -137.8335654018973457 ) ) ;
#119218=ORIENTED_EDGE ( 'NONE', *, *, #171220, .F. ) ;
#119225=DIRECTION ( 'NONE',  ( 0.000000000000000000, 0.000000000000000000, -1.000000000000000000 ) ) ;
#119273=CARTESIAN_POINT ( 'NONE',  ( 21.05000000000000426, -0.01681986837452038863, -94.19257478043464005 ) ) ;
#119297=CARTESIAN_POINT ( 'NONE',  ( 20.95561247346651967, 10.59500736521470721, -108.0937827669816755 ) ) ;
#119322=ORIENTED_EDGE ( 'NONE', *, *, #225967, .T. ) ;
#119331=EDGE_CURVE ( 'NONE', #137137, #159306, #18176, .T. ) ;
#119349=ADVANCED_FACE ( 'NONE', ( #113427 ), #16907, .F. ) ;
#119356=ORIENTED_EDGE ( 'NONE', *, *, #116315, .T. ) ;
#119447=VECTOR ( 'NONE', #134281, 1000.000000000000000 ) ;
#119449=VERTEX_POINT ( 'NONE', #118582 ) ;
#119483=ORIENTED_EDGE ( 'NONE', *, *, #184261, .F. ) ;
#119492=CARTESIAN_POINT ( 'NONE',  ( 20.04142135623731136, 11.75000000001116263, -125.1500000000000341 ) ) ;
#119525=EDGE_LOOP ( 'NONE', ( #238636, #130027, #96056, #14954 ) ) ;
#119528=DIRECTION ( 'NONE',  ( 0.000000000000000000, 0.000000000000000000, -1.000000000000000000 ) ) ;
#119535=EDGE_CURVE ( 'NONE', #34846, #168030, #254473, .T. ) ;
#119568=DIRECTION ( 'NONE',  ( 1.000000000000000000, -0.000000000000000000, 0.000000000000000000 ) ) ;
#119593=AXIS2_PLACEMENT_3D ( 'NONE', #147659, #130653, #185502 ) ;
#119617=ORIENTED_EDGE ( 'NONE', *, *, #77922, .F. ) ;
#119619=ORIENTED_EDGE ( 'NONE', *, *, #188597, .T. ) ;
#119624=CARTESIAN_POINT ( 'NONE',  ( -20.64999999999999858, 7.250000000011155521, -121.7500000000000426 ) ) ;
#119625=CARTESIAN_POINT ( 'NONE',  ( -22.39999999999999858, 0.1000000000111554016, -100.5000000000000284 ) ) ;
#119665=CARTESIAN_POINT ( 'NONE',  ( 20.94999999999999929, -12.41227409413852811, -131.0000000000000284 ) ) ;
#119702=DIRECTION ( 'NONE',  ( -0.000000000000000000, -0.000000000000000000, 1.000000000000000000 ) ) ;
#119721=EDGE_LOOP ( 'NONE', ( #219450, #113117, #220986, #131592 ) ) ;
#119772=CIRCLE ( 'NONE', #65580, 0.09999999999999939493 ) ;
#119787=DIRECTION ( 'NONE',  ( -1.000000000000000000, -1.836970198721029934E-16, 0.000000000000000000 ) ) ;
#119807=DIRECTION ( 'NONE',  ( 0.000000000000000000, 0.000000000000000000, 1.000000000000000000 ) ) ;
#119821=CARTESIAN_POINT ( 'NONE',  ( -18.59999999999999787, 1.835341550235567887, -112.0551512925630249 ) ) ;
#119823=EDGE_CURVE ( 'NONE', #5450, #27558, #125331, .T. ) ;
#119828=EDGE_CURVE ( 'NONE', #118818, #253025, #63133, .T. ) ;
#119847=CIRCLE ( 'NONE', #228158, 11.65000000000000036 ) ;
#119856=ORIENTED_EDGE ( 'NONE', *, *, #240845, .T. ) ;
#119882=DIRECTION ( 'NONE',  ( 0.000000000000000000, 0.9908441862701596881, -0.1350103645451904977 ) ) ;
#119918=ADVANCED_FACE ( 'NONE', ( #9853 ), #64689, .T. ) ;
#119954=CARTESIAN_POINT ( 'NONE',  ( 18.58143601961908331, 10.43572941510574026, -125.2500000000000568 ) ) ;
#119956=CIRCLE ( 'NONE', #215581, 0.5000000000000004441 ) ;
#119978=CIRCLE ( 'NONE', #136480, 0.09999999999999939493 ) ;
#119980=CIRCLE ( 'NONE', #253209, 0.09999999999999749367 ) ;
#120021=ORIENTED_EDGE ( 'NONE', *, *, #223594, .T. ) ;
#120065=TOROIDAL_SURFACE ( 'NONE', #132505, 0.4000000000000005773, 0.1000000000000000056 ) ;
#120073=CARTESIAN_POINT ( 'NONE',  ( -23.25000000000000000, -11.74999999998884448, -100.5000000000000284 ) ) ;
#120087=ORIENTED_EDGE ( 'NONE', *, *, #3682, .T. ) ;
#120088=ORIENTED_EDGE ( 'NONE', *, *, #86594, .F. ) ;
#120095=EDGE_CURVE ( 'NONE', #238954, #111525, #181462, .T. ) ;
#120096=CIRCLE ( 'NONE', #3520, 4.000000000000003553 ) ;
#120100=ORIENTED_EDGE ( 'NONE', *, *, #143546, .T. ) ;
#120105=AXIS2_PLACEMENT_3D ( 'NONE', #155407, #152838, #94100 ) ;
#120115=ORIENTED_EDGE ( 'NONE', *, *, #238665, .F. ) ;
#120142=DIRECTION ( 'NONE',  ( 0.000000000000000000, 0.000000000000000000, -1.000000000000000000 ) ) ;
#120145=CIRCLE ( 'NONE', #36946, 0.1000000000000000472 ) ;
#120161=EDGE_LOOP ( 'NONE', ( #83303, #35152, #15200, #69068 ) ) ;
#120184=DIRECTION ( 'NONE',  ( -1.000000000000000000, 0.000000000000000000, 0.000000000000000000 ) ) ;
#120196=SPHERICAL_SURFACE ( 'NONE', #213790, 0.1000000000000000056 ) ;
#120197=CARTESIAN_POINT ( 'NONE',  ( -21.05000000000011795, -0.01771943329734000649, -94.05891531152838070 ) ) ;
#120201=DIRECTION ( 'NONE',  ( -0.7071067811865388020, 0.7071067811865561215, 0.000000000000000000 ) ) ;
#120228=CARTESIAN_POINT ( 'NONE',  ( -23.25000000000000000, -11.74999999998884448, -100.5000000000000284 ) ) ;
#120243=FACE_OUTER_BOUND ( 'NONE', #88953, .T. ) ;
#120254=VERTEX_POINT ( 'NONE', #150043 ) ;
#120280=FACE_OUTER_BOUND ( 'NONE', #210261, .T. ) ;
#120284=CARTESIAN_POINT ( 'NONE',  ( -18.50000000000000711, 11.65000000001115232, -107.5148057706540357 ) ) ;
#120288=CARTESIAN_POINT ( 'NONE',  ( -20.94999999999999929, 1.115650877919449575E-11, -138.1000000000000227 ) ) ;
#120310=VECTOR ( 'NONE', #245523, 999.9999999999998863 ) ;
#120373=ADVANCED_FACE ( 'NONE', ( #97718 ), #71552, .T. ) ;
#120400=CARTESIAN_POINT ( 'NONE',  ( 18.59999999999999076, 7.120270961708750512, -137.6595630418393625 ) ) ;
#120404=CARTESIAN_POINT ( 'NONE',  ( -21.07016717457010557, 1.116512752478288073E-11, -94.17905916189914706 ) ) ;
#120421=ORIENTED_EDGE ( 'NONE', *, *, #115668, .T. ) ;
#120422=FACE_OUTER_BOUND ( 'NONE', #192151, .T. ) ;
#120456=CARTESIAN_POINT ( 'NONE',  ( -20.96428641294275153, 11.75000000001149481, -127.1748931779423089 ) ) ;
#120462=DIRECTION ( 'NONE',  ( 0.000000000000000000, -0.1495327102803586661, -0.9887567792719350601 ) ) ;
#120466=DIRECTION ( 'NONE',  ( 1.000000000000000000, -0.000000000000000000, 0.000000000000000000 ) ) ;
#120467=EDGE_CURVE ( 'NONE', #97170, #213795, #155376, .T. ) ;
#120474=ORIENTED_EDGE ( 'NONE', *, *, #38892, .T. ) ;
#120509=DIRECTION ( 'NONE',  ( 1.000000000000000000, -0.000000000000000000, -0.000000000000000000 ) ) ;
#120516=EDGE_CURVE ( 'NONE', #5450, #64377, #179876, .T. ) ;
#120517=AXIS2_PLACEMENT_3D ( 'NONE', #191464, #92316, #171901 ) ;
#120532=VERTEX_POINT ( 'NONE', #203267 ) ;
#120534=DIRECTION ( 'NONE',  ( 1.000000000000000000, 0.000000000000000000, -0.000000000000000000 ) ) ;
#120594=EDGE_CURVE ( 'NONE', #20729, #128969, #199445, .T. ) ;
#120648=ORIENTED_EDGE ( 'NONE', *, *, #160574, .F. ) ;
#120649=CARTESIAN_POINT ( 'NONE',  ( 21.05000000000000071, 11.75000000001115907, -127.1583993101029790 ) ) ;
#120714=EDGE_CURVE ( 'NONE', #168971, #74036, #180047, .T. ) ;
#120718=AXIS2_PLACEMENT_3D ( 'NONE', #11265, #9974, #208192 ) ;
#120723=VERTEX_POINT ( 'NONE', #210981 ) ;
#120768=AXIS2_PLACEMENT_3D ( 'NONE', #122103, #162528, #222445 ) ;
#120779=ORIENTED_EDGE ( 'NONE', *, *, #120467, .T. ) ;
#120792=CARTESIAN_POINT ( 'NONE',  ( 19.99999999738043144, 11.75000000001116263, -125.1871719496315905 ) ) ;
#120800=DIRECTION ( 'NONE',  ( 0.000000000000000000, 0.000000000000000000, -1.000000000000000000 ) ) ;
#120853=VERTEX_POINT ( 'NONE', #179569 ) ;
#120859=CARTESIAN_POINT ( 'NONE',  ( 20.85000000000000142, 1.115600667400684642E-11, -141.9000000000000341 ) ) ;
#120865=LINE ( 'NONE', #178269, #227774 ) ;
#120888=ORIENTED_EDGE ( 'NONE', *, *, #213307, .T. ) ;
#120890=VECTOR ( 'NONE', #150877, 1000.000000000000000 ) ;
#120908=DIRECTION ( 'NONE',  ( 1.000000000000000000, 0.000000000000000000, 0.000000000000000000 ) ) ;
#120922=DIRECTION ( 'NONE',  ( 0.000000000000000000, 0.000000000000000000, -1.000000000000000000 ) ) ;
#120951=VERTEX_POINT ( 'NONE', #227649 ) ;
#120963=DIRECTION ( 'NONE',  ( 0.000000000000000000, -0.000000000000000000, -1.000000000000000000 ) ) ;
#120968=CARTESIAN_POINT ( 'NONE',  ( -20.94999999999999929, -11.48912529306489994, -131.1000000000000227 ) ) ;
#120969=DIRECTION ( 'NONE',  ( 0.000000000000000000, -1.000000000000000000, 0.000000000000000000 ) ) ;
#120978=DIRECTION ( 'NONE',  ( 0.000000000000000000, 0.000000000000000000, 1.000000000000000000 ) ) ;
#121021=ADVANCED_FACE ( 'NONE', ( #66017 ), #185966, .T. ) ;
#121038=CARTESIAN_POINT ( 'NONE',  ( -18.40904629823842953, -9.499999999988851584, -140.6001895624823135 ) ) ;
#121068=CYLINDRICAL_SURFACE ( 'NONE', #234511, 0.5000000000000004441 ) ;
#121101=VERTEX_POINT ( 'NONE', #33355 ) ;
#121113=ORIENTED_EDGE ( 'NONE', *, *, #38088, .T. ) ;
#121116=CYLINDRICAL_SURFACE ( 'NONE', #214098, 0.1000000000000028644 ) ;
#121182=FACE_OUTER_BOUND ( 'NONE', #220418, .T. ) ;
#121248=CARTESIAN_POINT ( 'NONE',  ( 18.49999999999999289, 10.49142135624846439, -125.3500000000000512 ) ) ;
#121294=CARTESIAN_POINT ( 'NONE',  ( 20.94999999999999929, -1.835341550213257733, -112.0551512925630249 ) ) ;
#121296=ORIENTED_EDGE ( 'NONE', *, *, #13424, .T. ) ;
#121309=EDGE_CURVE ( 'NONE', #124703, #64997, #30395, .T. ) ;
#121311=AXIS2_PLACEMENT_3D ( 'NONE', #62232, #63494, #179625 ) ;
#121320=ORIENTED_EDGE ( 'NONE', *, *, #224447, .T. ) ;
#121361=AXIS2_PLACEMENT_3D ( 'NONE', #90352, #5660, #244289 ) ;
#121370=EDGE_CURVE ( 'NONE', #209835, #2822, #192884, .T. ) ;
#121378=EDGE_LOOP ( 'NONE', ( #212412, #161038 ) ) ;
#121386=ORIENTED_EDGE ( 'NONE', *, *, #28810, .F. ) ;
#121390=EDGE_CURVE ( 'NONE', #97776, #222832, #46147, .T. ) ;
#121392=DIRECTION ( 'NONE',  ( 0.000000000000000000, 0.000000000000000000, 1.000000000000000000 ) ) ;
#121408=LINE ( 'NONE', #237465, #232534 ) ;
#121423=CARTESIAN_POINT ( 'NONE',  ( 18.42595409746858692, -9.499999812553779677, -107.4993623517473793 ) ) ;
#121456=ORIENTED_EDGE ( 'NONE', *, *, #116010, .F. ) ;
#121457=VERTEX_POINT ( 'NONE', #152998 ) ;
#121459=ADVANCED_FACE ( 'NONE', ( #130823 ), #192108, .T. ) ;
#121543=LINE ( 'NONE', #181500, #86999 ) ;
#121544=FACE_OUTER_BOUND ( 'NONE', #236228, .T. ) ;
#121545=DIRECTION ( 'NONE',  ( 0.000000000000000000, -0.9915357197604971473, 0.1298341882519111479 ) ) ;
#121553=ADVANCED_FACE ( 'NONE', ( #176397 ), #80408, .T. ) ;
#121603=SPHERICAL_SURFACE ( 'NONE', #116795, 0.1000000000000000056 ) ;
#121604=ORIENTED_EDGE ( 'NONE', *, *, #154200, .T. ) ;
#121629=ORIENTED_EDGE ( 'NONE', *, *, #203589, .T. ) ;
#121662=PLANE ( 'NONE',  #215197 ) ;
#121686=DIRECTION ( 'NONE',  ( 0.000000000000000000, 0.000000000000000000, -1.000000000000000000 ) ) ;
#121687=DIRECTION ( 'NONE',  ( 0.000000000000000000, 0.000000000000000000, 1.000000000000000000 ) ) ;
#121716=AXIS2_PLACEMENT_3D ( 'NONE', #178068, #99765, #20270 ) ;
#121723=AXIS2_PLACEMENT_3D ( 'NONE', #25727, #67415, #127397 ) ;
#121726=CARTESIAN_POINT ( 'NONE',  ( -20.85000000106584750, 11.75000000001115197, -127.1555046564734113 ) ) ;
#121732=CARTESIAN_POINT ( 'NONE',  ( 21.08884785362045378, 6.357193367436396514, -100.4502169049331997 ) ) ;
#121738=CIRCLE ( 'NONE', #238234, 0.5000000000000004441 ) ;
#121742=CARTESIAN_POINT ( 'NONE',  ( 21.05000000000000426, 10.72371710471867701, -108.0944173916131774 ) ) ;
#121762=EDGE_CURVE ( 'NONE', #137271, #6219, #135874, .T. ) ;
#121774=CARTESIAN_POINT ( 'NONE',  ( -21.14999999999999858, 11.75000000001115552, -100.5000000000000284 ) ) ;
#121779=DIRECTION ( 'NONE',  ( 0.000000000000000000, 0.000000000000000000, 1.000000000000000000 ) ) ;
#121790=AXIS2_PLACEMENT_3D ( 'NONE', #11508, #250106, #131430 ) ;
#121799=CIRCLE ( 'NONE', #76003, 0.1000000000000028644 ) ;
#121808=DIRECTION ( 'NONE',  ( 1.000000000000000000, 3.265361837132813093E-16, -0.000000000000000000 ) ) ;
#121835=CARTESIAN_POINT ( 'NONE',  ( -21.37071067811865532, 8.070710678129811910, -121.7500000000000426 ) ) ;
#121868=DIRECTION ( 'NONE',  ( 0.000000000000000000, -1.000000000000000000, 0.000000000000000000 ) ) ;
#121885=CARTESIAN_POINT ( 'NONE',  ( -21.05000000000000071, 6.258842723548828424, -100.4679863068123211 ) ) ;
#121891=ORIENTED_EDGE ( 'NONE', *, *, #128003, .T. ) ;
#121901=AXIS2_PLACEMENT_3D ( 'NONE', #126971, #13454, #66994 ) ;
#121933=DIRECTION ( 'NONE',  ( 0.000000000000000000, -1.000000000000000000, 0.000000000000000000 ) ) ;
#121984=CARTESIAN_POINT ( 'NONE',  ( 21.14999999999999858, 11.65000000001116298, -112.7500000000000284 ) ) ;
#122002=CARTESIAN_POINT ( 'NONE',  ( 23.14999999999999858, 4.813084112160680661, -112.4415177565238650 ) ) ;
#122019=CARTESIAN_POINT ( 'NONE',  ( 21.05000000000000071, 8.876614585098254295, -108.8850804788447135 ) ) ;
#122027=DIRECTION ( 'NONE',  ( -1.000000000000000000, 0.000000000000000000, 0.000000000000000000 ) ) ;
#122034=ORIENTED_EDGE ( 'NONE', *, *, #39688, .T. ) ;
#122052=CARTESIAN_POINT ( 'NONE',  ( 19.80993210785715775, 11.75000000001116263, -125.2671177488815175 ) ) ;
#122071=ORIENTED_EDGE ( 'NONE', *, *, #177385, .T. ) ;
#122080=DIRECTION ( 'NONE',  ( 0.000000000000000000, 0.000000000000000000, -1.000000000000000000 ) ) ;
#122083=CARTESIAN_POINT ( 'NONE',  ( -21.53752568617674612, 6.786807874515071504, -100.4010255387293284 ) ) ;
#122103=CARTESIAN_POINT ( 'NONE',  ( -23.15000000000000213, 1.115600667400684642E-11, -136.1000000000000227 ) ) ;
#122107=DIRECTION ( 'NONE',  ( -0.7071067811865475727, -0.7071067811865475727, -0.000000000000000000 ) ) ;
#122156=FACE_OUTER_BOUND ( 'NONE', #125476, .T. ) ;
#122170=CIRCLE ( 'NONE', #76342, 12.87499999999999822 ) ;
#122193=FACE_OUTER_BOUND ( 'NONE', #23793, .T. ) ;
#122225=CARTESIAN_POINT ( 'NONE',  ( 23.14999999999999147, -4.149999999988843058, -100.5000000000000284 ) ) ;
#122232=DIRECTION ( 'NONE',  ( 0.000000000000000000, 0.000000000000000000, -1.000000000000000000 ) ) ;
#122276=TOROIDAL_SURFACE ( 'NONE', #59706, 11.70000000000000107, 0.1000000000000000056 ) ;
#122288=ADVANCED_FACE ( 'NONE', ( #190571 ), #32799, .F. ) ;
#122292=CARTESIAN_POINT ( 'NONE',  ( -18.52309608778520555, -9.642476320044044868, -140.7145963411697096 ) ) ;
#122312=VERTEX_POINT ( 'NONE', #9336 ) ;
#122317=CARTESIAN_POINT ( 'NONE',  ( -21.05000000000000071, 11.62071067812980907, -107.3684166523410823 ) ) ;
#122336=EDGE_LOOP ( 'NONE', ( #149637, #132389, #215449, #114236, #137916 ) ) ;
#122337=CIRCLE ( 'NONE', #109844, 0.09999999999999939493 ) ;
#122340=ORIENTED_EDGE ( 'NONE', *, *, #35118, .T. ) ;
#122345=CYLINDRICAL_SURFACE ( 'NONE', #58626, 0.09999999999999939493 ) ;
#122367=CARTESIAN_POINT ( 'NONE',  ( 20.94999999999999574, 8.926614585098251453, -108.9716830192231498 ) ) ;
#122378=DIRECTION ( 'NONE',  ( 0.000000000000000000, -0.9915357197604971473, 0.1298341882519111479 ) ) ;
#122386=CARTESIAN_POINT ( 'NONE',  ( 18.59999999999999076, 6.450000000011156587, -110.5170271704400591 ) ) ;
#122397=ORIENTED_EDGE ( 'NONE', *, *, #218753, .T. ) ;
#122414=CARTESIAN_POINT ( 'NONE',  ( -21.14999999999999858, 1.115600667400684642E-11, -100.5000000000000284 ) ) ;
#122462=ORIENTED_EDGE ( 'NONE', *, *, #52908, .T. ) ;
#122476=ORIENTED_EDGE ( 'NONE', *, *, #122991, .T. ) ;
#122492=CARTESIAN_POINT ( 'NONE',  ( -18.59999999999999787, -1.162701749926853712, -108.6000000000000227 ) ) ;
#122497=DIRECTION ( 'NONE',  ( 0.000000000000000000, -0.1455152366551721865, -0.9893560106964475187 ) ) ;
#122510=EDGE_LOOP ( 'NONE', ( #9126, #178178, #158437, #191919 ) ) ;
#122518=CIRCLE ( 'NONE', #55823, 0.09999999999999939493 ) ;
#122521=ADVANCED_FACE ( 'NONE', ( #143407 ), #62598, .T. ) ;
#122564=CARTESIAN_POINT ( 'NONE',  ( 21.05000005001280172, 8.871279691782062216, -112.6779475882458570 ) ) ;
#122582=DIRECTION ( 'NONE',  ( -1.000000000000000000, 0.000000000000000000, -0.000000000000000000 ) ) ;
#122602=FACE_OUTER_BOUND ( 'NONE', #195747, .T. ) ;
#122605=EDGE_CURVE ( 'NONE', #8700, #215032, #114307, .T. ) ;
#122628=B_SPLINE_CURVE_WITH_KNOTS ( 'NONE', 3,
 ( #30105, #249149, #170932, #27555, #246547, #107030 ),
 .UNSPECIFIED., .F., .F.,
 ( 4, 2, 4 ),
 ( 0.000000000000000000, 0.0001891491689349539989, 0.0003782983378699079978 ),
 .UNSPECIFIED. ) ;
#122647=ORIENTED_EDGE ( 'NONE', *, *, #44, .F. ) ;
#122673=EDGE_CURVE ( 'NONE', #220305, #74961, #109403, .T. ) ;
#122681=ORIENTED_EDGE ( 'NONE', *, *, #141157, .T. ) ;
#122713=ADVANCED_FACE ( 'NONE', ( #177120 ), #132848, .T. ) ;
#122744=DIRECTION ( 'NONE',  ( 1.000000000000000000, -0.000000000000000000, -0.000000000000000000 ) ) ;
#122749=CARTESIAN_POINT ( 'NONE',  ( -21.05000000000000426, 0.09843750001115451898, -94.20076908991316600 ) ) ;
#122771=ORIENTED_EDGE ( 'NONE', *, *, #36632, .T. ) ;
#122773=ADVANCED_FACE ( 'NONE', ( #195400 ), #172007, .T. ) ;
#122804=ORIENTED_EDGE ( 'NONE', *, *, #155117, .F. ) ;
#122813=CYLINDRICAL_SURFACE ( 'NONE', #128424, 0.09999999999999939493 ) ;
#122820=AXIS2_PLACEMENT_3D ( 'NONE', #104982, #165001, #758 ) ;
#122823=CIRCLE ( 'NONE', #243602, 0.09999999999998898659 ) ;
#122824=DIRECTION ( 'NONE',  ( 0.000000000000000000, 0.000000000000000000, 1.000000000000000000 ) ) ;
#122847=ORIENTED_EDGE ( 'NONE', *, *, #249123, .T. ) ;
#122861=AXIS2_PLACEMENT_3D ( 'NONE', #190925, #52652, #111361 ) ;
#122870=LINE ( 'NONE', #184106, #214640 ) ;
#122918=ORIENTED_EDGE ( 'NONE', *, *, #94026, .T. ) ;
#122926=ORIENTED_EDGE ( 'NONE', *, *, #103790, .F. ) ;
#122944=CARTESIAN_POINT ( 'NONE',  ( 22.50927854361889047, -0.1008580735143608520, -88.75043287397312497 ) ) ;
#122961=ORIENTED_EDGE ( 'NONE', *, *, #232181, .F. ) ;
#122991=EDGE_CURVE ( 'NONE', #142111, #103006, #59734, .T. ) ;
#123007=CARTESIAN_POINT ( 'NONE',  ( -23.15000000000000213, 1.910280373842930812, -121.3686321448010972 ) ) ;
#123011=ADVANCED_FACE ( 'NONE', ( #52648 ), #190922, .T. ) ;
#123037=DIRECTION ( 'NONE',  ( 0.000000000000000000, -1.000000000000000000, 0.000000000000000000 ) ) ;
#123055=CIRCLE ( 'NONE', #156403, 0.1999999999999987899 ) ;
#123065=ORIENTED_EDGE ( 'NONE', *, *, #124392, .T. ) ;
#123106=AXIS2_PLACEMENT_3D ( 'NONE', #240593, #163636, #84034 ) ;
#123113=CARTESIAN_POINT ( 'NONE',  ( 23.25000000000000355, -22.45632476061176774, -107.2938984477316353 ) ) ;
#123117=CARTESIAN_POINT ( 'NONE',  ( 20.04142135623730070, 11.75000000001115907, -121.8500000000000369 ) ) ;
#123139=AXIS2_PLACEMENT_3D ( 'NONE', #221690, #101732, #165613 ) ;
#123148=CARTESIAN_POINT ( 'NONE',  ( 21.05000000000000071, 5.000000000011153745, -122.0947339810869465 ) ) ;
#123160=CARTESIAN_POINT ( 'NONE',  ( -21.07954640115341505, 6.329287696035425625, -100.4339922928603102 ) ) ;
#123167=CARTESIAN_POINT ( 'NONE',  ( 22.49533356619863156, 11.65000000631534149, -100.4348774196772638 ) ) ;
#123169=ORIENTED_EDGE ( 'NONE', *, *, #196047, .T. ) ;
#123187=CIRCLE ( 'NONE', #202298, 0.6000000000000015321 ) ;
#123192=EDGE_CURVE ( 'NONE', #210115, #183119, #201410, .T. ) ;
#123196=CARTESIAN_POINT ( 'NONE',  ( 20.94560253601876809, 11.75000000001115907, -127.0100835125151093 ) ) ;
#123205=ORIENTED_EDGE ( 'NONE', *, *, #87278, .T. ) ;
#123252=EDGE_CURVE ( 'NONE', #231172, #95681, #51348, .T. ) ;
#123261=LINE ( 'NONE', #184503, #221813 ) ;
#123284=VERTEX_POINT ( 'NONE', #6812 ) ;
#123285=ORIENTED_EDGE ( 'NONE', *, *, #68482, .T. ) ;
#123303=EDGE_CURVE ( 'NONE', #81295, #113518, #10675, .T. ) ;
#123311=CARTESIAN_POINT ( 'NONE',  ( 21.05000000000000071, 8.815452279208699338, -108.9203925526142882 ) ) ;
#123327=VERTEX_POINT ( 'NONE', #128052 ) ;
#123330=ORIENTED_EDGE ( 'NONE', *, *, #139843, .T. ) ;
#123334=ORIENTED_EDGE ( 'NONE', *, *, #16060, .F. ) ;
#123336=CARTESIAN_POINT ( 'NONE',  ( -1.739115166359751801E-14, 11.65000000001114699, -121.8500000000000369 ) ) ;
#123339=CARTESIAN_POINT ( 'NONE',  ( 19.75857864376269291, 11.75000000001116263, -125.3500000000000512 ) ) ;
#123348=EDGE_CURVE ( 'NONE', #138064, #59138, #131900, .T. ) ;
#123364=CARTESIAN_POINT ( 'NONE',  ( -18.50000000000000000, 9.150000000011157653, -112.8500000000000369 ) ) ;
#123392=LINE ( 'NONE', #105058, #31321 ) ;
#123410=ADVANCED_FACE ( 'NONE', ( #112351 ), #150195, .F. ) ;
#123420=CARTESIAN_POINT ( 'NONE',  ( 18.52928932188133970, 10.27928932189250411, -121.8500000000000369 ) ) ;
#123447=CIRCLE ( 'NONE', #219295, 0.1000000000000028644 ) ;
#123463=CYLINDRICAL_SURFACE ( 'NONE', #110424, 0.09999999999999939493 ) ;
#123469=VECTOR ( 'NONE', #218520, 1000.000000000000000 ) ;
#123492=ORIENTED_EDGE ( 'NONE', *, *, #247931, .T. ) ;
#123520=CIRCLE ( 'NONE', #11090, 0.5000000000000004441 ) ;
#123521=CARTESIAN_POINT ( 'NONE',  ( 20.95512820512820440, 8.876151316299271343, -109.0586289951409924 ) ) ;
#123531=VERTEX_POINT ( 'NONE', #156641 ) ;
#123538=DIRECTION ( 'NONE',  ( 0.000000000000000000, 0.000000000000000000, -1.000000000000000000 ) ) ;
#123547=AXIS2_PLACEMENT_3D ( 'NONE', #231493, #15016, #254831 ) ;
#123550=VECTOR ( 'NONE', #65012, 1000.000000000000000 ) ;
#123553=ORIENTED_EDGE ( 'NONE', *, *, #30708, .F. ) ;
#123563=EDGE_CURVE ( 'NONE', #107956, #256826, #139013, .T. ) ;
#123573=CARTESIAN_POINT ( 'NONE',  ( -18.33682934331484304, -9.511185591082512047, -140.9056547686735428 ) ) ;
#123612=CARTESIAN_POINT ( 'NONE',  ( 22.40736611211992368, 1.115600667400684642E-11, -88.85042919245522341 ) ) ;
#123613=CARTESIAN_POINT ( 'NONE',  ( 23.14999999999999858, 4.775700934590584090, -112.3487681040460160 ) ) ;
#123648=CARTESIAN_POINT ( 'NONE',  ( 20.94999999999999929, 1.115600667400684642E-11, -134.0000000000000284 ) ) ;
#123678=VECTOR ( 'NONE', #113940, 1000.000000000000000 ) ;
#123680=TOROIDAL_SURFACE ( 'NONE', #219509, 7.791421356237335338, 0.1000000000000000056 ) ;
#123695=LINE ( 'NONE', #28479, #256893 ) ;
#123696=CARTESIAN_POINT ( 'NONE',  ( 21.05000000000000071, 1.115600667400684642E-11, -100.5000000000000284 ) ) ;
#123714=ORIENTED_EDGE ( 'NONE', *, *, #256031, .T. ) ;
#123761=ORIENTED_EDGE ( 'NONE', *, *, #207785, .T. ) ;
#123772=CARTESIAN_POINT ( 'NONE',  ( -18.50000000000000000, 10.29270135741298375, -139.4573618871519614 ) ) ;
#123783=LINE ( 'NONE', #203320, #6285 ) ;
#123790=CARTESIAN_POINT ( 'NONE',  ( -20.00857864376270001, 9.250000000011157297, -121.6500000000000341 ) ) ;
#123809=DIRECTION ( 'NONE',  ( 1.000000000000000000, 3.265361837132813093E-16, -0.000000000000000000 ) ) ;
#123810=CIRCLE ( 'NONE', #40455, 12.77500000000000036 ) ;
#123822=CARTESIAN_POINT ( 'NONE',  ( -21.14999999999999858, 1.115600667400684642E-11, -93.95934304829879125 ) ) ;
#123834=ORIENTED_EDGE ( 'NONE', *, *, #29435, .F. ) ;
#123844=ADVANCED_FACE ( 'NONE', ( #149894 ), #148602, .F. ) ;
#123903=EDGE_CURVE ( 'NONE', #198122, #250577, #97565, .T. ) ;
#123910=AXIS2_PLACEMENT_3D ( 'NONE', #171893, #231847, #109294 ) ;
#123977=CIRCLE ( 'NONE', #257187, 0.1000000000000043493 ) ;
#123986=CARTESIAN_POINT ( 'NONE',  ( -21.00250684356851849, 11.75000000001115197, -107.5148057687598566 ) ) ;
#123996=CIRCLE ( 'NONE', #207203, 0.09999999999999824307 ) ;
#124005=DIRECTION ( 'NONE',  ( 0.000000000000000000, 1.000000000000000000, 0.000000000000000000 ) ) ;
#124021=CARTESIAN_POINT ( 'NONE',  ( -21.07928932188134041, 0.09889514566555070163, -94.17148334360673800 ) ) ;
#124053=VECTOR ( 'NONE', #114749, 1000.000000000000000 ) ;
#124075=CARTESIAN_POINT ( 'NONE',  ( -18.50000000000000000, 9.350000000011156942, -112.8500000000000369 ) ) ;
#124139=DIRECTION ( 'NONE',  ( 0.000000000000000000, 1.000000000000000000, 0.000000000000000000 ) ) ;
#124178=AXIS2_PLACEMENT_3D ( 'NONE', #78564, #254619, #235092 ) ;
#124270=EDGE_CURVE ( 'NONE', #195862, #67969, #195133, .T. ) ;
#124298=ORIENTED_EDGE ( 'NONE', *, *, #17247, .F. ) ;
#124301=ORIENTED_EDGE ( 'NONE', *, *, #88169, .F. ) ;
#124305=ORIENTED_EDGE ( 'NONE', *, *, #138285, .F. ) ;
#124324=EDGE_LOOP ( 'NONE', ( #8370, #55265 ) ) ;
#124336=DIRECTION ( 'NONE',  ( 0.000000000000000000, 1.000000000000000000, 2.891205793294679805E-16 ) ) ;
#124385=EDGE_CURVE ( 'NONE', #216892, #156398, #16487, .T. ) ;
#124386=DIRECTION ( 'NONE',  ( -1.000000000000000000, -0.000000000000000000, -0.000000000000000000 ) ) ;
#124392=EDGE_CURVE ( 'NONE', #127698, #36453, #223632, .T. ) ;
#124409=ORIENTED_EDGE ( 'NONE', *, *, #36762, .T. ) ;
#124425=ORIENTED_EDGE ( 'NONE', *, *, #201985, .F. ) ;
#124438=DIRECTION ( 'NONE',  ( 0.000000000000000000, -0.000000000000000000, -1.000000000000000000 ) ) ;
#124440=CARTESIAN_POINT ( 'NONE',  ( 21.04999999999998650, 6.650000000011155876, -112.7500000000000284 ) ) ;
#124471=ADVANCED_FACE ( 'NONE', ( #249651 ), #145389, .T. ) ;
#124505=AXIS2_PLACEMENT_3D ( 'NONE', #114354, #92209, #190043 ) ;
#124532=CARTESIAN_POINT ( 'NONE',  ( -23.25000000000000000, 11.65000000001115588, -121.8500000000000227 ) ) ;
#124540=CIRCLE ( 'NONE', #45421, 7.800000000000001599 ) ;
#124562=CIRCLE ( 'NONE', #95335, 0.1000000000000028644 ) ;
#124578=CYLINDRICAL_SURFACE ( 'NONE', #85250, 0.1000000000000028644 ) ;
#124626=DIRECTION ( 'NONE',  ( 0.000000000000000000, 0.9654727137038715545, 0.2605042016806676242 ) ) ;
#124633=CARTESIAN_POINT ( 'NONE',  ( 20.21494484322224849, 9.303170737879936425, -108.8402651917702713 ) ) ;
#124636=CIRCLE ( 'NONE', #82896, 0.1000000000000010186 ) ;
#124647=CARTESIAN_POINT ( 'NONE',  ( -21.46681500593313885, 6.857511159395392575, -100.5000000000000426 ) ) ;
#124650=EDGE_CURVE ( 'NONE', #242007, #222495, #211808, .T. ) ;
#124661=ORIENTED_EDGE ( 'NONE', *, *, #8594, .T. ) ;
#124672=CARTESIAN_POINT ( 'NONE',  ( -20.89192007715127986, 10.32898536001801304, -139.5826683222764757 ) ) ;
#124696=VERTEX_POINT ( 'NONE', #1393 ) ;
#124703=VERTEX_POINT ( 'NONE', #80931 ) ;
#124706=ORIENTED_EDGE ( 'NONE', *, *, #20206, .T. ) ;
#124729=EDGE_CURVE ( 'NONE', #162338, #213938, #93810, .T. ) ;
#124743=VERTEX_POINT ( 'NONE', #240033 ) ;
#124745=VERTEX_POINT ( 'NONE', #256967 ) ;
#124794=DIRECTION ( 'NONE',  ( -1.000000000000000000, 0.000000000000000000, 0.000000000000000000 ) ) ;
#124797=ORIENTED_EDGE ( 'NONE', *, *, #110199, .T. ) ;
#124800=CARTESIAN_POINT ( 'NONE',  ( 21.05000000000000071, 1.115600667400684642E-11, -100.5000000000000284 ) ) ;
#124801=CARTESIAN_POINT ( 'NONE',  ( 23.15000000000000213, -11.74999999998883560, -112.6500000000000341 ) ) ;
#124802=CARTESIAN_POINT ( 'NONE',  ( 20.95392731769792150, 8.883061479199918509, -109.0222279795713405 ) ) ;
#124819=AXIS2_PLACEMENT_3D ( 'NONE', #64460, #63151, #47435 ) ;
#124857=CARTESIAN_POINT ( 'NONE',  ( -18.39999999999999503, -9.682403433465244902, -140.6568433774128266 ) ) ;
#124863=DIRECTION ( 'NONE',  ( 1.000000000000000000, 0.000000000000000000, 0.000000000000000000 ) ) ;
#124950=DIRECTION ( 'NONE',  ( 1.000000000000000000, 0.000000000000000000, 0.000000000000000000 ) ) ;
#124958=ORIENTED_EDGE ( 'NONE', *, *, #151567, .F. ) ;
#124965=CIRCLE ( 'NONE', #191451, 0.1000000000000028644 ) ;
#124968=EDGE_LOOP ( 'NONE', ( #121113, #242352, #220974, #179703 ) ) ;
#124993=DIRECTION ( 'NONE',  ( -0.000000000000000000, 1.000000000000000000, 2.891205793294679805E-16 ) ) ;
#124995=VECTOR ( 'NONE', #252554, 1000.000000000000000 ) ;
#124996=AXIS2_PLACEMENT_3D ( 'NONE', #35680, #209138, #30534 ) ;
#124998=EDGE_LOOP ( 'NONE', ( #223606, #170532, #35725, #28750 ) ) ;
#125001=DIRECTION ( 'NONE',  ( 0.000000000000000000, 0.1350103645451904977, 0.9908441862701596881 ) ) ;
#125039=EDGE_LOOP ( 'NONE', ( #67843, #72864, #56217, #231999, #214652 ) ) ;
#125051=EDGE_LOOP ( 'NONE', ( #234597, #128239, #115697, #54339 ) ) ;
#125076=ADVANCED_FACE ( 'NONE', ( #201730 ), #84287, .T. ) ;
#125078=DIRECTION ( 'NONE',  ( 1.000000000000000000, 2.952720810173289112E-16, -0.000000000000000000 ) ) ;
#125122=EDGE_LOOP ( 'NONE', ( #60467, #46371, #15891, #118173 ) ) ;
#125131=DIRECTION ( 'NONE',  ( 0.000000000000000000, 0.000000000000000000, 1.000000000000000000 ) ) ;
#125152=DIRECTION ( 'NONE',  ( -1.000000000000000000, -0.000000000000000000, -0.000000000000000000 ) ) ;
#125158=DIRECTION ( 'NONE',  ( 0.000000000000000000, 0.000000000000000000, -1.000000000000000000 ) ) ;
#125162=VECTOR ( 'NONE', #78029, 1000.000000000000000 ) ;
#125179=DIRECTION ( 'NONE',  ( 0.000000000000000000, 0.000000000000000000, -1.000000000000000000 ) ) ;
#125188=AXIS2_PLACEMENT_3D ( 'NONE', #207540, #151422, #189254 ) ;
#125199=ORIENTED_EDGE ( 'NONE', *, *, #88220, .T. ) ;
#125277=CIRCLE ( 'NONE', #12860, 0.3999999999999975797 ) ;
#125296=ORIENTED_EDGE ( 'NONE', *, *, #84117, .T. ) ;
#125322=EDGE_LOOP ( 'NONE', ( #150724, #53565, #244939, #122771, #38625, #125656, #211494, #245498, #192608, #71507 ) ) ;
#125326=CARTESIAN_POINT ( 'NONE',  ( 22.47071067811865319, 7.720074744509199505, -100.4009075452974287 ) ) ;
#125331=CIRCLE ( 'NONE', #46373, 0.09999999999999484301 ) ;
#125337=DIRECTION ( 'NONE',  ( 0.000000000000000000, 0.000000000000000000, -1.000000000000000000 ) ) ;
#125394=ORIENTED_EDGE ( 'NONE', *, *, #33233, .T. ) ;
#125417=DIRECTION ( 'NONE',  ( 1.000000000000000000, 0.000000000000000000, 0.000000000000000000 ) ) ;
#125458=CIRCLE ( 'NONE', #129724, 0.1000000000000028644 ) ;
#125476=EDGE_LOOP ( 'NONE', ( #12792, #84300, #23897, #66906 ) ) ;
#125486=CARTESIAN_POINT ( 'NONE',  ( -21.14999999999999858, 1.115600667400684642E-11, -100.5000000000000284 ) ) ;
#125526=DIRECTION ( 'NONE',  ( 0.000000000000000000, 0.000000000000000000, -1.000000000000000000 ) ) ;
#125538=VERTEX_POINT ( 'NONE', #52226 ) ;
#125562=DIRECTION ( 'NONE',  ( 3.616040088954497272E-32, -1.224646799147352961E-16, 1.000000000000000000 ) ) ;
#125570=ORIENTED_EDGE ( 'NONE', *, *, #124385, .T. ) ;
#125575=DIRECTION ( 'NONE',  ( 1.000000000000000000, -0.000000000000000000, -0.000000000000000000 ) ) ;
#125582=ORIENTED_EDGE ( 'NONE', *, *, #77243, .T. ) ;
#125597=CYLINDRICAL_SURFACE ( 'NONE', #206883, 7.899999999999990585 ) ;
#125603=DIRECTION ( 'NONE',  ( -1.000000000000000000, -0.000000000000000000, -0.000000000000000000 ) ) ;
#125606=DIRECTION ( 'NONE',  ( 4.239556034732056743E-17, -0.1298341882520022694, -0.9915357197604852679 ) ) ;
#125609=ORIENTED_EDGE ( 'NONE', *, *, #218307, .F. ) ;
#125627=AXIS2_PLACEMENT_3D ( 'NONE', #58327, #98724, #257783 ) ;
#125656=ORIENTED_EDGE ( 'NONE', *, *, #82528, .T. ) ;
#125657=EDGE_CURVE ( 'NONE', #116815, #92883, #110933, .T. ) ;
#125660=DIRECTION ( 'NONE',  ( 1.000000000000000000, 0.000000000000000000, 0.000000000000000000 ) ) ;
#125663=CARTESIAN_POINT ( 'NONE',  ( -20.94999999999999929, -1.162701749926853712, -108.6000000000000227 ) ) ;
#125705=EDGE_CURVE ( 'NONE', #30650, #135846, #15276, .T. ) ;
#125744=DIRECTION ( 'NONE',  ( -1.000000000000000000, -0.000000000000000000, -0.000000000000000000 ) ) ;
#125785=ORIENTED_EDGE ( 'NONE', *, *, #196254, .F. ) ;
#125799=CIRCLE ( 'NONE', #4980, 0.1000000000000028644 ) ;
#125818=ORIENTED_EDGE ( 'NONE', *, *, #143676, .F. ) ;
#125827=ORIENTED_EDGE ( 'NONE', *, *, #181020, .T. ) ;
#125830=EDGE_LOOP ( 'NONE', ( #38454, #43951, #2570, #22792 ) ) ;
#125834=DIRECTION ( 'NONE',  ( 1.000000000000000000, -0.000000000000000000, 0.000000000000000000 ) ) ;
#125843=FACE_OUTER_BOUND ( 'NONE', #88851, .T. ) ;
#125863=EDGE_CURVE ( 'NONE', #162071, #4043, #156932, .T. ) ;
#125891=VECTOR ( 'NONE', #243790, 1000.000000000000000 ) ;
#125897=DIRECTION ( 'NONE',  ( -1.000000000000000000, 0.000000000000000000, 0.000000000000000000 ) ) ;
#125935=DIRECTION ( 'NONE',  ( -1.000000000000000000, 0.000000000000000000, 0.000000000000000000 ) ) ;
#125939=EDGE_LOOP ( 'NONE', ( #161126, #176853, #111336, #197837 ) ) ;
#125980=CYLINDRICAL_SURFACE ( 'NONE', #96301, 0.09999999999999781286 ) ;
#126004=AXIS2_PLACEMENT_3D ( 'NONE', #204149, #247130, #245865 ) ;
#126005=VERTEX_POINT ( 'NONE', #80120 ) ;
#126014=FACE_OUTER_BOUND ( 'NONE', #207418, .T. ) ;
#126016=DIRECTION ( 'NONE',  ( 0.000000000000000000, 3.469446951953515108E-14, 1.000000000000000000 ) ) ;
#126018=CARTESIAN_POINT ( 'NONE',  ( 22.00356870068398862, -8.772485052120828773E-13, -93.24575763823901298 ) ) ;
#126028=EDGE_CURVE ( 'NONE', #95552, #193662, #53025, .T. ) ;
#126062=DIRECTION ( 'NONE',  ( 0.000000000000000000, -0.000000000000000000, 1.000000000000000000 ) ) ;
#126086=CARTESIAN_POINT ( 'NONE',  ( 19.75857864376268935, 11.65000000001115943, -125.2500000000000284 ) ) ;
#126114=AXIS2_PLACEMENT_3D ( 'NONE', #123648, #160227, #181063 ) ;
#126117=CARTESIAN_POINT ( 'NONE',  ( -18.43459694179555441, -9.494210124986889099, -140.6170052026611188 ) ) ;
#126148=CARTESIAN_POINT ( 'NONE',  ( -18.59999999999999787, 5.950000000011100632, -110.8057023050348988 ) ) ;
#126153=DIRECTION ( 'NONE',  ( 0.000000000000000000, 0.000000000000000000, -1.000000000000000000 ) ) ;
#126166=EDGE_CURVE ( 'NONE', #243362, #238459, #57103, .T. ) ;
#126175=ADVANCED_FACE ( 'NONE', ( #188253 ), #50025, .F. ) ;
#126182=EDGE_CURVE ( 'NONE', #140362, #13818, #177948, .T. ) ;
#126197=DIRECTION ( 'NONE',  ( 1.000000000000000000, 0.000000000000000000, 0.000000000000000000 ) ) ;
#126198=LINE ( 'NONE', #248730, #68247 ) ;
#126207=ORIENTED_EDGE ( 'NONE', *, *, #133909, .F. ) ;
#126233=EDGE_LOOP ( 'NONE', ( #112406, #71031, #93465, #129752 ) ) ;
#126255=DIRECTION ( 'NONE',  ( -0.7071067811865388020, 0.7071067811865561215, 0.000000000000000000 ) ) ;
#126261=CARTESIAN_POINT ( 'NONE',  ( 18.59999999999999076, 11.75000000001115907, -108.6000000000000227 ) ) ;
#126275=CIRCLE ( 'NONE', #30626, 0.1000000000000001860 ) ;
#126281=ORIENTED_EDGE ( 'NONE', *, *, #135079, .T. ) ;
#126316=AXIS2_PLACEMENT_3D ( 'NONE', #134816, #151871, #54020 ) ;
#126344=LINE ( 'NONE', #147193, #110830 ) ;
#126348=CIRCLE ( 'NONE', #193004, 0.09999999999999939493 ) ;
#126364=CIRCLE ( 'NONE', #47234, 0.1000000000000096922 ) ;
#126372=ORIENTED_EDGE ( 'NONE', *, *, #59120, .T. ) ;
#126383=DIRECTION ( 'NONE',  ( 0.000000000000000000, -0.000000000000000000, -1.000000000000000000 ) ) ;
#126386=CARTESIAN_POINT ( 'NONE',  ( 18.49999999999999289, 10.29270135741298731, -139.4573618871519614 ) ) ;
#126425=ORIENTED_EDGE ( 'NONE', *, *, #69519, .F. ) ;
#126440=PLANE ( 'NONE',  #67496 ) ;
#126463=EDGE_LOOP ( 'NONE', ( #219790, #235646, #1656, #176830 ) ) ;
#126499=CIRCLE ( 'NONE', #84949, 0.1000000000000028644 ) ;
#126515=EDGE_CURVE ( 'NONE', #86438, #240059, #3123, .T. ) ;
#126516=ORIENTED_EDGE ( 'NONE', *, *, #151790, .F. ) ;
#126533=ADVANCED_FACE ( 'NONE', ( #232233 ), #191831, .T. ) ;
#126537=EDGE_LOOP ( 'NONE', ( #65198, #124706, #6901 ) ) ;
#126543=CARTESIAN_POINT ( 'NONE',  ( -20.94999999999999929, 11.60000000001115339, -107.4282032302755852 ) ) ;
#126544=CARTESIAN_POINT ( 'NONE',  ( 21.12802099929860944, 8.780552590233368093, -112.7481899849316420 ) ) ;
#126603=CARTESIAN_POINT ( 'NONE',  ( 21.30740335185486245, 6.556657922039159203, -100.4010654742241826 ) ) ;
#126615=EDGE_LOOP ( 'NONE', ( #39346, #111714, #136122, #144220 ) ) ;
#126637=VERTEX_POINT ( 'NONE', #139514 ) ;
#126709=VERTEX_POINT ( 'NONE', #239925 ) ;
#126723=FACE_OUTER_BOUND ( 'NONE', #216340, .T. ) ;
#126730=CYLINDRICAL_SURFACE ( 'NONE', #161344, 12.87499999999999822 ) ;
#126790=DIRECTION ( 'NONE',  ( -1.836970198721029934E-16, 1.000000000000000000, 0.000000000000000000 ) ) ;
#126813=ORIENTED_EDGE ( 'NONE', *, *, #28086, .T. ) ;
#126834=EDGE_CURVE ( 'NONE', #84341, #186134, #170644, .T. ) ;
#126852=DIRECTION ( 'NONE',  ( 0.000000000000000000, -0.9915357197604792727, 0.1298341882520475943 ) ) ;
#126858=ORIENTED_EDGE ( 'NONE', *, *, #86451, .F. ) ;
#126898=CYLINDRICAL_SURFACE ( 'NONE', #128824, 0.1000000000000004496 ) ;
#126899=CARTESIAN_POINT ( 'NONE',  ( 20.94999999999999929, 6.650000000011155876, -112.6500000000000341 ) ) ;
#126910=DIRECTION ( 'NONE',  ( 0.000000000000000000, -0.000000000000000000, 1.000000000000000000 ) ) ;
#126911=DIRECTION ( 'NONE',  ( 0.000000000000000000, 0.000000000000000000, -1.000000000000000000 ) ) ;
#126920=DIRECTION ( 'NONE',  ( -1.000000000000000000, -2.952720810173289112E-16, 0.000000000000000000 ) ) ;
#126971=CARTESIAN_POINT ( 'NONE',  ( -20.94999999999999929, 14.05000000001115623, -128.4863049292391395 ) ) ;
#126973=ADVANCED_FACE ( 'NONE', ( #51956 ), #128902, .F. ) ;
#126996=CARTESIAN_POINT ( 'NONE',  ( -20.94999999999999929, 5.850000000011108092, -110.6324972242780120 ) ) ;
#127056=CARTESIAN_POINT ( 'NONE',  ( -18.42609945526379178, -9.499999710479226422, -107.4993624902486431 ) ) ;
#127072=CARTESIAN_POINT ( 'NONE',  ( -21.12230431290519306, 6.457566653304161797, -100.4947901483110400 ) ) ;
#127085=LINE ( 'NONE', #107513, #27501 ) ;
#127100=DIRECTION ( 'NONE',  ( -1.000000000000000000, -2.952720810173289112E-16, 0.000000000000000000 ) ) ;
#127128=DIRECTION ( 'NONE',  ( 0.000000000000000000, 3.469446951953995998E-14, 1.000000000000000000 ) ) ;
#127135=VERTEX_POINT ( 'NONE', #105173 ) ;
#127145=DIRECTION ( 'NONE',  ( 1.000000000000000000, 0.000000000000000000, 0.000000000000000000 ) ) ;
#127146=DIRECTION ( 'NONE',  ( 0.000000000000000000, 0.000000000000000000, -1.000000000000000000 ) ) ;
#127162=CIRCLE ( 'NONE', #6349, 0.09999999999998898659 ) ;
#127179=CIRCLE ( 'NONE', #235499, 0.09999999999999971412 ) ;
#127181=DIRECTION ( 'NONE',  ( 0.000000000000000000, 8.673617379884087537E-15, -1.000000000000000000 ) ) ;
#127218=FILL_AREA_STYLE_COLOUR ( '', #210712 ) ;
#127237=DIRECTION ( 'NONE',  ( 0.000000000000000000, 0.000000000000000000, 1.000000000000000000 ) ) ;
#127243=FACE_OUTER_BOUND ( 'NONE', #2033, .T. ) ;
#127252=CARTESIAN_POINT ( 'NONE',  ( -20.54999999999999716, 1.115600667400684642E-11, -135.9000000000000625 ) ) ;
#127258=DIRECTION ( 'NONE',  ( 1.000000000000000000, 0.000000000000000000, 0.000000000000000000 ) ) ;
#127293=EDGE_CURVE ( 'NONE', #61914, #85377, #54046, .T. ) ;
#127298=CARTESIAN_POINT ( 'NONE',  ( 23.15000000000000213, -8.663551401857999323, -124.4758988819327215 ) ) ;
#127310=DIRECTION ( 'NONE',  ( 0.000000000000000000, 1.000000000000000000, 0.000000000000000000 ) ) ;
#127331=CARTESIAN_POINT ( 'NONE',  ( -22.59999999999999787, 0.1000000000111554016, -88.85042919245522341 ) ) ;
#127351=AXIS2_PLACEMENT_3D ( 'NONE', #13303, #169852, #88962 ) ;
#127353=CARTESIAN_POINT ( 'NONE',  ( 21.05000000000000071, 1.115600667400684642E-11, -134.0000000000000284 ) ) ;
#127361=CARTESIAN_POINT ( 'NONE',  ( -23.25000000000000000, 1.115600667400684642E-11, -134.0000000000000284 ) ) ;
#127390=CARTESIAN_POINT ( 'NONE',  ( -20.94999999999999929, 1.851028230152016674, -112.1539132694225316 ) ) ;
#127397=DIRECTION ( 'NONE',  ( 0.000000000000000000, 1.084202172485510997E-13, -1.000000000000000000 ) ) ;
#127402=AXIS2_PLACEMENT_3D ( 'NONE', #196767, #215059, #153860 ) ;
#127413=CARTESIAN_POINT ( 'NONE',  ( 20.94999999999997442, -1.263275465206102233, -141.9018646667464338 ) ) ;
#127447=EDGE_CURVE ( 'NONE', #83522, #60627, #158163, .T. ) ;
#127449=CYLINDRICAL_SURFACE ( 'NONE', #167882, 0.1000000000000028644 ) ;
#127451=EDGE_CURVE ( 'NONE', #237722, #169627, #234146, .T. ) ;
#127484=EDGE_LOOP ( 'NONE', ( #21595, #30562, #139521, #207638 ) ) ;
#127510=DIRECTION ( 'NONE',  ( 0.000000000000000000, 0.000000000000000000, -1.000000000000000000 ) ) ;
#127555=FACE_OUTER_BOUND ( 'NONE', #165867, .T. ) ;
#127569=ORIENTED_EDGE ( 'NONE', *, *, #43350, .T. ) ;
#127574=CYLINDRICAL_SURFACE ( 'NONE', #179040, 0.1000000000000098310 ) ;
#127575=EDGE_CURVE ( 'NONE', #72307, #227912, #245404, .T. ) ;
#127587=ADVANCED_FACE ( 'NONE', ( #87581 ), #126730, .T. ) ;
#127604=LINE ( 'NONE', #50609, #239241 ) ;
#127668=LINE ( 'NONE', #151079, #141112 ) ;
#127681=CARTESIAN_POINT ( 'NONE',  ( -21.05000000000000071, 1.162701749949165642, -108.6000000000000227 ) ) ;
#127695=CARTESIAN_POINT ( 'NONE',  ( 18.59999999999999787, -1.835341550213255957, -112.0551512925630107 ) ) ;
#127698=VERTEX_POINT ( 'NONE', #34088 ) ;
#127711=DIRECTION ( 'NONE',  ( -0.000000000000000000, -0.000000000000000000, 1.000000000000000000 ) ) ;
#127732=CIRCLE ( 'NONE', #174117, 0.09999999999999939493 ) ;
#127782=ADVANCED_FACE ( 'NONE', ( #61319 ), #133186, .T. ) ;
#127803=EDGE_LOOP ( 'NONE', ( #122340, #70989, #199679, #107602 ) ) ;
#127810=CARTESIAN_POINT ( 'NONE',  ( -21.05000000000000071, 11.65000000001115232, -107.2838656629781724 ) ) ;
#127812=DIRECTION ( 'NONE',  ( 1.000000000000000000, 0.000000000000000000, -0.000000000000000000 ) ) ;
#127825=TOROIDAL_SURFACE ( 'NONE', #81990, 11.70000000000000639, 0.1000000000000000056 ) ;
#127835=CARTESIAN_POINT ( 'NONE',  ( 21.04999999999908411, 8.776282895301829257, -112.6579090026525307 ) ) ;
#127878=ORIENTED_EDGE ( 'NONE', *, *, #123252, .F. ) ;
#127883=CARTESIAN_POINT ( 'NONE',  ( -21.05000000000000071, -1.835341550213255957, -112.1551512925630050 ) ) ;
#127897=EDGE_CURVE ( 'NONE', #186134, #28381, #84686, .T. ) ;
#127907=AXIS2_PLACEMENT_3D ( 'NONE', #240124, #44496, #141025 ) ;
#127909=LINE ( 'NONE', #66651, #258054 ) ;
#127913=DIRECTION ( 'NONE',  ( 0.000000000000000000, 0.000000000000000000, -1.000000000000000000 ) ) ;
#127931=EDGE_LOOP ( 'NONE', ( #94976, #87348, #113491, #205309, #19178, #25253, #27601, #31558, #214023, #62795, #256940, #184536 ) ) ;
#127933=DIRECTION ( 'NONE',  ( -0.000000000000000000, 1.000000000000000000, -1.224646799147352961E-16 ) ) ;
#127972=ORIENTED_EDGE ( 'NONE', *, *, #32961, .F. ) ;
#127997=ORIENTED_EDGE ( 'NONE', *, *, #255726, .T. ) ;
#128003=EDGE_CURVE ( 'NONE', #241028, #196984, #16668, .T. ) ;
#128028=CARTESIAN_POINT ( 'NONE',  ( -22.48660254037843487, 11.65000000001115588, -100.4500000000000597 ) ) ;
#128052=CARTESIAN_POINT ( 'NONE',  ( 20.94999999999999929, 4.850467289730772791, -112.5342674090017141 ) ) ;
#128074=FACE_OUTER_BOUND ( 'NONE', #85547, .T. ) ;
#128075=ORIENTED_EDGE ( 'NONE', *, *, #211385, .F. ) ;
#128085=AXIS2_PLACEMENT_3D ( 'NONE', #206057, #44429, #183926 ) ;
#128097=ORIENTED_EDGE ( 'NONE', *, *, #41371, .F. ) ;
#128118=ORIENTED_EDGE ( 'NONE', *, *, #22746, .T. ) ;
#128133=CARTESIAN_POINT ( 'NONE',  ( 23.24999999999999289, 6.650000000011155876, -121.6500000000000341 ) ) ;
#128141=DIRECTION ( 'NONE',  ( 0.000000000000000000, 0.000000000000000000, 1.000000000000000000 ) ) ;
#128146=EDGE_CURVE ( 'NONE', #67578, #189375, #119847, .T. ) ;
#128180=DIRECTION ( 'NONE',  ( 1.000000000000000000, 0.000000000000000000, 0.000000000000000000 ) ) ;
#128182=DIRECTION ( 'NONE',  ( -0.000000000000000000, -0.000000000000000000, 1.000000000000000000 ) ) ;
#128200=ADVANCED_FACE ( 'NONE', ( #144358 ), #206935, .T. ) ;
#128204=ORIENTED_EDGE ( 'NONE', *, *, #111803, .F. ) ;
#128212=LINE ( 'NONE', #109912, #145098 ) ;
#128239=ORIENTED_EDGE ( 'NONE', *, *, #58461, .F. ) ;
#128246=FACE_OUTER_BOUND ( 'NONE', #145982, .T. ) ;
#128272=AXIS2_PLACEMENT_3D ( 'NONE', #53882, #172593, #12207 ) ;
#128308=DIRECTION ( 'NONE',  ( 1.000000000000000000, 3.265361837132813093E-16, -0.000000000000000000 ) ) ;
#128312=AXIS2_PLACEMENT_3D ( 'NONE', #52802, #191072, #55343 ) ;
#128344=CARTESIAN_POINT ( 'NONE',  ( 20.94999999999999929, 11.75000000001115552, -127.2161343370219413 ) ) ;
#128349=EDGE_CURVE ( 'NONE', #100304, #25027, #142643, .T. ) ;
#128352=CARTESIAN_POINT ( 'NONE',  ( -18.49999999999996803, -9.321008403350131033, -107.7359382490779183 ) ) ;
#128371=ORIENTED_EDGE ( 'NONE', *, *, #165090, .T. ) ;
#128411=ORIENTED_EDGE ( 'NONE', *, *, #78544, .F. ) ;
#128415=VERTEX_POINT ( 'NONE', #236613 ) ;
#128424=AXIS2_PLACEMENT_3D ( 'NONE', #186634, #107073, #143633 ) ;
#128433=VECTOR ( 'NONE', #244010, 1000.000000000000114 ) ;
#128447=CIRCLE ( 'NONE', #16058, 0.09999999999998898659 ) ;
#128448=AXIS2_PLACEMENT_3D ( 'NONE', #231652, #131246, #132539 ) ;
#128471=EDGE_LOOP ( 'NONE', ( #125296, #184552, #95379, #16141 ) ) ;
#128480=CARTESIAN_POINT ( 'NONE',  ( 20.11144452914179226, 9.933610851133071407, -108.3902934539540439 ) ) ;
#128483=LINE ( 'NONE', #172789, #205986 ) ;
#128485=PLANE ( 'NONE',  #42812 ) ;
#128493=ORIENTED_EDGE ( 'NONE', *, *, #243650, .F. ) ;
#128513=ADVANCED_FACE ( 'NONE', ( #128246 ), #165822, .F. ) ;
#128520=CARTESIAN_POINT ( 'NONE',  ( -18.59999999999999787, 11.60000000001115872, -107.4282032302755852 ) ) ;
#128601=CARTESIAN_POINT ( 'NONE',  ( 22.39999999999999858, 7.790779598384538929, -100.4000000000000341 ) ) ;
#128643=EDGE_CURVE ( 'NONE', #156135, #223255, #178295, .T. ) ;
#128644=DIRECTION ( 'NONE',  ( -1.000000000000000000, 0.000000000000000000, 0.000000000000000000 ) ) ;
#128654=ORIENTED_EDGE ( 'NONE', *, *, #252259, .F. ) ;
#128678=CARTESIAN_POINT ( 'NONE',  ( -23.15000000000000213, 1.115600667400684642E-11, -137.9000000000000341 ) ) ;
#128700=EDGE_CURVE ( 'NONE', #18904, #149886, #145294, .T. ) ;
#128723=DIRECTION ( 'NONE',  ( 0.000000000000000000, 0.000000000000000000, 1.000000000000000000 ) ) ;
#128755=DIRECTION ( 'NONE',  ( -2.602085213965226419E-14, -0.000000000000000000, 1.000000000000000000 ) ) ;
#128758=CARTESIAN_POINT ( 'NONE',  ( -20.54999999999999716, -8.730841121484170131, -124.4019252810157070 ) ) ;
#128780=ORIENTED_EDGE ( 'NONE', *, *, #5710, .F. ) ;
#128824=AXIS2_PLACEMENT_3D ( 'NONE', #132030, #91622, #112484 ) ;
#128858=DIRECTION ( 'NONE',  ( 0.000000000000000000, 1.000000000000000000, 0.000000000000000000 ) ) ;
#128867=AXIS2_PLACEMENT_3D ( 'NONE', #135696, #116165, #99128 ) ;
#128885=CARTESIAN_POINT ( 'NONE',  ( 21.05000000000000071, 1.115600667400684642E-11, -138.0000000000000284 ) ) ;
#128894=CARTESIAN_POINT ( 'NONE',  ( -18.39999999999999858, -9.519327731081281385, -107.4729763765593589 ) ) ;
#128902=TOROIDAL_SURFACE ( 'NONE', #62252, 0.4000000000000010214, 0.1000000000000000056 ) ;
#128910=CARTESIAN_POINT ( 'NONE',  ( 21.05000000000000071, -8.999999999988842703, -124.1060308773475924 ) ) ;
#128928=FACE_OUTER_BOUND ( 'NONE', #149648, .T. ) ;
#128940=DIRECTION ( 'NONE',  ( 0.000000000000000000, 0.000000000000000000, -1.000000000000000000 ) ) ;
#128969=VERTEX_POINT ( 'NONE', #223319 ) ;
#128988=AXIS2_PLACEMENT_3D ( 'NONE', #163265, #241505, #221910 ) ;
#129026=ORIENTED_EDGE ( 'NONE', *, *, #86983, .F. ) ;
#129027=ORIENTED_EDGE ( 'NONE', *, *, #70521, .T. ) ;
#129038=EDGE_CURVE ( 'NONE', #46619, #221229, #86359, .T. ) ;
#129056=VECTOR ( 'NONE', #169516, 1000.000000000000000 ) ;
#129063=ORIENTED_EDGE ( 'NONE', *, *, #155929, .F. ) ;
#129073=EDGE_LOOP ( 'NONE', ( #122071, #194229, #174701, #71746 ) ) ;
#129074=DIRECTION ( 'NONE',  ( 0.000000000000000000, 0.000000000000000000, 1.000000000000000000 ) ) ;
#129088=ORIENTED_EDGE ( 'NONE', *, *, #26939, .T. ) ;
#129096=EDGE_LOOP ( 'NONE', ( #244531, #224609, #122647 ) ) ;
#129140=DIRECTION ( 'NONE',  ( -0.000000000000000000, 0.000000000000000000, 1.000000000000000000 ) ) ;
#129171=CARTESIAN_POINT ( 'NONE',  ( 20.93975676684922504, 10.31104185824063002, -139.5204516983105805 ) ) ;
#129181=AXIS2_PLACEMENT_3D ( 'NONE', #106700, #109270, #145831 ) ;
#129192=CIRCLE ( 'NONE', #83543, 0.09999999999998898659 ) ;
#129209=CARTESIAN_POINT ( 'NONE',  ( 18.59999999999999432, -1.162701749926855266, -108.6000000000000227 ) ) ;
#129232=DIRECTION ( 'NONE',  ( -1.000000000000000000, 0.000000000000000000, 0.000000000000000000 ) ) ;
#129253=FACE_OUTER_BOUND ( 'NONE', #8289, .T. ) ;
#129304=DIRECTION ( 'NONE',  ( 0.000000000000000000, 0.000000000000000000, -1.000000000000000000 ) ) ;
#129309=CARTESIAN_POINT ( 'NONE',  ( 20.04142135623730070, 11.65000000001115943, -125.1500000000000341 ) ) ;
#129331=DIRECTION ( 'NONE',  ( -1.000000000000000000, -2.952720810173289112E-16, 0.000000000000000000 ) ) ;
#129343=EDGE_CURVE ( 'NONE', #232908, #109044, #37185, .T. ) ;
#129369=FACE_OUTER_BOUND ( 'NONE', #238176, .T. ) ;
#129374=ORIENTED_EDGE ( 'NONE', *, *, #87413, .T. ) ;
#129388=EDGE_LOOP ( 'NONE', ( #4321, #28566, #221316, #112396 ) ) ;
#129418=CYLINDRICAL_SURFACE ( 'NONE', #201336, 0.1000000000000004496 ) ;
#129421=AXIS2_PLACEMENT_3D ( 'NONE', #183655, #25867, #4974 ) ;
#129433=CARTESIAN_POINT ( 'NONE',  ( 21.14999999999999858, 10.71339244341104013, -112.7500000000000284 ) ) ;
#129438=CIRCLE ( 'NONE', #229409, 0.09999999999999939493 ) ;
#129441=VERTEX_POINT ( 'NONE', #166613 ) ;
#129487=B_SPLINE_CURVE_WITH_KNOTS ( 'NONE', 3,
 ( #125326, #43222, #163178, #142304, #66634, #27546, #225670, #84865, #126603, #206143 ),
 .UNSPECIFIED., .F., .F.,
 ( 4, 3, 3, 4 ),
 ( 0.000000000000000000, 0.0002000000000002884074, 0.001000000000045112589, 0.001967863649472103085 ),
 .UNSPECIFIED. ) ;
#129536=VERTEX_POINT ( 'NONE', #19054 ) ;
#129581=CARTESIAN_POINT ( 'NONE',  ( 21.00000000000000000, 9.750000000011153745, -121.7500000000000426 ) ) ;
#129612=EDGE_LOOP ( 'NONE', ( #47128, #138944, #238670, #156884, #225218, #52950, #120421, #61389, #226794, #199819, #139396, #109392 ) ) ;
#129637=VECTOR ( 'NONE', #249852, 1000.000000000000000 ) ;
#129664=ORIENTED_EDGE ( 'NONE', *, *, #178116, .T. ) ;
#129707=VECTOR ( 'NONE', #10741, 1000.000000000000000 ) ;
#129717=CARTESIAN_POINT ( 'NONE',  ( -18.39999999999999858, -9.682403433465239573, -140.6568433774128266 ) ) ;
#129724=AXIS2_PLACEMENT_3D ( 'NONE', #77994, #237086, #153756 ) ;
#129731=CYLINDRICAL_SURFACE ( 'NONE', #2807, 0.09999999999999939493 ) ;
#129733=FACE_OUTER_BOUND ( 'NONE', #3149, .T. ) ;
#129752=ORIENTED_EDGE ( 'NONE', *, *, #198332, .F. ) ;
#129758=CARTESIAN_POINT ( 'NONE',  ( 20.30531438145591139, 10.09690106110208596, -108.2960178072733868 ) ) ;
#129774=CARTESIAN_POINT ( 'NONE',  ( 22.60000000000000142, 11.74956712350054744, -100.3991416309013260 ) ) ;
#129787=DIRECTION ( 'NONE',  ( 0.000000000000000000, 0.2605042016806715099, 0.9654727137038706664 ) ) ;
#129793=CARTESIAN_POINT ( 'NONE',  ( -23.25000000000000000, 4.250000000011156409, -112.6500000000000483 ) ) ;
#129802=CIRCLE ( 'NONE', #46575, 0.09999999999998898659 ) ;
#129831=ORIENTED_EDGE ( 'NONE', *, *, #193584, .F. ) ;
#129834=CARTESIAN_POINT ( 'NONE',  ( -21.14999999999999858, -11.64999999998884483, -100.5000000000000284 ) ) ;
#129849=FACE_OUTER_BOUND ( 'NONE', #135244, .T. ) ;
#129869=DIRECTION ( 'NONE',  ( 0.000000000000000000, -0.1455152366551721865, -0.9893560106964475187 ) ) ;
#129909=ORIENTED_EDGE ( 'NONE', *, *, #209895, .T. ) ;
#129966=DIRECTION ( 'NONE',  ( 2.952720810173289112E-16, -1.000000000000000000, -0.000000000000000000 ) ) ;
#130009=ORIENTED_EDGE ( 'NONE', *, *, #80610, .F. ) ;
#130013=ORIENTED_EDGE ( 'NONE', *, *, #40616, .T. ) ;
#130027=ORIENTED_EDGE ( 'NONE', *, *, #167776, .T. ) ;
#130049=TOROIDAL_SURFACE ( 'NONE', #171798, 12.97499999999999787, 0.1000000000000000056 ) ;
#130071=ORIENTED_EDGE ( 'NONE', *, *, #232382, .T. ) ;
#130082=ORIENTED_EDGE ( 'NONE', *, *, #60001, .T. ) ;
#130113=DIRECTION ( 'NONE',  ( -1.000000000000000000, 0.000000000000000000, 0.000000000000000000 ) ) ;
#130155=CARTESIAN_POINT ( 'NONE',  ( -18.52139480978222963, -9.481358845055737561, -107.5245565671190917 ) ) ;
#130161=ORIENTED_EDGE ( 'NONE', *, *, #15626, .T. ) ;
#130186=DIRECTION ( 'NONE',  ( 2.952720810173289112E-16, -1.000000000000000000, 0.000000000000000000 ) ) ;
#130190=EDGE_CURVE ( 'NONE', #122312, #164528, #145282, .T. ) ;
#130229=DIRECTION ( 'NONE',  ( 0.000000000000000000, 0.000000000000000000, -1.000000000000000000 ) ) ;
#130253=CARTESIAN_POINT ( 'NONE',  ( -20.54999999999999716, 1.115600667400684642E-11, -100.5000000000000284 ) ) ;
#130269=ORIENTED_EDGE ( 'NONE', *, *, #47699, .T. ) ;
#130294=ADVANCED_FACE ( 'NONE', ( #155440 ), #154158, .T. ) ;
#130325=CARTESIAN_POINT ( 'NONE',  ( 23.14999999999999858, 6.650000000011155876, -112.8500000000000369 ) ) ;
#130353=ORIENTED_EDGE ( 'NONE', *, *, #18431, .F. ) ;
#130383=CARTESIAN_POINT ( 'NONE',  ( 18.59999996954842771, -9.523204137847017137, -140.8830417119173433 ) ) ;
#130395=ADVANCED_FACE ( 'NONE', ( #240078 ), #24705, .T. ) ;
#130398=ORIENTED_EDGE ( 'NONE', *, *, #223156, .T. ) ;
#130401=CARTESIAN_POINT ( 'NONE',  ( 21.56666275994539461, 1.115600667400684642E-11, -93.54263159310670517 ) ) ;
#130404=DIRECTION ( 'NONE',  ( 0.7071067811865487940, 0.000000000000000000, -0.7071067811865463515 ) ) ;
#130443=CARTESIAN_POINT ( 'NONE',  ( 20.93302460841142931, 10.31565961587945424, -139.5364194119178478 ) ) ;
#130451=ADVANCED_FACE ( 'NONE', ( #202232 ), #242627, .F. ) ;
#130474=CYLINDRICAL_SURFACE ( 'NONE', #67368, 0.1000000000000028644 ) ;
#130552=ORIENTED_EDGE ( 'NONE', *, *, #23536, .T. ) ;
#130571=EDGE_LOOP ( 'NONE', ( #218942, #170887, #149606 ) ) ;
#130600=ORIENTED_EDGE ( 'NONE', *, *, #223473, .F. ) ;
#130606=VERTEX_POINT ( 'NONE', #228223 ) ;
#130622=AXIS2_PLACEMENT_3D ( 'NONE', #216109, #41363, #98696 ) ;
#130628=DIRECTION ( 'NONE',  ( 1.000000000000000000, 0.000000000000000000, 0.000000000000000000 ) ) ;
#130631=ADVANCED_FACE ( 'NONE', ( #195533 ), #14330, .T. ) ;
#130637=EDGE_LOOP ( 'NONE', ( #256289, #83351, #64506, #233777 ) ) ;
#130653=DIRECTION ( 'NONE',  ( -1.000000000000000000, 0.000000000000000000, 0.000000000000000000 ) ) ;
#130672=ORIENTED_EDGE ( 'NONE', *, *, #137999, .T. ) ;
#130673=DIRECTION ( 'NONE',  ( 1.000000000000000000, 1.875376730785737719E-16, 0.000000000000000000 ) ) ;
#130682=EDGE_LOOP ( 'NONE', ( #55843, #199655, #96408, #183291, #19198 ) ) ;
#130705=DIRECTION ( 'NONE',  ( 0.000000000000000000, -0.1350103645451904977, -0.9908441862701596881 ) ) ;
#130755=ADVANCED_FACE ( 'NONE', ( #81929 ), #200643, .T. ) ;
#130759=CIRCLE ( 'NONE', #243174, 0.1999999999999996503 ) ;
#130768=DIRECTION ( 'NONE',  ( 0.000000000000000000, -0.8660254037844247188, 0.5000000000000245359 ) ) ;
#130807=EDGE_LOOP ( 'NONE', ( #177508, #114529, #167271, #151815 ) ) ;
#130810=FACE_OUTER_BOUND ( 'NONE', #179422, .T. ) ;
#130823=FACE_OUTER_BOUND ( 'NONE', #149554, .T. ) ;
#130834=CARTESIAN_POINT ( 'NONE',  ( 22.60000000000000142, 1.115600667400684642E-11, -100.5000000000000284 ) ) ;
#130880=TOROIDAL_SURFACE ( 'NONE', #164224, 0.2000000000000000111, 0.1000000000000000056 ) ;
#130923=ORIENTED_EDGE ( 'NONE', *, *, #223054, .T. ) ;
#130983=DIRECTION ( 'NONE',  ( 1.000000000000000000, 0.000000000000000000, 0.000000000000000000 ) ) ;
#131018=EDGE_CURVE ( 'NONE', #111525, #251571, #237253, .T. ) ;
#131040=CARTESIAN_POINT ( 'NONE',  ( 20.41140022480589522, 10.41043084241237615, -108.1150013036349549 ) ) ;
#131077=CARTESIAN_POINT ( 'NONE',  ( -22.59999999999999787, 11.74956712350054744, -100.3991416309013260 ) ) ;
#131083=DIRECTION ( 'NONE',  ( 0.000000000000000000, 1.000000000000000000, 0.000000000000000000 ) ) ;
#131088=AXIS2_PLACEMENT_3D ( 'NONE', #152915, #212864, #116339 ) ;
#131089=PLANE ( 'NONE',  #140095 ) ;
#131169=DIRECTION ( 'NONE',  ( 7.589415207398576792E-15, -1.000000000000000000, -0.000000000000000000 ) ) ;
#131215=EDGE_CURVE ( 'NONE', #196436, #204472, #83857, .T. ) ;
#131221=VECTOR ( 'NONE', #136374, 1000.000000000000114 ) ;
#131244=CARTESIAN_POINT ( 'NONE',  ( -21.05000000000000071, 1.261786168576181755, -108.5864989635455089 ) ) ;
#131246=DIRECTION ( 'NONE',  ( 0.000000000000000000, 0.000000000000000000, -1.000000000000000000 ) ) ;
#131268=DIRECTION ( 'NONE',  ( 0.000000000000000000, 0.000000000000000000, 1.000000000000000000 ) ) ;
#131276=CARTESIAN_POINT ( 'NONE',  ( 21.05000000000000071, -11.74999999998883560, -131.1000000000000227 ) ) ;
#131280=AXIS2_PLACEMENT_3D ( 'NONE', #200878, #22262, #23572 ) ;
#131294=DIRECTION ( 'NONE',  ( 1.000000000000000000, 0.000000000000000000, -0.000000000000000000 ) ) ;
#131324=DIRECTION ( 'NONE',  ( -1.000000000000000000, 0.000000000000000000, 0.000000000000000000 ) ) ;
#131334=CARTESIAN_POINT ( 'NONE',  ( -20.64999999999999858, -9.499999999988846255, -124.1060308773475924 ) ) ;
#131336=DIRECTION ( 'NONE',  ( -3.469446951953605354E-14, 1.000000000000000000, 0.000000000000000000 ) ) ;
#131350=CARTESIAN_POINT ( 'NONE',  ( -18.42637059832564006, -9.496945461878548045, -140.6090773097999147 ) ) ;
#131368=ORIENTED_EDGE ( 'NONE', *, *, #125863, .T. ) ;
#131379=DIRECTION ( 'NONE',  ( 0.000000000000000000, 0.000000000000000000, -1.000000000000000000 ) ) ;
#131380=DIRECTION ( 'NONE',  ( 0.000000000000000000, 1.000000000000000000, 0.000000000000000000 ) ) ;
#131397=ORIENTED_EDGE ( 'NONE', *, *, #194001, .T. ) ;
#131430=DIRECTION ( 'NONE',  ( 0.000000000000000000, -0.8777080977375715243, 0.4791956752370512551 ) ) ;
#131458=AXIS2_PLACEMENT_3D ( 'NONE', #143144, #107886, #222681 ) ;
#131469=CARTESIAN_POINT ( 'NONE',  ( 21.13461538461538680, 10.61458296203670848, -112.7500000000000142 ) ) ;
#131495=CYLINDRICAL_SURFACE ( 'NONE', #47270, 0.1000000000000028644 ) ;
#131520=DIRECTION ( 'NONE',  ( -1.000000000000000000, -0.000000000000000000, 0.000000000000000000 ) ) ;
#131556=ADVANCED_FACE ( 'NONE', ( #142287 ), #101857, .T. ) ;
#131592=ORIENTED_EDGE ( 'NONE', *, *, #202823, .T. ) ;
#131609=VERTEX_POINT ( 'NONE', #199725 ) ;
#131616=CARTESIAN_POINT ( 'NONE',  ( -23.25000000000000000, 1.115650265596050101E-11, -96.45000000000003126 ) ) ;
#131682=CARTESIAN_POINT ( 'NONE',  ( -20.54999999999999716, 1.115600667400684642E-11, -113.4750000000000369 ) ) ;
#131685=CARTESIAN_POINT ( 'NONE',  ( 21.05000000000000071, -9.499999999988848032, -110.3939691226524786 ) ) ;
#131734=VERTEX_POINT ( 'NONE', #226970 ) ;
#131747=CARTESIAN_POINT ( 'NONE',  ( 21.05000000000000071, 5.850000000011105428, -110.6324972242780120 ) ) ;
#131785=AXIS2_PLACEMENT_3D ( 'NONE', #236815, #13938, #34806 ) ;
#131890=ORIENTED_EDGE ( 'NONE', *, *, #71450, .F. ) ;
#131892=EDGE_LOOP ( 'NONE', ( #123169, #223672, #173923, #45374 ) ) ;
#131900=LINE ( 'NONE', #231026, #110017 ) ;
#131909=AXIS2_PLACEMENT_3D ( 'NONE', #108326, #9215, #168341 ) ;
#131912=CARTESIAN_POINT ( 'NONE',  ( 18.39999999999999858, -9.519327731081283162, -107.4729763765593589 ) ) ;
#131959=EDGE_LOOP ( 'NONE', ( #20748, #97163, #10392, #173112 ) ) ;
#131961=LINE ( 'NONE', #134511, #71477 ) ;
#131970=EDGE_CURVE ( 'NONE', #116815, #104317, #187740, .T. ) ;
#131974=EDGE_LOOP ( 'NONE', ( #38959, #98577, #126516, #41297 ) ) ;
#131976=FACE_OUTER_BOUND ( 'NONE', #66417, .T. ) ;
#131980=DIRECTION ( 'NONE',  ( 0.000000000000000000, -0.9999176327611369874, 0.01283462868041984617 ) ) ;
#131998=ADVANCED_FACE ( 'NONE', ( #121182 ), #200689, .F. ) ;
#131999=AXIS2_PLACEMENT_3D ( 'NONE', #77155, #120184, #155460 ) ;
#132015=ORIENTED_EDGE ( 'NONE', *, *, #176999, .T. ) ;
#132030=CARTESIAN_POINT ( 'NONE',  ( 18.59999999999999432, 5.699452464332755319, -87.95772604343019907 ) ) ;
#132031=DIRECTION ( 'NONE',  ( 1.000000000000000000, -0.000000000000000000, -0.000000000000000000 ) ) ;
#132036=ORIENTED_EDGE ( 'NONE', *, *, #54348, .T. ) ;
#132042=VECTOR ( 'NONE', #108801, 1000.000000000000000 ) ;
#132047=AXIS2_PLACEMENT_3D ( 'NONE', #242342, #186233, #47988 ) ;
#132075=DIRECTION ( 'NONE',  ( 0.000000000000000000, -0.000000000000000000, 1.000000000000000000 ) ) ;
#132129=VERTEX_POINT ( 'NONE', #204519 ) ;
#132148=CARTESIAN_POINT ( 'NONE',  ( 18.47149038651512143, -9.671457157995547504, -140.6727863347384186 ) ) ;
#132165=AXIS2_PLACEMENT_3D ( 'NONE', #193564, #169213, #57874 ) ;
#132172=AXIS2_PLACEMENT_3D ( 'NONE', #136584, #196569, #97444 ) ;
#132180=VECTOR ( 'NONE', #251813, 1000.000000000000000 ) ;
#132183=CARTESIAN_POINT ( 'NONE',  ( -20.64999999999999858, 7.150000000011155876, -121.6500000000000341 ) ) ;
#132217=EDGE_CURVE ( 'NONE', #8209, #96344, #104657, .T. ) ;
#132295=CARTESIAN_POINT ( 'NONE',  ( 23.14999999999999503, 11.65000000001116298, -88.75000000000004263 ) ) ;
#132309=DIRECTION ( 'NONE',  ( -1.000000000000000000, 0.000000000000000000, -0.000000000000000000 ) ) ;
#132322=CARTESIAN_POINT ( 'NONE',  ( 20.12518398540832365, 9.975088720679844201, -108.4966682524699593 ) ) ;
#132373=EDGE_CURVE ( 'NONE', #239657, #117118, #175455, .T. ) ;
#132378=FACE_OUTER_BOUND ( 'NONE', #38739, .T. ) ;
#132389=ORIENTED_EDGE ( 'NONE', *, *, #92151, .T. ) ;
#132395=DIRECTION ( 'NONE',  ( -1.000000000000000000, 0.000000000000000000, 0.000000000000000000 ) ) ;
#132424=AXIS2_PLACEMENT_3D ( 'NONE', #110047, #190908, #12261 ) ;
#132489=CARTESIAN_POINT ( 'NONE',  ( 22.57320508075687115, 11.75000000001115552, -100.5000000000000284 ) ) ;
#132505=AXIS2_PLACEMENT_3D ( 'NONE', #128910, #233163, #111924 ) ;
#132525=CIRCLE ( 'NONE', #3315, 0.09999999999999864553 ) ;
#132529=EDGE_CURVE ( 'NONE', #46680, #186401, #196448, .T. ) ;
#132531=EDGE_LOOP ( 'NONE', ( #184192, #14523, #147683, #241595 ) ) ;
#132539=DIRECTION ( 'NONE',  ( -1.000000000000000000, 0.000000000000000000, 0.000000000000000000 ) ) ;
#132542=CIRCLE ( 'NONE', #120105, 12.87499999999999822 ) ;
#132563=AXIS2_PLACEMENT_3D ( 'NONE', #218804, #40212, #102691 ) ;
#132586=CIRCLE ( 'NONE', #16095, 3.899999999999987033 ) ;
#132590=VECTOR ( 'NONE', #107557, 1000.000000000000000 ) ;
#132591=LINE ( 'NONE', #167892, #64015 ) ;
#132625=EDGE_LOOP ( 'NONE', ( #73900, #31913, #110436, #166641, #194361 ) ) ;
#132629=DIRECTION ( 'NONE',  ( 0.000000000000000000, 1.265107689135680095E-16, -1.000000000000000000 ) ) ;
#132711=EDGE_CURVE ( 'NONE', #39467, #257268, #101987, .T. ) ;
#132720=TOROIDAL_SURFACE ( 'NONE', #186891, 12.97499999999999609, 0.1000000000000000056 ) ;
#132744=CARTESIAN_POINT ( 'NONE',  ( -23.25000000000000000, 1.115649040949250830E-11, -130.1000000000000512 ) ) ;
#132796=EDGE_CURVE ( 'NONE', #5506, #144728, #193124, .T. ) ;
#132803=VECTOR ( 'NONE', #6849, 1000.000000000000000 ) ;
#132848=CYLINDRICAL_SURFACE ( 'NONE', #255340, 0.09999999999999939493 ) ;
#132902=ORIENTED_EDGE ( 'NONE', *, *, #165966, .T. ) ;
#132942=ORIENTED_EDGE ( 'NONE', *, *, #150324, .T. ) ;
#132946=VERTEX_POINT ( 'NONE', #80842 ) ;
#132956=DIRECTION ( 'NONE',  ( -1.000000000000000000, 0.000000000000000000, 0.000000000000000000 ) ) ;
#132973=ORIENTED_EDGE ( 'NONE', *, *, #174246, .F. ) ;
#132979=CARTESIAN_POINT ( 'NONE',  ( 18.46932045258648358, -9.670685200254535374, -140.6738603729967565 ) ) ;
#132981=DIRECTION ( 'NONE',  ( 0.000000000000000000, 0.000000000000000000, -1.000000000000000000 ) ) ;
#132988=TOROIDAL_SURFACE ( 'NONE', #174717, 3.899999999999999467, 0.1000000000000000056 ) ;
#133007=CARTESIAN_POINT ( 'NONE',  ( -22.47120815636973745, 0.02890382191504723905, -88.85006801124653464 ) ) ;
#133026=AXIS2_PLACEMENT_3D ( 'NONE', #238478, #76834, #177258 ) ;
#133029=TOROIDAL_SURFACE ( 'NONE', #49626, 12.77500000000000036, 0.1000000000000000056 ) ;
#133030=AXIS2_PLACEMENT_3D ( 'NONE', #14955, #214412, #233977 ) ;
#133053=DIRECTION ( 'NONE',  ( 2.710505431213777355E-16, -1.000000000000000000, 0.000000000000000000 ) ) ;
#133062=CARTESIAN_POINT ( 'NONE',  ( -23.15000000000000213, 11.75000000001115552, -121.8500000000000227 ) ) ;
#133101=LINE ( 'NONE', #113531, #39631 ) ;
#133107=ORIENTED_EDGE ( 'NONE', *, *, #80264, .F. ) ;
#133112=DIRECTION ( 'NONE',  ( 1.000000000000000000, -0.000000000000000000, -0.000000000000000000 ) ) ;
#133115=CARTESIAN_POINT ( 'NONE',  ( 22.39999999999999858, 0.1000000000111554016, -92.70922040162665212 ) ) ;
#133140=EDGE_LOOP ( 'NONE', ( #167297, #45306, #67084 ) ) ;
#133147=EDGE_CURVE ( 'NONE', #154121, #239256, #5145, .T. ) ;
#133165=CARTESIAN_POINT ( 'NONE',  ( 23.24999999999999645, -3.899999999988843502, -134.0000000000000284 ) ) ;
#133166=DIRECTION ( 'NONE',  ( 1.000000000000000000, -0.000000000000000000, -0.000000000000000000 ) ) ;
#133175=DIRECTION ( 'NONE',  ( 0.000000000000000000, -1.000000000000000000, 0.000000000000000000 ) ) ;
#133186=( BOUNDED_SURFACE ( )  B_SPLINE_SURFACE ( 3, 2, ( 
 ( #118739, #83412, #100414 ),
 ( #219087, #198248, #79570 ),
 ( #159159, #40511, #22208 ),
 ( #241254, #80856, #78293 ) ),
 .UNSPECIFIED., .F., .F., .F. ) 
 B_SPLINE_SURFACE_WITH_KNOTS ( ( 4, 4 ),
 ( 3, 3 ),
 ( -2.710505431213761085E-20, 0.0003124336117481265837 ),
 ( 0.000000000000000000, 1.000000000000000000 ),
 .UNSPECIFIED. ) 
 GEOMETRIC_REPRESENTATION_ITEM ( )  RATIONAL_B_SPLINE_SURFACE ( (
 ( 1.000000000000000000, 0.7040654476015975050, 1.000000000000000000),
 ( 1.000000000000000000, 0.7039193538782316795, 1.000000000000000000),
 ( 1.000000000000000000, 0.7089171279145296545, 1.000000000000000000),
 ( 1.000000000000000000, 0.7071067811865506814, 1.000000000000000000) ) ) 
 REPRESENTATION_ITEM ( '' )  SURFACE ( )  );
#133209=AXIS2_PLACEMENT_3D ( 'NONE', #170605, #192689, #190123 ) ;
#133220=DIRECTION ( 'NONE',  ( 1.000000000000000000, 0.000000000000000000, 0.000000000000000000 ) ) ;
#133240=EDGE_LOOP ( 'NONE', ( #185080, #59670, #62083, #126858 ) ) ;
#133241=ORIENTED_EDGE ( 'NONE', *, *, #22698, .T. ) ;
#133310=CARTESIAN_POINT ( 'NONE',  ( -20.54999999999999716, -8.999999999988844479, -124.1060308773475924 ) ) ;
#133314=ORIENTED_EDGE ( 'NONE', *, *, #5853, .F. ) ;
#133342=ORIENTED_EDGE ( 'NONE', *, *, #154948, .T. ) ;
#133359=ORIENTED_EDGE ( 'NONE', *, *, #60318, .F. ) ;
#133402=CARTESIAN_POINT ( 'NONE',  ( -18.55807992284872299, 10.32898536001801304, -139.5826683222764757 ) ) ;
#133404=CARTESIAN_POINT ( 'NONE',  ( -21.14999999999999858, 11.65000000001115588, -100.6000000000000369 ) ) ;
#133431=DIRECTION ( 'NONE',  ( 0.000000000000000000, 0.000000000000000000, -1.000000000000000000 ) ) ;
#133435=CARTESIAN_POINT ( 'NONE',  ( 18.59999999999999432, -1.637172712959223952, -112.0821533654720383 ) ) ;
#133443=CIRCLE ( 'NONE', #21036, 11.80000000000000426 ) ;
#133445=CARTESIAN_POINT ( 'NONE',  ( -23.25000000000000000, 1.115600667400684642E-11, -113.2750000000000341 ) ) ;
#133491=LINE ( 'NONE', #211754, #257371 ) ;
#133534=AXIS2_PLACEMENT_3D ( 'NONE', #233270, #213676, #235794 ) ;
#133553=AXIS2_PLACEMENT_3D ( 'NONE', #85189, #6971, #227302 ) ;
#133557=LINE ( 'NONE', #194847, #34579 ) ;
#133566=CARTESIAN_POINT ( 'NONE',  ( 23.24999999999999289, 6.450000000011156587, -112.8500000000000369 ) ) ;
#133593=VERTEX_POINT ( 'NONE', #226451 ) ;
#133605=EDGE_CURVE ( 'NONE', #240102, #231259, #117723, .T. ) ;
#133606=CIRCLE ( 'NONE', #42062, 0.09999999999999939493 ) ;
#133609=DIRECTION ( 'NONE',  ( -5.603264701231743991E-32, 1.897661533703520143E-16, -1.000000000000000000 ) ) ;
#133626=CARTESIAN_POINT ( 'NONE',  ( -18.59999999999999787, 6.846123162363745074, -137.7377262668498759 ) ) ;
#133628=ORIENTED_EDGE ( 'NONE', *, *, #161271, .F. ) ;
#133633=EDGE_LOOP ( 'NONE', ( #256034, #107204 ) ) ;
#133669=CIRCLE ( 'NONE', #21276, 0.1000000000000028644 ) ;
#133682=CYLINDRICAL_SURFACE ( 'NONE', #179368, 11.80000000000000426 ) ;
#133702=AXIS2_PLACEMENT_3D ( 'NONE', #75491, #153770, #256604 ) ;
#133749=ORIENTED_EDGE ( 'NONE', *, *, #87254, .F. ) ;
#133762=DIRECTION ( 'NONE',  ( -4.391705002472929091E-16, 1.000000000000000000, 0.000000000000000000 ) ) ;
#133768=ORIENTED_EDGE ( 'NONE', *, *, #164212, .T. ) ;
#133781=AXIS2_PLACEMENT_3D ( 'NONE', #19516, #199448, #155196 ) ;
#133786=DIRECTION ( 'NONE',  ( -0.000000000000000000, 0.1350103645451876666, 0.9908441862701600211 ) ) ;
#133815=AXIS2_PLACEMENT_3D ( 'NONE', #248863, #148480, #28582 ) ;
#133818=EDGE_CURVE ( 'NONE', #160208, #40304, #88896, .T. ) ;
#133821=SPHERICAL_SURFACE ( 'NONE', #43430, 0.1000000000000000056 ) ;
#133825=FACE_OUTER_BOUND ( 'NONE', #108651, .T. ) ;
#133829=ORIENTED_EDGE ( 'NONE', *, *, #194513, .T. ) ;
#133864=CARTESIAN_POINT ( 'NONE',  ( -21.14999999999999858, -0.09999999998884338825, -88.85042919245522341 ) ) ;
#133884=DIRECTION ( 'NONE',  ( -3.265361837132813093E-16, 1.000000000000000000, 0.000000000000000000 ) ) ;
#133885=( BOUNDED_CURVE ( )  B_SPLINE_CURVE ( 3, ( #138237, #195695, #178707, #212673 ),
 .UNSPECIFIED., .F., .F. ) 
 B_SPLINE_CURVE_WITH_KNOTS ( ( 4, 4 ),
 ( 1.570796326794896558, 3.141592653589793116 ),
 .UNSPECIFIED. ) 
 CURVE ( )  GEOMETRIC_REPRESENTATION_ITEM ( )  RATIONAL_B_SPLINE_CURVE ( ( 1.000000000000000000, 0.8047378541243649375, 0.8047378541243649375, 1.000000000000000000 ) ) 
 REPRESENTATION_ITEM ( '' )  );
#133905=CARTESIAN_POINT ( 'NONE',  ( 21.07964655665547582, 8.774889614989714204, -112.7219165829640843 ) ) ;
#133909=EDGE_CURVE ( 'NONE', #37861, #144467, #134447, .T. ) ;
#133911=AXIS2_PLACEMENT_3D ( 'NONE', #11182, #209372, #52857 ) ;
#133912=ORIENTED_EDGE ( 'NONE', *, *, #93140, .F. ) ;
#133951=ORIENTED_EDGE ( 'NONE', *, *, #98361, .T. ) ;
#133988=EDGE_CURVE ( 'NONE', #229099, #255159, #63737, .T. ) ;
#134031=CARTESIAN_POINT ( 'NONE',  ( 18.59999999999999076, 1.835341550235567887, -112.0551512925630249 ) ) ;
#134078=ORIENTED_EDGE ( 'NONE', *, *, #240644, .T. ) ;
#134083=DIRECTION ( 'NONE',  ( 3.616040088954497272E-32, -1.224646799147352961E-16, 1.000000000000000000 ) ) ;
#134094=ORIENTED_EDGE ( 'NONE', *, *, #28625, .F. ) ;
#134123=FACE_OUTER_BOUND ( 'NONE', #39756, .T. ) ;
#134149=CARTESIAN_POINT ( 'NONE',  ( -21.14999999999999858, 1.115600667400684642E-11, -88.85042919245522341 ) ) ;
#134165=DIRECTION ( 'NONE',  ( 0.000000000000000000, 0.000000000000000000, -1.000000000000000000 ) ) ;
#134209=DIRECTION ( 'NONE',  ( 0.000000000000000000, 0.000000000000000000, -1.000000000000000000 ) ) ;
#134210=VERTEX_POINT ( 'NONE', #183857 ) ;
#134220=ORIENTED_EDGE ( 'NONE', *, *, #257494, .F. ) ;
#134229=CARTESIAN_POINT ( 'NONE',  ( -21.05000000000000426, 6.332272273946814245, -100.5375360632857138 ) ) ;
#134233=ADVANCED_FACE ( 'NONE', ( #242541 ), #182595, .T. ) ;
#134245=CARTESIAN_POINT ( 'NONE',  ( -18.39999999999999858, -9.499999999988849808, -107.5320693966997112 ) ) ;
#134253=DIRECTION ( 'NONE',  ( -1.000000000000000000, 0.000000000000000000, 0.000000000000000000 ) ) ;
#134255=DIRECTION ( 'NONE',  ( 0.000000000000000000, 0.000000000000000000, -1.000000000000000000 ) ) ;
#134258=FACE_OUTER_BOUND ( 'NONE', #256055, .T. ) ;
#134281=DIRECTION ( 'NONE',  ( -0.000000000000000000, -0.000000000000000000, 1.000000000000000000 ) ) ;
#134291=CARTESIAN_POINT ( 'NONE',  ( -20.94999999999999929, 0.2561057921033771945, -100.4651035583277405 ) ) ;
#134306=ORIENTED_EDGE ( 'NONE', *, *, #23322, .F. ) ;
#134324=DIRECTION ( 'NONE',  ( -0.000000000000000000, 0.8660254037844383745, -0.5000000000000003331 ) ) ;
#134333=CARTESIAN_POINT ( 'NONE',  ( 22.57320508075687115, 11.75000000001115552, -100.5000000000000284 ) ) ;
#134355=AXIS2_PLACEMENT_3D ( 'NONE', #11206, #88130, #244661 ) ;
#134376=ORIENTED_EDGE ( 'NONE', *, *, #157163, .F. ) ;
#134418=VECTOR ( 'NONE', #239481, 1000.000000000000000 ) ;
#134447=CIRCLE ( 'NONE', #251147, 7.720710678118663850 ) ;
#134480=ORIENTED_EDGE ( 'NONE', *, *, #240732, .T. ) ;
#134502=CARTESIAN_POINT ( 'NONE',  ( 21.14999999999999858, 6.650000000011155876, -112.6500000000000341 ) ) ;
#134506=LINE ( 'NONE', #40606, #44300 ) ;
#134511=CARTESIAN_POINT ( 'NONE',  ( 18.50000000000000000, -9.499999999988842703, -107.5320693966997112 ) ) ;
#134521=ORIENTED_EDGE ( 'NONE', *, *, #57040, .T. ) ;
#134537=CIRCLE ( 'NONE', #22155, 0.09999999999999939493 ) ;
#134538=ORIENTED_EDGE ( 'NONE', *, *, #96442, .T. ) ;
#134545=CARTESIAN_POINT ( 'NONE',  ( -18.59999999999999787, -1.162701749926853712, -108.6000000000000227 ) ) ;
#134567=CARTESIAN_POINT ( 'NONE',  ( -21.05000000000000071, 5.850000000011105428, -110.6324972242780120 ) ) ;
#134568=FACE_OUTER_BOUND ( 'NONE', #113057, .T. ) ;
#134570=LINE ( 'NONE', #13371, #86051 ) ;
#134588=AXIS2_PLACEMENT_3D ( 'NONE', #40753, #17317, #78543 ) ;
#134598=LINE ( 'NONE', #77205, #249557 ) ;
#134615=PLANE ( 'NONE',  #193912 ) ;
#134627=DIRECTION ( 'NONE',  ( 0.000000000000000000, -0.5000000000000078826, -0.8660254037844340447 ) ) ;
#134664=AXIS2_PLACEMENT_3D ( 'NONE', #183248, #185806, #48861 ) ;
#134692=DIRECTION ( 'NONE',  ( 0.000000000000000000, -1.000000000000000000, 0.000000000000000000 ) ) ;
#134697=DIRECTION ( 'NONE',  ( 1.000000000000000000, 0.000000000000000000, 0.000000000000000000 ) ) ;
#134708=AXIS2_PLACEMENT_3D ( 'NONE', #18988, #158538, #170761 ) ;
#134716=DIRECTION ( 'NONE',  ( -0.000000000000000000, -0.1298341882519805091, -0.9915357197604881545 ) ) ;
#134778=EDGE_CURVE ( 'NONE', #102643, #6436, #192725, .T. ) ;
#134803=ADVANCED_FACE ( 'NONE', ( #191278 ), #171718, .T. ) ;
#134805=ORIENTED_EDGE ( 'NONE', *, *, #245354, .F. ) ;
#134814=CARTESIAN_POINT ( 'NONE',  ( -18.50000000000000000, -1.736257131586239844, -112.0686523290175245 ) ) ;
#134816=CARTESIAN_POINT ( 'NONE',  ( 20.94999999999999929, 1.115600667400684642E-11, -100.5000000000000284 ) ) ;
#134822=AXIS2_PLACEMENT_3D ( 'NONE', #253679, #150748, #93329 ) ;
#134833=VECTOR ( 'NONE', #146282, 1000.000000000000000 ) ;
#134835=CARTESIAN_POINT ( 'NONE',  ( 23.14999999999999858, 1.115600667400684642E-11, -134.0000000000000284 ) ) ;
#134906=LINE ( 'NONE', #214461, #233058 ) ;
#134910=DIRECTION ( 'NONE',  ( 0.000000000000000000, 0.1350103645451876666, -0.9908441862701600211 ) ) ;
#134982=FACE_OUTER_BOUND ( 'NONE', #182121, .T. ) ;
#134998=CARTESIAN_POINT ( 'NONE',  ( -21.44999999999999929, 7.350000000011155166, -121.6500000000000341 ) ) ;
#135000=CARTESIAN_POINT ( 'NONE',  ( 21.05000000000000071, -8.730841121484166578, -124.4019252810156928 ) ) ;
#135008=AXIS2_PLACEMENT_3D ( 'NONE', #229399, #91157, #172023 ) ;
#135037=CARTESIAN_POINT ( 'NONE',  ( 18.59999999999999432, -1.162701749926853712, -108.5000000000000426 ) ) ;
#135050=DIRECTION ( 'NONE',  ( 0.000000000000000000, 0.000000000000000000, 1.000000000000000000 ) ) ;
#135079=EDGE_CURVE ( 'NONE', #163256, #20965, #159839, .T. ) ;
#135092=DIRECTION ( 'NONE',  ( 1.000000000000000000, -0.000000000000000000, -0.000000000000000000 ) ) ;
#135160=DIRECTION ( 'NONE',  ( 0.000000000000000000, 0.000000000000000000, 1.000000000000000000 ) ) ;
#135189=DIRECTION ( 'NONE',  ( -7.304098846218134667E-16, -1.000000000000000000, 0.000000000000000000 ) ) ;
#135214=CIRCLE ( 'NONE', #22828, 0.09999999999999892308 ) ;
#135219=FACE_OUTER_BOUND ( 'NONE', #232524, .T. ) ;
#135221=CARTESIAN_POINT ( 'NONE',  ( 23.14999999999999858, 5.000000000011153745, -112.9052660189131245 ) ) ;
#135244=EDGE_LOOP ( 'NONE', ( #57638, #87119, #20138, #249925 ) ) ;
#135249=EDGE_LOOP ( 'NONE', ( #113452, #135288, #206979, #30304 ) ) ;
#135288=ORIENTED_EDGE ( 'NONE', *, *, #64967, .T. ) ;
#135303=LINE ( 'NONE', #119624, #157217 ) ;
#135310=CARTESIAN_POINT ( 'NONE',  ( -22.59999999999999787, 11.64957080755595520, -100.4000000000000483 ) ) ;
#135357=EDGE_LOOP ( 'NONE', ( #246136, #50513, #188286, #63649 ) ) ;
#135359=DIRECTION ( 'NONE',  ( 2.952720810173289112E-16, -1.000000000000000000, 0.000000000000000000 ) ) ;
#135367=CARTESIAN_POINT ( 'NONE',  ( -18.50000000000000000, 3.912899247244609580, -111.9818229730110062 ) ) ;
#135391=CARTESIAN_POINT ( 'NONE',  ( 20.94999999999999929, 5.850000000011156942, -123.8675027757221159 ) ) ;
#135416=AXIS2_PLACEMENT_3D ( 'NONE', #126899, #69513, #250685 ) ;
#135426=FACE_OUTER_BOUND ( 'NONE', #105349, .T. ) ;
#135448=FACE_OUTER_BOUND ( 'NONE', #209559, .T. ) ;
#135453=CARTESIAN_POINT ( 'NONE',  ( 21.09696443733127325, 10.72400988392963228, -112.7347775270482657 ) ) ;
#135493=EDGE_CURVE ( 'NONE', #26411, #200879, #238874, .T. ) ;
#135513=EDGE_CURVE ( 'NONE', #96344, #172822, #47304, .T. ) ;
#135529=CARTESIAN_POINT ( 'NONE',  ( -18.46856557590792391, -9.474215907775336731, -107.6019862408823116 ) ) ;
#135541=CARTESIAN_POINT ( 'NONE',  ( -21.05000000000000071, -9.519327731081284938, -107.4729763765593589 ) ) ;
#135551=DIRECTION ( 'NONE',  ( 0.7070776581708965169, 0.000000000000000000, 0.7071359030027827286 ) ) ;
#135696=CARTESIAN_POINT ( 'NONE',  ( -23.15000000000000213, 1.115600667400684642E-11, -100.5000000000000284 ) ) ;
#135738=DIRECTION ( 'NONE',  ( 1.000000000000000000, 0.000000000000000000, 0.000000000000000000 ) ) ;
#135757=AXIS2_PLACEMENT_3D ( 'NONE', #155003, #18025, #59697 ) ;
#135828=VERTEX_POINT ( 'NONE', #37230 ) ;
#135831=VERTEX_POINT ( 'NONE', #3203 ) ;
#135833=CARTESIAN_POINT ( 'NONE',  ( -21.13498764882296044, 0.001656394742484908677, -94.00438185652609491 ) ) ;
#135844=VECTOR ( 'NONE', #151233, 1000.000000000000000 ) ;
#135846=VERTEX_POINT ( 'NONE', #116747 ) ;
#135849=LINE ( 'NONE', #4996, #85500 ) ;
#135851=CARTESIAN_POINT ( 'NONE',  ( 23.14999999999999503, 6.650000000011155876, -112.7500000000000284 ) ) ;
#135874=B_SPLINE_CURVE_WITH_KNOTS ( 'NONE', 3,
 ( #141448, #44930, #206569, #240560, #82728, #203992, #4498 ),
 .UNSPECIFIED., .F., .F.,
 ( 4, 3, 4 ),
 ( 0.000000000000000000, 0.0009834301579439998740, 0.001767853679402675614 ),
 .UNSPECIFIED. ) ;
#135893=EDGE_CURVE ( 'NONE', #188307, #238064, #222457, .T. ) ;
#135896=ORIENTED_EDGE ( 'NONE', *, *, #137352, .F. ) ;
#135915=DIRECTION ( 'NONE',  ( 0.000000000000000000, -0.8660254037844384856, 0.5000000000000003331 ) ) ;
#135975=CARTESIAN_POINT ( 'NONE',  ( -23.25000000000000000, -1.164121893230052995, -141.9148480855716343 ) ) ;
#135984=CARTESIAN_POINT ( 'NONE',  ( -23.15000000000000213, 2.500000000011154633, -120.7753780772379315 ) ) ;
#136000=AXIS2_PLACEMENT_3D ( 'NONE', #113599, #133166, #236111 ) ;
#136031=CIRCLE ( 'NONE', #131785, 0.1999999999999987899 ) ;
#136041=EDGE_CURVE ( 'NONE', #249313, #30919, #97550, .T. ) ;
#136052=DIRECTION ( 'NONE',  ( -0.000000000000000000, -0.000000000000000000, -1.000000000000000000 ) ) ;
#136058=AXIS2_PLACEMENT_3D ( 'NONE', #5778, #257829, #256541 ) ;
#136072=CARTESIAN_POINT ( 'NONE',  ( -20.54999999999999716, 7.150000000011155876, -112.8500000000000369 ) ) ;
#136102=EDGE_CURVE ( 'NONE', #237605, #138314, #138204, .T. ) ;
#136122=ORIENTED_EDGE ( 'NONE', *, *, #227842, .F. ) ;
#136179=CARTESIAN_POINT ( 'NONE',  ( 21.05000000000000071, 4.813084112160684214, -122.0584822434762060 ) ) ;
#136225=DIRECTION ( 'NONE',  ( -1.000000000000000000, -0.000000000000000000, -0.000000000000000000 ) ) ;
#136230=CARTESIAN_POINT ( 'NONE',  ( 18.49999999999998934, 6.650000000011155876, -112.8500000000000369 ) ) ;
#136262=CARTESIAN_POINT ( 'NONE',  ( -21.05000000000000426, 6.497017786443685772, -100.5145456905711256 ) ) ;
#136287=TOROIDAL_SURFACE ( 'NONE', #77862, 11.70000000000000462, 0.1000000000000000056 ) ;
#136298=DIRECTION ( 'NONE',  ( -1.000000000000000000, 0.000000000000000000, 0.000000000000000000 ) ) ;
#136302=PLANE ( 'NONE',  #146098 ) ;
#136306=DIRECTION ( 'NONE',  ( 0.000000000000000000, -0.9908441862701596881, 0.1350103645451904977 ) ) ;
#136316=DIRECTION ( 'NONE',  ( 0.000000000000000000, 0.000000000000000000, -1.000000000000000000 ) ) ;
#136337=LINE ( 'NONE', #52974, #115060 ) ;
#136356=DIRECTION ( 'NONE',  ( 0.000000000000000000, 1.000000000000000000, 0.000000000000000000 ) ) ;
#136374=DIRECTION ( 'NONE',  ( 0.000000000000000000, -0.1350103645451876666, -0.9908441862701600211 ) ) ;
#136389=CARTESIAN_POINT ( 'NONE',  ( -18.50000000000000000, -9.399999999988850163, -107.7972597596633193 ) ) ;
#136423=FACE_OUTER_BOUND ( 'NONE', #175030, .T. ) ;
#136463=DIRECTION ( 'NONE',  ( 0.000000000000000000, 0.000000000000000000, 1.000000000000000000 ) ) ;
#136471=DIRECTION ( 'NONE',  ( 0.000000000000000000, 0.1495327102803586661, 0.9887567792719350601 ) ) ;
#136475=ORIENTED_EDGE ( 'NONE', *, *, #252273, .F. ) ;
#136480=AXIS2_PLACEMENT_3D ( 'NONE', #249764, #107677, #166408 ) ;
#136511=ORIENTED_EDGE ( 'NONE', *, *, #42577, .F. ) ;
#136583=FACE_OUTER_BOUND ( 'NONE', #251158, .T. ) ;
#136584=CARTESIAN_POINT ( 'NONE',  ( -21.29999999999995808, 1.115600667400684642E-11, -100.5000000000000284 ) ) ;
#136595=VECTOR ( 'NONE', #8108, 1000.000000000000000 ) ;
#136609=CYLINDRICAL_SURFACE ( 'NONE', #147120, 0.09999999999999939493 ) ;
#136623=CIRCLE ( 'NONE', #157340, 0.5000000000000004441 ) ;
#136641=DIRECTION ( 'NONE',  ( 0.000000000000000000, 1.000000000000000000, 0.000000000000000000 ) ) ;
#136669=ORIENTED_EDGE ( 'NONE', *, *, #178712, .F. ) ;
#136677=AXIS2_PLACEMENT_3D ( 'NONE', #183230, #39889, #144073 ) ;
#136763=AXIS2_PLACEMENT_3D ( 'NONE', #98715, #105128, #205540 ) ;
#136765=ORIENTED_EDGE ( 'NONE', *, *, #192191, .T. ) ;
#136770=EDGE_CURVE ( 'NONE', #4150, #252923, #77099, .T. ) ;
#136780=VERTEX_POINT ( 'NONE', #33414 ) ;
#136806=AXIS2_PLACEMENT_3D ( 'NONE', #26271, #110931, #7995 ) ;
#136810=AXIS2_PLACEMENT_3D ( 'NONE', #187952, #11899, #211367 ) ;
#136869=VECTOR ( 'NONE', #124005, 1000.000000000000000 ) ;
#136927=DIRECTION ( 'NONE',  ( -1.000000000000000000, 0.000000000000000000, 0.000000000000000000 ) ) ;
#136952=CARTESIAN_POINT ( 'NONE',  ( 20.94999999999999929, 6.550000000011156231, -112.6500000000000341 ) ) ;
#136987=CARTESIAN_POINT ( 'NONE',  ( -22.39999999999999858, 7.790779598384560245, -100.5000000000000284 ) ) ;
#136989=DIRECTION ( 'NONE',  ( 1.000000000000000000, 0.000000000000000000, 0.000000000000000000 ) ) ;
#137007=DIRECTION ( 'NONE',  ( 1.000000000000000000, 0.000000000000000000, 0.000000000000000000 ) ) ;
#137008=CIRCLE ( 'NONE', #253689, 0.09999999999998898659 ) ;
#137020=EDGE_CURVE ( 'NONE', #40869, #179371, #31541, .T. ) ;
#137037=DIRECTION ( 'NONE',  ( -1.000000000000000000, 3.469446951953635015E-14, 0.000000000000000000 ) ) ;
#137045=CARTESIAN_POINT ( 'NONE',  ( -20.94999999999999929, -11.74999999998884448, -103.4000000000000341 ) ) ;
#137051=ORIENTED_EDGE ( 'NONE', *, *, #233616, .T. ) ;
#137068=ORIENTED_EDGE ( 'NONE', *, *, #229216, .F. ) ;
#137093=DIRECTION ( 'NONE',  ( 0.000000000000000000, 0.000000000000000000, -1.000000000000000000 ) ) ;
#137122=CARTESIAN_POINT ( 'NONE',  ( 20.04142135623730070, 11.65000000001115943, -121.8500000000000369 ) ) ;
#137137=VERTEX_POINT ( 'NONE', #14508 ) ;
#137204=CIRCLE ( 'NONE', #253715, 12.77499999999999503 ) ;
#137207=CARTESIAN_POINT ( 'NONE',  ( -23.15000000000000213, 11.60000000001115517, -127.0717967697245143 ) ) ;
#137215=DIRECTION ( 'NONE',  ( 0.000000000000000000, -0.000000000000000000, -1.000000000000000000 ) ) ;
#137270=CARTESIAN_POINT ( 'NONE',  ( -20.54999999999999716, 2.500000000011154633, -120.7753780772379315 ) ) ;
#137271=VERTEX_POINT ( 'NONE', #136987 ) ;
#137302=DIRECTION ( 'NONE',  ( 1.000000000000000000, -0.000000000000000000, -0.000000000000000000 ) ) ;
#137319=DIRECTION ( 'NONE',  ( -1.000000000000000000, 0.000000000000000000, 0.000000000000000000 ) ) ;
#137352=EDGE_CURVE ( 'NONE', #242494, #95316, #79564, .T. ) ;
#137376=EDGE_CURVE ( 'NONE', #102466, #30919, #173205, .T. ) ;
#137387=PLANE ( 'NONE',  #48004 ) ;
#137440=VECTOR ( 'NONE', #50034, 1000.000000000000000 ) ;
#137447=CIRCLE ( 'NONE', #245802, 12.97499999999999964 ) ;
#137472=CARTESIAN_POINT ( 'NONE',  ( -22.39999999999999503, 7.790779598384560245, -100.4000000000000341 ) ) ;
#137492=ORIENTED_EDGE ( 'NONE', *, *, #85711, .F. ) ;
#137537=ORIENTED_EDGE ( 'NONE', *, *, #88689, .T. ) ;
#137549=DIRECTION ( 'NONE',  ( -1.000000000000000000, 0.000000000000000000, 0.000000000000000000 ) ) ;
#137556=CARTESIAN_POINT ( 'NONE',  ( -21.05000000000000071, 6.413662734880552385, -100.5855928633623790 ) ) ;
#137557=CARTESIAN_POINT ( 'NONE',  ( 21.14999999999999858, 11.65000000001115943, -112.6500000000000341 ) ) ;
#137567=DIRECTION ( 'NONE',  ( -1.000000000000000000, -0.000000000000000000, 0.000000000000000000 ) ) ;
#137571=ORIENTED_EDGE ( 'NONE', *, *, #97017, .F. ) ;
#137583=EDGE_CURVE ( 'NONE', #145162, #110428, #155222, .T. ) ;
#137593=DIRECTION ( 'NONE',  ( -0.000000000000000000, 0.000000000000000000, -1.000000000000000000 ) ) ;
#137601=DIRECTION ( 'NONE',  ( 1.000000000000000000, -0.000000000000000000, -0.000000000000000000 ) ) ;
#137661=DIRECTION ( 'NONE',  ( -0.000000000000000000, -0.000000000000000000, 1.000000000000000000 ) ) ;
#137672=CARTESIAN_POINT ( 'NONE',  ( -21.14999999999999858, -11.74999999998884448, -100.5000000000000284 ) ) ;
#137679=FACE_OUTER_BOUND ( 'NONE', #162015, .T. ) ;
#137687=CIRCLE ( 'NONE', #108490, 7.900000000000000355 ) ;
#137694=CIRCLE ( 'NONE', #171095, 0.2000000000000057288 ) ;
#137724=ADVANCED_FACE ( 'NONE', ( #67407 ), #80308, .T. ) ;
#137729=ORIENTED_EDGE ( 'NONE', *, *, #93768, .T. ) ;
#137767=DIRECTION ( 'NONE',  ( 0.000000000000000000, 0.000000000000000000, -1.000000000000000000 ) ) ;
#137812=EDGE_LOOP ( 'NONE', ( #251860, #114682, #198499, #217740 ) ) ;
#137822=CIRCLE ( 'NONE', #112898, 0.1000000000000028644 ) ;
#137825=ORIENTED_EDGE ( 'NONE', *, *, #90610, .T. ) ;
#137832=FACE_OUTER_BOUND ( 'NONE', #89148, .T. ) ;
#137850=ORIENTED_EDGE ( 'NONE', *, *, #175835, .F. ) ;
#137855=FACE_OUTER_BOUND ( 'NONE', #142554, .T. ) ;
#137864=CARTESIAN_POINT ( 'NONE',  ( 21.14999999999999858, 11.65000000001115943, -112.6500000000000341 ) ) ;
#137867=CARTESIAN_POINT ( 'NONE',  ( 20.94999999999999929, 1.115600667400684642E-11, -134.0000000000000284 ) ) ;
#137870=DIRECTION ( 'NONE',  ( 1.000000000000000000, -0.000000000000000000, -0.000000000000000000 ) ) ;
#137879=EDGE_LOOP ( 'NONE', ( #17796, #176364, #231236, #202880 ) ) ;
#137916=ORIENTED_EDGE ( 'NONE', *, *, #237566, .T. ) ;
#137922=DIRECTION ( 'NONE',  ( -1.000000000000000000, -2.952720810173289112E-16, 0.000000000000000000 ) ) ;
#137929=EDGE_CURVE ( 'NONE', #142111, #217887, #159474, .T. ) ;
#137941=DIRECTION ( 'NONE',  ( 0.000000000000000000, 0.000000000000000000, -1.000000000000000000 ) ) ;
#137949=CARTESIAN_POINT ( 'NONE',  ( -23.25000000000000000, 11.75000000001115552, -100.5000000000000284 ) ) ;
#137966=DIRECTION ( 'NONE',  ( -7.304098846218134667E-16, -1.000000000000000000, 0.000000000000000000 ) ) ;
#137976=EDGE_CURVE ( 'NONE', #110957, #224935, #251023, .T. ) ;
#137999=EDGE_CURVE ( 'NONE', #186169, #197596, #30490, .T. ) ;
#138003=ORIENTED_EDGE ( 'NONE', *, *, #74145, .T. ) ;
#138015=DIRECTION ( 'NONE',  ( 1.000000000000000000, 0.000000000000000000, 0.000000000000000000 ) ) ;
#138043=CIRCLE ( 'NONE', #100611, 2.000000000000001776 ) ;
#138046=EDGE_LOOP ( 'NONE', ( #235342, #249305, #249013, #216995 ) ) ;
#138061=DIRECTION ( 'NONE',  ( 1.000000000000000000, 0.000000000000000000, -0.000000000000000000 ) ) ;
#138064=VERTEX_POINT ( 'NONE', #219746 ) ;
#138109=DIRECTION ( 'NONE',  ( -1.000000000000000000, -7.304098846218134667E-16, 0.000000000000000000 ) ) ;
#138121=DIRECTION ( 'NONE',  ( 0.000000000000000000, 0.000000000000000000, -1.000000000000000000 ) ) ;
#138138=ORIENTED_EDGE ( 'NONE', *, *, #232337, .T. ) ;
#138140=CARTESIAN_POINT ( 'NONE',  ( -21.14999999999999858, 11.75000000001115552, -107.2261306360592243 ) ) ;
#138176=CARTESIAN_POINT ( 'NONE',  ( 18.49999999999999289, 10.44006789215403330, -125.2671177488814607 ) ) ;
#138204=LINE ( 'NONE', #178682, #180805 ) ;
#138209=CARTESIAN_POINT ( 'NONE',  ( 18.39999999999999858, -9.682403433465241349, -140.6568433774128266 ) ) ;
#138237=CARTESIAN_POINT ( 'NONE',  ( 18.49999999999999289, 10.49142135624846439, -125.3500000000000512 ) ) ;
#138247=CIRCLE ( 'NONE', #213087, 4.000000000000003553 ) ;
#138265=ORIENTED_EDGE ( 'NONE', *, *, #107408, .F. ) ;
#138266=LINE ( 'NONE', #20941, #177986 ) ;
#138285=EDGE_CURVE ( 'NONE', #14082, #59138, #88894, .T. ) ;
#138309=DIRECTION ( 'NONE',  ( 0.000000000000000000, -0.9893560106964500722, 0.1455152366551550613 ) ) ;
#138314=VERTEX_POINT ( 'NONE', #17402 ) ;
#138367=CARTESIAN_POINT ( 'NONE',  ( -21.05000000000000071, 5.900000000011102586, -110.7190997646564483 ) ) ;
#138370=CARTESIAN_POINT ( 'NONE',  ( -20.85000000000000142, -1.835859311432481045, -145.5044391687985694 ) ) ;
#138378=DIRECTION ( 'NONE',  ( 0.000000000000000000, -1.000000000000000000, 0.000000000000000000 ) ) ;
#138388=ORIENTED_EDGE ( 'NONE', *, *, #28824, .T. ) ;
#138406=ORIENTED_EDGE ( 'NONE', *, *, #185636, .T. ) ;
#138424=DIRECTION ( 'NONE',  ( 1.000000000000000000, 0.000000000000000000, 0.000000000000000000 ) ) ;
#138450=DIRECTION ( 'NONE',  ( 1.875376730785737719E-16, -1.000000000000000000, 0.000000000000000000 ) ) ;
#138487=CARTESIAN_POINT ( 'NONE',  ( 23.24999999999999645, 1.115600667400684642E-11, -134.0000000000000284 ) ) ;
#138541=CARTESIAN_POINT ( 'NONE',  ( 18.49999999999998934, 6.550000000011156231, -110.5170271704400591 ) ) ;
#138561=CARTESIAN_POINT ( 'NONE',  ( 20.94999999999999929, 5.900000000011162093, -123.7809002353436654 ) ) ;
#138576=AXIS2_PLACEMENT_3D ( 'NONE', #130325, #72968, #194186 ) ;
#138592=AXIS2_PLACEMENT_3D ( 'NONE', #195771, #138309, #101741 ) ;
#138610=ORIENTED_EDGE ( 'NONE', *, *, #250962, .T. ) ;
#138619=EDGE_CURVE ( 'NONE', #72909, #85365, #238955, .T. ) ;
#138628=CARTESIAN_POINT ( 'NONE',  ( 23.25000000000000000, -11.64999999998883595, -130.9000000000000341 ) ) ;
#138643=ORIENTED_EDGE ( 'NONE', *, *, #124385, .F. ) ;
#138663=DIRECTION ( 'NONE',  ( 0.000000000000000000, -1.000000000000000000, 2.775557561562884094E-14 ) ) ;
#138684=CIRCLE ( 'NONE', #26317, 7.899999999999990585 ) ;
#138713=CARTESIAN_POINT ( 'NONE',  ( 21.05000000000000071, -0.02138556592644420135, -94.19503888731547647 ) ) ;
#138728=DIRECTION ( 'NONE',  ( 0.000000000000000000, -0.9908441862701596881, -0.1350103645451904977 ) ) ;
#138733=AXIS2_PLACEMENT_3D ( 'NONE', #14899, #250905, #13603 ) ;
#138756=DIRECTION ( 'NONE',  ( -0.000000000000000000, -0.000000000000000000, 1.000000000000000000 ) ) ;
#138769=VECTOR ( 'NONE', #45341, 1000.000000000000000 ) ;
#138779=CARTESIAN_POINT ( 'NONE',  ( 18.49999999999999645, -1.835859311432484375, -145.5044391687985694 ) ) ;
#138863=CARTESIAN_POINT ( 'NONE',  ( -22.50000000000000000, 11.75000000001115552, -100.5000000000000284 ) ) ;
#138864=TOROIDAL_SURFACE ( 'NONE', #63907, 11.70000000000000107, 0.1000000000000000056 ) ;
#138880=CIRCLE ( 'NONE', #226380, 11.64999999999999325 ) ;
#138893=CARTESIAN_POINT ( 'NONE',  ( 23.24999999999999645, 4.775700934590591196, -122.1512318959540551 ) ) ;
#138902=VECTOR ( 'NONE', #83029, 1000.000000000000000 ) ;
#138917=ORIENTED_EDGE ( 'NONE', *, *, #106827, .T. ) ;
#138944=ORIENTED_EDGE ( 'NONE', *, *, #97017, .T. ) ;
#138965=FACE_OUTER_BOUND ( 'NONE', #58892, .T. ) ;
#139002=DIRECTION ( 'NONE',  ( -0.000000000000000000, 0.000000000000000000, 1.000000000000000000 ) ) ;
#139013=CIRCLE ( 'NONE', #30942, 0.1000000000000028644 ) ;
#139041=DIRECTION ( 'NONE',  ( 1.000000000000000000, -0.000000000000000000, -0.000000000000000000 ) ) ;
#139053=ORIENTED_EDGE ( 'NONE', *, *, #240337, .F. ) ;
#139065=ORIENTED_EDGE ( 'NONE', *, *, #99677, .T. ) ;
#139107=DIRECTION ( 'NONE',  ( -0.000000000000000000, 0.8660254037844502539, 0.4999999999999799050 ) ) ;
#139172=VECTOR ( 'NONE', #30859, 1000.000000000000227 ) ;
#139173=CIRCLE ( 'NONE', #185000, 0.09999999999999971412 ) ;
#139191=ORIENTED_EDGE ( 'NONE', *, *, #111558, .T. ) ;
#139192=FACE_OUTER_BOUND ( 'NONE', #149820, .T. ) ;
#139277=ORIENTED_EDGE ( 'NONE', *, *, #150665, .T. ) ;
#139284=EDGE_CURVE ( 'NONE', #208590, #246420, #78970, .T. ) ;
#139293=EDGE_CURVE ( 'NONE', #25027, #193635, #188660, .T. ) ;
#139326=FACE_OUTER_BOUND ( 'NONE', #18828, .T. ) ;
#139339=DIRECTION ( 'NONE',  ( -1.000000000000000000, 0.000000000000000000, 0.000000000000000000 ) ) ;
#139344=EDGE_CURVE ( 'NONE', #203753, #186169, #109544, .T. ) ;
#139347=DIRECTION ( 'NONE',  ( 1.000000000000000000, 0.000000000000000000, 0.000000000000000000 ) ) ;
#139348=EDGE_LOOP ( 'NONE', ( #94385, #160126, #9471, #115008 ) ) ;
#139360=CARTESIAN_POINT ( 'NONE',  ( 23.15000000000000213, -8.596261682231833845, -109.9501275171503210 ) ) ;
#139374=CARTESIAN_POINT ( 'NONE',  ( -18.42554971533678199, -9.497159669426592288, -107.5398269135486800 ) ) ;
#139375=EDGE_CURVE ( 'NONE', #150422, #144467, #105426, .T. ) ;
#139379=CARTESIAN_POINT ( 'NONE',  ( -18.59999999999999787, 7.021664781911246322, -137.6335654018973287 ) ) ;
#139392=ORIENTED_EDGE ( 'NONE', *, *, #155117, .T. ) ;
#139393=ADVANCED_FACE ( 'NONE', ( #222334 ), #104948, .T. ) ;
#139394=CARTESIAN_POINT ( 'NONE',  ( -21.14999999999999858, -0.09999999998884338825, -94.25000000000002842 ) ) ;
#139396=ORIENTED_EDGE ( 'NONE', *, *, #201848, .F. ) ;
#139399=ADVANCED_FACE ( 'NONE', ( #166283 ), #45016, .F. ) ;
#139414=ORIENTED_EDGE ( 'NONE', *, *, #207935, .T. ) ;
#139421=ORIENTED_EDGE ( 'NONE', *, *, #73362, .F. ) ;
#139424=DIRECTION ( 'NONE',  ( 1.000000000000000000, -0.000000000000000000, -0.000000000000000000 ) ) ;
#139448=DIRECTION ( 'NONE',  ( 1.000000000000000000, -7.304098846218134667E-16, 0.000000000000000000 ) ) ;
#139460=ORIENTED_EDGE ( 'NONE', *, *, #141799, .T. ) ;
#139490=EDGE_CURVE ( 'NONE', #76616, #60113, #147153, .T. ) ;
#139514=CARTESIAN_POINT ( 'NONE',  ( 18.59999999999999432, 1.736257131608553550, -112.0686523290175245 ) ) ;
#139521=ORIENTED_EDGE ( 'NONE', *, *, #6804, .F. ) ;
#139523=ORIENTED_EDGE ( 'NONE', *, *, #238884, .T. ) ;
#139528=CARTESIAN_POINT ( 'NONE',  ( 23.24999999999999645, 5.600000000011153389, -88.75000000000004263 ) ) ;
#139568=ORIENTED_EDGE ( 'NONE', *, *, #179536, .F. ) ;
#139607=ORIENTED_EDGE ( 'NONE', *, *, #42577, .T. ) ;
#139636=AXIS2_PLACEMENT_3D ( 'NONE', #135310, #194045, #214862 ) ;
#139652=VERTEX_POINT ( 'NONE', #37038 ) ;
#139695=ORIENTED_EDGE ( 'NONE', *, *, #218853, .F. ) ;
#139698=CARTESIAN_POINT ( 'NONE',  ( -21.05000000000000071, 0.09779029131994597390, -94.24218538952392521 ) ) ;
#139705=DIRECTION ( 'NONE',  ( 1.000000000000000000, 0.000000000000000000, 0.000000000000000000 ) ) ;
#139707=DIRECTION ( 'NONE',  ( 0.000000000000000000, 0.000000000000000000, -1.000000000000000000 ) ) ;
#139713=CARTESIAN_POINT ( 'NONE',  ( 20.94999999999999929, 1.835341550235569663, -112.0551512925630249 ) ) ;
#139765=EDGE_CURVE ( 'NONE', #241028, #55613, #32758, .T. ) ;
#139797=CYLINDRICAL_SURFACE ( 'NONE', #105192, 0.09999999999999939493 ) ;
#139806=CIRCLE ( 'NONE', #223006, 0.1000000000000028644 ) ;
#139813=DIRECTION ( 'NONE',  ( 0.000000000000000000, 1.000000000000000000, 2.891205793294679805E-16 ) ) ;
#139819=CARTESIAN_POINT ( 'NONE',  ( 23.14999999999999858, 1.115600667400684642E-11, -134.0000000000000284 ) ) ;
#139826=ORIENTED_EDGE ( 'NONE', *, *, #148612, .T. ) ;
#139834=PLANE ( 'NONE',  #229053 ) ;
#139838=DIRECTION ( 'NONE',  ( -1.000000000000000000, -2.952720810173289112E-16, 0.000000000000000000 ) ) ;
#139843=EDGE_CURVE ( 'NONE', #127135, #232908, #245405, .T. ) ;
#139844=CARTESIAN_POINT ( 'NONE',  ( 21.70464131381650219, 7.095358018979006864, -100.5000000000000284 ) ) ;
#139869=AXIS2_PLACEMENT_3D ( 'NONE', #95424, #214090, #138378 ) ;
#139952=EDGE_LOOP ( 'NONE', ( #131368, #125582, #121456, #187691 ) ) ;
#139959=DIRECTION ( 'NONE',  ( 0.000000000000000000, 0.000000000000000000, -1.000000000000000000 ) ) ;
#140016=CARTESIAN_POINT ( 'NONE',  ( 21.05000000000000071, 0.09779029132038109806, -94.24218538951851087 ) ) ;
#140017=ORIENTED_EDGE ( 'NONE', *, *, #124729, .F. ) ;
#140095=AXIS2_PLACEMENT_3D ( 'NONE', #56650, #34581, #134910 ) ;
#140097=CARTESIAN_POINT ( 'NONE',  ( -22.50485643085239928, -0.07878633906603055292, -88.75020506082762495 ) ) ;
#140132=ORIENTED_EDGE ( 'NONE', *, *, #3215, .F. ) ;
#140144=FACE_OUTER_BOUND ( 'NONE', #146442, .T. ) ;
#140212=ORIENTED_EDGE ( 'NONE', *, *, #123348, .F. ) ;
#140247=CARTESIAN_POINT ( 'NONE',  ( 20.94999999999999574, -11.48912529306490349, -103.5000000000000426 ) ) ;
#140281=FACE_OUTER_BOUND ( 'NONE', #27403, .T. ) ;
#140296=EDGE_CURVE ( 'NONE', #53618, #76942, #151651, .T. ) ;
#140354=CARTESIAN_POINT ( 'NONE',  ( -23.15000000000000213, 1.115600667400684642E-11, -134.0000000000000284 ) ) ;
#140362=VERTEX_POINT ( 'NONE', #29918 ) ;
#140425=CARTESIAN_POINT ( 'NONE',  ( 21.05000000000000071, 0.09779029131994770863, -94.24218538952391100 ) ) ;
#140474=VERTEX_POINT ( 'NONE', #138893 ) ;
#140544=DIRECTION ( 'NONE',  ( 1.000000000000000000, 0.000000000000000000, 0.000000000000000000 ) ) ;
#140591=CARTESIAN_POINT ( 'NONE',  ( 20.94999999999999929, 1.115600667400684642E-11, -134.0000000000000284 ) ) ;
#140594=CARTESIAN_POINT ( 'NONE',  ( 21.05000000000000071, 1.115600667400684642E-11, -100.5000000000000284 ) ) ;
#140609=DIRECTION ( 'NONE',  ( -1.000000000000000000, -8.673617379884087537E-15, 0.000000000000000000 ) ) ;
#140611=EDGE_CURVE ( 'NONE', #112449, #229099, #89223, .T. ) ;
#140634=ORIENTED_EDGE ( 'NONE', *, *, #13424, .F. ) ;
#140720=VERTEX_POINT ( 'NONE', #90501 ) ;
#140726=DIRECTION ( 'NONE',  ( -2.978066053179067751E-16, 1.000000000000000000, 0.000000000000000000 ) ) ;
#140729=AXIS2_PLACEMENT_3D ( 'NONE', #33079, #50021, #190856 ) ;
#140744=AXIS2_PLACEMENT_3D ( 'NONE', #161102, #141517, #239347 ) ;
#140780=CARTESIAN_POINT ( 'NONE',  ( -18.50000000000000000, -1.164121893230052995, -141.9148480855716343 ) ) ;
#140786=CARTESIAN_POINT ( 'NONE',  ( -23.15000000000000213, -11.74999999998884448, -100.5000000000000284 ) ) ;
#140800=CIRCLE ( 'NONE', #232588, 0.1000000000000028644 ) ;
#140813=DIRECTION ( 'NONE',  ( 1.000000000000000000, 0.000000000000000000, -0.000000000000000000 ) ) ;
#140847=DIRECTION ( 'NONE',  ( -1.000000000000000000, 0.000000000000000000, 0.000000000000000000 ) ) ;
#140868=ORIENTED_EDGE ( 'NONE', *, *, #254971, .T. ) ;
#140880=CARTESIAN_POINT ( 'NONE',  ( -23.25000000000000000, -1.249999999988843369, -141.8004807544151333 ) ) ;
#140894=DIRECTION ( 'NONE',  ( -2.915501640297153790E-16, 1.000000000000000000, 0.000000000000000000 ) ) ;
#140964=CARTESIAN_POINT ( 'NONE',  ( 18.59999994388910238, -9.363566187059737089, -107.6811172368012848 ) ) ;
#140988=CARTESIAN_POINT ( 'NONE',  ( 18.49999999999999645, 1.162701749949165642, -108.6000000000000227 ) ) ;
#140996=EDGE_CURVE ( 'NONE', #167341, #214263, #185305, .T. ) ;
#141025=DIRECTION ( 'NONE',  ( 1.000000000000000000, 0.000000000000000000, 0.000000000000000000 ) ) ;
#141039=VERTEX_POINT ( 'NONE', #165924 ) ;
#141049=AXIS2_PLACEMENT_3D ( 'NONE', #228854, #252247, #48916 ) ;
#141056=CARTESIAN_POINT ( 'NONE',  ( -23.25000000000000000, 2.000000000011154189, -120.7753780772379315 ) ) ;
#141060=ORIENTED_EDGE ( 'NONE', *, *, #233172, .F. ) ;
#141093=CYLINDRICAL_SURFACE ( 'NONE', #235220, 0.1000000000000028644 ) ;
#141105=EDGE_CURVE ( 'NONE', #74036, #34485, #194475, .T. ) ;
#141112=VECTOR ( 'NONE', #111964, 1000.000000000000000 ) ;
#141123=ORIENTED_EDGE ( 'NONE', *, *, #85711, .T. ) ;
#141157=EDGE_CURVE ( 'NONE', #10689, #180521, #164465, .T. ) ;
#141211=EDGE_CURVE ( 'NONE', #208590, #253025, #147898, .T. ) ;
#141216=CARTESIAN_POINT ( 'NONE',  ( -21.53752568622132557, 0.09897446127749523481, -93.71319212545147082 ) ) ;
#141245=VERTEX_POINT ( 'NONE', #156646 ) ;
#141286=CARTESIAN_POINT ( 'NONE',  ( 21.04999999999999716, 10.68430915749624610, -108.0266967903268807 ) ) ;
#141290=CARTESIAN_POINT ( 'NONE',  ( 18.59999999999999432, 1.162701749949165642, -108.6000000000000227 ) ) ;
#141292=CYLINDRICAL_SURFACE ( 'NONE', #77823, 0.09999999999999939493 ) ;
#141307=DIRECTION ( 'NONE',  ( -1.000000000000000000, -2.952720810173289112E-16, 0.000000000000000000 ) ) ;
#141326=CARTESIAN_POINT ( 'NONE',  ( 21.05000000000000071, -0.09999999998884512298, -93.95934304829877703 ) ) ;
#141352=DIRECTION ( 'NONE',  ( -1.000000000000000000, 0.000000000000000000, 0.000000000000000000 ) ) ;
#141366=EDGE_CURVE ( 'NONE', #20965, #124745, #248018, .T. ) ;
#141372=AXIS2_PLACEMENT_3D ( 'NONE', #157156, #220939, #97113 ) ;
#141383=DIRECTION ( 'NONE',  ( -0.7071067811865474617, 0.7071067811865474617, 0.000000000000000000 ) ) ;
#141393=CIRCLE ( 'NONE', #174770, 4.099999999999992539 ) ;
#141404=DIRECTION ( 'NONE',  ( 1.000000000000000000, 0.000000000000000000, 0.000000000000000000 ) ) ;
#141406=DIRECTION ( 'NONE',  ( 0.000000000000000000, 0.000000000000000000, -1.000000000000000000 ) ) ;
#141409=ADVANCED_FACE ( 'NONE', ( #204700 ), #206005, .T. ) ;
#141445=ORIENTED_EDGE ( 'NONE', *, *, #89721, .T. ) ;
#141448=CARTESIAN_POINT ( 'NONE',  ( -22.39999999999999858, 7.790779598384560245, -100.5000000000000284 ) ) ;
#141456=ORIENTED_EDGE ( 'NONE', *, *, #109385, .F. ) ;
#141498=ORIENTED_EDGE ( 'NONE', *, *, #61700, .F. ) ;
#141517=DIRECTION ( 'NONE',  ( 1.000000000000000000, 0.000000000000000000, -0.000000000000000000 ) ) ;
#141593=ORIENTED_EDGE ( 'NONE', *, *, #100706, .T. ) ;
#141597=DIRECTION ( 'NONE',  ( -2.342056488767301376E-15, -0.1350103645451904977, 0.9908441862701596881 ) ) ;
#141606=CARTESIAN_POINT ( 'NONE',  ( 19.81427058490545789, 11.66856398039208820, -125.2500000000000568 ) ) ;
#141639=ORIENTED_EDGE ( 'NONE', *, *, #43945, .F. ) ;
#141641=CIRCLE ( 'NONE', #195845, 4.049999999999998934 ) ;
#141655=CARTESIAN_POINT ( 'NONE',  ( -18.59999999999999787, 9.350000000011156942, -121.7500000000000426 ) ) ;
#141667=CARTESIAN_POINT ( 'NONE',  ( -18.59999999999999787, -1.851617760457748618, -145.6031897196037050 ) ) ;
#141678=VECTOR ( 'NONE', #182614, 1000.000000000000000 ) ;
#141744=CARTESIAN_POINT ( 'NONE',  ( 23.15000000000000213, -11.64999999998883595, -130.9000000000000341 ) ) ;
#141756=ORIENTED_EDGE ( 'NONE', *, *, #231509, .F. ) ;
#141799=EDGE_CURVE ( 'NONE', #210814, #38481, #69177, .T. ) ;
#141807=CIRCLE ( 'NONE', #183516, 0.09999999999998898659 ) ;
#141808=CARTESIAN_POINT ( 'NONE',  ( 21.05000000000000071, 1.349084418638171412, -108.4864989635455146 ) ) ;
#141840=CARTESIAN_POINT ( 'NONE',  ( -18.48179518609124727, -9.518325300484486107, -140.8897055767626227 ) ) ;
#141861=CIRCLE ( 'NONE', #29483, 0.09999999999998898659 ) ;
#141873=VECTOR ( 'NONE', #74611, 1000.000000000000000 ) ;
#141889=CARTESIAN_POINT ( 'NONE',  ( 23.14999999999999503, 11.65000000001116298, -112.6500000000000341 ) ) ;
#141934=ORIENTED_EDGE ( 'NONE', *, *, #200912, .T. ) ;
#141974=ORIENTED_EDGE ( 'NONE', *, *, #45591, .F. ) ;
#141980=DIRECTION ( 'NONE',  ( 0.000000000000000000, 1.000000000000000000, 0.000000000000000000 ) ) ;
#141985=CARTESIAN_POINT ( 'NONE',  ( -23.15000000000000213, -11.64999999998884483, -100.5000000000000284 ) ) ;
#142011=CIRCLE ( 'NONE', #171301, 4.049999999999998046 ) ;
#142014=AXIS2_PLACEMENT_3D ( 'NONE', #228910, #206778, #112813 ) ;
#142041=CARTESIAN_POINT ( 'NONE',  ( 18.49999999999999289, 10.20857864609425825, -125.2025068656296156 ) ) ;
#142071=EDGE_LOOP ( 'NONE', ( #141756, #212479, #98513, #230517 ) ) ;
#142080=CARTESIAN_POINT ( 'NONE',  ( -18.59999999999999787, -1.835859311432481045, -145.6044391687985637 ) ) ;
#142081=FACE_OUTER_BOUND ( 'NONE', #128471, .T. ) ;
#142084=EDGE_CURVE ( 'NONE', #29706, #8700, #38616, .T. ) ;
#142111=VERTEX_POINT ( 'NONE', #201528 ) ;
#142127=CIRCLE ( 'NONE', #34029, 11.70000000000000284 ) ;
#142221=LINE ( 'NONE', #17458, #10004 ) ;
#142224=FACE_OUTER_BOUND ( 'NONE', #144537, .T. ) ;
#142247=DIRECTION ( 'NONE',  ( 0.000000000000000000, 1.734723475976997999E-14, 1.000000000000000000 ) ) ;
#142271=VERTEX_POINT ( 'NONE', #70722 ) ;
#142286=DIRECTION ( 'NONE',  ( 0.000000000000000000, 1.000000000000000000, 0.000000000000000000 ) ) ;
#142287=FACE_OUTER_BOUND ( 'NONE', #220854, .T. ) ;
#142288=ORIENTED_EDGE ( 'NONE', *, *, #154278, .F. ) ;
#142290=FACE_OUTER_BOUND ( 'NONE', #239274, .T. ) ;
#142299=CARTESIAN_POINT ( 'NONE',  ( 18.49999999999999289, 11.65000000001115943, -125.3500000000000512 ) ) ;
#142304=CARTESIAN_POINT ( 'NONE',  ( 22.32929514600007792, 7.578647565387638174, -100.4009243218861229 ) ) ;
#142309=ORIENTED_EDGE ( 'NONE', *, *, #226884, .F. ) ;
#142314=DIRECTION ( 'NONE',  ( 0.000000000000000000, 0.000000000000000000, 1.000000000000000000 ) ) ;
#142355=ORIENTED_EDGE ( 'NONE', *, *, #49651, .T. ) ;
#142358=ORIENTED_EDGE ( 'NONE', *, *, #150001, .F. ) ;
#142405=ORIENTED_EDGE ( 'NONE', *, *, #227452, .F. ) ;
#142411=VERTEX_POINT ( 'NONE', #240045 ) ;
#142418=EDGE_CURVE ( 'NONE', #120853, #154121, #231657, .T. ) ;
#142425=CARTESIAN_POINT ( 'NONE',  ( 20.94999999999999929, 4.813084112160680661, -112.4415177565238650 ) ) ;
#142429=CARTESIAN_POINT ( 'NONE',  ( -21.05000000000000071, 1.115650877919449575E-11, -138.1000000000000227 ) ) ;
#142477=ORIENTED_EDGE ( 'NONE', *, *, #193060, .F. ) ;
#142554=EDGE_LOOP ( 'NONE', ( #224003, #93306, #195002, #193869 ) ) ;
#142576=CARTESIAN_POINT ( 'NONE',  ( -20.54999999999999716, 2.400000000011155432, -124.1060308773475924 ) ) ;
#142577=DIRECTION ( 'NONE',  ( 0.000000000000000000, 0.000000000000000000, -1.000000000000000000 ) ) ;
#142609=DIRECTION ( 'NONE',  ( -1.000000000000000000, 0.000000000000000000, 0.000000000000000000 ) ) ;
#142628=DIRECTION ( 'NONE',  ( 0.000000000000000000, 2.891205793294679805E-16, -1.000000000000000000 ) ) ;
#142643=LINE ( 'NONE', #123113, #161723 ) ;
#142671=EDGE_CURVE ( 'NONE', #252923, #97941, #251586, .T. ) ;
#142691=ORIENTED_EDGE ( 'NONE', *, *, #17247, .T. ) ;
#142701=ORIENTED_EDGE ( 'NONE', *, *, #28824, .F. ) ;
#142704=CIRCLE ( 'NONE', #92820, 0.1000000000000028644 ) ;
#142771=CARTESIAN_POINT ( 'NONE',  ( 18.49999999999999645, 1.115600667400684642E-11, -100.5000000000000284 ) ) ;
#142773=AXIS2_PLACEMENT_3D ( 'NONE', #160979, #80097, #22763 ) ;
#142777=EDGE_CURVE ( 'NONE', #205, #249334, #40332, .T. ) ;
#142794=CARTESIAN_POINT ( 'NONE',  ( 21.05000000000000071, 6.299230910098046365, -100.4015625000000398 ) ) ;
#142802=CIRCLE ( 'NONE', #42891, 0.1000000000000013933 ) ;
#142813=VERTEX_POINT ( 'NONE', #115935 ) ;
#142831=CARTESIAN_POINT ( 'NONE',  ( 21.05000000000000071, 10.56271494673975120, -107.9568021056449680 ) ) ;
#142851=EDGE_LOOP ( 'NONE', ( #199010, #104604 ) ) ;
#142866=AXIS2_PLACEMENT_3D ( 'NONE', #160634, #143603, #21120 ) ;
#142907=DIRECTION ( 'NONE',  ( 0.000000000000000000, 0.000000000000000000, -1.000000000000000000 ) ) ;
#142934=VERTEX_POINT ( 'NONE', #25814 ) ;
#142968=ORIENTED_EDGE ( 'NONE', *, *, #126028, .F. ) ;
#142972=CARTESIAN_POINT ( 'NONE',  ( 23.15000000000000213, -9.499999999988848032, -110.3939691226524786 ) ) ;
#142993=CARTESIAN_POINT ( 'NONE',  ( 23.14999999999999503, 6.650000000011155876, -121.7500000000000426 ) ) ;
#143041=ADVANCED_FACE ( 'NONE', ( #188729 ), #107910, .F. ) ;
#143136=CYLINDRICAL_SURFACE ( 'NONE', #163768, 0.09999999999999939493 ) ;
#143144=CARTESIAN_POINT ( 'NONE',  ( -21.05000000000000071, -1.835341550213255957, -112.0551512925630107 ) ) ;
#143169=CIRCLE ( 'NONE', #55858, 0.09999999999999939493 ) ;
#143178=EDGE_LOOP ( 'NONE', ( #189054, #141974, #31726, #138610 ) ) ;
#143179=VERTEX_POINT ( 'NONE', #98571 ) ;
#143182=ORIENTED_EDGE ( 'NONE', *, *, #175711, .F. ) ;
#143241=EDGE_LOOP ( 'NONE', ( #147675, #190534, #155843, #247991 ) ) ;
#143286=EDGE_CURVE ( 'NONE', #173371, #139652, #39960, .T. ) ;
#143295=AXIS2_PLACEMENT_3D ( 'NONE', #22533, #370, #82454 ) ;
#143310=PLANE ( 'NONE',  #83886 ) ;
#143325=CARTESIAN_POINT ( 'NONE',  ( 18.49999999999999289, 10.25000000001115730, -125.1500000000000483 ) ) ;
#143328=CARTESIAN_POINT ( 'NONE',  ( -21.45000000000000284, 7.708578643773852157, -121.7500000000000426 ) ) ;
#143337=CARTESIAN_POINT ( 'NONE',  ( -20.85000000000000142, 10.33248238083635151, -139.5948465439131780 ) ) ;
#143352=ORIENTED_EDGE ( 'NONE', *, *, #107713, .T. ) ;
#143385=DIRECTION ( 'NONE',  ( -1.000000000000000000, -1.875376730785737719E-16, -0.000000000000000000 ) ) ;
#143407=FACE_OUTER_BOUND ( 'NONE', #51155, .T. ) ;
#143446=ORIENTED_EDGE ( 'NONE', *, *, #52908, .F. ) ;
#143508=CARTESIAN_POINT ( 'NONE',  ( 18.49713797159848383, -9.446482327567720105, -107.5714581216104193 ) ) ;
#143525=FACE_OUTER_BOUND ( 'NONE', #36700, .T. ) ;
#143546=EDGE_CURVE ( 'NONE', #136780, #188768, #11078, .T. ) ;
#143570=CARTESIAN_POINT ( 'NONE',  ( -21.04999999999931504, 0.05132743235277388572, -94.19981666373327300 ) ) ;
#143580=AXIS2_PLACEMENT_3D ( 'NONE', #107807, #188625, #90798 ) ;
#143587=CARTESIAN_POINT ( 'NONE',  ( -18.59999999999999787, -9.321008403350132809, -107.7359382490779183 ) ) ;
#143603=DIRECTION ( 'NONE',  ( 1.000000000000000000, -0.000000000000000000, -0.000000000000000000 ) ) ;
#143611=DIRECTION ( 'NONE',  ( 0.000000000000000000, 0.000000000000000000, -1.000000000000000000 ) ) ;
#143629=CARTESIAN_POINT ( 'NONE',  ( -18.59999999999999787, 7.021664781911246322, -137.8335654018973457 ) ) ;
#143633=DIRECTION ( 'NONE',  ( -1.000000000000000000, 0.000000000000000000, 0.000000000000000000 ) ) ;
#143640=AXIS2_PLACEMENT_3D ( 'NONE', #201554, #161162, #3339 ) ;
#143676=EDGE_CURVE ( 'NONE', #100043, #256383, #140800, .T. ) ;
#143692=DIRECTION ( 'NONE',  ( 1.000000000000000000, -0.000000000000000000, -0.000000000000000000 ) ) ;
#143710=DIRECTION ( 'NONE',  ( 1.000000000000000000, -0.000000000000000000, -0.000000000000000000 ) ) ;
#143714=ADVANCED_FACE ( 'NONE', ( #35127 ), #191631, .F. ) ;
#143760=EDGE_CURVE ( 'NONE', #252923, #106008, #38479, .T. ) ;
#143767=CARTESIAN_POINT ( 'NONE',  ( -22.47007471830798409, 1.116756697967097312E-11, -92.77928934807356143 ) ) ;
#143768=EDGE_CURVE ( 'NONE', #245837, #222623, #113338, .T. ) ;
#143800=ORIENTED_EDGE ( 'NONE', *, *, #82726, .T. ) ;
#143803=VERTEX_POINT ( 'NONE', #172068 ) ;
#143818=DIRECTION ( 'NONE',  ( 0.000000000000000000, 3.122502256758250246E-14, -1.000000000000000000 ) ) ;
#143819=DIRECTION ( 'NONE',  ( 0.000000000000000000, -0.9654727137038715545, 0.2605042016806676242 ) ) ;
#143826=CARTESIAN_POINT ( 'NONE',  ( 21.12757541349815682, 6.473380571262609351, -100.4948387841902786 ) ) ;
#143867=DIRECTION ( 'NONE',  ( 1.000000000000000000, -0.000000000000000000, -0.000000000000000000 ) ) ;
#143879=ADVANCED_FACE ( 'NONE', ( #199306 ), #11831, .F. ) ;
#143890=ORIENTED_EDGE ( 'NONE', *, *, #137976, .T. ) ;
#143893=ORIENTED_EDGE ( 'NONE', *, *, #766, .F. ) ;
#143942=ORIENTED_EDGE ( 'NONE', *, *, #153960, .T. ) ;
#143964=ORIENTED_EDGE ( 'NONE', *, *, #83520, .F. ) ;
#143974=DIRECTION ( 'NONE',  ( 0.000000000000000000, 0.01562499999998609446, -0.9998779222360101304 ) ) ;
#143977=CARTESIAN_POINT ( 'NONE',  ( -20.94999999999999929, 1.162701749949165642, -108.5000000000000426 ) ) ;
#144019=ORIENTED_EDGE ( 'NONE', *, *, #255441, .T. ) ;
#144034=DIRECTION ( 'NONE',  ( 0.000000000000000000, 0.000000000000000000, 1.000000000000000000 ) ) ;
#144062=VERTEX_POINT ( 'NONE', #55582 ) ;
#144073=DIRECTION ( 'NONE',  ( 0.000000000000000000, 0.000000000000000000, -1.000000000000000000 ) ) ;
#144084=CYLINDRICAL_SURFACE ( 'NONE', #53641, 0.09999999999999939493 ) ;
#144133=ORIENTED_EDGE ( 'NONE', *, *, #58461, .T. ) ;
#144139=VECTOR ( 'NONE', #15715, 1000.000000000000000 ) ;
#144156=CARTESIAN_POINT ( 'NONE',  ( 19.75857864376268935, 11.75000000001116440, -125.2500000000000426 ) ) ;
#144204=CARTESIAN_POINT ( 'NONE',  ( -20.94999027547553894, 10.29326151435327219, -139.4592822510415147 ) ) ;
#144220=ORIENTED_EDGE ( 'NONE', *, *, #83225, .F. ) ;
#144344=ORIENTED_EDGE ( 'NONE', *, *, #26939, .F. ) ;
#144358=FACE_OUTER_BOUND ( 'NONE', #182933, .T. ) ;
#144378=ADVANCED_FACE ( 'NONE', ( #89296 ), #102685, .F. ) ;
#144384=CARTESIAN_POINT ( 'NONE',  ( -18.59999994787167310, -9.523637689750636071, -140.8824495347722632 ) ) ;
#144414=VECTOR ( 'NONE', #93562, 1000.000000000000000 ) ;
#144417=ORIENTED_EDGE ( 'NONE', *, *, #93490, .F. ) ;
#144420=LINE ( 'NONE', #205695, #48323 ) ;
#144433=CARTESIAN_POINT ( 'NONE',  ( -23.15000000000000213, 11.65000000001115588, -112.6500000000000341 ) ) ;
#144460=ORIENTED_EDGE ( 'NONE', *, *, #128349, .F. ) ;
#144465=VERTEX_POINT ( 'NONE', #174029 ) ;
#144467=VERTEX_POINT ( 'NONE', #193557 ) ;
#144511=CARTESIAN_POINT ( 'NONE',  ( 20.94999999999999574, -1.851028230129704522, -112.1539132694225316 ) ) ;
#144537=EDGE_LOOP ( 'NONE', ( #148867, #160909, #130600, #4253 ) ) ;
#144557=ORIENTED_EDGE ( 'NONE', *, *, #54275, .T. ) ;
#144610=DIRECTION ( 'NONE',  ( 0.000000000000000000, 0.4930308989875230585, 0.8700118002898322711 ) ) ;
#144631=CARTESIAN_POINT ( 'NONE',  ( 23.15000000000000213, -11.39257802169451139, -130.9260504201681101 ) ) ;
#144708=VERTEX_POINT ( 'NONE', #181694 ) ;
#144711=EDGE_CURVE ( 'NONE', #188649, #207918, #144865, .T. ) ;
#144724=DIRECTION ( 'NONE',  ( 1.000000000000000000, 0.000000000000000000, 0.000000000000000000 ) ) ;
#144728=VERTEX_POINT ( 'NONE', #206391 ) ;
#144777=CARTESIAN_POINT ( 'NONE',  ( 18.49351773456750792, -9.443025695134291908, -107.6853255260268440 ) ) ;
#144787=AXIS2_PLACEMENT_3D ( 'NONE', #93193, #172784, #213143 ) ;
#144789=AXIS2_PLACEMENT_3D ( 'NONE', #86248, #165836, #249211 ) ;
#144804=DIRECTION ( 'NONE',  ( 0.000000000000000000, 0.000000000000000000, -1.000000000000000000 ) ) ;
#144865=CIRCLE ( 'NONE', #178024, 0.09999999999999982514 ) ;
#144884=DIRECTION ( 'NONE',  ( -0.000000000000000000, -0.9887567792719339499, -0.1495327102803676589 ) ) ;
#144901=DIRECTION ( 'NONE',  ( 0.000000000000000000, 0.000000000000000000, 1.000000000000000000 ) ) ;
#144905=CARTESIAN_POINT ( 'NONE',  ( 20.94999999999999929, -8.999999999988842703, -124.6060308773475924 ) ) ;
#144915=ORIENTED_EDGE ( 'NONE', *, *, #154200, .F. ) ;
#144928=ADVANCED_FACE ( 'NONE', ( #188110 ), #113705, .F. ) ;
#144959=ORIENTED_EDGE ( 'NONE', *, *, #154609, .T. ) ;
#144969=DIRECTION ( 'NONE',  ( 0.000000000000000000, -0.000000000000000000, -1.000000000000000000 ) ) ;
#144970=ORIENTED_EDGE ( 'NONE', *, *, #54037, .F. ) ;
#144976=AXIS2_PLACEMENT_3D ( 'NONE', #78459, #175060, #52467 ) ;
#144980=DIRECTION ( 'NONE',  ( 1.000000000000000000, -0.000000000000000000, -0.000000000000000000 ) ) ;
#144982=ORIENTED_EDGE ( 'NONE', *, *, #70985, .F. ) ;
#145012=CARTESIAN_POINT ( 'NONE',  ( -23.15000000000000213, 11.65000000001115588, -126.9851942293460922 ) ) ;
#145016=PRODUCT_DEFINITION_SHAPE ( 'NONE', 'NONE',  #75539 ) ;
#145022=CARTESIAN_POINT ( 'NONE',  ( -21.55000000000000071, 7.250000000011155521, -112.8500000000000369 ) ) ;
#145065=LINE ( 'NONE', #68112, #132803 ) ;
#145068=ORIENTED_EDGE ( 'NONE', *, *, #43296, .F. ) ;
#145075=DIRECTION ( 'NONE',  ( 1.000000000000000000, 0.000000000000000000, 0.000000000000000000 ) ) ;
#145096=ORIENTED_EDGE ( 'NONE', *, *, #249532, .T. ) ;
#145098=VECTOR ( 'NONE', #30405, 1000.000000000000000 ) ;
#145125=ADVANCED_FACE ( 'NONE', ( #163125 ), #84814, .T. ) ;
#145127=AXIS2_PLACEMENT_3D ( 'NONE', #209320, #32002, #167661 ) ;
#145162=VERTEX_POINT ( 'NONE', #131682 ) ;
#145250=FACE_OUTER_BOUND ( 'NONE', #15810, .T. ) ;
#145257=DIRECTION ( 'NONE',  ( 1.000000000000000000, 0.000000000000000000, 0.000000000000000000 ) ) ;
#145278=DIRECTION ( 'NONE',  ( -0.000000000000000000, -1.000000000000000000, -0.000000000000000000 ) ) ;
#145282=CIRCLE ( 'NONE', #199483, 0.09999999999998898659 ) ;
#145294=CIRCLE ( 'NONE', #236884, 6.329289321881370611 ) ;
#145298=ORIENTED_EDGE ( 'NONE', *, *, #223987, .T. ) ;
#145308=CARTESIAN_POINT ( 'NONE',  ( 20.94999999999999929, 11.65000000001115943, -127.2161343370219413 ) ) ;
#145311=EDGE_CURVE ( 'NONE', #182294, #240102, #132586, .T. ) ;
#145317=CARTESIAN_POINT ( 'NONE',  ( -18.50000000000001066, -9.421308209727826011, -107.7423632140509397 ) ) ;
#145318=LINE ( 'NONE', #103610, #36060 ) ;
#145320=CARTESIAN_POINT ( 'NONE',  ( -20.54999999999999716, 1.115600667400684642E-11, -100.5000000000000284 ) ) ;
#145338=VECTOR ( 'NONE', #175384, 1000.000000000000000 ) ;
#145357=EDGE_CURVE ( 'NONE', #126709, #110634, #245014, .T. ) ;
#145369=ADVANCED_FACE ( 'NONE', ( #29416 ), #170235, .F. ) ;
#145374=DIRECTION ( 'NONE',  ( 1.734723475976817507E-14, 0.000000000000000000, -1.000000000000000000 ) ) ;
#145388=DIRECTION ( 'NONE',  ( 0.000000000000000000, 0.000000000000000000, 1.000000000000000000 ) ) ;
#145389=CYLINDRICAL_SURFACE ( 'NONE', #2029, 0.09999999999999939493 ) ;
#145405=ORIENTED_EDGE ( 'NONE', *, *, #194513, .F. ) ;
#145437=EDGE_CURVE ( 'NONE', #224935, #61278, #28594, .T. ) ;
#145461=DIRECTION ( 'NONE',  ( 0.000000000000000000, -0.9908441862701596881, -0.1350103645451904977 ) ) ;
#145549=DIRECTION ( 'NONE',  ( 0.000000000000000000, 0.000000000000000000, -1.000000000000000000 ) ) ;
#145581=CARTESIAN_POINT ( 'NONE',  ( 22.47007471830798764, 1.115784145324971765E-11, -92.77928934807357564 ) ) ;
#145624=CARTESIAN_POINT ( 'NONE',  ( 20.95512820512820440, 8.876151316299271343, -109.0586289951409924 ) ) ;
#145641=CIRCLE ( 'NONE', #103934, 0.1000000000000001027 ) ;
#145655=CARTESIAN_POINT ( 'NONE',  ( 19.88284271247461987, 11.69142135624847256, -125.2500000000000284 ) ) ;
#145684=CARTESIAN_POINT ( 'NONE',  ( -18.46154800491015635, -9.480206274230829067, -140.6574508383815214 ) ) ;
#145706=ORIENTED_EDGE ( 'NONE', *, *, #61335, .F. ) ;
#145718=DIRECTION ( 'NONE',  ( 0.000000000000000000, 0.000000000000000000, 1.000000000000000000 ) ) ;
#145776=LINE ( 'NONE', #66262, #27671 ) ;
#145796=ORIENTED_EDGE ( 'NONE', *, *, #77058, .T. ) ;
#145817=CIRCLE ( 'NONE', #66725, 0.09999999999999996392 ) ;
#145831=DIRECTION ( 'NONE',  ( 0.000000000000000000, 0.8660254037844411501, 0.4999999999999956701 ) ) ;
#145852=VECTOR ( 'NONE', #90605, 1000.000000000000000 ) ;
#145882=ADVANCED_FACE ( 'NONE', ( #26524 ), #12352, .F. ) ;
#145903=CONICAL_SURFACE ( 'NONE', #179257, 6.250000000000005329, 0.7853981633974431720 ) ;
#145904=DIRECTION ( 'NONE',  ( 1.000000000000000000, 0.000000000000000000, 0.000000000000000000 ) ) ;
#145910=AXIS2_PLACEMENT_3D ( 'NONE', #247609, #75419, #96223 ) ;
#145916=AXIS2_PLACEMENT_3D ( 'NONE', #244105, #224544, #83715 ) ;
#145943=DIRECTION ( 'NONE',  ( 1.000000000000000000, 0.000000000000000000, 0.000000000000000000 ) ) ;
#145981=DIRECTION ( 'NONE',  ( 1.000000000000000000, 0.000000000000000000, 0.000000000000000000 ) ) ;
#145982=EDGE_LOOP ( 'NONE', ( #89900, #252452, #64964, #203908 ) ) ;
#145986=AXIS2_PLACEMENT_3D ( 'NONE', #50523, #210908, #74001 ) ;
#146002=VECTOR ( 'NONE', #7451, 1000.000000000000000 ) ;
#146006=CARTESIAN_POINT ( 'NONE',  ( -23.25000000000000000, 1.115600667400684642E-11, -134.0000000000000284 ) ) ;
#146019=AXIS2_PLACEMENT_3D ( 'NONE', #200049, #120534, #163486 ) ;
#146059=ORIENTED_EDGE ( 'NONE', *, *, #153106, .F. ) ;
#146084=VERTEX_POINT ( 'NONE', #199732 ) ;
#146085=ORIENTED_EDGE ( 'NONE', *, *, #55285, .T. ) ;
#146090=ORIENTED_EDGE ( 'NONE', *, *, #211550, .T. ) ;
#146098=AXIS2_PLACEMENT_3D ( 'NONE', #179338, #196299, #22837 ) ;
#146116=CARTESIAN_POINT ( 'NONE',  ( 21.14999999999999858, 1.115600667400684642E-11, -93.95934304829877703 ) ) ;
#146168=ORIENTED_EDGE ( 'NONE', *, *, #82528, .F. ) ;
#146183=CARTESIAN_POINT ( 'NONE',  ( 20.94999999999999574, 14.00000000001115730, -105.9270925303825663 ) ) ;
#146186=DIRECTION ( 'NONE',  ( 0.000000000000000000, -0.9908441862701596881, 0.1350103645451904977 ) ) ;
#146199=LINE ( 'NONE', #144905, #24208 ) ;
#146225=CARTESIAN_POINT ( 'NONE',  ( -22.57320508075687115, 11.65000000001115588, -100.5000000000000568 ) ) ;
#146245=VERTEX_POINT ( 'NONE', #143587 ) ;
#146250=CIRCLE ( 'NONE', #54665, 0.6000000000000033085 ) ;
#146267=CARTESIAN_POINT ( 'NONE',  ( -18.50000000000000000, 11.65000000001115232, -107.5148057706540357 ) ) ;
#146274=EDGE_CURVE ( 'NONE', #247168, #81511, #48334, .T. ) ;
#146282=DIRECTION ( 'NONE',  ( -0.000000000000000000, -0.000000000000000000, -1.000000000000000000 ) ) ;
#146303=FACE_OUTER_BOUND ( 'NONE', #46413, .T. ) ;
#146350=CARTESIAN_POINT ( 'NONE',  ( -2.995603634470891112E-16, 6.650000000011155876, -121.7500000000000426 ) ) ;
#146442=EDGE_LOOP ( 'NONE', ( #225860, #169854, #68, #50444 ) ) ;
#146464=DIRECTION ( 'NONE',  ( 0.000000000000000000, 0.000000000000000000, 1.000000000000000000 ) ) ;
#146494=CARTESIAN_POINT ( 'NONE',  ( 21.14999999999999858, 6.650000000011155876, -112.6500000000000341 ) ) ;
#146507=ORIENTED_EDGE ( 'NONE', *, *, #180240, .T. ) ;
#146525=DIRECTION ( 'NONE',  ( 0.000000000000000000, 0.000000000000000000, -1.000000000000000000 ) ) ;
#146527=CARTESIAN_POINT ( 'NONE',  ( 23.24999999999999289, 11.65000000001116298, -112.6500000000000341 ) ) ;
#146557=DIRECTION ( 'NONE',  ( 0.000000000000000000, 0.000000000000000000, -1.000000000000000000 ) ) ;
#146558=DIRECTION ( 'NONE',  ( 0.1538461538461510236, 0.9880948137434718559, 0.000000000000000000 ) ) ;
#146588=CARTESIAN_POINT ( 'NONE',  ( -18.54159361262949091, -9.463132135481851392, -107.5491222162930569 ) ) ;
#146609=CARTESIAN_POINT ( 'NONE',  ( -21.08479644141223019, 6.345038657743049093, -100.4414455574359124 ) ) ;
#146665=ORIENTED_EDGE ( 'NONE', *, *, #110384, .F. ) ;
#146693=EDGE_CURVE ( 'NONE', #242494, #253135, #116742, .T. ) ;
#146694=LINE ( 'NONE', #178849, #202100 ) ;
#146766=EDGE_CURVE ( 'NONE', #247339, #127698, #66861, .T. ) ;
#146771=DIRECTION ( 'NONE',  ( 1.000000000000000000, 0.000000000000000000, 0.000000000000000000 ) ) ;
#146826=FACE_OUTER_BOUND ( 'NONE', #54199, .T. ) ;
#146830=ORIENTED_EDGE ( 'NONE', *, *, #216977, .F. ) ;
#146841=CARTESIAN_POINT ( 'NONE',  ( -20.85000000000000142, -1.835859311432481045, -145.5044391687985694 ) ) ;
#146870=VERTEX_POINT ( 'NONE', #210962 ) ;
#146916=AXIS2_PLACEMENT_3D ( 'NONE', #68588, #12476, #151997 ) ;
#146921=ORIENTED_EDGE ( 'NONE', *, *, #233033, .T. ) ;
#146939=ORIENTED_EDGE ( 'NONE', *, *, #12374, .F. ) ;
#146945=ORIENTED_EDGE ( 'NONE', *, *, #192717, .F. ) ;
#146956=AXIS2_PLACEMENT_3D ( 'NONE', #245297, #27567, #151347 ) ;
#146968=CARTESIAN_POINT ( 'NONE',  ( -22.50000000000000000, 1.115600667400684642E-11, -88.85042919245522341 ) ) ;
#146990=DIRECTION ( 'NONE',  ( 0.000000000000000000, -1.000000000000000000, 0.000000000000000000 ) ) ;
#147050=CARTESIAN_POINT ( 'NONE',  ( 19.99999999999998934, 11.65000000001115943, -121.7500000000000426 ) ) ;
#147061=DIRECTION ( 'NONE',  ( 0.000000000000000000, -0.5000000000000014433, 0.8660254037844378194 ) ) ;
#147066=EDGE_CURVE ( 'NONE', #55645, #31259, #91976, .T. ) ;
#147109=ORIENTED_EDGE ( 'NONE', *, *, #256031, .F. ) ;
#147120=AXIS2_PLACEMENT_3D ( 'NONE', #96206, #216152, #177066 ) ;
#147142=LINE ( 'NONE', #110587, #160675 ) ;
#147153=CIRCLE ( 'NONE', #138733, 0.1000000000000033223 ) ;
#147173=EDGE_LOOP ( 'NONE', ( #67114, #204989, #91751, #3340 ) ) ;
#147182=CARTESIAN_POINT ( 'NONE',  ( 20.95052659398289308, 10.47982436779105875, -108.0752387558656409 ) ) ;
#147183=CARTESIAN_POINT ( 'NONE',  ( -23.15000000000000213, 11.65000000001115588, -126.9851942293460922 ) ) ;
#147193=CARTESIAN_POINT ( 'NONE',  ( 23.15000000000000213, -12.41227409413852811, -131.0000000000000284 ) ) ;
#147204=EDGE_LOOP ( 'NONE', ( #214103, #103381, #166962, #166925, #186085, #66901, #93036 ) ) ;
#147231=DIRECTION ( 'NONE',  ( 0.000000000000000000, 0.000000000000000000, 1.000000000000000000 ) ) ;
#147303=DIRECTION ( 'NONE',  ( 0.000000000000000000, 0.000000000000000000, 1.000000000000000000 ) ) ;
#147305=VECTOR ( 'NONE', #238281, 1000.000000000000000 ) ;
#147307=ORIENTED_EDGE ( 'NONE', *, *, #221318, .F. ) ;
#147310=EDGE_CURVE ( 'NONE', #30650, #46758, #141861, .T. ) ;
#147329=AXIS2_PLACEMENT_3D ( 'NONE', #57079, #96224, #197892 ) ;
#147336=CIRCLE ( 'NONE', #18352, 0.09999999999998898659 ) ;
#147341=ORIENTED_EDGE ( 'NONE', *, *, #190234, .T. ) ;
#147361=CARTESIAN_POINT ( 'NONE',  ( -23.15000000000000213, 1.115600667400684642E-11, -100.5000000000000284 ) ) ;
#147371=DIRECTION ( 'NONE',  ( 0.000000000000000000, 0.000000000000000000, 1.000000000000000000 ) ) ;
#147443=VECTOR ( 'NONE', #171075, 1000.000000000000000 ) ;
#147465=DIRECTION ( 'NONE',  ( 0.000000000000000000, 1.000000000000000000, 2.891205793294679805E-16 ) ) ;
#147480=CARTESIAN_POINT ( 'NONE',  ( 21.14999999999999858, 8.786607556611267356, -112.7500000000000284 ) ) ;
#147510=FACE_OUTER_BOUND ( 'NONE', #221348, .T. ) ;
#147574=EDGE_CURVE ( 'NONE', #15812, #144708, #139806, .T. ) ;
#147582=ORIENTED_EDGE ( 'NONE', *, *, #169483, .F. ) ;
#147591=ORIENTED_EDGE ( 'NONE', *, *, #13256, .T. ) ;
#147608=CARTESIAN_POINT ( 'NONE',  ( 23.14999999999999858, 1.115600667400684642E-11, -134.0000000000000284 ) ) ;
#147659=CARTESIAN_POINT ( 'NONE',  ( -20.94999999999999929, -1.164121893230052995, -141.9148480855716343 ) ) ;
#147674=FACE_OUTER_BOUND ( 'NONE', #253756, .T. ) ;
#147675=ORIENTED_EDGE ( 'NONE', *, *, #30531, .T. ) ;
#147683=ORIENTED_EDGE ( 'NONE', *, *, #219163, .F. ) ;
#147732=DIRECTION ( 'NONE',  ( 0.000000000000000000, 1.000000000000000000, 0.000000000000000000 ) ) ;
#147757=EDGE_CURVE ( 'NONE', #113518, #225274, #101348, .T. ) ;
#147786=EDGE_CURVE ( 'NONE', #257484, #248313, #31702, .T. ) ;
#147795=ORIENTED_EDGE ( 'NONE', *, *, #147310, .T. ) ;
#147839=DIRECTION ( 'NONE',  ( 0.000000000000000000, 0.8660254037844411501, 0.4999999999999956701 ) ) ;
#147857=DIRECTION ( 'NONE',  ( 0.000000000000000000, 0.000000000000000000, -1.000000000000000000 ) ) ;
#147866=FACE_OUTER_BOUND ( 'NONE', #175955, .T. ) ;
#147897=CARTESIAN_POINT ( 'NONE',  ( 21.07928932188134397, 0.09889514566555242248, -94.17148334360672379 ) ) ;
#147898=CIRCLE ( 'NONE', #218594, 0.1999999999999987899 ) ;
#147900=ORIENTED_EDGE ( 'NONE', *, *, #40911, .F. ) ;
#147906=B_SPLINE_CURVE_WITH_KNOTS ( 'NONE', 3,
 ( #227047, #48408, #169698, #30161, #150111, #8023 ),
 .UNSPECIFIED., .F., .F.,
 ( 4, 2, 4 ),
 ( 0.000000000000000000, 0.0001895189928937381313, 0.0003790379857874762626 ),
 .UNSPECIFIED. ) ;
#147912=FACE_BOUND ( 'NONE', #38039, .T. ) ;
#147915=CARTESIAN_POINT ( 'NONE',  ( -18.43599941264906050, -9.519327428583675754, -107.4729767895213115 ) ) ;
#147917=ORIENTED_EDGE ( 'NONE', *, *, #48496, .T. ) ;
#147964=DIRECTION ( 'NONE',  ( -1.000000000000000000, 0.000000000000000000, 0.000000000000000000 ) ) ;
#147974=ADVANCED_FACE ( 'NONE', ( #33466 ), #19197, .F. ) ;
#147994=EDGE_CURVE ( 'NONE', #224903, #212285, #136337, .T. ) ;
#148020=EDGE_CURVE ( 'NONE', #231975, #40984, #193785, .T. ) ;
#148027=TOROIDAL_SURFACE ( 'NONE', #35645, 0.2000000000000000111, 0.1000000000000000056 ) ;
#148044=FACE_OUTER_BOUND ( 'NONE', #38813, .T. ) ;
#148067=PRESENTATION_STYLE_ASSIGNMENT (( #68533 ) ) ;
#148124=CARTESIAN_POINT ( 'NONE',  ( 23.24999999999999645, 5.600000000011153389, -121.5947339810869465 ) ) ;
#148177=ORIENTED_EDGE ( 'NONE', *, *, #250212, .F. ) ;
#148201=PLANE ( 'NONE',  #108094 ) ;
#148207=DIRECTION ( 'NONE',  ( 0.000000000000000000, 0.000000000000000000, 1.000000000000000000 ) ) ;
#148208=DIRECTION ( 'NONE',  ( 0.000000000000000000, -1.000000000000000000, 0.000000000000000000 ) ) ;
#148240=VECTOR ( 'NONE', #21581, 1000.000000000000000 ) ;
#148245=CARTESIAN_POINT ( 'NONE',  ( 23.25000000000000000, -8.596261682231828516, -124.5498724828497501 ) ) ;
#148256=CARTESIAN_POINT ( 'NONE',  ( 20.85000000000000142, -11.64999999998883595, -131.1000000000000227 ) ) ;
#148306=CYLINDRICAL_SURFACE ( 'NONE', #131458, 0.1000000000000028644 ) ;
#148307=FACE_OUTER_BOUND ( 'NONE', #91442, .T. ) ;
#148325=CARTESIAN_POINT ( 'NONE',  ( -21.52071067811865746, 7.779289321892505882, -112.8500000000000369 ) ) ;
#148328=ORIENTED_EDGE ( 'NONE', *, *, #198319, .T. ) ;
#148353=CARTESIAN_POINT ( 'NONE',  ( -18.49513951962167724, -9.437725026666550221, -140.7780725750292277 ) ) ;
#148364=LINE ( 'NONE', #11434, #6779 ) ;
#148381=VECTOR ( 'NONE', #118092, 1000.000000000000000 ) ;
#148389=FACE_OUTER_BOUND ( 'NONE', #164551, .T. ) ;
#148393=DIRECTION ( 'NONE',  ( 0.000000000000000000, -0.000000000000000000, 1.000000000000000000 ) ) ;
#148412=AXIS2_PLACEMENT_3D ( 'NONE', #247234, #210689, #72481 ) ;
#148414=DIRECTION ( 'NONE',  ( 0.000000000000000000, -0.000000000000000000, -1.000000000000000000 ) ) ;
#148441=AXIS2_PLACEMENT_3D ( 'NONE', #213336, #235468, #198918 ) ;
#148447=ADVANCED_FACE ( 'NONE', ( #119081 ), #121662, .F. ) ;
#148453=DIRECTION ( 'NONE',  ( 1.000000000000000000, 0.000000000000000000, 0.000000000000000000 ) ) ;
#148463=DIRECTION ( 'NONE',  ( 0.7071067811865487940, 8.659560562354918067E-17, 0.7071067811865463515 ) ) ;
#148464=CIRCLE ( 'NONE', #152768, 0.1000000000000028644 ) ;
#148470=CIRCLE ( 'NONE', #202624, 11.80000000000000426 ) ;
#148480=DIRECTION ( 'NONE',  ( 1.000000000000000000, 0.000000000000000000, 0.000000000000000000 ) ) ;
#148496=DIRECTION ( 'NONE',  ( 1.000000000000000000, -0.000000000000000000, -0.000000000000000000 ) ) ;
#148544=AXIS2_PLACEMENT_3D ( 'NONE', #32076, #111593, #211989 ) ;
#148562=FACE_OUTER_BOUND ( 'NONE', #178830, .T. ) ;
#148579=EDGE_CURVE ( 'NONE', #233201, #121101, #186157, .T. ) ;
#148589=VERTEX_POINT ( 'NONE', #223291 ) ;
#148602=PLANE ( 'NONE',  #189319 ) ;
#148607=EDGE_CURVE ( 'NONE', #60113, #137137, #207206, .T. ) ;
#148612=EDGE_CURVE ( 'NONE', #177351, #80403, #96603, .T. ) ;
#148616=EDGE_CURVE ( 'NONE', #107956, #193635, #53659, .T. ) ;
#148620=ORIENTED_EDGE ( 'NONE', *, *, #57051, .T. ) ;
#148632=ORIENTED_EDGE ( 'NONE', *, *, #194515, .T. ) ;
#148645=ORIENTED_EDGE ( 'NONE', *, *, #232293, .F. ) ;
#148659=ORIENTED_EDGE ( 'NONE', *, *, #94238, .T. ) ;
#148668=CARTESIAN_POINT ( 'NONE',  ( 21.30000000000002558, 1.115600667400684642E-11, -100.5000000000000284 ) ) ;
#148679=AXIS2_PLACEMENT_3D ( 'NONE', #245883, #226286, #222428 ) ;
#148689=CARTESIAN_POINT ( 'NONE',  ( 21.14999999999999858, 8.786607556611267356, -112.7500000000000284 ) ) ;
#148691=CARTESIAN_POINT ( 'NONE',  ( 18.52326479938690440, -9.642364444904249154, -140.7147574134058061 ) ) ;
#148695=LINE ( 'NONE', #228226, #231664 ) ;
#148699=AXIS2_PLACEMENT_3D ( 'NONE', #254, #77219, #81064 ) ;
#148709=CARTESIAN_POINT ( 'NONE',  ( 20.94999999999999574, -1.349084418615859482, -108.4864989635455146 ) ) ;
#148716=LINE ( 'NONE', #228251, #226516 ) ;
#148718=VERTEX_POINT ( 'NONE', #105254 ) ;
#148742=CARTESIAN_POINT ( 'NONE',  ( 20.87600722750343252, 10.33112638556969465, -139.5901228926975080 ) ) ;
#148748=CIRCLE ( 'NONE', #53036, 0.09999999999999693856 ) ;
#148772=FACE_OUTER_BOUND ( 'NONE', #88717, .T. ) ;
#148789=CIRCLE ( 'NONE', #115641, 0.09999999999998898659 ) ;
#148795=EDGE_CURVE ( 'NONE', #234572, #225274, #107029, .T. ) ;
#148820=VERTEX_POINT ( 'NONE', #72613 ) ;
#148867=ORIENTED_EDGE ( 'NONE', *, *, #141366, .T. ) ;
#148875=CIRCLE ( 'NONE', #157259, 11.80000000000000426 ) ;
#148889=DIRECTION ( 'NONE',  ( -4.408576920032448588E-17, 0.1350103645451876944, -0.9908441862701601321 ) ) ;
#148897=ORIENTED_EDGE ( 'NONE', *, *, #72936, .F. ) ;
#148921=CIRCLE ( 'NONE', #36520, 2.000000000000002665 ) ;
#148963=DIRECTION ( 'NONE',  ( 0.000000000000000000, -0.8068669527897506244, -0.5907332058516622242 ) ) ;
#149023=DIRECTION ( 'NONE',  ( 0.000000000000000000, 0.000000000000000000, 1.000000000000000000 ) ) ;
#149029=DIRECTION ( 'NONE',  ( -1.000000000000000000, 0.000000000000000000, 0.000000000000000000 ) ) ;
#149031=CARTESIAN_POINT ( 'NONE',  ( -20.00857864376270001, 9.150000000011157653, -112.8500000000000369 ) ) ;
#149033=ORIENTED_EDGE ( 'NONE', *, *, #64454, .T. ) ;
#149034=DIRECTION ( 'NONE',  ( 1.000000000000000000, 0.000000000000000000, 0.000000000000000000 ) ) ;
#149038=ORIENTED_EDGE ( 'NONE', *, *, #109479, .F. ) ;
#149047=CARTESIAN_POINT ( 'NONE',  ( -21.05000000000000071, 1.835341550235567887, -112.1551512925630192 ) ) ;
#149086=CIRCLE ( 'NONE', #165840, 0.1000000000000028644 ) ;
#149096=EDGE_LOOP ( 'NONE', ( #36565, #63144, #40240, #14598 ) ) ;
#149110=CARTESIAN_POINT ( 'NONE',  ( 20.94999999999999574, -1.835341550213255957, -112.0551512925630249 ) ) ;
#149149=DIRECTION ( 'NONE',  ( -0.000000000000000000, 0.8660254037844411501, 0.4999999999999956146 ) ) ;
#149194=ORIENTED_EDGE ( 'NONE', *, *, #251064, .T. ) ;
#149200=ORIENTED_EDGE ( 'NONE', *, *, #106662, .F. ) ;
#149233=CARTESIAN_POINT ( 'NONE',  ( 18.49999999999999289, 6.650000000011155876, -121.6500000000000341 ) ) ;
#149290=DIRECTION ( 'NONE',  ( 0.000000000000000000, -1.734723475983068283E-15, 1.000000000000000000 ) ) ;
#149306=CARTESIAN_POINT ( 'NONE',  ( -23.15000000000000213, 1.115600667400684642E-11, -121.1250000000000426 ) ) ;
#149336=SPHERICAL_SURFACE ( 'NONE', #141049, 0.1000000000000000056 ) ;
#149349=LINE ( 'NONE', #228863, #223264 ) ;
#149364=EDGE_CURVE ( 'NONE', #43405, #54821, #214365, .T. ) ;
#149393=ORIENTED_EDGE ( 'NONE', *, *, #57890, .F. ) ;
#149413=AXIS2_PLACEMENT_3D ( 'NONE', #37855, #234748, #56082 ) ;
#149463=DIRECTION ( 'NONE',  ( -0.4999999999999799050, 0.000000000000000000, -0.8660254037844502539 ) ) ;
#149472=VECTOR ( 'NONE', #181946, 1000.000000000000000 ) ;
#149494=AXIS2_PLACEMENT_3D ( 'NONE', #14350, #112159, #169592 ) ;
#149503=ORIENTED_EDGE ( 'NONE', *, *, #129343, .T. ) ;
#149536=ORIENTED_EDGE ( 'NONE', *, *, #207365, .T. ) ;
#149546=ORIENTED_EDGE ( 'NONE', *, *, #105900, .T. ) ;
#149554=EDGE_LOOP ( 'NONE', ( #62165, #159935, #154968 ) ) ;
#149558=DIRECTION ( 'NONE',  ( 1.000000000000000000, -0.000000000000000000, -0.000000000000000000 ) ) ;
#149567=CARTESIAN_POINT ( 'NONE',  ( -20.64999999999999858, -8.999999999988846255, -110.3939691226524786 ) ) ;
#149570=CARTESIAN_POINT ( 'NONE',  ( -23.25000000000000000, 2.600000000011156054, -113.7246219227621395 ) ) ;
#149577=ORIENTED_EDGE ( 'NONE', *, *, #60318, .T. ) ;
#149605=SPHERICAL_SURFACE ( 'NONE', #80544, 0.1000000000000000056 ) ;
#149606=ORIENTED_EDGE ( 'NONE', *, *, #85324, .F. ) ;
#149614=DIRECTION ( 'NONE',  ( 0.000000000000000000, 0.7397360091702755991, -0.6728971962616832059 ) ) ;
#149619=CARTESIAN_POINT ( 'NONE',  ( -20.64999999999999858, 1.115600667400684642E-11, -132.0000000000000284 ) ) ;
#149637=ORIENTED_EDGE ( 'NONE', *, *, #129038, .T. ) ;
#149648=EDGE_LOOP ( 'NONE', ( #253444, #4225, #257987, #74679, #72014 ) ) ;
#149649=DIRECTION ( 'NONE',  ( 0.000000000000000000, 0.000000000000000000, -1.000000000000000000 ) ) ;
#149660=TOROIDAL_SURFACE ( 'NONE', #12285, 2.100000000000002309, 0.1000000000000000056 ) ;
#149663=FACE_OUTER_BOUND ( 'NONE', #129073, .T. ) ;
#149674=DIRECTION ( 'NONE',  ( 0.000000000000000000, -6.028164079019231987E-13, 1.000000000000000000 ) ) ;
#149682=EDGE_LOOP ( 'NONE', ( #215334, #25856, #249824, #38276 ) ) ;
#149683=ORIENTED_EDGE ( 'NONE', *, *, #198319, .F. ) ;
#149694=AXIS2_PLACEMENT_3D ( 'NONE', #212192, #89646, #252571 ) ;
#149697=DIRECTION ( 'NONE',  ( 1.000000000000000000, 0.000000000000000000, 0.000000000000000000 ) ) ;
#149762=EDGE_CURVE ( 'NONE', #37339, #68945, #132542, .T. ) ;
#149794=CARTESIAN_POINT ( 'NONE',  ( -20.85000000000000142, -11.74999999998884448, -134.0000000000000284 ) ) ;
#149802=EDGE_LOOP ( 'NONE', ( #102282, #200137, #122926, #176626 ) ) ;
#149806=DIRECTION ( 'NONE',  ( -1.000000000000000000, -2.952720810173289112E-16, 0.000000000000000000 ) ) ;
#149820=EDGE_LOOP ( 'NONE', ( #87883, #250770, #83791, #6864, #229259 ) ) ;
#149830=CARTESIAN_POINT ( 'NONE',  ( -22.50000000000000000, 11.64957080755595520, -100.4000000000000483 ) ) ;
#149849=AXIS2_PLACEMENT_3D ( 'NONE', #67261, #131083, #146771 ) ;
#149886=VERTEX_POINT ( 'NONE', #200911 ) ;
#149892=CARTESIAN_POINT ( 'NONE',  ( 21.14999999999999503, 11.65000000001116298, -100.5000000000000284 ) ) ;
#149894=FACE_OUTER_BOUND ( 'NONE', #109765, .T. ) ;
#149919=B_SPLINE_CURVE_WITH_KNOTS ( 'NONE', 3,
 ( #206769, #228902, #107659, #144204, #50239, #223744, #110223, #189770, #249746, #187225, #185917, #45126, #7270, #124672, #5979, #85492, #175372, #33305, #72411 ),
 .UNSPECIFIED., .F., .F.,
 ( 4, 3, 3, 3, 3, 3, 4 ),
 ( -2.000416914645579387E-06, 0.000000000000000000, 4.714008503745887181E-05, 9.979203887778629440E-05, 0.0001372215519229621735, 0.0001635031576221138031, 0.0001900083748504299125 ),
 .UNSPECIFIED. ) ;
#149935=ORIENTED_EDGE ( 'NONE', *, *, #90000, .F. ) ;
#149940=VECTOR ( 'NONE', #4203, 1000.000000000000000 ) ;
#149959=CARTESIAN_POINT ( 'NONE',  ( -20.94999999999999929, 1.115600667400684642E-11, -122.3000000000000398 ) ) ;
#149981=VERTEX_POINT ( 'NONE', #6557 ) ;
#149995=DIRECTION ( 'NONE',  ( -1.000000000000000000, 0.000000000000000000, 0.000000000000000000 ) ) ;
#149996=DIRECTION ( 'NONE',  ( 0.000000000000000000, 1.000000000000000000, 0.000000000000000000 ) ) ;
#150001=EDGE_CURVE ( 'NONE', #98538, #238064, #153432, .T. ) ;
#150003=DIRECTION ( 'NONE',  ( 0.000000000000000000, 0.000000000000000000, 1.000000000000000000 ) ) ;
#150025=ORIENTED_EDGE ( 'NONE', *, *, #92615, .F. ) ;
#150026=CYLINDRICAL_SURFACE ( 'NONE', #183852, 0.5000000000000004441 ) ;
#150043=CARTESIAN_POINT ( 'NONE',  ( -23.25000000000000000, 1.115600667400684642E-11, -104.6500000000000341 ) ) ;
#150064=EDGE_LOOP ( 'NONE', ( #201363, #229733 ) ) ;
#150097=CARTESIAN_POINT ( 'NONE',  ( -23.15000000000000213, -11.74999999998884448, -130.9000000000000341 ) ) ;
#150111=CARTESIAN_POINT ( 'NONE',  ( 21.05000000000000426, 6.258817194692619879, -100.4663672646664168 ) ) ;
#150125=DIRECTION ( 'NONE',  ( 0.000000000000000000, 0.000000000000000000, -1.000000000000000000 ) ) ;
#150130=VERTEX_POINT ( 'NONE', #190356 ) ;
#150134=DIRECTION ( 'NONE',  ( 1.000000000000000000, 0.000000000000000000, -0.000000000000000000 ) ) ;
#150172=ORIENTED_EDGE ( 'NONE', *, *, #28374, .T. ) ;
#150180=SPHERICAL_SURFACE ( 'NONE', #205257, 0.1000000000000000056 ) ;
#150195=CYLINDRICAL_SURFACE ( 'NONE', #201588, 0.1000000000000028644 ) ;
#150208=VECTOR ( 'NONE', #167069, 1000.000000000000000 ) ;
#150212=DIRECTION ( 'NONE',  ( 1.000000000000000000, 0.000000000000000000, 0.000000000000000000 ) ) ;
#150224=EDGE_CURVE ( 'NONE', #92785, #179371, #173908, .T. ) ;
#150250=ORIENTED_EDGE ( 'NONE', *, *, #44466, .F. ) ;
#150263=DIRECTION ( 'NONE',  ( -1.000000000000000000, 0.000000000000000000, 0.000000000000000000 ) ) ;
#150280=CARTESIAN_POINT ( 'NONE',  ( -18.59999999999999787, 1.115600667400684642E-11, -134.0000000000000284 ) ) ;
#150324=EDGE_CURVE ( 'NONE', #187769, #78774, #102757, .T. ) ;
#150359=EDGE_CURVE ( 'NONE', #62504, #163148, #148748, .T. ) ;
#150384=CIRCLE ( 'NONE', #37966, 0.09999999999999939493 ) ;
#150422=VERTEX_POINT ( 'NONE', #104040 ) ;
#150429=ADVANCED_FACE ( 'NONE', ( #183613 ), #196127, .T. ) ;
#150503=EDGE_CURVE ( 'NONE', #72909, #242360, #165684, .T. ) ;
#150516=EDGE_LOOP ( 'NONE', ( #119856, #140212, #30717, #86470 ) ) ;
#150540=ORIENTED_EDGE ( 'NONE', *, *, #166940, .F. ) ;
#150576=EDGE_CURVE ( 'NONE', #61948, #188649, #148921, .T. ) ;
#150588=FACE_OUTER_BOUND ( 'NONE', #78105, .T. ) ;
#150595=AXIS2_PLACEMENT_3D ( 'NONE', #204801, #129140, #245242 ) ;
#150618=DIRECTION ( 'NONE',  ( 0.000000000000000000, 1.000000000000000000, 0.000000000000000000 ) ) ;
#150627=FACE_OUTER_BOUND ( 'NONE', #161462, .T. ) ;
#150639=CYLINDRICAL_SURFACE ( 'NONE', #226079, 0.1000000000000028644 ) ;
#150661=DIRECTION ( 'NONE',  ( 6.938893903907224433E-15, -1.000000000000000000, -2.891205793294679805E-16 ) ) ;
#150665=EDGE_CURVE ( 'NONE', #70455, #97941, #256035, .T. ) ;
#150679=EDGE_CURVE ( 'NONE', #48720, #72307, #232321, .T. ) ;
#150689=DIRECTION ( 'NONE',  ( 1.000000000000000000, -0.000000000000000000, -0.000000000000000000 ) ) ;
#150694=CARTESIAN_POINT ( 'NONE',  ( -18.59999999999999787, -1.162701749926853712, -108.6000000000000227 ) ) ;
#150695=CYLINDRICAL_SURFACE ( 'NONE', #235826, 0.09999999999998898659 ) ;
#150699=EDGE_CURVE ( 'NONE', #218820, #93357, #153222, .T. ) ;
#150714=DIRECTION ( 'NONE',  ( 0.000000000000000000, -1.000000000000000000, 0.000000000000000000 ) ) ;
#150724=ORIENTED_EDGE ( 'NONE', *, *, #119331, .T. ) ;
#150725=CARTESIAN_POINT ( 'NONE',  ( 22.50000000000000000, 7.790779598384538929, -100.4000000000000341 ) ) ;
#150748=DIRECTION ( 'NONE',  ( -1.000000000000000000, -2.952720810173289112E-16, 0.000000000000000000 ) ) ;
#150769=CARTESIAN_POINT ( 'NONE',  ( 23.14999999999999858, 11.65000000001116298, -126.9851942293460922 ) ) ;
#150777=EDGE_LOOP ( 'NONE', ( #62429, #233327, #127972, #101635, #124425 ) ) ;
#150864=DIRECTION ( 'NONE',  ( -1.000000000000000000, -0.000000000000000000, -0.000000000000000000 ) ) ;
#150867=CARTESIAN_POINT ( 'NONE',  ( 22.49436431346199683, 0.06690352973341695542, -88.85004905234657713 ) ) ;
#150871=CARTESIAN_POINT ( 'NONE',  ( -18.59999999999999787, 11.65000000001115232, -112.6500000000000341 ) ) ;
#150873=VECTOR ( 'NONE', #172427, 999.9999999999998863 ) ;
#150877=DIRECTION ( 'NONE',  ( 0.000000000000000000, 0.000000000000000000, 1.000000000000000000 ) ) ;
#150883=ADVANCED_FACE ( 'NONE', ( #238899 ), #153413, .T. ) ;
#150940=CARTESIAN_POINT ( 'NONE',  ( -18.50000000000000000, 7.021664781911246322, -137.8335654018973457 ) ) ;
#150946=VECTOR ( 'NONE', #39509, 1000.000000000000000 ) ;
#150958=CARTESIAN_POINT ( 'NONE',  ( 21.00000000000000000, 9.750000000011153745, -121.6500000000000341 ) ) ;
#150976=LINE ( 'NONE', #29778, #99066 ) ;
#151019=ORIENTED_EDGE ( 'NONE', *, *, #93768, .F. ) ;
#151028=EDGE_CURVE ( 'NONE', #165636, #111732, #132525, .T. ) ;
#151039=EDGE_CURVE ( 'NONE', #221499, #64997, #146199, .T. ) ;
#151052=ADVANCED_FACE ( 'NONE', ( #23731 ), #122813, .T. ) ;
#151064=DIRECTION ( 'NONE',  ( 0.000000000000000000, 0.5000000000000078826, 0.8660254037844340447 ) ) ;
#151067=CARTESIAN_POINT ( 'NONE',  ( 18.49999999999999289, 11.65000000001115943, -88.75000000000004263 ) ) ;
#151068=EDGE_LOOP ( 'NONE', ( #74561, #85625, #67399, #143352 ) ) ;
#151079=CARTESIAN_POINT ( 'NONE',  ( -21.05000000000000071, -1.851028230129704522, -112.1539132694225316 ) ) ;
#151095=( NAMED_UNIT ( * ) SI_UNIT ( $, .STERADIAN. ) SOLID_ANGLE_UNIT ( ) );
#151103=DIRECTION ( 'NONE',  ( -0.000000000000000000, 0.1350103645451876666, 0.9908441862701600211 ) ) ;
#151151=VERTEX_POINT ( 'NONE', #34007 ) ;
#151192=DIRECTION ( 'NONE',  ( 1.441126678808781001E-14, 0.9876197685951252359, 0.1568667991644863424 ) ) ;
#151194=CARTESIAN_POINT ( 'NONE',  ( 18.59999999999999076, 6.450000000011156587, -110.5170271704400591 ) ) ;
#151223=VERTEX_POINT ( 'NONE', #238583 ) ;
#151233=DIRECTION ( 'NONE',  ( -0.000000000000000000, 1.000000000000000000, 0.000000000000000000 ) ) ;
#151250=ORIENTED_EDGE ( 'NONE', *, *, #194864, .T. ) ;
#151258=CARTESIAN_POINT ( 'NONE',  ( 18.44208962362687387, -9.552340496897866018, -140.8421730554626095 ) ) ;
#151286=ADVANCED_FACE ( 'NONE', ( #256803 ), #157700, .T. ) ;
#151305=VECTOR ( 'NONE', #62788, 1000.000000000000000 ) ;
#151345=CARTESIAN_POINT ( 'NONE',  ( -20.94999999999999929, 11.65000000001115232, -127.2161343370219413 ) ) ;
#151347=DIRECTION ( 'NONE',  ( 0.000000000000000000, 0.000000000000000000, -1.000000000000000000 ) ) ;
#151348=PRODUCT_CONTEXT ( 'NONE', #7431, 'mechanical' ) ;
#151359=ORIENTED_EDGE ( 'NONE', *, *, #207845, .T. ) ;
#151408=AXIS2_PLACEMENT_3D ( 'NONE', #33092, #93013, #89153 ) ;
#151422=DIRECTION ( 'NONE',  ( -0.000000000000000000, -0.9875055080513799322, 0.1575844902526464253 ) ) ;
#151430=CARTESIAN_POINT ( 'NONE',  ( -20.54999999999999716, 1.925233644870972816, -113.2302435331261563 ) ) ;
#151490=AXIS2_PLACEMENT_3D ( 'NONE', #5044, #84561, #61199 ) ;
#151521=AXIS2_PLACEMENT_3D ( 'NONE', #224940, #24212, #67173 ) ;
#151552=ORIENTED_EDGE ( 'NONE', *, *, #95038, .F. ) ;
#151567=EDGE_CURVE ( 'NONE', #253683, #214758, #215437, .T. ) ;
#151595=CARTESIAN_POINT ( 'NONE',  ( 23.14999999999999503, 11.65000000001116298, -88.75000000000004263 ) ) ;
#151605=EDGE_LOOP ( 'NONE', ( #28848, #56586, #23117, #79337, #45114, #139392, #35016, #59892, #100360, #80941, #231396 ) ) ;
#151614=DIRECTION ( 'NONE',  ( 0.000000000000000000, 0.000000000000000000, 1.000000000000000000 ) ) ;
#151651=CIRCLE ( 'NONE', #222509, 0.1000000000000028644 ) ;
#151709=DIRECTION ( 'NONE',  ( 2.952720810173289112E-16, -1.000000000000000000, 0.000000000000000000 ) ) ;
#151721=DIRECTION ( 'NONE',  ( 1.000000000000000000, 0.000000000000000000, 0.000000000000000000 ) ) ;
#151739=DIRECTION ( 'NONE',  ( -0.000000000000000000, 0.000000000000000000, 1.000000000000000000 ) ) ;
#151763=AXIS2_PLACEMENT_3D ( 'NONE', #156395, #53408, #71709 ) ;
#151765=DIRECTION ( 'NONE',  ( 1.000000000000000000, 2.952720810173289112E-16, -0.000000000000000000 ) ) ;
#151790=EDGE_CURVE ( 'NONE', #54821, #140474, #236941, .T. ) ;
#151797=CYLINDRICAL_SURFACE ( 'NONE', #24228, 0.09999999999999881206 ) ;
#151815=ORIENTED_EDGE ( 'NONE', *, *, #158772, .F. ) ;
#151871=DIRECTION ( 'NONE',  ( 1.000000000000000000, -0.000000000000000000, -0.000000000000000000 ) ) ;
#151874=DIRECTION ( 'NONE',  ( 1.000000000000000000, 0.000000000000000000, -0.000000000000000000 ) ) ;
#151907=CARTESIAN_POINT ( 'NONE',  ( 21.05000000000000071, -11.64999999998883595, -130.9000000000000341 ) ) ;
#151940=( NAMED_UNIT ( * ) SI_UNIT ( $, .STERADIAN. ) SOLID_ANGLE_UNIT ( ) );
#151948=DIRECTION ( 'NONE',  ( 0.000000000000000000, 0.000000000000000000, -1.000000000000000000 ) ) ;
#151966=AXIS2_PLACEMENT_3D ( 'NONE', #246676, #68049, #191883 ) ;
#151997=DIRECTION ( 'NONE',  ( 6.938893903907991995E-14, 0.000000000000000000, 1.000000000000000000 ) ) ;
#152065=ADVANCED_FACE ( 'NONE', ( #77281 ), #158162, .T. ) ;
#152095=EDGE_CURVE ( 'NONE', #112449, #75197, #207527, .T. ) ;
#152105=DIRECTION ( 'NONE',  ( 0.000000000000000000, -1.000000000000000000, 0.000000000000000000 ) ) ;
#152119=ORIENTED_EDGE ( 'NONE', *, *, #115761, .T. ) ;
#152121=ORIENTED_EDGE ( 'NONE', *, *, #249238, .F. ) ;
#152132=EDGE_LOOP ( 'NONE', ( #79333, #8905, #47309 ) ) ;
#152172=ORIENTED_EDGE ( 'NONE', *, *, #32517, .F. ) ;
#152182=EDGE_CURVE ( 'NONE', #97170, #173551, #162311, .T. ) ;
#152192=CARTESIAN_POINT ( 'NONE',  ( -21.05000000000000071, -11.64999999998884483, -103.5000000000000426 ) ) ;
#152195=CARTESIAN_POINT ( 'NONE',  ( -23.25000000000000000, 4.350000000011156054, -121.8500000000000227 ) ) ;
#152211=ORIENTED_EDGE ( 'NONE', *, *, #29435, .T. ) ;
#152227=CARTESIAN_POINT ( 'NONE',  ( 20.99142135623731065, 11.60000000001116049, -127.0717967697245570 ) ) ;
#152234=B_SPLINE_CURVE_WITH_KNOTS ( 'NONE', 3,
 ( #248647, #49161, #28359, #70038, #167860, #109123, #50423, #209523, #30922, #110417, #189966, #236773, #253765, #214647, #157277, #174301, #56831, #34771, #78964 ),
 .UNSPECIFIED., .F., .F.,
 ( 4, 3, 3, 3, 3, 3, 4 ),
 ( -2.000416914663624153E-06, 0.000000000000000000, 4.714008503747321038E-05, 9.979203887777386673E-05, 0.0001372215519229492986, 0.0001635031576221004674, 0.0001900083748504117793 ),
 .UNSPECIFIED. ) ;
#152261=DIRECTION ( 'NONE',  ( 0.000000000000000000, 1.224646799142185182E-16, 1.000000000000000000 ) ) ;
#152263=CARTESIAN_POINT ( 'NONE',  ( -18.50000000000000000, 1.115600667400684642E-11, -134.0000000000000284 ) ) ;
#152264=CARTESIAN_POINT ( 'NONE',  ( -20.64999999999999858, 1.115600667400684642E-11, -113.4750000000000369 ) ) ;
#152300=CIRCLE ( 'NONE', #81493, 4.099999999999992539 ) ;
#152316=FACE_OUTER_BOUND ( 'NONE', #247291, .T. ) ;
#152392=CARTESIAN_POINT ( 'NONE',  ( 21.05000000000000071, -11.48912529306489994, -131.0000000000000284 ) ) ;
#152395=CARTESIAN_POINT ( 'NONE',  ( -23.25000000000000000, 4.150000000011156764, -121.6500000000000341 ) ) ;
#152418=VECTOR ( 'NONE', #170894, 1000.000000000000000 ) ;
#152422=CIRCLE ( 'NONE', #35884, 0.1000000000000028644 ) ;
#152428=DIRECTION ( 'NONE',  ( 0.000000000000000000, 0.8700118002898322711, -0.4930308989875231140 ) ) ;
#152432=ORIENTED_EDGE ( 'NONE', *, *, #243975, .F. ) ;
#152469=ORIENTED_EDGE ( 'NONE', *, *, #115052, .F. ) ;
#152480=VERTEX_POINT ( 'NONE', #136952 ) ;
#152498=ADVANCED_FACE ( 'NONE', ( #179948 ), #1278, .T. ) ;
#152512=DIRECTION ( 'NONE',  ( -3.265361837132813093E-16, 1.000000000000000000, 0.000000000000000000 ) ) ;
#152562=CARTESIAN_POINT ( 'NONE',  ( 18.50000000000000355, -9.399999999988841282, -140.8820418481727188 ) ) ;
#152581=LINE ( 'NONE', #110847, #220409 ) ;
#152591=CARTESIAN_POINT ( 'NONE',  ( -22.42253884134832020, 0.001932351146464885046, -88.85039430265160831 ) ) ;
#152598=DIRECTION ( 'NONE',  ( 0.7071359030027593029, 0.000000000000000000, -0.7070776581709197206 ) ) ;
#152609=ADVANCED_FACE ( 'NONE', ( #142081 ), #224824, .T. ) ;
#152610=CARTESIAN_POINT ( 'NONE',  ( -20.85000000000000142, 11.75000000001115552, -134.0000000000000284 ) ) ;
#152612=CARTESIAN_POINT ( 'NONE',  ( 20.85882249326303040, 10.33248238083634796, -139.5948465439131780 ) ) ;
#152634=ADVANCED_FACE ( 'NONE', ( #230627, #53267, #207218 ), #51953, .F. ) ;
#152636=CARTESIAN_POINT ( 'NONE',  ( -23.25000000000000000, 11.65000000001115588, -112.6500000000000483 ) ) ;
#152638=ORIENTED_EDGE ( 'NONE', *, *, #24891, .F. ) ;
#152650=DIRECTION ( 'NONE',  ( 0.000000000000000000, 0.000000000000000000, -1.000000000000000000 ) ) ;
#152695=AXIS2_PLACEMENT_3D ( 'NONE', #212363, #131520, #113239 ) ;
#152725=CARTESIAN_POINT ( 'NONE',  ( 21.06277459767431637, 8.872862438279403463, -112.7039991923567044 ) ) ;
#152764=ORIENTED_EDGE ( 'NONE', *, *, #119331, .F. ) ;
#152765=AXIS2_PLACEMENT_3D ( 'NONE', #168640, #164734, #6934 ) ;
#152768=AXIS2_PLACEMENT_3D ( 'NONE', #46137, #106089, #185658 ) ;
#152775=CARTESIAN_POINT ( 'NONE',  ( -18.59999999999999787, 11.65000000001115232, -134.0000000000000284 ) ) ;
#152779=AXIS2_PLACEMENT_3D ( 'NONE', #208951, #131980, #49870 ) ;
#152782=DIRECTION ( 'NONE',  ( 0.000000000000000000, 1.000000000000000000, 0.000000000000000000 ) ) ;
#152818=EDGE_CURVE ( 'NONE', #84132, #28041, #237034, .T. ) ;
#152829=EDGE_LOOP ( 'NONE', ( #29469, #146945, #221468, #13306 ) ) ;
#152836=ORIENTED_EDGE ( 'NONE', *, *, #235684, .T. ) ;
#152838=DIRECTION ( 'NONE',  ( -1.000000000000000000, -0.000000000000000000, -0.000000000000000000 ) ) ;
#152887=DIRECTION ( 'NONE',  ( 0.000000000000000000, 0.000000000000000000, -1.000000000000000000 ) ) ;
#152902=PLANE ( 'NONE',  #231842 ) ;
#152915=CARTESIAN_POINT ( 'NONE',  ( 23.14999999999999858, 1.115600667400684642E-11, -134.0000000000000284 ) ) ;
#152920=ORIENTED_EDGE ( 'NONE', *, *, #129038, .F. ) ;
#152921=CARTESIAN_POINT ( 'NONE',  ( 21.14999999999999858, 8.786607556611267356, -112.8500000000000369 ) ) ;
#152922=CARTESIAN_POINT ( 'NONE',  ( -23.15000000000000213, -8.999999999988844479, -124.6060308773475924 ) ) ;
#152931=CIRCLE ( 'NONE', #207068, 0.1999999999999999833 ) ;
#152936=CYLINDRICAL_SURFACE ( 'NONE', #113868, 12.87499999999999822 ) ;
#152970=DIRECTION ( 'NONE',  ( 0.000000000000000000, 0.000000000000000000, -1.000000000000000000 ) ) ;
#152998=CARTESIAN_POINT ( 'NONE',  ( 21.05000000000000071, 8.776282895303632259, -109.0586289951409924 ) ) ;
#153004=CARTESIAN_POINT ( 'NONE',  ( 19.97071067811864609, 11.72071067812981404, -121.8500000000000369 ) ) ;
#153006=EDGE_CURVE ( 'NONE', #8700, #164965, #133443, .T. ) ;
#153039=CARTESIAN_POINT ( 'NONE',  ( 18.58719872626880587, -9.566644397587481308, -140.8224781963970713 ) ) ;
#153045=LINE ( 'NONE', #214265, #202291 ) ;
#153077=CARTESIAN_POINT ( 'NONE',  ( 21.14999999999999858, 1.115600667400684642E-11, -88.85042919245522341 ) ) ;
#153106=EDGE_CURVE ( 'NONE', #95552, #198561, #62712, .T. ) ;
#153129=VERTEX_POINT ( 'NONE', #196301 ) ;
#153157=PLANE ( 'NONE',  #10482 ) ;
#153161=B_SPLINE_CURVE_WITH_KNOTS ( 'NONE', 3,
 ( #134333, #184368, #85242, #157817 ),
 .UNSPECIFIED., .F., .F.,
 ( 4, 4 ),
 ( 3.469446951953614189E-18, 0.0001058379652594569419 ),
 .UNSPECIFIED. ) ;
#153162=ADVANCED_FACE ( 'NONE', ( #232898 ), #54220, .F. ) ;
#153169=EDGE_CURVE ( 'NONE', #253301, #226312, #137687, .T. ) ;
#153207=CARTESIAN_POINT ( 'NONE',  ( 20.85000000000000142, -1.835859311432481045, -145.6044391687985637 ) ) ;
#153218=LINE ( 'NONE', #30695, #242714 ) ;
#153219=CIRCLE ( 'NONE', #53233, 0.09999999999998898659 ) ;
#153222=CIRCLE ( 'NONE', #49122, 4.149999999999999467 ) ;
#153225=AXIS2_PLACEMENT_3D ( 'NONE', #60512, #97043, #141352 ) ;
#153273=ORIENTED_EDGE ( 'NONE', *, *, #105381, .F. ) ;
#153281=CIRCLE ( 'NONE', #24266, 3.899999999999999467 ) ;
#153291=DIRECTION ( 'NONE',  ( 0.000000000000000000, -1.000000000000000000, 0.000000000000000000 ) ) ;
#153300=CYLINDRICAL_SURFACE ( 'NONE', #192266, 0.09999999999999939493 ) ;
#153333=CYLINDRICAL_SURFACE ( 'NONE', #195256, 0.1000000000000028644 ) ;
#153413=TOROIDAL_SURFACE ( 'NONE', #215707, 0.2000000000000000111, 0.1000000000000000056 ) ;
#153414=DIRECTION ( 'NONE',  ( 0.000000000000000000, 0.000000000000000000, -1.000000000000000000 ) ) ;
#153432=CIRCLE ( 'NONE', #257366, 0.09999999999998898659 ) ;
#153461=CARTESIAN_POINT ( 'NONE',  ( -21.05000000000000071, -1.835341550213255957, -112.1551512925630050 ) ) ;
#153474=AXIS2_PLACEMENT_3D ( 'NONE', #216763, #19873, #79800 ) ;
#153482=EDGE_CURVE ( 'NONE', #20141, #208598, #254352, .T. ) ;
#153503=CARTESIAN_POINT ( 'NONE',  ( -20.64999999999999858, 7.250000000011155521, -112.7500000000000284 ) ) ;
#153508=CARTESIAN_POINT ( 'NONE',  ( 18.50000000000000000, -9.399999999988843058, -140.8820418481727188 ) ) ;
#153513=CARTESIAN_POINT ( 'NONE',  ( 0.000000000000000000, 0.000000000000000000, 0.000000000000000000 ) ) ;
#153531=CARTESIAN_POINT ( 'NONE',  ( 21.07199075132371746, 8.774944999127242795, -112.7135321616128891 ) ) ;
#153539=CARTESIAN_POINT ( 'NONE',  ( -18.39999999999999858, -9.499999999988849808, -140.6001893912220737 ) ) ;
#153559=CIRCLE ( 'NONE', #186842, 0.1000000000000028644 ) ;
#153612=LINE ( 'NONE', #71481, #26672 ) ;
#153617=DIRECTION ( 'NONE',  ( 0.000000000000000000, 0.000000000000000000, -1.000000000000000000 ) ) ;
#153704=DIRECTION ( 'NONE',  ( 0.000000000000000000, 0.000000000000000000, -1.000000000000000000 ) ) ;
#153718=LINE ( 'NONE', #118393, #76159 ) ;
#153722=CARTESIAN_POINT ( 'NONE',  ( -23.15000000000000213, 11.75000000001115552, -121.8500000000000369 ) ) ;
#153726=VERTEX_POINT ( 'NONE', #85977 ) ;
#153756=DIRECTION ( 'NONE',  ( 0.000000000000000000, 0.000000000000000000, -1.000000000000000000 ) ) ;
#153770=DIRECTION ( 'NONE',  ( 0.000000000000000000, 0.9876197685951252359, -0.1568667991644863424 ) ) ;
#153797=EDGE_CURVE ( 'NONE', #91963, #183616, #83869, .T. ) ;
#153798=CIRCLE ( 'NONE', #28904, 0.1000000000000000472 ) ;
#153806=CARTESIAN_POINT ( 'NONE',  ( 21.11701782572533048, 10.72160911601861244, -112.7450374295112567 ) ) ;
#153821=ADVANCED_FACE ( 'NONE', ( #148562 ), #228105, .F. ) ;
#153860=DIRECTION ( 'NONE',  ( 0.000000000000000000, 0.000000000000000000, -1.000000000000000000 ) ) ;
#153862=CARTESIAN_POINT ( 'NONE',  ( 20.85000000000000142, -1.263275465206102233, -141.9018646667464338 ) ) ;
#153866=EDGE_CURVE ( 'NONE', #106114, #39467, #87981, .T. ) ;
#153883=DIRECTION ( 'NONE',  ( 1.000000000000000000, -0.000000000000000000, -0.000000000000000000 ) ) ;
#153894=CARTESIAN_POINT ( 'NONE',  ( -22.47886152344871036, 0.03750093887284931121, -88.85001135695209484 ) ) ;
#153918=CARTESIAN_POINT ( 'NONE',  ( 20.86777300164945004, 10.33200063080771969, -139.5931674956643462 ) ) ;
#153920=VECTOR ( 'NONE', #229528, 999.9999999999998863 ) ;
#153921=CARTESIAN_POINT ( 'NONE',  ( 18.59999999999999432, -9.480686695267811714, -140.9411151687579036 ) ) ;
#153960=EDGE_CURVE ( 'NONE', #139652, #120723, #118424, .T. ) ;
#153962=LINE ( 'NONE', #176070, #107026 ) ;
#153966=CARTESIAN_POINT ( 'NONE',  ( 20.94999999999999929, -8.999999999988842703, -124.1060308773475924 ) ) ;
#153979=DIRECTION ( 'NONE',  ( 0.000000000000000000, 0.000000000000000000, -1.000000000000000000 ) ) ;
#154011=DIRECTION ( 'NONE',  ( 0.000000000000000000, 0.000000000000000000, -1.000000000000000000 ) ) ;
#154012=B_SPLINE_CURVE_WITH_KNOTS ( 'NONE', 3,
 ( #33253, #11091, #73655, #28106, #107611, #51462, #227558, #250958, #192298, #171480 ),
 .UNSPECIFIED., .F., .F.,
 ( 4, 3, 3, 4 ),
 ( 0.000000000000000000, 0.0002000000000008536833, 0.001000000000082972495, 0.001967863649483305062 ),
 .UNSPECIFIED. ) ;
#154094=EDGE_CURVE ( 'NONE', #34485, #204479, #250688, .T. ) ;
#154121=VERTEX_POINT ( 'NONE', #101356 ) ;
#154144=ORIENTED_EDGE ( 'NONE', *, *, #202456, .T. ) ;
#154158=SPHERICAL_SURFACE ( 'NONE', #28830, 0.1000000000000000056 ) ;
#154178=CARTESIAN_POINT ( 'NONE',  ( -21.08198257630413508, 0.07264332379574613141, -94.16340326598496802 ) ) ;
#154200=EDGE_CURVE ( 'NONE', #198561, #95552, #138247, .T. ) ;
#154206=CYLINDRICAL_SURFACE ( 'NONE', #73759, 0.09999999999999939493 ) ;
#154220=DIRECTION ( 'NONE',  ( 0.9880948137434723000, 0.1538461538461484146, -0.000000000000000000 ) ) ;
#154221=ADVANCED_FACE ( 'NONE', ( #231646 ), #44824, .F. ) ;
#154227=TOROIDAL_SURFACE ( 'NONE', #25199, 0.2000000000000000111, 0.1000000000000000056 ) ;
#154230=CARTESIAN_POINT ( 'NONE',  ( -21.45000000000000284, 7.708578643773852157, -121.6500000000000341 ) ) ;
#154257=EDGE_CURVE ( 'NONE', #243362, #213681, #252457, .T. ) ;
#154264=AXIS2_PLACEMENT_3D ( 'NONE', #216504, #194407, #155288 ) ;
#154278=EDGE_CURVE ( 'NONE', #257618, #63374, #163222, .T. ) ;
#154284=CARTESIAN_POINT ( 'NONE',  ( 23.15000000000000213, -11.74999999998883560, -130.9000000000000341 ) ) ;
#154297=ORIENTED_EDGE ( 'NONE', *, *, #163530, .F. ) ;
#154316=AXIS2_PLACEMENT_3D ( 'NONE', #84006, #243132, #64505 ) ;
#154322=EDGE_LOOP ( 'NONE', ( #245179, #154144, #759, #191499 ) ) ;
#154327=LINE ( 'NONE', #233822, #195756 ) ;
#154355=VERTEX_POINT ( 'NONE', #15159 ) ;
#154382=VERTEX_POINT ( 'NONE', #33040 ) ;
#154412=CARTESIAN_POINT ( 'NONE',  ( -21.44999999999999929, 7.150000000011155876, -121.7500000000000426 ) ) ;
#154420=ORIENTED_EDGE ( 'NONE', *, *, #43528, .T. ) ;
#154431=EDGE_LOOP ( 'NONE', ( #199958, #191688, #216020, #257824 ) ) ;
#154436=EDGE_CURVE ( 'NONE', #256383, #208604, #9565, .T. ) ;
#154440=EDGE_CURVE ( 'NONE', #238954, #114550, #190813, .T. ) ;
#154454=DIRECTION ( 'NONE',  ( 0.000000000000000000, 0.000000000000000000, -1.000000000000000000 ) ) ;
#154527=DIRECTION ( 'NONE',  ( -1.000000000000000000, -0.000000000000000000, -0.000000000000000000 ) ) ;
#154607=CARTESIAN_POINT ( 'NONE',  ( -20.94999999999999929, -11.48912529306490349, -103.6000000000000369 ) ) ;
#154609=EDGE_CURVE ( 'NONE', #253301, #111732, #171805, .T. ) ;
#154662=LINE ( 'NONE', #17673, #51371 ) ;
#154670=DIRECTION ( 'NONE',  ( -0.000000000000000000, 1.000000000000000000, 0.000000000000000000 ) ) ;
#154683=DIRECTION ( 'NONE',  ( 0.000000000000000000, 0.000000000000000000, -1.000000000000000000 ) ) ;
#154694=FACE_OUTER_BOUND ( 'NONE', #28312, .T. ) ;
#154734=ORIENTED_EDGE ( 'NONE', *, *, #178207, .F. ) ;
#154745=FACE_OUTER_BOUND ( 'NONE', #70778, .T. ) ;
#154785=CYLINDRICAL_SURFACE ( 'NONE', #222320, 0.5000000000000004441 ) ;
#154797=CIRCLE ( 'NONE', #133911, 0.3999999999999975797 ) ;
#154803=CARTESIAN_POINT ( 'NONE',  ( -22.39999999999999858, 11.65000000001115588, -100.4000000000000483 ) ) ;
#154829=DIRECTION ( 'NONE',  ( 1.000000000000000000, 0.000000000000000000, 0.000000000000000000 ) ) ;
#154839=TOROIDAL_SURFACE ( 'NONE', #163196, 0.2000000000000000111, 0.1000000000000000056 ) ;
#154910=ORIENTED_EDGE ( 'NONE', *, *, #254176, .F. ) ;
#154931=CIRCLE ( 'NONE', #175768, 0.1000000000000000472 ) ;
#154948=EDGE_CURVE ( 'NONE', #32589, #104317, #25465, .T. ) ;
#154968=ORIENTED_EDGE ( 'NONE', *, *, #43702, .F. ) ;
#154983=EDGE_LOOP ( 'NONE', ( #28419, #2427, #109465, #121891 ) ) ;
#154988=DIRECTION ( 'NONE',  ( 0.000000000000000000, 0.4930308989874729320, 0.8700118002898605818 ) ) ;
#154994=CARTESIAN_POINT ( 'NONE',  ( 20.85000000000000142, -1.149570369564537842, -141.8159124845019790 ) ) ;
#155003=CARTESIAN_POINT ( 'NONE',  ( -23.15000000000000213, -11.64999999998884483, -88.75000000000004263 ) ) ;
#155066=CARTESIAN_POINT ( 'NONE',  ( -21.05000000000000071, -1.835341550213255957, -112.0551512925630107 ) ) ;
#155075=ORIENTED_EDGE ( 'NONE', *, *, #251254, .F. ) ;
#155081=ORIENTED_EDGE ( 'NONE', *, *, #238215, .F. ) ;
#155106=DIRECTION ( 'NONE',  ( 0.000000000000000000, 0.000000000000000000, 1.000000000000000000 ) ) ;
#155117=EDGE_CURVE ( 'NONE', #83513, #45115, #146250, .T. ) ;
#155132=DIRECTION ( 'NONE',  ( 1.000000000000000000, -0.000000000000000000, -0.000000000000000000 ) ) ;
#155166=ORIENTED_EDGE ( 'NONE', *, *, #188771, .T. ) ;
#155193=CARTESIAN_POINT ( 'NONE',  ( 22.49231231312462853, 11.64998490368843953, -100.4389471123986652 ) ) ;
#155196=DIRECTION ( 'NONE',  ( 2.715809747126116508E-16, -1.000000000000000000, 0.000000000000000000 ) ) ;
#155222=CIRCLE ( 'NONE', #250843, 12.97499999999999964 ) ;
#155272=FACE_OUTER_BOUND ( 'NONE', #241256, .T. ) ;
#155277=EDGE_LOOP ( 'NONE', ( #243097, #198196, #34077, #10649 ) ) ;
#155280=CARTESIAN_POINT ( 'NONE',  ( 23.24999999999999645, -2.099999999988846344, -134.0000000000000284 ) ) ;
#155284=VERTEX_POINT ( 'NONE', #185311 ) ;
#155288=DIRECTION ( 'NONE',  ( 0.000000000000000000, 0.000000000000000000, -1.000000000000000000 ) ) ;
#155290=ORIENTED_EDGE ( 'NONE', *, *, #246313, .T. ) ;
#155321=LINE ( 'NONE', #113592, #132180 ) ;
#155339=AXIS2_PLACEMENT_3D ( 'NONE', #80653, #61110, #122378 ) ;
#155364=ORIENTED_EDGE ( 'NONE', *, *, #15054, .F. ) ;
#155367=EDGE_LOOP ( 'NONE', ( #48523, #66802, #20709, #69386 ) ) ;
#155376=B_SPLINE_CURVE_WITH_KNOTS ( 'NONE', 3,
 ( #99003, #254237, #212578, #33974, #155193, #242387, #159038 ),
 .UNSPECIFIED., .F., .F.,
 ( 4, 3, 4 ),
 ( 0.000000000000000000, 3.357501770813415632E-05, 5.199112466348475308E-05 ),
 .UNSPECIFIED. ) ;
#155377=ORIENTED_EDGE ( 'NONE', *, *, #166940, .T. ) ;
#155397=EDGE_CURVE ( 'NONE', #79959, #243325, #138043, .T. ) ;
#155407=CARTESIAN_POINT ( 'NONE',  ( -20.64999999999999858, 1.115600667400684642E-11, -100.5000000000000284 ) ) ;
#155415=AXIS2_PLACEMENT_3D ( 'NONE', #180183, #101881, #1513 ) ;
#155440=FACE_OUTER_BOUND ( 'NONE', #174957, .T. ) ;
#155459=CARTESIAN_POINT ( 'NONE',  ( -21.08376601933334271, 0.06377601094103638180, -94.15805272872430010 ) ) ;
#155460=DIRECTION ( 'NONE',  ( 0.000000000000000000, 0.000000000000000000, 1.000000000000000000 ) ) ;
#155479=DIRECTION ( 'NONE',  ( 0.000000000000000000, 0.000000000000000000, -1.000000000000000000 ) ) ;
#155482=FACE_OUTER_BOUND ( 'NONE', #68164, .T. ) ;
#155483=DIRECTION ( 'NONE',  ( 1.000000000000000000, 0.000000000000000000, 0.000000000000000000 ) ) ;
#155491=VECTOR ( 'NONE', #127711, 1000.000000000000000 ) ;
#155517=CARTESIAN_POINT ( 'NONE',  ( -21.55000000000000426, 7.708578643773852157, -112.8500000000000369 ) ) ;
#155524=ORIENTED_EDGE ( 'NONE', *, *, #28374, .F. ) ;
#155541=DIRECTION ( 'NONE',  ( 1.000000000000000000, 0.000000000000000000, 0.000000000000000000 ) ) ;
#155558=FACE_OUTER_BOUND ( 'NONE', #109806, .T. ) ;
#155581=VECTOR ( 'NONE', #148463, 1000.000000000000000 ) ;
#155613=EDGE_LOOP ( 'NONE', ( #216586, #150025, #132973, #78377 ) ) ;
#155619=ORIENTED_EDGE ( 'NONE', *, *, #247931, .F. ) ;
#155622=EDGE_CURVE ( 'NONE', #34485, #168568, #204870, .T. ) ;
#155647=ORIENTED_EDGE ( 'NONE', *, *, #142084, .T. ) ;
#155653=CARTESIAN_POINT ( 'NONE',  ( -21.05000000000000071, -11.64999999998884306, -131.1000000000000227 ) ) ;
#155680=CARTESIAN_POINT ( 'NONE',  ( 20.94999999999999574, 10.62357026049396680, -107.9919452032305855 ) ) ;
#155682=DIRECTION ( 'NONE',  ( -1.000000000000000000, 0.000000000000000000, 0.000000000000000000 ) ) ;
#155693=CONICAL_SURFACE ( 'NONE', #255563, 4.049999999999998046, 0.7853981633974604915 ) ;
#155732=DIRECTION ( 'NONE',  ( 1.000000000000000000, 2.952720810173289112E-16, -0.000000000000000000 ) ) ;
#155738=DIRECTION ( 'NONE',  ( -0.000000000000000000, -0.000000000000000000, -1.000000000000000000 ) ) ;
#155774=AXIS2_PLACEMENT_3D ( 'NONE', #61058, #117196, #36398 ) ;
#155815=CARTESIAN_POINT ( 'NONE',  ( -18.50000000000000000, 11.75000000001115197, -121.8500000000000369 ) ) ;
#155843=ORIENTED_EDGE ( 'NONE', *, *, #18120, .F. ) ;
#155860=ORIENTED_EDGE ( 'NONE', *, *, #5272, .T. ) ;
#155919=DIRECTION ( 'NONE',  ( -0.000000000000000000, 0.1298341882520022694, 0.9915357197604853789 ) ) ;
#155920=VERTEX_POINT ( 'NONE', #114453 ) ;
#155922=CARTESIAN_POINT ( 'NONE',  ( -20.64999999999999858, 1.115600667400684642E-11, -135.9000000000000625 ) ) ;
#155929=EDGE_CURVE ( 'NONE', #79905, #164965, #221791, .T. ) ;
#155965=ADVANCED_FACE ( 'NONE', ( #117020 ), #109377, .T. ) ;
#155966=ORIENTED_EDGE ( 'NONE', *, *, #125705, .F. ) ;
#155973=EDGE_LOOP ( 'NONE', ( #76699, #9752, #250848, #137571 ) ) ;
#155986=CARTESIAN_POINT ( 'NONE',  ( 22.48660254037844197, 11.65000000001116298, -100.4500000000000455 ) ) ;
#156053=AXIS2_PLACEMENT_3D ( 'NONE', #156217, #230604, #151064 ) ;
#156096=CARTESIAN_POINT ( 'NONE',  ( -20.85000000000000142, -1.164121893230052995, -141.7148480855716457 ) ) ;
#156118=CYLINDRICAL_SURFACE ( 'NONE', #199580, 0.09999999999999939493 ) ;
#156135=VERTEX_POINT ( 'NONE', #43901 ) ;
#156172=DIRECTION ( 'NONE',  ( -1.000000000000000000, -2.952720810173289112E-16, 0.000000000000000000 ) ) ;
#156199=CARTESIAN_POINT ( 'NONE',  ( 23.14999999999998792, 11.65000000001115588, -100.5000000000000284 ) ) ;
#156203=DIRECTION ( 'NONE',  ( 0.000000000000000000, 0.000000000000000000, -1.000000000000000000 ) ) ;
#156217=CARTESIAN_POINT ( 'NONE',  ( -23.15000000000000213, -4.831324760611774849, -117.4696969421987802 ) ) ;
#156249=DIRECTION ( 'NONE',  ( 0.000000000000000000, 6.308085367182471812E-16, 1.000000000000000000 ) ) ;
#156255=PLANE ( 'NONE',  #108166 ) ;
#156344=DIRECTION ( 'NONE',  ( 0.000000000000000000, 0.000000000000000000, 1.000000000000000000 ) ) ;
#156349=DIRECTION ( 'NONE',  ( 1.000000000000000000, -0.000000000000000000, -0.000000000000000000 ) ) ;
#156351=CARTESIAN_POINT ( 'NONE',  ( 21.07189867249812210, 10.72498027010430377, -112.7124514422767732 ) ) ;
#156353=CARTESIAN_POINT ( 'NONE',  ( 20.95000000000000284, 11.60000000001116227, -127.0717967697245143 ) ) ;
#156379=CARTESIAN_POINT ( 'NONE',  ( 18.59999999999999076, 5.950000000011100632, -110.8057023050348988 ) ) ;
#156391=ORIENTED_EDGE ( 'NONE', *, *, #54037, .T. ) ;
#156395=CARTESIAN_POINT ( 'NONE',  ( 21.14999999999999858, 11.65000000001115943, -100.6000000000000369 ) ) ;
#156396=DIRECTION ( 'NONE',  ( -1.000000000000000000, -0.000000000000000000, -0.000000000000000000 ) ) ;
#156398=VERTEX_POINT ( 'NONE', #287 ) ;
#156399=ADVANCED_FACE ( 'NONE', ( #79805 ), #238913, .T. ) ;
#156403=AXIS2_PLACEMENT_3D ( 'NONE', #65220, #121392, #63949 ) ;
#156414=ADVANCED_FACE ( 'NONE', ( #246600 ), #47663, .T. ) ;
#156425=AXIS2_PLACEMENT_3D ( 'NONE', #205720, #131324, #207019 ) ;
#156447=CARTESIAN_POINT ( 'NONE',  ( -20.85000000000000142, -1.164121893230052995, -141.9148480855716343 ) ) ;
#156475=CARTESIAN_POINT ( 'NONE',  ( -22.42357213249529124, 0.09908696401271366305, -92.82706761364009651 ) ) ;
#156498=AXIS2_PLACEMENT_3D ( 'NONE', #200945, #65286, #224356 ) ;
#156507=CARTESIAN_POINT ( 'NONE',  ( 18.59999999999999787, -1.835341550213255957, -112.1551512925630050 ) ) ;
#156540=CARTESIAN_POINT ( 'NONE',  ( -18.59999999999999787, -1.162701749926853712, -108.5000000000000426 ) ) ;
#156550=ORIENTED_EDGE ( 'NONE', *, *, #172920, .F. ) ;
#156551=ADVANCED_FACE ( 'NONE', ( #147510 ), #48398, .F. ) ;
#156591=VECTOR ( 'NONE', #66337, 1000.000000000000000 ) ;
#156621=CARTESIAN_POINT ( 'NONE',  ( -20.54999999999999716, -8.663551401858001100, -124.4758988819327215 ) ) ;
#156624=DIRECTION ( 'NONE',  ( 0.000000000000000000, 0.000000000000000000, 1.000000000000000000 ) ) ;
#156641=CARTESIAN_POINT ( 'NONE',  ( 19.75857864376268935, 11.65000000001115943, -125.2500000000000284 ) ) ;
#156646=CARTESIAN_POINT ( 'NONE',  ( -18.59999999999999787, 6.933893972137497030, -137.7856458343736108 ) ) ;
#156662=CIRCLE ( 'NONE', #94071, 11.90000000000000213 ) ;
#156669=CARTESIAN_POINT ( 'NONE',  ( -23.15000000000000213, 1.115600667400684642E-11, -134.0000000000000284 ) ) ;
#156672=CARTESIAN_POINT ( 'NONE',  ( -18.59999999999999787, -1.736705739456431807, -145.5174225876237699 ) ) ;
#156739=CARTESIAN_POINT ( 'NONE',  ( 20.94999999999999929, 1.115600667400684642E-11, -136.0000000000000284 ) ) ;
#156743=CARTESIAN_POINT ( 'NONE',  ( 18.59999999999999432, -1.162701749926853712, -108.6000000000000227 ) ) ;
#156759=FACE_OUTER_BOUND ( 'NONE', #127931, .T. ) ;
#156762=FACE_OUTER_BOUND ( 'NONE', #2662, .T. ) ;
#156790=DIRECTION ( 'NONE',  ( 1.000000000000000000, -0.000000000000000000, -0.000000000000000000 ) ) ;
#156816=CARTESIAN_POINT ( 'NONE',  ( 21.13461538461538325, 8.885417037985616773, -112.8500000000000369 ) ) ;
#156827=ORIENTED_EDGE ( 'NONE', *, *, #101487, .F. ) ;
#156854=ADVANCED_FACE ( 'NONE', ( #245015 ), #70266, .T. ) ;
#156862=VECTOR ( 'NONE', #198166, 1000.000000000000227 ) ;
#156874=EDGE_CURVE ( 'NONE', #58429, #217887, #48093, .T. ) ;
#156881=DIRECTION ( 'NONE',  ( 0.000000000000000000, 0.000000000000000000, 1.000000000000000000 ) ) ;
#156884=ORIENTED_EDGE ( 'NONE', *, *, #119025, .T. ) ;
#156887=CARTESIAN_POINT ( 'NONE',  ( 22.39999999999999503, 7.790779598384535376, -100.5000000000000284 ) ) ;
#156912=ORIENTED_EDGE ( 'NONE', *, *, #198020, .T. ) ;
#156928=VECTOR ( 'NONE', #1523, 1000.000000000000227 ) ;
#156932=CIRCLE ( 'NONE', #148544, 0.1000000000000028644 ) ;
#156954=ORIENTED_EDGE ( 'NONE', *, *, #127293, .T. ) ;
#157034=DIRECTION ( 'NONE',  ( 0.000000000000000000, 0.000000000000000000, 1.000000000000000000 ) ) ;
#157038=DIRECTION ( 'NONE',  ( 0.000000000000000000, -1.000000000000000000, 0.000000000000000000 ) ) ;
#157039=CARTESIAN_POINT ( 'NONE',  ( 23.14999999999998437, 1.115600667400684642E-11, -100.5000000000000284 ) ) ;
#157056=ORIENTED_EDGE ( 'NONE', *, *, #137020, .T. ) ;
#157090=CARTESIAN_POINT ( 'NONE',  ( 20.94999999999999574, -1.835341550213255957, -112.0551512925630107 ) ) ;
#157092=VECTOR ( 'NONE', #125575, 1000.000000000000000 ) ;
#157104=ORIENTED_EDGE ( 'NONE', *, *, #9622, .T. ) ;
#157135=DIRECTION ( 'NONE',  ( 0.000000000000000000, 0.000000000000000000, 1.000000000000000000 ) ) ;
#157150=ORIENTED_EDGE ( 'NONE', *, *, #151790, .T. ) ;
#157156=CARTESIAN_POINT ( 'NONE',  ( -20.54999999999999716, 1.115600667400684642E-11, -134.0000000000000284 ) ) ;
#157163=EDGE_CURVE ( 'NONE', #143179, #94985, #127162, .T. ) ;
#157216=DIRECTION ( 'NONE',  ( 0.000000000000000000, 1.000000000000000000, -6.308085367188393199E-16 ) ) ;
#157217=VECTOR ( 'NONE', #157489, 1000.000000000000000 ) ;
#157259=AXIS2_PLACEMENT_3D ( 'NONE', #72823, #32416, #93637 ) ;
#157273=CARTESIAN_POINT ( 'NONE',  ( -18.59999999999999787, 1.115600667400684642E-11, -100.5000000000000284 ) ) ;
#157276=CARTESIAN_POINT ( 'NONE',  ( 21.04999999999999716, 6.300183336278410984, -100.4486725676586474 ) ) ;
#157277=CARTESIAN_POINT ( 'NONE',  ( 18.56579813702274961, 10.33025634372637747, -139.5870929282639281 ) ) ;
#157298=CARTESIAN_POINT ( 'NONE',  ( 23.14999999999998437, 1.115600667400684642E-11, -104.5500000000000256 ) ) ;
#157313=DIRECTION ( 'NONE',  ( -1.000000000000000000, 0.000000000000000000, 0.000000000000000000 ) ) ;
#157318=DIRECTION ( 'NONE',  ( 0.000000000000000000, 0.000000000000000000, 1.000000000000000000 ) ) ;
#157336=ORIENTED_EDGE ( 'NONE', *, *, #49663, .T. ) ;
#157340=AXIS2_PLACEMENT_3D ( 'NONE', #149567, #28351, #71312 ) ;
#157362=ORIENTED_EDGE ( 'NONE', *, *, #158371, .T. ) ;
#157391=AXIS2_PLACEMENT_3D ( 'NONE', #242051, #238196, #59534 ) ;
#157419=DIRECTION ( 'NONE',  ( 2.879366945564059217E-14, -0.9875055080513751582, 0.1575844902526747915 ) ) ;
#157435=LINE ( 'NONE', #79117, #231996 ) ;
#157440=TOROIDAL_SURFACE ( 'NONE', #94850, 0.6000000000000017542, 0.1000000000000000056 ) ;
#157489=DIRECTION ( 'NONE',  ( 0.000000000000000000, 1.000000000000000000, 0.000000000000000000 ) ) ;
#157491=EDGE_CURVE ( 'NONE', #214758, #4150, #159735, .T. ) ;
#157496=ADVANCED_FACE ( 'NONE', ( #140144 ), #239270, .T. ) ;
#157538=ADVANCED_FACE ( 'NONE', ( #175462 ), #251847, .F. ) ;
#157546=CYLINDRICAL_SURFACE ( 'NONE', #37008, 0.1000000000000028644 ) ;
#157561=CIRCLE ( 'NONE', #195141, 0.09999999999999864553 ) ;
#157571=CARTESIAN_POINT ( 'NONE',  ( 20.85000000000000142, -1.835859311432481045, -145.5044391687985694 ) ) ;
#157588=DIRECTION ( 'NONE',  ( -1.000000000000000000, -3.265361837132813093E-16, 0.000000000000000000 ) ) ;
#157597=FACE_OUTER_BOUND ( 'NONE', #32859, .T. ) ;
#157598=ORIENTED_EDGE ( 'NONE', *, *, #153482, .T. ) ;
#157612=ORIENTED_EDGE ( 'NONE', *, *, #96436, .F. ) ;
#157622=VECTOR ( 'NONE', #129232, 1000.000000000000000 ) ;
#157624=PLANE ( 'NONE',  #168178 ) ;
#157629=( BOUNDED_SURFACE ( )  B_SPLINE_SURFACE ( 3, 2, ( 
 ( #220750, #143767, #182924 ),
 ( #42133, #203756, #62957 ),
 ( #141216, #199922, #219445 ),
 ( #40861, #120404, #162079 ) ),
 .UNSPECIFIED., .F., .F., .F. ) 
 B_SPLINE_SURFACE_WITH_KNOTS ( ( 4, 4 ),
 ( 3, 3 ),
 ( 0.000000000000000000, 0.001979672783031562362 ),
 ( 0.000000000000000000, 1.000000000000000000 ),
 .UNSPECIFIED. ) 
 GEOMETRIC_REPRESENTATION_ITEM ( )  RATIONAL_B_SPLINE_SURFACE ( (
 ( 1.000000000000000000, 0.7103081912008540888, 1.000000000000000000),
 ( 1.000000000000000000, 0.7104998333558795176, 1.000000000000000000),
 ( 1.000000000000000000, 0.7107238315754857982, 1.000000000000000000),
 ( 1.000000000000000000, 0.7110073749539714827, 1.000000000000000000) ) ) 
 REPRESENTATION_ITEM ( '' )  SURFACE ( )  );
#157630=DIRECTION ( 'NONE',  ( 0.000000000000000000, 0.000000000000000000, -1.000000000000000000 ) ) ;
#157700=TOROIDAL_SURFACE ( 'NONE', #245139, 11.89999999999999858, 0.1000000000000000056 ) ;
#157729=CIRCLE ( 'NONE', #57708, 7.900000000000000355 ) ;
#157736=CARTESIAN_POINT ( 'NONE',  ( -20.94999999999999929, 11.75000000001115552, -107.5148057706540357 ) ) ;
#157757=DIRECTION ( 'NONE',  ( 0.000000000000000000, -1.000000000000000000, 2.775557561562888827E-14 ) ) ;
#157764=TOROIDAL_SURFACE ( 'NONE', #20349, 1.900000000000002576, 0.1000000000000000056 ) ;
#157799=ORIENTED_EDGE ( 'NONE', *, *, #212165, .F. ) ;
#157817=CARTESIAN_POINT ( 'NONE',  ( 22.60000000000000142, 11.74956712350054744, -100.3991416309013260 ) ) ;
#157831=EDGE_LOOP ( 'NONE', ( #217396, #142701, #140132, #155081 ) ) ;
#157837=DIRECTION ( 'NONE',  ( 0.000000000000000000, 0.000000000000000000, -1.000000000000000000 ) ) ;
#157874=ORIENTED_EDGE ( 'NONE', *, *, #64441, .F. ) ;
#157888=VERTEX_POINT ( 'NONE', #133445 ) ;
#157934=VERTEX_POINT ( 'NONE', #84844 ) ;
#157946=ORIENTED_EDGE ( 'NONE', *, *, #15655, .F. ) ;
#157947=ADVANCED_FACE ( 'NONE', ( #203550 ), #243952, .T. ) ;
#157980=ORIENTED_EDGE ( 'NONE', *, *, #189391, .T. ) ;
#158000=AXIS2_PLACEMENT_3D ( 'NONE', #184581, #86749, #248417 ) ;
#158040=DIRECTION ( 'NONE',  ( -1.000000000000000000, 0.000000000000000000, 0.000000000000000000 ) ) ;
#158052=VECTOR ( 'NONE', #189422, 1000.000000000000000 ) ;
#158069=EDGE_CURVE ( 'NONE', #104851, #37861, #39687, .T. ) ;
#158077=EDGE_LOOP ( 'NONE', ( #4812, #140868, #165846, #206961 ) ) ;
#158086=AXIS2_PLACEMENT_3D ( 'NONE', #18793, #98298, #17508 ) ;
#158121=EDGE_CURVE ( 'NONE', #9426, #253084, #73305, .T. ) ;
#158125=LINE ( 'NONE', #237622, #31729 ) ;
#158141=CARTESIAN_POINT ( 'NONE',  ( -18.50000972452446035, 10.29326151435326508, -139.4592822510415431 ) ) ;
#158162=SPHERICAL_SURFACE ( 'NONE', #112248, 0.1000000000000000056 ) ;
#158163=CIRCLE ( 'NONE', #78963, 0.1000000000000000472 ) ;
#158252=ORIENTED_EDGE ( 'NONE', *, *, #137583, .F. ) ;
#158280=ORIENTED_EDGE ( 'NONE', *, *, #110199, .F. ) ;
#158291=CARTESIAN_POINT ( 'NONE',  ( 23.24999999999999289, 11.75000000001116263, -88.75000000000004263 ) ) ;
#158309=CARTESIAN_POINT ( 'NONE',  ( 20.94999999999999929, -8.730841121484171907, -110.0980747189843640 ) ) ;
#158311=LINE ( 'NONE', #18755, #102774 ) ;
#158321=EDGE_CURVE ( 'NONE', #193662, #192673, #152300, .T. ) ;
#158358=ADVANCED_FACE ( 'NONE', ( #101750 ), #222988, .T. ) ;
#158361=CARTESIAN_POINT ( 'NONE',  ( 21.11825140030092030, 0.007203620643717282591, -94.05459243457964646 ) ) ;
#158370=AXIS2_PLACEMENT_3D ( 'NONE', #88095, #242060, #127258 ) ;
#158371=EDGE_CURVE ( 'NONE', #231172, #188954, #123055, .T. ) ;
#158403=CARTESIAN_POINT ( 'NONE',  ( -18.59999999999999787, 1.115600667400684642E-11, -141.9000000000000341 ) ) ;
#158416=DIRECTION ( 'NONE',  ( 1.000000000000000000, 0.000000000000000000, -0.000000000000000000 ) ) ;
#158421=CARTESIAN_POINT ( 'NONE',  ( -21.05000000000000071, 1.115600667400684642E-11, -104.7999999999999972 ) ) ;
#158437=ORIENTED_EDGE ( 'NONE', *, *, #94026, .F. ) ;
#158451=DIRECTION ( 'NONE',  ( 0.000000000000000000, 1.000000000000000000, 0.000000000000000000 ) ) ;
#158478=DIRECTION ( 'NONE',  ( 2.952720810173289112E-16, -1.000000000000000000, -0.000000000000000000 ) ) ;
#158516=AXIS2_PLACEMENT_3D ( 'NONE', #11917, #211383, #168455 ) ;
#158538=DIRECTION ( 'NONE',  ( 1.000000000000000000, 0.000000000000000000, 0.000000000000000000 ) ) ;
#158554=EDGE_CURVE ( 'NONE', #75372, #110439, #235645, .T. ) ;
#158559=CARTESIAN_POINT ( 'NONE',  ( 21.05000000000001492, 6.540656951712398914, -100.5000000000000426 ) ) ;
#158580=ORIENTED_EDGE ( 'NONE', *, *, #136041, .T. ) ;
#158605=DIRECTION ( 'NONE',  ( 0.000000000000000000, 0.8700118002898321601, -0.4930308989875230030 ) ) ;
#158613=ORIENTED_EDGE ( 'NONE', *, *, #119823, .T. ) ;
#158634=FACE_OUTER_BOUND ( 'NONE', #75565, .T. ) ;
#158638=CARTESIAN_POINT ( 'NONE',  ( -21.55000000000000071, 7.350000000011155166, -112.7500000000000284 ) ) ;
#158672=EDGE_CURVE ( 'NONE', #225371, #88314, #227447, .T. ) ;
#158710=DIRECTION ( 'NONE',  ( 0.000000000000000000, 0.000000000000000000, -1.000000000000000000 ) ) ;
#158751=VECTOR ( 'NONE', #179253, 1000.000000000000114 ) ;
#158772=EDGE_CURVE ( 'NONE', #157934, #240710, #63533, .T. ) ;
#158788=CARTESIAN_POINT ( 'NONE',  ( -18.50000000000000711, 11.75000000001115197, -107.5148057706540357 ) ) ;
#158804=CARTESIAN_POINT ( 'NONE',  ( -23.25000000000000000, -0.1008583690875562017, -88.75043287651064361 ) ) ;
#158815=DIRECTION ( 'NONE',  ( 1.000000000000000000, -0.000000000000000000, -0.000000000000000000 ) ) ;
#158842=LINE ( 'NONE', #141808, #71263 ) ;
#158846=DIRECTION ( 'NONE',  ( 0.000000000000000000, -0.8660254037844383745, 0.5000000000000003331 ) ) ;
#158851=FACE_OUTER_BOUND ( 'NONE', #186729, .T. ) ;
#158855=ORIENTED_EDGE ( 'NONE', *, *, #15751, .F. ) ;
#158867=EDGE_CURVE ( 'NONE', #34960, #237722, #214982, .T. ) ;
#158882=ADVANCED_FACE ( 'NONE', ( #209564 ), #212143, .F. ) ;
#158896=EDGE_LOOP ( 'NONE', ( #19938, #114983, #235260 ) ) ;
#158938=DIRECTION ( 'NONE',  ( 1.000000000000000000, -0.000000000000000000, -0.000000000000000000 ) ) ;
#158956=DIRECTION ( 'NONE',  ( 0.000000000000000000, -1.000000000000000000, -1.734723475976807292E-15 ) ) ;
#158966=ADVANCED_FACE ( 'NONE', ( #154745 ), #217237, .F. ) ;
#158967=EDGE_CURVE ( 'NONE', #172421, #35530, #136031, .T. ) ;
#159031=CARTESIAN_POINT ( 'NONE',  ( 21.14999999999999858, 11.75000000001116263, -100.6000000000000369 ) ) ;
#159035=CARTESIAN_POINT ( 'NONE',  ( -21.07928932188134041, 0.09889514566555068775, -94.17148334360673800 ) ) ;
#159038=CARTESIAN_POINT ( 'NONE',  ( 22.48660254037844197, 11.65000000001116298, -100.4500000000000455 ) ) ;
#159046=CIRCLE ( 'NONE', #753, 0.5000000000000004441 ) ;
#159063=LINE ( 'NONE', #42944, #246653 ) ;
#159072=CARTESIAN_POINT ( 'NONE',  ( 18.52928932188133970, 10.27928932189250055, -125.1500000000000341 ) ) ;
#159103=ORIENTED_EDGE ( 'NONE', *, *, #23974, .F. ) ;
#159141=AXIS2_PLACEMENT_3D ( 'NONE', #43545, #21431, #42258 ) ;
#159153=EDGE_CURVE ( 'NONE', #66665, #96344, #237674, .T. ) ;
#159159=CARTESIAN_POINT ( 'NONE',  ( -22.50000000000088463, 0.04536165659886851748, -88.84949116579235806 ) ) ;
#159173=TOROIDAL_SURFACE ( 'NONE', #217378, 11.65000000000000036, 0.1000000000000000056 ) ;
#159198=DIRECTION ( 'NONE',  ( 1.836970198721029934E-16, -1.000000000000000000, -0.000000000000000000 ) ) ;
#159199=EDGE_CURVE ( 'NONE', #172696, #112449, #94352, .T. ) ;
#159205=FACE_OUTER_BOUND ( 'NONE', #211908, .T. ) ;
#159225=DIRECTION ( 'NONE',  ( 0.000000000000000000, -1.000000000000000000, 0.000000000000000000 ) ) ;
#159226=DIRECTION ( 'NONE',  ( 0.000000000000000000, 0.1298341882520022694, 0.9915357197604852679 ) ) ;
#159229=CARTESIAN_POINT ( 'NONE',  ( 20.85000000000000142, 11.65000000001115943, -127.2161343370219413 ) ) ;
#159290=DIRECTION ( 'NONE',  ( 0.000000000000000000, 0.01562500000001045344, 0.9998779222360096863 ) ) ;
#159298=CIRCLE ( 'NONE', #13542, 4.150000000000001243 ) ;
#159300=EDGE_CURVE ( 'NONE', #213068, #83513, #219427, .T. ) ;
#159306=VERTEX_POINT ( 'NONE', #202530 ) ;
#159326=VECTOR ( 'NONE', #188212, 1000.000000000000000 ) ;
#159351=ORIENTED_EDGE ( 'NONE', *, *, #64909, .F. ) ;
#159362=CARTESIAN_POINT ( 'NONE',  ( 20.85000000000000142, -0.3238857010591806307, -133.9575895893140398 ) ) ;
#159387=DIRECTION ( 'NONE',  ( 0.000000000000000000, 0.000000000000000000, -1.000000000000000000 ) ) ;
#159437=AXIS2_PLACEMENT_3D ( 'NONE', #173864, #254601, #238924 ) ;
#159467=CIRCLE ( 'NONE', #242843, 0.09999999999999939493 ) ;
#159474=CIRCLE ( 'NONE', #5310, 0.1000000000000028644 ) ;
#159475=DIRECTION ( 'NONE',  ( 1.000000000000000000, -0.000000000000000000, -0.000000000000000000 ) ) ;
#159507=ORIENTED_EDGE ( 'NONE', *, *, #193021, .T. ) ;
#159537=ORIENTED_EDGE ( 'NONE', *, *, #149762, .F. ) ;
#159553=EDGE_CURVE ( 'NONE', #190980, #111426, #218885, .T. ) ;
#159563=LINE ( 'NONE', #239097, #120310 ) ;
#159565=CARTESIAN_POINT ( 'NONE',  ( 18.59999999999999076, -1.249999999988843369, -108.5000000000000284 ) ) ;
#159566=DIRECTION ( 'NONE',  ( 1.000000000000000000, 0.000000000000000000, 0.000000000000000000 ) ) ;
#159613=CARTESIAN_POINT ( 'NONE',  ( 21.14999999999999858, 1.115486826172573664E-11, -93.95934304829877703 ) ) ;
#159623=TOROIDAL_SURFACE ( 'NONE', #80464, 11.65000000000000036, 0.1000000000000000056 ) ;
#159639=CYLINDRICAL_SURFACE ( 'NONE', #153225, 0.09999999999999939493 ) ;
#159648=DIRECTION ( 'NONE',  ( 1.000000000000000000, -0.000000000000000000, -0.000000000000000000 ) ) ;
#159671=AXIS2_PLACEMENT_3D ( 'NONE', #66697, #186655, #49694 ) ;
#159674=VERTEX_POINT ( 'NONE', #97643 ) ;
#159677=FACE_OUTER_BOUND ( 'NONE', #107472, .T. ) ;
#159693=CARTESIAN_POINT ( 'NONE',  ( -22.39999999999999858, -0.1008583690875579364, -88.75043287651064361 ) ) ;
#159714=VERTEX_POINT ( 'NONE', #75572 ) ;
#159732=TOROIDAL_SURFACE ( 'NONE', #176491, 0.6000000000000009770, 0.1000000000000000056 ) ;
#159735=LINE ( 'NONE', #254911, #60313 ) ;
#159742=EDGE_CURVE ( 'NONE', #256826, #245711, #105330, .T. ) ;
#159818=ORIENTED_EDGE ( 'NONE', *, *, #106455, .T. ) ;
#159835=CARTESIAN_POINT ( 'NONE',  ( 21.04999999999976978, 6.441084688482524356, -100.5177194333089119 ) ) ;
#159839=LINE ( 'NONE', #181961, #34695 ) ;
#159866=ORIENTED_EDGE ( 'NONE', *, *, #81399, .T. ) ;
#159878=DIRECTION ( 'NONE',  ( 0.000000000000000000, 1.776356839400254803E-15, 1.000000000000000000 ) ) ;
#159894=CARTESIAN_POINT ( 'NONE',  ( -20.00857864376270001, 9.250000000011157297, -112.8500000000000369 ) ) ;
#159935=ORIENTED_EDGE ( 'NONE', *, *, #255603, .F. ) ;
#159959=CARTESIAN_POINT ( 'NONE',  ( -21.05000000000000071, 1.116121084443477685E-11, -103.4000000000000199 ) ) ;
#159976=B_SPLINE_CURVE_WITH_KNOTS ( 'NONE', 3,
 ( #54138, #234060, #39753, #55393, #119273, #198785, #93267, #41029 ),
 .UNSPECIFIED., .F., .F.,
 ( 4, 2, 2, 4 ),
 ( 0.000000000000000000, 0.0001881495939909276559, 0.0002822243909863914567, 0.0003762991879818553117 ),
 .UNSPECIFIED. ) ;
#160042=DIRECTION ( 'NONE',  ( 0.000000000000000000, 0.000000000000000000, -1.000000000000000000 ) ) ;
#160059=VECTOR ( 'NONE', #17326, 1000.000000000000000 ) ;
#160071=EDGE_LOOP ( 'NONE', ( #122462, #219876, #92624, #253104 ) ) ;
#160076=VECTOR ( 'NONE', #76592, 1000.000000000000000 ) ;
#160079=CYLINDRICAL_SURFACE ( 'NONE', #103091, 0.09999999999999939493 ) ;
#160080=UNCERTAINTY_MEASURE_WITH_UNIT (LENGTH_MEASURE( 1.000000000000000082E-05 ), #208057, 'distance_accuracy_value', 'NONE');
#160095=ORIENTED_EDGE ( 'NONE', *, *, #227842, .T. ) ;
#160102=CYLINDRICAL_SURFACE ( 'NONE', #243456, 0.09999999999999939493 ) ;
#160123=CARTESIAN_POINT ( 'NONE',  ( 20.94999999999999929, 6.650000000011155876, -121.7500000000000426 ) ) ;
#160126=ORIENTED_EDGE ( 'NONE', *, *, #169361, .F. ) ;
#160161=CARTESIAN_POINT ( 'NONE',  ( -18.46919391072055561, -9.670724388266535243, -140.6738035317996491 ) ) ;
#160208=VERTEX_POINT ( 'NONE', #170228 ) ;
#160227=DIRECTION ( 'NONE',  ( 1.000000000000000000, 0.000000000000000000, 0.000000000000000000 ) ) ;
#160255=DIRECTION ( 'NONE',  ( 0.000000000000000000, 0.000000000000000000, -1.000000000000000000 ) ) ;
#160259=DIRECTION ( 'NONE',  ( 0.000000000000000000, 0.000000000000000000, -1.000000000000000000 ) ) ;
#160299=LINE ( 'NONE', #243654, #123550 ) ;
#160301=CARTESIAN_POINT ( 'NONE',  ( -18.39999999999999858, -9.399999999988850163, -88.75000000000004263 ) ) ;
#160363=CARTESIAN_POINT ( 'NONE',  ( 18.49999999999999289, 10.20857864377384416, -125.1500000000000341 ) ) ;
#160379=EDGE_CURVE ( 'NONE', #236931, #100676, #28316, .T. ) ;
#160402=CARTESIAN_POINT ( 'NONE',  ( -20.54999999999999716, 7.250000000011155521, -121.7500000000000426 ) ) ;
#160408=VERTEX_POINT ( 'NONE', #102151 ) ;
#160425=EDGE_CURVE ( 'NONE', #6219, #185072, #184285, .T. ) ;
#160430=ORIENTED_EDGE ( 'NONE', *, *, #169526, .T. ) ;
#160432=AXIS2_PLACEMENT_3D ( 'NONE', #21651, #122027, #221114 ) ;
#160454=DIRECTION ( 'NONE',  ( 0.000000000000000000, 1.000000000000000000, -6.308085367188393199E-16 ) ) ;
#160463=ORIENTED_EDGE ( 'NONE', *, *, #127451, .T. ) ;
#160481=EDGE_CURVE ( 'NONE', #43391, #97776, #169918, .T. ) ;
#160502=ORIENTED_EDGE ( 'NONE', *, *, #232448, .F. ) ;
#160517=DIRECTION ( 'NONE',  ( 0.000000000000000000, 0.9915357197604971473, -0.1298341882519111479 ) ) ;
#160564=LINE ( 'NONE', #237516, #20510 ) ;
#160574=EDGE_CURVE ( 'NONE', #109956, #53442, #12105, .T. ) ;
#160582=( BOUNDED_SURFACE ( )  B_SPLINE_SURFACE ( 3, 2, ( 
 ( #118717, #95280, #113561 ),
 ( #97815, #253062, #193110 ),
 ( #177420, #58697, #19610 ),
 ( #21, #152725, #14489 ),
 ( #5131, #122564, #40485 ),
 ( #63858, #65130, #43020 ) ),
 .UNSPECIFIED., .F., .F., .F. ) 
 B_SPLINE_SURFACE_WITH_KNOTS ( ( 4, 2, 4 ),
 ( 3, 3 ),
 ( 0.0001381104793128061785, 0.0002947094729387751515, 0.0004513084665647441244 ),
 ( 0.000000000000000000, 1.000000000000000000 ),
 .UNSPECIFIED. ) 
 GEOMETRIC_REPRESENTATION_ITEM ( )  RATIONAL_B_SPLINE_SURFACE ( (
 ( 1.000000000000000000, 0.7071067811865966446, 1.000000000000000000),
 ( 1.000000000000000000, 0.6919563088098851233, 1.000000000000000000),
 ( 1.000000000000000000, 0.6959445945717438464, 1.000000000000000000),
 ( 1.000000000000000000, 0.7137882985313120932, 1.000000000000000000),
 ( 1.000000000000000000, 0.7257496306096493655, 1.000000000000000000),
 ( 1.000000000000000000, 0.7250110520819876836, 1.000000000000000000) ) ) 
 REPRESENTATION_ITEM ( '' )  SURFACE ( )  );
#160590=ORIENTED_EDGE ( 'NONE', *, *, #27317, .T. ) ;
#160599=CARTESIAN_POINT ( 'NONE',  ( -21.04999999999989768, 0.01485563490472031727, -94.15564095795694755 ) ) ;
#160634=CARTESIAN_POINT ( 'NONE',  ( -21.05000000000000071, -1.835341550213255957, -112.0551512925630107 ) ) ;
#160665=CARTESIAN_POINT ( 'NONE',  ( -20.85000000000000142, -11.64999999998884306, -134.0000000000000284 ) ) ;
#160675=VECTOR ( 'NONE', #229269, 999.9999999999998863 ) ;
#160687=EDGE_CURVE ( 'NONE', #23430, #211300, #61784, .T. ) ;
#160693=CARTESIAN_POINT ( 'NONE',  ( -18.50000000000000000, 7.120270961708746960, -137.6595630418393625 ) ) ;
#160705=CIRCLE ( 'NONE', #156425, 4.049999999999998046 ) ;
#160750=DIRECTION ( 'NONE',  ( 0.000000000000000000, 1.000000000000000000, 1.224646799147353207E-16 ) ) ;
#160807=CARTESIAN_POINT ( 'NONE',  ( 22.45380639572243453, 1.426819239903859335E-07, -88.74956710889316014 ) ) ;
#160857=CARTESIAN_POINT ( 'NONE',  ( 21.14999999999999858, 6.540656951712400691, -100.5000000000000284 ) ) ;
#160864=EDGE_CURVE ( 'NONE', #120254, #142271, #86881, .T. ) ;
#160905=DIRECTION ( 'NONE',  ( 1.000000000000000000, -0.000000000000000000, -0.000000000000000000 ) ) ;
#160908=ORIENTED_EDGE ( 'NONE', *, *, #4953, .F. ) ;
#160909=ORIENTED_EDGE ( 'NONE', *, *, #213307, .F. ) ;
#160920=AXIS2_PLACEMENT_3D ( 'NONE', #237471, #199649, #82206 ) ;
#160955=CARTESIAN_POINT ( 'NONE',  ( 20.94999999999999929, -11.64999999998883595, -131.0000000000000284 ) ) ;
#160979=CARTESIAN_POINT ( 'NONE',  ( 23.15000000000000213, -8.999999999988842703, -124.1060308773475924 ) ) ;
#160985=ORIENTED_EDGE ( 'NONE', *, *, #22381, .F. ) ;
#160993=CARTESIAN_POINT ( 'NONE',  ( -21.14999999999999858, -0.09999999998884338825, -93.95934304829879125 ) ) ;
#161038=ORIENTED_EDGE ( 'NONE', *, *, #246478, .T. ) ;
#161039=( GEOMETRIC_REPRESENTATION_CONTEXT ( 3 ) GLOBAL_UNCERTAINTY_ASSIGNED_CONTEXT ( ( #89489 ) ) GLOBAL_UNIT_ASSIGNED_CONTEXT ( ( #53275, #55795, #151095 ) ) REPRESENTATION_CONTEXT ( 'NONE', 'WORKASPACE' ) );
#161062=AXIS2_PLACEMENT_3D ( 'NONE', #98248, #218209, #154454 ) ;
#161088=CIRCLE ( 'NONE', #256890, 0.09999999999999824307 ) ;
#161097=CARTESIAN_POINT ( 'NONE',  ( -21.40925344232282512, 6.658518859401606704, -100.4010498113803891 ) ) ;
#161102=CARTESIAN_POINT ( 'NONE',  ( -23.25000000000000000, 2.000000000011154189, -113.7246219227621395 ) ) ;
#161109=CIRCLE ( 'NONE', #40349, 0.09999999999999939493 ) ;
#161114=CARTESIAN_POINT ( 'NONE',  ( 21.13422380239052245, 6.493326514816728512, -100.5000000000000426 ) ) ;
#161119=CARTESIAN_POINT ( 'NONE',  ( 18.59999999999999076, 6.550000000011156231, -121.7500000000000426 ) ) ;
#161126=ORIENTED_EDGE ( 'NONE', *, *, #28625, .T. ) ;
#161135=CIRCLE ( 'NONE', #48685, 0.09999999999998898659 ) ;
#161136=AXIS2_PLACEMENT_3D ( 'NONE', #31692, #126910, #70813 ) ;
#161157=CARTESIAN_POINT ( 'NONE',  ( 23.24999999999999289, 11.65000000001116298, -88.75000000000004263 ) ) ;
#161161=ADVANCED_FACE ( 'NONE', ( #237249 ), #132720, .F. ) ;
#161162=DIRECTION ( 'NONE',  ( 0.000000000000000000, 0.000000000000000000, 1.000000000000000000 ) ) ;
#161165=VERTEX_POINT ( 'NONE', #65983 ) ;
#161182=CARTESIAN_POINT ( 'NONE',  ( 19.83283456528358002, 11.75000000001116263, -125.3499999994178182 ) ) ;
#161185=DIRECTION ( 'NONE',  ( 0.000000000000000000, 0.000000000000000000, -1.000000000000000000 ) ) ;
#161190=DIRECTION ( 'NONE',  ( -1.000000000000000000, -0.000000000000000000, -0.000000000000000000 ) ) ;
#161197=CYLINDRICAL_SURFACE ( 'NONE', #101532, 0.09999999999999939493 ) ;
#161242=AXIS2_PLACEMENT_3D ( 'NONE', #134545, #130705, #169893 ) ;
#161251=EDGE_CURVE ( 'NONE', #155284, #257108, #12112, .T. ) ;
#161271=EDGE_CURVE ( 'NONE', #211300, #232157, #28883, .T. ) ;
#161309=DIRECTION ( 'NONE',  ( 0.000000000000000000, 1.000000000000000000, 0.000000000000000000 ) ) ;
#161324=ADVANCED_FACE ( 'NONE', ( #51519 ), #62160, .F. ) ;
#161341=EDGE_CURVE ( 'NONE', #81511, #92883, #199552, .T. ) ;
#161344=AXIS2_PLACEMENT_3D ( 'NONE', #227099, #49757, #225800 ) ;
#161349=EDGE_CURVE ( 'NONE', #251571, #164116, #236592, .T. ) ;
#161367=CARTESIAN_POINT ( 'NONE',  ( -23.15000000000000213, 11.75000000001115552, -100.5000000000000284 ) ) ;
#161368=CARTESIAN_POINT ( 'NONE',  ( 20.95289811251229750, 8.893168004469750088, -109.0018094939185431 ) ) ;
#161397=DIRECTION ( 'NONE',  ( 0.000000000000000000, -1.000000000000000000, 0.000000000000000000 ) ) ;
#161457=CARTESIAN_POINT ( 'NONE',  ( -20.94999999999999929, 11.60000000001115161, -107.4282032302755852 ) ) ;
#161459=EDGE_CURVE ( 'NONE', #17513, #95681, #256103, .T. ) ;
#161462=EDGE_LOOP ( 'NONE', ( #64972, #104695, #136765, #244277 ) ) ;
#161466=AXIS2_PLACEMENT_3D ( 'NONE', #40361, #125001, #119882 ) ;
#161551=DIRECTION ( 'NONE',  ( 1.000000000000000000, 0.000000000000000000, -0.000000000000000000 ) ) ;
#161555=CARTESIAN_POINT ( 'NONE',  ( -22.50000000000000000, 11.64957080755595520, -100.4000000000000483 ) ) ;
#161569=LINE ( 'NONE', #221496, #238237 ) ;
#161602=EDGE_CURVE ( 'NONE', #164082, #21483, #115938, .T. ) ;
#161605=CARTESIAN_POINT ( 'NONE',  ( -20.85000000000000142, 1.115600667400684642E-11, -134.0000000000000284 ) ) ;
#161640=CARTESIAN_POINT ( 'NONE',  ( 18.53691006697058796, 10.30215155716188669, -125.2021987172991260 ) ) ;
#161685=DIRECTION ( 'NONE',  ( 0.000000000000000000, -1.000000000000000000, 0.000000000000000000 ) ) ;
#161693=CARTESIAN_POINT ( 'NONE',  ( 20.94999999999999574, -1.162701749926853712, -108.6000000000000227 ) ) ;
#161705=ORIENTED_EDGE ( 'NONE', *, *, #14697, .F. ) ;
#161723=VECTOR ( 'NONE', #100918, 1000.000000000000114 ) ;
#161734=( BOUNDED_SURFACE ( )  B_SPLINE_SURFACE ( 3, 2, ( 
 ( #101157, #240729, #201586 ),
 ( #22992, #102457, #3375 ),
 ( #82893, #63353, #243272 ),
 ( #222406, #45089, #124633 ),
 ( #204145, #192310, #73668 ),
 ( #250974, #128480, #132322 ),
 ( #129758, #108906, #252261 ),
 ( #13666, #131040, #172785 ),
 ( #68510, #52772, #211885 ),
 ( #210583, #171491, #31970 ),
 ( #51475, #12406, #208035 ),
 ( #247126, #8533, #90616 ) ),
 .UNSPECIFIED., .F., .F., .T. ) 
 B_SPLINE_SURFACE_WITH_KNOTS ( ( 4, 2, 2, 2, 2, 4 ),
 ( 3, 3 ),
 ( 3.174653483277205090, 3.943930578431714018, 4.713207673586222946, 5.482484768740731873, 5.867123316317986337, 6.251761863895240801 ),
 ( 0.000000000000000000, 1.000000000000000000 ),
 .UNSPECIFIED. ) 
 GEOMETRIC_REPRESENTATION_ITEM ( )  RATIONAL_B_SPLINE_SURFACE ( (
 ( 1.000000000000000000, 0.8659465255642401216, 1.000000000000000000),
 ( 1.000000000000000000, 0.8648614068469322458, 1.000000000000000000),
 ( 1.000000000000000000, 0.8489031841349031771, 1.000000000000000000),
 ( 1.000000000000000000, 0.7927507630136544359, 1.000000000000000000),
 ( 1.000000000000000000, 0.7523013858965486023, 1.000000000000000000),
 ( 1.000000000000000000, 0.6616226951240427034, 1.000000000000000000),
 ( 1.000000000000000000, 0.6112214368649029339, 1.000000000000000000),
 ( 1.000000000000000000, 0.5507684314535757908, 1.000000000000000000),
 ( 1.000000000000000000, 0.5333267243109209854, 1.000000000000000000),
 ( 1.000000000000000000, 0.5084565446523154897, 1.000000000000000000),
 ( 1.000000000000000000, 0.5010722703418952761, 1.000000000000000000),
 ( 1.000000000000000000, 0.5001234037138393429, 1.000000000000000000) ) ) 
 REPRESENTATION_ITEM ( '' )  SURFACE ( )  );
#161760=FACE_OUTER_BOUND ( 'NONE', #35570, .T. ) ;
#161778=ADVANCED_FACE ( 'NONE', ( #246288 ), #120065, .F. ) ;
#161804=DIRECTION ( 'NONE',  ( 0.000000000000000000, 1.897661533703519897E-16, -1.000000000000000000 ) ) ;
#161813=ORIENTED_EDGE ( 'NONE', *, *, #159153, .F. ) ;
#161817=ADVANCED_FACE ( 'NONE', ( #251415 ), #213117, .F. ) ;
#161825=CARTESIAN_POINT ( 'NONE',  ( 18.50000000000000355, -9.421456145484059519, -107.7419820840196252 ) ) ;
#161835=VERTEX_POINT ( 'NONE', #74099 ) ;
#161863=CARTESIAN_POINT ( 'NONE',  ( 21.97500000000000497, 9.750000000011153745, -121.7500000000000426 ) ) ;
#161873=CARTESIAN_POINT ( 'NONE',  ( 21.05000000000000071, -11.29603075032412995, -103.5478991596638991 ) ) ;
#161877=CARTESIAN_POINT ( 'NONE',  ( -21.05000000000000071, 1.115526128501326264E-11, -93.95934304829879125 ) ) ;
#161909=ADVANCED_FACE ( 'NONE', ( #60903, #136583 ), #38794, .T. ) ;
#161915=ORIENTED_EDGE ( 'NONE', *, *, #100580, .T. ) ;
#161943=DIRECTION ( 'NONE',  ( 1.000000000000000000, -0.000000000000000000, -0.000000000000000000 ) ) ;
#161960=ORIENTED_EDGE ( 'NONE', *, *, #2633, .T. ) ;
#161974=ORIENTED_EDGE ( 'NONE', *, *, #22865, .T. ) ;
#161975=EDGE_CURVE ( 'NONE', #205348, #110564, #19222, .T. ) ;
#161979=VECTOR ( 'NONE', #130404, 1000.000000000000000 ) ;
#162015=EDGE_LOOP ( 'NONE', ( #114193, #168867, #117564, #169721 ) ) ;
#162049=EDGE_CURVE ( 'NONE', #21483, #33839, #20269, .T. ) ;
#162050=LINE ( 'NONE', #62929, #84897 ) ;
#162071=VERTEX_POINT ( 'NONE', #102574 ) ;
#162079=CARTESIAN_POINT ( 'NONE',  ( -21.00023020733502932, 1.115542391533913547E-11, -94.10913075473168021 ) ) ;
#162091=CIRCLE ( 'NONE', #182935, 0.5000000000000004441 ) ;
#162092=ORIENTED_EDGE ( 'NONE', *, *, #15054, .T. ) ;
#162120=EDGE_LOOP ( 'NONE', ( #132036, #213097, #34880, #115658 ) ) ;
#162144=DIRECTION ( 'NONE',  ( 0.000000000000000000, -1.000000000000000000, 0.000000000000000000 ) ) ;
#162158=DIRECTION ( 'NONE',  ( -6.938893903907209445E-14, -0.9999176327611370985, -0.01283462868040260302 ) ) ;
#162170=DIRECTION ( 'NONE',  ( 0.000000000000000000, 0.000000000000000000, -1.000000000000000000 ) ) ;
#162190=CIRCLE ( 'NONE', #49740, 0.09999999999999939493 ) ;
#162219=DIRECTION ( 'NONE',  ( 0.000000000000000000, -0.1298341882520124002, -0.9915357197604841577 ) ) ;
#162242=EDGE_CURVE ( 'NONE', #50377, #217495, #253475, .T. ) ;
#162249=CIRCLE ( 'NONE', #124819, 0.09999999999999939493 ) ;
#162274=ADVANCED_FACE ( 'NONE', ( #134982 ), #153333, .T. ) ;
#162311=CIRCLE ( 'NONE', #128988, 0.09999999999999917288 ) ;
#162338=VERTEX_POINT ( 'NONE', #108411 ) ;
#162339=CARTESIAN_POINT ( 'NONE',  ( 21.04386569057559697, 11.75000000001105427, -127.1428373517806563 ) ) ;
#162368=VECTOR ( 'NONE', #23672, 1000.000000000000000 ) ;
#162405=CIRCLE ( 'NONE', #25052, 0.2000000000000057288 ) ;
#162419=ORIENTED_EDGE ( 'NONE', *, *, #4399, .F. ) ;
#162508=ORIENTED_EDGE ( 'NONE', *, *, #231633, .T. ) ;
#162528=DIRECTION ( 'NONE',  ( 0.000000000000000000, -1.000000000000000000, 0.000000000000000000 ) ) ;
#162536=DIRECTION ( 'NONE',  ( -4.448008912761043807E-16, 1.000000000000000000, 0.000000000000000000 ) ) ;
#162537=ORIENTED_EDGE ( 'NONE', *, *, #193929, .T. ) ;
#162601=CARTESIAN_POINT ( 'NONE',  ( 21.00023020733502932, 1.115541036281197940E-11, -94.10913075473168021 ) ) ;
#162633=DIRECTION ( 'NONE',  ( -1.000000000000000000, 0.000000000000000000, 0.000000000000000000 ) ) ;
#162639=DIRECTION ( 'NONE',  ( 1.000000000000000000, 0.000000000000000000, 0.000000000000000000 ) ) ;
#162673=ORIENTED_EDGE ( 'NONE', *, *, #180931, .F. ) ;
#162687=VERTEX_POINT ( 'NONE', #217747 ) ;
#162690=AXIS2_PLACEMENT_3D ( 'NONE', #169977, #112538, #175119 ) ;
#162745=ORIENTED_EDGE ( 'NONE', *, *, #193242, .T. ) ;
#162756=AXIS2_PLACEMENT_3D ( 'NONE', #77796, #256386, #119528 ) ;
#162775=ORIENTED_EDGE ( 'NONE', *, *, #95046, .T. ) ;
#162783=ORIENTED_EDGE ( 'NONE', *, *, #243650, .T. ) ;
#162792=CARTESIAN_POINT ( 'NONE',  ( -23.15000000000000213, 1.115600667400684642E-11, -100.5000000000000284 ) ) ;
#162796=AXIS2_PLACEMENT_3D ( 'NONE', #22060, #141980, #198110 ) ;
#162827=EDGE_CURVE ( 'NONE', #37616, #224306, #178884, .T. ) ;
#162834=DIRECTION ( 'NONE',  ( 0.000000000000000000, 0.000000000000000000, -1.000000000000000000 ) ) ;
#162892=FACE_OUTER_BOUND ( 'NONE', #203676, .T. ) ;
#162932=CARTESIAN_POINT ( 'NONE',  ( -20.54999999999999716, -11.74999999998884448, -117.2500000000000284 ) ) ;
#162987=CARTESIAN_POINT ( 'NONE',  ( 23.14999999999998437, 11.75000000001115552, -100.5000000000000284 ) ) ;
#163018=VERTEX_POINT ( 'NONE', #72851 ) ;
#163036=VERTEX_POINT ( 'NONE', #188918 ) ;
#163059=ORIENTED_EDGE ( 'NONE', *, *, #152818, .T. ) ;
#163082=ORIENTED_EDGE ( 'NONE', *, *, #180474, .T. ) ;
#163100=CARTESIAN_POINT ( 'NONE',  ( 18.58703555224997928, -9.406336740777952343, -107.6249446412463726 ) ) ;
#163116=ORIENTED_EDGE ( 'NONE', *, *, #166898, .T. ) ;
#163125=FACE_OUTER_BOUND ( 'NONE', #110493, .T. ) ;
#163135=ORIENTED_EDGE ( 'NONE', *, *, #250813, .T. ) ;
#163139=DIRECTION ( 'NONE',  ( 1.000000000000000000, 0.000000000000000000, 0.000000000000000000 ) ) ;
#163148=VERTEX_POINT ( 'NONE', #19258 ) ;
#163153=DIRECTION ( 'NONE',  ( -1.000000000000000000, 0.000000000000000000, -0.000000000000000000 ) ) ;
#163159=LINE ( 'NONE', #223107, #240336 ) ;
#163160=CARTESIAN_POINT ( 'NONE',  ( -20.05000000000000426, 9.250000000011157297, -121.7500000000000426 ) ) ;
#163170=CARTESIAN_POINT ( 'NONE',  ( 20.04142135623730070, 11.65000000001115943, -121.7500000000000426 ) ) ;
#163178=CARTESIAN_POINT ( 'NONE',  ( 22.37643362114956247, 7.625789993969535274, -100.4009186263186564 ) ) ;
#163179=DIRECTION ( 'NONE',  ( 1.000000000000000000, -0.000000000000000000, -0.000000000000000000 ) ) ;
#163183=CARTESIAN_POINT ( 'NONE',  ( 23.14999999999999503, 11.65000000001116298, -112.6500000000000341 ) ) ;
#163196=AXIS2_PLACEMENT_3D ( 'NONE', #32670, #53473, #96424 ) ;
#163222=CIRCLE ( 'NONE', #188163, 0.2000000000000057288 ) ;
#163236=CARTESIAN_POINT ( 'NONE',  ( 23.24999999999999289, 11.65000000001116298, -88.75000000000004263 ) ) ;
#163256=VERTEX_POINT ( 'NONE', #106464 ) ;
#163257=ADVANCED_FACE ( 'NONE', ( #240883 ), #7388, .F. ) ;
#163265=CARTESIAN_POINT ( 'NONE',  ( 22.59999999999999787, 11.64957080755595520, -100.4000000000000483 ) ) ;
#163330=DIRECTION ( 'NONE',  ( -1.000000000000000000, -0.000000000000000000, -0.000000000000000000 ) ) ;
#163337=AXIS2_PLACEMENT_3D ( 'NONE', #112556, #193385, #74743 ) ;
#163354=CARTESIAN_POINT ( 'NONE',  ( 22.59999954896768770, -0.008828232233007798913, -88.74949132593202705 ) ) ;
#163356=ORIENTED_EDGE ( 'NONE', *, *, #18120, .T. ) ;
#163378=DIRECTION ( 'NONE',  ( 1.000000000000000000, -0.000000000000000000, -0.000000000000000000 ) ) ;
#163384=ORIENTED_EDGE ( 'NONE', *, *, #14430, .F. ) ;
#163418=FACE_OUTER_BOUND ( 'NONE', #147173, .T. ) ;
#163458=FACE_OUTER_BOUND ( 'NONE', #56572, .T. ) ;
#163486=DIRECTION ( 'NONE',  ( 0.000000000000000000, 0.000000000000000000, -1.000000000000000000 ) ) ;
#163501=AXIS2_PLACEMENT_3D ( 'NONE', #202105, #140847, #196951 ) ;
#163510=LINE ( 'NONE', #160955, #248324 ) ;
#163530=EDGE_CURVE ( 'NONE', #213938, #33839, #98437, .T. ) ;
#163538=ORIENTED_EDGE ( 'NONE', *, *, #42349, .F. ) ;
#163544=TOROIDAL_SURFACE ( 'NONE', #51072, 7.800000000000000711, 0.1000000000000000056 ) ;
#163545=EDGE_CURVE ( 'NONE', #196505, #109895, #58054, .T. ) ;
#163552=ADVANCED_FACE ( 'NONE', ( #18939 ), #66783, .F. ) ;
#163563=ORIENTED_EDGE ( 'NONE', *, *, #120714, .T. ) ;
#163579=CARTESIAN_POINT ( 'NONE',  ( 22.49999999999999645, 11.64957080755595520, -100.4000000000000483 ) ) ;
#163585=CIRCLE ( 'NONE', #34597, 0.09999999999999939493 ) ;
#163596=EDGE_CURVE ( 'NONE', #69817, #196984, #42369, .T. ) ;
#163611=CARTESIAN_POINT ( 'NONE',  ( 21.05000000000000071, 11.75000000001115907, -126.9851942293460922 ) ) ;
#163623=ORIENTED_EDGE ( 'NONE', *, *, #55272, .F. ) ;
#163636=DIRECTION ( 'NONE',  ( -0.000000000000000000, -0.4791956752371546169, -0.8777080977375152360 ) ) ;
#163642=ADVANCED_FACE ( 'NONE', ( #7085 ), #4512, .F. ) ;
#163692=CARTESIAN_POINT ( 'NONE',  ( 23.15000000000000213, -11.48912529306489994, -130.9000000000000341 ) ) ;
#163695=AXIS2_PLACEMENT_3D ( 'NONE', #125663, #48691, #189508 ) ;
#163700=ADVANCED_FACE ( 'NONE', ( #211736 ), #250828, .T. ) ;
#163722=EDGE_CURVE ( 'NONE', #144062, #91963, #187605, .T. ) ;
#163726=VERTEX_POINT ( 'NONE', #10958 ) ;
#163768=AXIS2_PLACEMENT_3D ( 'NONE', #118479, #257914, #98859 ) ;
#163779=CARTESIAN_POINT ( 'NONE',  ( -22.47071067811865674, 7.720074744509219045, -100.4009075452974429 ) ) ;
#163784=AXIS2_PLACEMENT_3D ( 'NONE', #23201, #101373, #19325 ) ;
#163786=AXIS2_PLACEMENT_3D ( 'NONE', #213295, #98447, #192465 ) ;
#163791=ORIENTED_EDGE ( 'NONE', *, *, #253867, .T. ) ;
#163802=VERTEX_POINT ( 'NONE', #113901 ) ;
#163822=CARTESIAN_POINT ( 'NONE',  ( 20.84999999999998721, 10.33248238083634440, -139.5948465439131780 ) ) ;
#163850=AXIS2_PLACEMENT_3D ( 'NONE', #59573, #218668, #38773 ) ;
#163861=CARTESIAN_POINT ( 'NONE',  ( -23.15000000000000213, 2.000000000011154189, -113.7246219227621395 ) ) ;
#163884=TOROIDAL_SURFACE ( 'NONE', #47328, 0.2000000000000000111, 0.1000000000000000056 ) ;
#163898=DIRECTION ( 'NONE',  ( 1.000000000000000000, -0.000000000000000000, -0.000000000000000000 ) ) ;
#163940=AXIS2_PLACEMENT_3D ( 'NONE', #151194, #31281, #173366 ) ;
#163990=CARTESIAN_POINT ( 'NONE',  ( -18.31572283045123939, -9.548437830874796362, -140.8506256510583796 ) ) ;
#164035=DIRECTION ( 'NONE',  ( 1.000000000000000000, 3.265361837132813093E-16, -0.000000000000000000 ) ) ;
#164066=CIRCLE ( 'NONE', #189007, 0.1000000000000028644 ) ;
#164082=VERTEX_POINT ( 'NONE', #154994 ) ;
#164111=ORIENTED_EDGE ( 'NONE', *, *, #216170, .T. ) ;
#164115=EDGE_LOOP ( 'NONE', ( #196862, #75540, #62959, #216469 ) ) ;
#164116=VERTEX_POINT ( 'NONE', #213660 ) ;
#164131=CARTESIAN_POINT ( 'NONE',  ( -23.15000000000000213, 1.115600667400684642E-11, -134.0000000000000284 ) ) ;
#164154=DIRECTION ( 'NONE',  ( -1.000000000000000000, -3.265361837132813093E-16, 0.000000000000000000 ) ) ;
#164191=CARTESIAN_POINT ( 'NONE',  ( 18.49999999999999645, -1.637172712959225507, -112.0821533654720383 ) ) ;
#164212=EDGE_CURVE ( 'NONE', #132946, #41194, #158842, .T. ) ;
#164224=AXIS2_PLACEMENT_3D ( 'NONE', #216565, #173651, #114902 ) ;
#164267=DIRECTION ( 'NONE',  ( 0.000000000000000000, 0.4999999999999949485, -0.8660254037844415942 ) ) ;
#164276=CARTESIAN_POINT ( 'NONE',  ( -2.995603634470891112E-16, 6.650000000011155876, -121.6500000000000341 ) ) ;
#164295=AXIS2_PLACEMENT_3D ( 'NONE', #206742, #122080, #25553 ) ;
#164307=CARTESIAN_POINT ( 'NONE',  ( -20.07928932188135107, 9.220710678129810489, -112.8500000000000369 ) ) ;
#164308=EDGE_CURVE ( 'NONE', #124696, #123531, #166698, .T. ) ;
#164316=CIRCLE ( 'NONE', #85144, 0.1000000000000028644 ) ;
#164323=CARTESIAN_POINT ( 'NONE',  ( -20.64999999999999858, 4.350000000011156054, -121.6500000000000341 ) ) ;
#164335=ORIENTED_EDGE ( 'NONE', *, *, #197483, .T. ) ;
#164357=ORIENTED_EDGE ( 'NONE', *, *, #27452, .F. ) ;
#164361=VERTEX_POINT ( 'NONE', #109095 ) ;
#164373=CARTESIAN_POINT ( 'NONE',  ( 18.49999999999998579, -9.321008403350155902, -107.7359382490778614 ) ) ;
#164390=CARTESIAN_POINT ( 'NONE',  ( -20.95613430942474054, 11.75000000001078604, -107.3571626482198695 ) ) ;
#164399=CARTESIAN_POINT ( 'NONE',  ( -20.85000000000000142, -1.835859311432481045, -145.5044391687985694 ) ) ;
#164422=AXIS2_PLACEMENT_3D ( 'NONE', #176464, #113899, #235135 ) ;
#164440=VECTOR ( 'NONE', #174958, 1000.000000000000000 ) ;
#164465=CIRCLE ( 'NONE', #64672, 11.70000000000000284 ) ;
#164493=CYLINDRICAL_SURFACE ( 'NONE', #53345, 0.09999999999999881206 ) ;
#164494=CARTESIAN_POINT ( 'NONE',  ( -23.15000000000000213, 2.000000000011154189, -113.2246219227621395 ) ) ;
#164520=ORIENTED_EDGE ( 'NONE', *, *, #133605, .T. ) ;
#164526=ORIENTED_EDGE ( 'NONE', *, *, #99099, .T. ) ;
#164528=VERTEX_POINT ( 'NONE', #76380 ) ;
#164551=EDGE_LOOP ( 'NONE', ( #163563, #224699, #249657, #51052, #102689 ) ) ;
#164624=ORIENTED_EDGE ( 'NONE', *, *, #21198, .F. ) ;
#164626=DIRECTION ( 'NONE',  ( 1.000000000000000000, 0.000000000000000000, 0.000000000000000000 ) ) ;
#164642=ORIENTED_EDGE ( 'NONE', *, *, #147066, .T. ) ;
#164652=ADVANCED_FACE ( 'NONE', ( #202763 ), #24151, .T. ) ;
#164663=DIRECTION ( 'NONE',  ( 0.000000000000000000, -1.000000000000000000, 0.000000000000000000 ) ) ;
#164680=CIRCLE ( 'NONE', #98013, 0.1000000000000028644 ) ;
#164689=DIRECTION ( 'NONE',  ( 0.000000000000000000, -1.000000000000000000, 0.000000000000000000 ) ) ;
#164690=CARTESIAN_POINT ( 'NONE',  ( -21.04386569057559697, 11.75000000001104539, -127.1428373517806421 ) ) ;
#164696=CARTESIAN_POINT ( 'NONE',  ( 21.08134388332232234, 6.334680580529114202, -100.4241810824930070 ) ) ;
#164706=ORIENTED_EDGE ( 'NONE', *, *, #57890, .T. ) ;
#164734=DIRECTION ( 'NONE',  ( 0.000000000000000000, 1.000000000000000000, -6.308085367188393199E-16 ) ) ;
#164742=DIRECTION ( 'NONE',  ( 0.000000000000000000, -1.000000000000000000, -0.000000000000000000 ) ) ;
#164762=CARTESIAN_POINT ( 'NONE',  ( 23.25000000000000000, -8.999999999988842703, -124.1060308773475924 ) ) ;
#164769=CARTESIAN_POINT ( 'NONE',  ( 21.87500000000000355, 9.750000000011153745, -112.8500000000000369 ) ) ;
#164779=EDGE_CURVE ( 'NONE', #99810, #211247, #209180, .T. ) ;
#164823=DIRECTION ( 'NONE',  ( -1.000000000000000000, -3.265361837132813093E-16, 0.000000000000000000 ) ) ;
#164826=EDGE_CURVE ( 'NONE', #50561, #64218, #208971, .T. ) ;
#164885=CARTESIAN_POINT ( 'NONE',  ( 22.39999999999999503, 0.1000000000111554016, -94.25000000000002842 ) ) ;
#164890=DIRECTION ( 'NONE',  ( 1.000000000000000000, 7.304098846218134667E-16, -0.000000000000000000 ) ) ;
#164899=CARTESIAN_POINT ( 'NONE',  ( -18.41799967126731730, -9.499999999988851584, -107.5320698132558306 ) ) ;
#164914=AXIS2_PLACEMENT_3D ( 'NONE', #182179, #163898, #46492 ) ;
#164924=ORIENTED_EDGE ( 'NONE', *, *, #123903, .F. ) ;
#164944=AXIS2_PLACEMENT_3D ( 'NONE', #192798, #134083, #32470 ) ;
#164945=DIRECTION ( 'NONE',  ( -1.000000000000000000, 0.000000000000000000, 0.000000000000000000 ) ) ;
#164947=CYLINDRICAL_SURFACE ( 'NONE', #252081, 4.049999999999998046 ) ;
#164965=VERTEX_POINT ( 'NONE', #69251 ) ;
#164972=DIRECTION ( 'NONE',  ( 0.000000000000000000, 0.000000000000000000, -1.000000000000000000 ) ) ;
#164986=CARTESIAN_POINT ( 'NONE',  ( -18.50000000000000000, 11.65000000001115232, -100.6000000000000369 ) ) ;
#165001=DIRECTION ( 'NONE',  ( 1.000000000000000000, -0.000000000000000000, -0.000000000000000000 ) ) ;
#165003=EDGE_LOOP ( 'NONE', ( #119617, #76371, #73211, #110650 ) ) ;
#165036=CARTESIAN_POINT ( 'NONE',  ( -23.25000000000000000, 4.350000000011156054, -121.6500000000000341 ) ) ;
#165059=AXIS2_PLACEMENT_3D ( 'NONE', #168328, #190433, #247815 ) ;
#165076=CARTESIAN_POINT ( 'NONE',  ( -21.05000000000000071, -1.360870587180885716, -108.5729979270909951 ) ) ;
#165090=EDGE_CURVE ( 'NONE', #142271, #120254, #159298, .T. ) ;
#165099=EDGE_CURVE ( 'NONE', #67969, #151223, #96697, .T. ) ;
#165105=CARTESIAN_POINT ( 'NONE',  ( -21.14999999999999858, -11.64999999998884483, -103.4000000000000341 ) ) ;
#165126=CARTESIAN_POINT ( 'NONE',  ( -18.59999999999999787, 11.75000000001115197, -107.5148057706540357 ) ) ;
#165130=ORIENTED_EDGE ( 'NONE', *, *, #193976, .T. ) ;
#165137=CIRCLE ( 'NONE', #152695, 12.77500000000000924 ) ;
#165203=CARTESIAN_POINT ( 'NONE',  ( 21.05000000000000071, 1.115600667400684642E-11, -135.9000000000000625 ) ) ;
#165221=ORIENTED_EDGE ( 'NONE', *, *, #166898, .F. ) ;
#165231=CARTESIAN_POINT ( 'NONE',  ( 19.97071067811864609, 11.72071067812981404, -125.1500000000000341 ) ) ;
#165232=ORIENTED_EDGE ( 'NONE', *, *, #243223, .F. ) ;
#165257=CARTESIAN_POINT ( 'NONE',  ( -20.94999999999999929, 1.835341550235569663, -112.0551512925630249 ) ) ;
#165293=CARTESIAN_POINT ( 'NONE',  ( 20.94999999999999929, 6.550000000011156231, -112.7500000000000284 ) ) ;
#165299=CARTESIAN_POINT ( 'NONE',  ( 22.44352723754029810, 0.009277095054436620969, -88.85027865465131924 ) ) ;
#165303=DIRECTION ( 'NONE',  ( 1.000000000000000000, 0.000000000000000000, 0.000000000000000000 ) ) ;
#165315=ORIENTED_EDGE ( 'NONE', *, *, #242760, .F. ) ;
#165344=LINE ( 'NONE', #244865, #230142 ) ;
#165348=ORIENTED_EDGE ( 'NONE', *, *, #65716, .F. ) ;
#165371=DIRECTION ( 'NONE',  ( 0.000000000000000000, 0.000000000000000000, -1.000000000000000000 ) ) ;
#165376=ORIENTED_EDGE ( 'NONE', *, *, #176999, .F. ) ;
#165379=VECTOR ( 'NONE', #72985, 1000.000000000000000 ) ;
#165424=DIRECTION ( 'NONE',  ( 0.000000000000000000, -0.4999999999999478195, -0.8660254037844686836 ) ) ;
#165436=EDGE_LOOP ( 'NONE', ( #65505, #33587, #182133, #113357 ) ) ;
#165450=DIRECTION ( 'NONE',  ( 0.000000000000000000, 0.000000000000000000, 1.000000000000000000 ) ) ;
#165508=AXIS2_PLACEMENT_3D ( 'NONE', #77900, #211014, #12831 ) ;
#165516=TOROIDAL_SURFACE ( 'NONE', #61454, 0.6000000000000009770, 0.1000000000000000056 ) ;
#165532=AXIS2_PLACEMENT_3D ( 'NONE', #257990, #238479, #160259 ) ;
#165558=CARTESIAN_POINT ( 'NONE',  ( -21.05000000000000071, 1.360870587203197646, -108.5729979270909951 ) ) ;
#165561=ADVANCED_FACE ( 'NONE', ( #172072 ), #21910, .T. ) ;
#165565=VECTOR ( 'NONE', #82927, 1000.000000000000114 ) ;
#165576=AXIS2_PLACEMENT_3D ( 'NONE', #169207, #210867, #70102 ) ;
#165613=DIRECTION ( 'NONE',  ( 0.000000000000000000, 0.000000000000000000, -1.000000000000000000 ) ) ;
#165636=VERTEX_POINT ( 'NONE', #35131 ) ;
#165656=AXIS2_PLACEMENT_3D ( 'NONE', #110100, #127100, #9713 ) ;
#165684=CIRCLE ( 'NONE', #44858, 12.87499999999999822 ) ;
#165692=CARTESIAN_POINT ( 'NONE',  ( -21.12844524849339223, 11.75000000001115197, -107.4044134708428260 ) ) ;
#165702=TOROIDAL_SURFACE ( 'NONE', #124178, 0.6000000000000004219, 0.1000000000000000056 ) ;
#165752=ADVANCED_FACE ( 'NONE', ( #40253 ), #117761, .T. ) ;
#165768=LINE ( 'NONE', #203585, #63418 ) ;
#165777=DIRECTION ( 'NONE',  ( 0.000000000000000000, 0.000000000000000000, 1.000000000000000000 ) ) ;
#165799=AXIS2_PLACEMENT_3D ( 'NONE', #220631, #61556, #103221 ) ;
#165808=CARTESIAN_POINT ( 'NONE',  ( -20.94999999999999929, 1.115600667400684642E-11, -108.4000000000000341 ) ) ;
#165822=TOROIDAL_SURFACE ( 'NONE', #95050, 0.4000000000000012990, 0.1000000000000000056 ) ;
#165836=DIRECTION ( 'NONE',  ( 1.000000000000000000, -0.000000000000000000, -0.000000000000000000 ) ) ;
#165840=AXIS2_PLACEMENT_3D ( 'NONE', #152264, #250054, #231788 ) ;
#165846=ORIENTED_EDGE ( 'NONE', *, *, #200111, .T. ) ;
#165861=VECTOR ( 'NONE', #72068, 1000.000000000000000 ) ;
#165867=EDGE_LOOP ( 'NONE', ( #158613, #209483, #243842, #57833 ) ) ;
#165894=ORIENTED_EDGE ( 'NONE', *, *, #122605, .T. ) ;
#165897=ADVANCED_FACE ( 'NONE', ( #215649 ), #73618, .T. ) ;
#165906=VECTOR ( 'NONE', #64407, 1000.000000000000000 ) ;
#165924=CARTESIAN_POINT ( 'NONE',  ( -20.94999999999999929, -1.851028230129704522, -112.1539132694225316 ) ) ;
#165927=ORIENTED_EDGE ( 'NONE', *, *, #23608, .T. ) ;
#165943=ORIENTED_EDGE ( 'NONE', *, *, #5792, .F. ) ;
#165966=EDGE_CURVE ( 'NONE', #194066, #172696, #133557, .T. ) ;
#165988=EDGE_CURVE ( 'NONE', #237460, #234652, #5493, .T. ) ;
#166052=DIRECTION ( 'NONE',  ( 0.000000000000000000, 2.891205793294679805E-16, -1.000000000000000000 ) ) ;
#166054=EDGE_LOOP ( 'NONE', ( #124661, #205221, #157874, #167440 ) ) ;
#166080=CARTESIAN_POINT ( 'NONE',  ( 21.05000000000000071, 4.850467289730776344, -121.9657325909983570 ) ) ;
#166083=DIRECTION ( 'NONE',  ( 0.000000000000000000, -0.9887567792719341719, -0.1495327102803664099 ) ) ;
#166089=TOROIDAL_SURFACE ( 'NONE', #53635, 7.800000000000000711, 0.1000000000000000056 ) ;
#166111=CIRCLE ( 'NONE', #232724, 0.1000000000000028644 ) ;
#166125=EDGE_CURVE ( 'NONE', #132946, #167562, #42942, .T. ) ;
#166144=EDGE_CURVE ( 'NONE', #70011, #183119, #90254, .T. ) ;
#166151=CARTESIAN_POINT ( 'NONE',  ( -18.59999999999999787, -1.162701749926853712, -108.6000000000000227 ) ) ;
#166179=ORIENTED_EDGE ( 'NONE', *, *, #32302, .T. ) ;
#166184=AXIS2_PLACEMENT_3D ( 'NONE', #100622, #195931, #116385 ) ;
#166185=CIRCLE ( 'NONE', #228709, 0.1000000000000028644 ) ;
#166192=CARTESIAN_POINT ( 'NONE',  ( -20.54999999999999716, 1.940186915899004161, -121.1708807889467039 ) ) ;
#166197=AXIS2_PLACEMENT_3D ( 'NONE', #167895, #150864, #227830 ) ;
#166216=CARTESIAN_POINT ( 'NONE',  ( -18.46093223321773635, -9.480682968263376864, -107.5845505139267146 ) ) ;
#166255=EDGE_LOOP ( 'NONE', ( #204073, #33251, #134480, #104990 ) ) ;
#166283=FACE_OUTER_BOUND ( 'NONE', #29387, .T. ) ;
#166338=EDGE_LOOP ( 'NONE', ( #219588, #253571, #106577, #7396, #72088 ) ) ;
#166377=CYLINDRICAL_SURFACE ( 'NONE', #148679, 0.1000000000000028644 ) ;
#166378=( NAMED_UNIT ( * ) PLANE_ANGLE_UNIT ( ) SI_UNIT ( $, .RADIAN. ) );
#166379=EDGE_CURVE ( 'NONE', #70455, #61914, #111125, .T. ) ;
#166408=DIRECTION ( 'NONE',  ( 1.000000000000000000, 0.000000000000000000, 0.000000000000000000 ) ) ;
#166411=VECTOR ( 'NONE', #122744, 1000.000000000000000 ) ;
#166446=CIRCLE ( 'NONE', #70587, 0.1000000000000000472 ) ;
#166448=ORIENTED_EDGE ( 'NONE', *, *, #230760, .F. ) ;
#166475=TOROIDAL_SURFACE ( 'NONE', #91445, 0.2000000000000000111, 0.1000000000000000056 ) ;
#166487=DIRECTION ( 'NONE',  ( 1.000000000000000000, 0.000000000000000000, 0.000000000000000000 ) ) ;
#166502=DIRECTION ( 'NONE',  ( -0.000000000000000000, 0.000000000000000000, -1.000000000000000000 ) ) ;
#166532=ORIENTED_EDGE ( 'NONE', *, *, #176756, .T. ) ;
#166613=CARTESIAN_POINT ( 'NONE',  ( 21.14999999999999858, 6.650000000011155876, -112.7500000000000284 ) ) ;
#166641=ORIENTED_EDGE ( 'NONE', *, *, #70967, .T. ) ;
#166658=DIRECTION ( 'NONE',  ( 1.000000000000000000, 0.000000000000000000, 0.000000000000000000 ) ) ;
#166677=ORIENTED_EDGE ( 'NONE', *, *, #46727, .T. ) ;
#166690=ORIENTED_EDGE ( 'NONE', *, *, #160864, .F. ) ;
#166698=( BOUNDED_CURVE ( )  B_SPLINE_CURVE ( 3, ( #165231, #66130, #145655, #126086 ),
 .UNSPECIFIED., .F., .F. ) 
 B_SPLINE_CURVE_WITH_KNOTS ( ( 4, 4 ),
 ( 0.000000000000000000, 1.570796326794916320 ),
 .UNSPECIFIED. ) 
 CURVE ( )  GEOMETRIC_REPRESENTATION_ITEM ( )  RATIONAL_B_SPLINE_CURVE ( ( 1.000000000000000000, 0.8047378541243603856, 0.8047378541243603856, 1.000000000000000000 ) ) 
 REPRESENTATION_ITEM ( '' )  );
#166717=DIRECTION ( 'NONE',  ( -3.265361837132813093E-16, 1.000000000000000000, 0.000000000000000000 ) ) ;
#166743=ORIENTED_EDGE ( 'NONE', *, *, #64967, .F. ) ;
#166768=LINE ( 'NONE', #29824, #155581 ) ;
#166769=DIRECTION ( 'NONE',  ( 0.000000000000000000, -1.000000000000000000, 0.000000000000000000 ) ) ;
#166774=ORIENTED_EDGE ( 'NONE', *, *, #190035, .F. ) ;
#166782=CARTESIAN_POINT ( 'NONE',  ( 18.47688499308724985, -9.464855950272976770, -140.7013477531374406 ) ) ;
#166786=CARTESIAN_POINT ( 'NONE',  ( 20.95017935633852346, 10.47548927963648246, -108.0774397973905252 ) ) ;
#166808=ORIENTED_EDGE ( 'NONE', *, *, #130190, .F. ) ;
#166866=CARTESIAN_POINT ( 'NONE',  ( -23.15000000000000213, 11.65000000001115588, -121.8500000000000227 ) ) ;
#166878=CARTESIAN_POINT ( 'NONE',  ( -20.94999999999999929, 1.835341550235569663, -112.0551512925630249 ) ) ;
#166891=DIRECTION ( 'NONE',  ( 0.000000000000000000, 0.008583690987124100932, -0.9999631594459055250 ) ) ;
#166898=EDGE_CURVE ( 'NONE', #43405, #104735, #80102, .T. ) ;
#166902=ORIENTED_EDGE ( 'NONE', *, *, #156874, .T. ) ;
#166925=ORIENTED_EDGE ( 'NONE', *, *, #218763, .T. ) ;
#166928=ORIENTED_EDGE ( 'NONE', *, *, #171541, .F. ) ;
#166940=EDGE_CURVE ( 'NONE', #24198, #188307, #39316, .T. ) ;
#166953=ORIENTED_EDGE ( 'NONE', *, *, #223244, .F. ) ;
#166961=CARTESIAN_POINT ( 'NONE',  ( -18.59999999999999787, -1.164121893230052995, -141.7148480855716457 ) ) ;
#166962=ORIENTED_EDGE ( 'NONE', *, *, #211279, .T. ) ;
#167015=DIRECTION ( 'NONE',  ( 0.000000000000000000, 0.000000000000000000, -1.000000000000000000 ) ) ;
#167017=CARTESIAN_POINT ( 'NONE',  ( -22.59999985501179154, 11.74986979301414358, -100.4344013302006857 ) ) ;
#167025=ORIENTED_EDGE ( 'NONE', *, *, #7748, .T. ) ;
#167069=DIRECTION ( 'NONE',  ( -1.000000000000000000, 0.000000000000000000, 0.000000000000000000 ) ) ;
#167109=CARTESIAN_POINT ( 'NONE',  ( 23.14999999999999147, 1.115600667400684642E-11, -100.5000000000000284 ) ) ;
#167122=DIRECTION ( 'NONE',  ( 1.000000000000000000, 0.000000000000000000, 0.000000000000000000 ) ) ;
#167134=EDGE_CURVE ( 'NONE', #208162, #207792, #122518, .T. ) ;
#167213=DIRECTION ( 'NONE',  ( 1.000000000000000000, 0.000000000000000000, 0.000000000000000000 ) ) ;
#167217=ADVANCED_FACE ( 'NONE', ( #149663 ), #253856, .F. ) ;
#167226=ORIENTED_EDGE ( 'NONE', *, *, #121762, .T. ) ;
#167271=ORIENTED_EDGE ( 'NONE', *, *, #240851, .F. ) ;
#167297=ORIENTED_EDGE ( 'NONE', *, *, #9540, .T. ) ;
#167325=CARTESIAN_POINT ( 'NONE',  ( -23.25000000000000000, 1.115600667400684642E-11, -134.0000000000000284 ) ) ;
#167341=VERTEX_POINT ( 'NONE', #19110 ) ;
#167407=FACE_OUTER_BOUND ( 'NONE', #237744, .T. ) ;
#167440=ORIENTED_EDGE ( 'NONE', *, *, #153482, .F. ) ;
#167472=ADVANCED_FACE ( 'NONE', ( #67221 ), #209397, .F. ) ;
#167549=EDGE_CURVE ( 'NONE', #150422, #200055, #153218, .T. ) ;
#167554=CIRCLE ( 'NONE', #230067, 0.09999999999998898659 ) ;
#167562=VERTEX_POINT ( 'NONE', #89337 ) ;
#167641=ADVANCED_FACE ( 'NONE', ( #210588 ), #128485, .T. ) ;
#167646=DIRECTION ( 'NONE',  ( 0.000000000000000000, -0.8777080977375715243, 0.4791956752370512551 ) ) ;
#167647=FILL_AREA_STYLE ('',( #127218 ) ) ;
#167661=DIRECTION ( 'NONE',  ( 0.000000000000000000, -0.1298341882520022694, -0.9915357197604853789 ) ) ;
#167666=CARTESIAN_POINT ( 'NONE',  ( 20.93284271247462414, 11.75000000001116085, -126.9851942293461065 ) ) ;
#167676=CARTESIAN_POINT ( 'NONE',  ( 23.14999999999998437, 1.115600667400684642E-11, -100.5000000000000284 ) ) ;
#167720=CARTESIAN_POINT ( 'NONE',  ( 21.14999999999999858, -11.64999999998883595, -100.5000000000000284 ) ) ;
#167732=ADVANCED_FACE ( 'NONE', ( #19791 ), #86657, .T. ) ;
#167776=EDGE_CURVE ( 'NONE', #164965, #15694, #208703, .T. ) ;
#167860=CARTESIAN_POINT ( 'NONE',  ( 18.50016250449482413, 10.29766095125186354, -139.4743663933279265 ) ) ;
#167882=AXIS2_PLACEMENT_3D ( 'NONE', #227824, #146990, #89586 ) ;
#167890=ADVANCED_FACE ( 'NONE', ( #134258 ), #229699, .T. ) ;
#167892=CARTESIAN_POINT ( 'NONE',  ( 21.14999999999999858, 11.75000000001116263, -88.75000000000004263 ) ) ;
#167895=CARTESIAN_POINT ( 'NONE',  ( 20.85000000000000142, 1.115600667400684642E-11, -134.0000000000000284 ) ) ;
#167897=DIRECTION ( 'NONE',  ( -1.000000000000000000, 0.000000000000000000, 0.000000000000000000 ) ) ;
#167915=VERTEX_POINT ( 'NONE', #75616 ) ;
#167927=VERTEX_POINT ( 'NONE', #114720 ) ;
#167974=ORIENTED_EDGE ( 'NONE', *, *, #59349, .T. ) ;
#167999=PLANE ( 'NONE',  #29238 ) ;
#168023=CIRCLE ( 'NONE', #97181, 0.09999999999998898659 ) ;
#168027=CARTESIAN_POINT ( 'NONE',  ( 23.14999999999999503, 14.10000000001115694, -128.3997023888606748 ) ) ;
#168030=VERTEX_POINT ( 'NONE', #23351 ) ;
#168040=AXIS2_PLACEMENT_3D ( 'NONE', #237016, #177063, #49711 ) ;
#168076=CARTESIAN_POINT ( 'NONE',  ( 20.97468175916186084, 10.62526516438217605, -112.7547614354131724 ) ) ;
#168100=EDGE_CURVE ( 'NONE', #164116, #34456, #161569, .T. ) ;
#168107=DIRECTION ( 'NONE',  ( 1.000000000000000000, 0.000000000000000000, 0.000000000000000000 ) ) ;
#168113=CARTESIAN_POINT ( 'NONE',  ( 18.59999999999998366, 1.115600667400684642E-11, -134.0000000000000284 ) ) ;
#168118=DIRECTION ( 'NONE',  ( 0.000000000000000000, 0.000000000000000000, 1.000000000000000000 ) ) ;
#168128=ORIENTED_EDGE ( 'NONE', *, *, #42349, .T. ) ;
#168137=AXIS2_PLACEMENT_3D ( 'NONE', #38203, #139838, #98121 ) ;
#168178=AXIS2_PLACEMENT_3D ( 'NONE', #216254, #92463, #113318 ) ;
#168209=ADVANCED_FACE ( 'NONE', ( #127555 ), #159173, .T. ) ;
#168261=CARTESIAN_POINT ( 'NONE',  ( -23.15000000000000213, 1.115649653272650466E-11, -138.0000000000000284 ) ) ;
#168282=CARTESIAN_POINT ( 'NONE',  ( -20.94999999999999574, 11.75000000001115552, -107.3416006898971631 ) ) ;
#168283=CARTESIAN_POINT ( 'NONE',  ( 21.05000000000000071, 8.776282895303632259, -112.6500000000000341 ) ) ;
#168305=CYLINDRICAL_SURFACE ( 'NONE', #178546, 0.1000000000000000472 ) ;
#168328=CARTESIAN_POINT ( 'NONE',  ( 20.94999999999999929, -8.999999999988842703, -124.1060308773475924 ) ) ;
#168341=DIRECTION ( 'NONE',  ( 0.000000000000000000, 0.000000000000000000, -1.000000000000000000 ) ) ;
#168372=DIRECTION ( 'NONE',  ( -0.000000000000000000, 0.9876197685951279004, -0.1568667991644694115 ) ) ;
#168395=FACE_OUTER_BOUND ( 'NONE', #58439, .T. ) ;
#168409=VERTEX_POINT ( 'NONE', #93556 ) ;
#168425=ORIENTED_EDGE ( 'NONE', *, *, #221028, .T. ) ;
#168455=DIRECTION ( 'NONE',  ( 0.000000000000000000, 0.000000000000000000, -1.000000000000000000 ) ) ;
#168473=DIRECTION ( 'NONE',  ( 1.000000000000000000, 0.000000000000000000, 0.000000000000000000 ) ) ;
#168481=DIRECTION ( 'NONE',  ( 0.000000000000000000, 0.000000000000000000, -1.000000000000000000 ) ) ;
#168501=CARTESIAN_POINT ( 'NONE',  ( 22.47071067811865319, 1.115600667400684642E-11, -100.5000000000000284 ) ) ;
#168502=VERTEX_POINT ( 'NONE', #239498 ) ;
#168505=LINE ( 'NONE', #185455, #186704 ) ;
#168555=TOROIDAL_SURFACE ( 'NONE', #93470, 0.2000000000000000111, 0.1000000000000000056 ) ;
#168562=ORIENTED_EDGE ( 'NONE', *, *, #45395, .F. ) ;
#168568=VERTEX_POINT ( 'NONE', #120859 ) ;
#168579=EDGE_CURVE ( 'NONE', #95316, #240059, #234319, .T. ) ;
#168612=DIRECTION ( 'NONE',  ( -1.000000000000000000, -2.952720810173289112E-16, 0.000000000000000000 ) ) ;
#168633=AXIS2_PLACEMENT_3D ( 'NONE', #115104, #254582, #195945 ) ;
#168640=CARTESIAN_POINT ( 'NONE',  ( 21.14999999999999858, 1.115600667400684642E-11, -100.6000000000000227 ) ) ;
#168641=CIRCLE ( 'NONE', #59652, 6.329289321881356400 ) ;
#168649=VECTOR ( 'NONE', #1077, 1000.000000000000000 ) ;
#168701=VECTOR ( 'NONE', #99816, 1000.000000000000000 ) ;
#168736=ADVANCED_FACE ( 'NONE', ( #132378 ), #175912, .F. ) ;
#168772=CARTESIAN_POINT ( 'NONE',  ( 21.14999999999999858, 10.71339244341104013, -112.8500000000000369 ) ) ;
#168787=CARTESIAN_POINT ( 'NONE',  ( 21.13614978966381841, 1.115648720638573240E-11, -94.00089529816622758 ) ) ;
#168814=CARTESIAN_POINT ( 'NONE',  ( -21.13614978966381130, 6.499104701844946597, -100.5000000000000142 ) ) ;
#168819=CIRCLE ( 'NONE', #114609, 0.09999999999998898659 ) ;
#168850=ORIENTED_EDGE ( 'NONE', *, *, #77891, .T. ) ;
#168867=ORIENTED_EDGE ( 'NONE', *, *, #112993, .T. ) ;
#168878=ORIENTED_EDGE ( 'NONE', *, *, #73923, .F. ) ;
#168888=CARTESIAN_POINT ( 'NONE',  ( -18.47140463609786210, -9.671474685209730637, -140.6727604582741264 ) ) ;
#168891=CARTESIAN_POINT ( 'NONE',  ( 18.42555734704283665, -9.497158361925555070, -107.5398304977349682 ) ) ;
#168894=TOROIDAL_SURFACE ( 'NONE', #218714, 0.2000000000000000111, 0.1000000000000000056 ) ;
#168971=VERTEX_POINT ( 'NONE', #112064 ) ;
#168980=ORIENTED_EDGE ( 'NONE', *, *, #153866, .F. ) ;
#168983=DIRECTION ( 'NONE',  ( 0.000000000000000000, 0.000000000000000000, 1.000000000000000000 ) ) ;
#169012=DIRECTION ( 'NONE',  ( 0.000000000000000000, -1.000000000000000000, -2.891205793294679805E-16 ) ) ;
#169046=EDGE_CURVE ( 'NONE', #257484, #46494, #92856, .T. ) ;
#169061=CARTESIAN_POINT ( 'NONE',  ( -20.64999999999999858, 1.115600667400684642E-11, -134.0000000000000284 ) ) ;
#169062=ORIENTED_EDGE ( 'NONE', *, *, #85324, .T. ) ;
#169072=AXIS2_PLACEMENT_3D ( 'NONE', #193824, #170455, #72606 ) ;
#169090=DIRECTION ( 'NONE',  ( 0.000000000000000000, 0.000000000000000000, 1.000000000000000000 ) ) ;
#169095=CARTESIAN_POINT ( 'NONE',  ( 20.95483826173899899, 8.876166204781142710, -109.0462755528995444 ) ) ;
#169135=VERTEX_POINT ( 'NONE', #220142 ) ;
#169140=ADVANCED_FACE ( 'NONE', ( #135448 ), #121068, .F. ) ;
#169160=EDGE_LOOP ( 'NONE', ( #116397, #120779, #56876, #237171, #76598 ) ) ;
#169184=CARTESIAN_POINT ( 'NONE',  ( 21.05000000000000071, -8.730841121484171907, -110.0980747189843640 ) ) ;
#169192=EDGE_CURVE ( 'NONE', #101017, #152480, #102721, .T. ) ;
#169207=CARTESIAN_POINT ( 'NONE',  ( -20.12071067811865888, 9.320710678129810134, -112.8500000000000369 ) ) ;
#169213=DIRECTION ( 'NONE',  ( 0.000000000000000000, -0.8660254037844412611, -0.4999999999999956701 ) ) ;
#169226=ORIENTED_EDGE ( 'NONE', *, *, #70521, .F. ) ;
#169235=ORIENTED_EDGE ( 'NONE', *, *, #167134, .F. ) ;
#169237=CARTESIAN_POINT ( 'NONE',  ( -18.45140287520618116, -9.486077739518409047, -140.6405231266861335 ) ) ;
#169244=CARTESIAN_POINT ( 'NONE',  ( 23.14999999999999858, -3.899999999988843502, -134.0000000000000284 ) ) ;
#169282=ORIENTED_EDGE ( 'NONE', *, *, #177946, .F. ) ;
#169294=ORIENTED_EDGE ( 'NONE', *, *, #163722, .F. ) ;
#169314=EDGE_CURVE ( 'NONE', #142934, #148718, #222200, .T. ) ;
#169344=CARTESIAN_POINT ( 'NONE',  ( -20.54999999999999716, 2.000000000011154189, -121.1753780772379230 ) ) ;
#169345=AXIS2_PLACEMENT_3D ( 'NONE', #160665, #137215, #82344 ) ;
#169355=CARTESIAN_POINT ( 'NONE',  ( 21.13461538461538325, 10.61458296203669427, -112.8500000000000369 ) ) ;
#169361=EDGE_CURVE ( 'NONE', #34456, #18989, #132591, .T. ) ;
#169382=ADVANCED_FACE ( 'NONE', ( #227827 ), #149605, .T. ) ;
#169427=AXIS2_PLACEMENT_3D ( 'NONE', #5263, #207363, #246471 ) ;
#169431=ORIENTED_EDGE ( 'NONE', *, *, #174582, .T. ) ;
#169443=DIRECTION ( 'NONE',  ( 1.000000000000000000, -0.000000000000000000, -0.000000000000000000 ) ) ;
#169460=ORIENTED_EDGE ( 'NONE', *, *, #90860, .T. ) ;
#169462=AXIS2_PLACEMENT_3D ( 'NONE', #175803, #158815, #77949 ) ;
#169483=EDGE_CURVE ( 'NONE', #203753, #255048, #247149, .T. ) ;
#169516=DIRECTION ( 'NONE',  ( -0.000000000000000000, -0.000000000000000000, -1.000000000000000000 ) ) ;
#169526=EDGE_CURVE ( 'NONE', #40984, #84132, #55575, .T. ) ;
#169532=ADVANCED_FACE ( 'NONE', ( #138965 ), #122276, .F. ) ;
#169534=VERTEX_POINT ( 'NONE', #16507 ) ;
#169546=DIRECTION ( 'NONE',  ( 0.000000000000000000, 1.000000000000000000, 0.000000000000000000 ) ) ;
#169569=CARTESIAN_POINT ( 'NONE',  ( 18.31572054635717706, -9.548475435767914021, -140.8505701647482056 ) ) ;
#169592=DIRECTION ( 'NONE',  ( 0.000000000000000000, 1.224646799142185182E-16, 1.000000000000000000 ) ) ;
#169600=CARTESIAN_POINT ( 'NONE',  ( -22.49756042579671700, 0.07804633702833754794, -88.85013503889771869 ) ) ;
#169627=VERTEX_POINT ( 'NONE', #45038 ) ;
#169647=DIRECTION ( 'NONE',  ( 1.000000000000000000, 0.000000000000000000, 0.000000000000000000 ) ) ;
#169688=DIRECTION ( 'NONE',  ( -1.000000000000000000, -2.952720810173289112E-16, 0.000000000000000000 ) ) ;
#169689=CARTESIAN_POINT ( 'NONE',  ( -20.64999999999999858, 1.115600667400684642E-11, -121.1250000000000426 ) ) ;
#169697=AXIS2_PLACEMENT_3D ( 'NONE', #53127, #51823, #131379 ) ;
#169698=CARTESIAN_POINT ( 'NONE',  ( 21.05000000000000426, 6.413826288824126642, -100.5857409370334636 ) ) ;
#169721=ORIENTED_EDGE ( 'NONE', *, *, #128643, .T. ) ;
#169728=DIRECTION ( 'NONE',  ( 0.000000000000000000, -1.000000000000000000, 0.000000000000000000 ) ) ;
#169736=ADVANCED_FACE ( 'NONE', ( #245814 ), #244512, .F. ) ;
#169744=CARTESIAN_POINT ( 'NONE',  ( -21.64999999999999858, 7.350000000011155166, -112.7500000000000284 ) ) ;
#169768=EDGE_CURVE ( 'NONE', #120951, #17092, #105676, .T. ) ;
#169780=ADVANCED_FACE ( 'NONE', ( #108861 ), #252212, .F. ) ;
#169788=AXIS2_PLACEMENT_3D ( 'NONE', #63220, #4534, #64522 ) ;
#169795=ORIENTED_EDGE ( 'NONE', *, *, #234793, .T. ) ;
#169817=CIRCLE ( 'NONE', #111510, 0.1000000000000002554 ) ;
#169845=ORIENTED_EDGE ( 'NONE', *, *, #43348, .F. ) ;
#169847=ADVANCED_FACE ( 'NONE', ( #73621 ), #176635, .F. ) ;
#169852=DIRECTION ( 'NONE',  ( 1.000000000000000000, 0.000000000000000000, -0.000000000000000000 ) ) ;
#169854=ORIENTED_EDGE ( 'NONE', *, *, #72926, .T. ) ;
#169893=DIRECTION ( 'NONE',  ( 0.000000000000000000, -0.9908441862701596881, 0.1350103645451904977 ) ) ;
#169918=LINE ( 'NONE', #47329, #165861 ) ;
#169941=EDGE_LOOP ( 'NONE', ( #111615, #227738, #175250, #196646 ) ) ;
#169977=CARTESIAN_POINT ( 'NONE',  ( -21.05000000000000071, -11.48912529306490349, -103.6000000000000369 ) ) ;
#169990=DIRECTION ( 'NONE',  ( 0.000000000000000000, 0.000000000000000000, -1.000000000000000000 ) ) ;
#170059=AXIS2_PLACEMENT_3D ( 'NONE', #198690, #20071, #162158 ) ;
#170061=CARTESIAN_POINT ( 'NONE',  ( -23.15000000000000213, 11.65000000001115588, -100.5000000000000284 ) ) ;
#170065=CIRCLE ( 'NONE', #86781, 0.1000000000000028644 ) ;
#170098=VECTOR ( 'NONE', #79778, 999.9999999999998863 ) ;
#170108=ADVANCED_FACE ( 'NONE', ( #103398 ), #208567, .T. ) ;
#170138=EDGE_CURVE ( 'NONE', #161165, #11869, #139173, .T. ) ;
#170152=EDGE_CURVE ( 'NONE', #220305, #53442, #251639, .T. ) ;
#170174=VERTEX_POINT ( 'NONE', #246777 ) ;
#170198=FACE_OUTER_BOUND ( 'NONE', #47952, .T. ) ;
#170220=ORIENTED_EDGE ( 'NONE', *, *, #185421, .T. ) ;
#170228=CARTESIAN_POINT ( 'NONE',  ( -20.64999999999999858, 7.250000000011155521, -112.8500000000000369 ) ) ;
#170235=TOROIDAL_SURFACE ( 'NONE', #111944, 4.099999999999999645, 0.1000000000000000056 ) ;
#170253=CARTESIAN_POINT ( 'NONE',  ( -20.54999999999999716, 2.400000000011155432, -113.7246219227621395 ) ) ;
#170300=DIRECTION ( 'NONE',  ( 0.000000000000000000, -1.000000000000000000, 0.000000000000000000 ) ) ;
#170310=ADVANCED_FACE ( 'NONE', ( #94128, #13323 ), #113698, .T. ) ;
#170342=EDGE_CURVE ( 'NONE', #186401, #104851, #114258, .T. ) ;
#170369=AXIS2_PLACEMENT_3D ( 'NONE', #241353, #22317, #185218 ) ;
#170424=ORIENTED_EDGE ( 'NONE', *, *, #181837, .F. ) ;
#170455=DIRECTION ( 'NONE',  ( -2.602085213965226419E-14, -0.000000000000000000, -1.000000000000000000 ) ) ;
#170475=DIRECTION ( 'NONE',  ( -1.000000000000000000, -0.000000000000000000, -0.000000000000000000 ) ) ;
#170511=CARTESIAN_POINT ( 'NONE',  ( 18.52928932188133970, 10.27928932189250411, -125.1500000000000341 ) ) ;
#170532=ORIENTED_EDGE ( 'NONE', *, *, #200971, .F. ) ;
#170538=EDGE_CURVE ( 'NONE', #189217, #247064, #64329, .T. ) ;
#170573=DIRECTION ( 'NONE',  ( -3.265361837132813093E-16, 1.000000000000000000, 0.000000000000000000 ) ) ;
#170582=EDGE_LOOP ( 'NONE', ( #17669, #240689, #238357, #35147 ) ) ;
#170586=DIRECTION ( 'NONE',  ( 0.000000000000000000, 0.9908441862701600211, -0.1350103645451876666 ) ) ;
#170603=AXIS2_PLACEMENT_3D ( 'NONE', #160123, #239640, #35061 ) ;
#170605=CARTESIAN_POINT ( 'NONE',  ( 20.04142135623730070, 11.65000000001115943, -121.8500000000000369 ) ) ;
#170608=DIRECTION ( 'NONE',  ( 0.000000000000000000, 0.000000000000000000, 1.000000000000000000 ) ) ;
#170642=ORIENTED_EDGE ( 'NONE', *, *, #88206, .T. ) ;
#170644=CIRCLE ( 'NONE', #8101, 0.1000000000000028644 ) ;
#170672=DIRECTION ( 'NONE',  ( 0.000000000000000000, -1.000000000000000000, -0.000000000000000000 ) ) ;
#170700=CARTESIAN_POINT ( 'NONE',  ( -21.05000000000000071, 1.115649653272650466E-11, -138.0000000000000284 ) ) ;
#170710=CARTESIAN_POINT ( 'NONE',  ( -23.15000000000000213, 1.115600667400684642E-11, -104.6500000000000341 ) ) ;
#170731=CIRCLE ( 'NONE', #183163, 7.800000000000000711 ) ;
#170751=EDGE_LOOP ( 'NONE', ( #255003, #31429, #236568, #222529 ) ) ;
#170756=DIRECTION ( 'NONE',  ( 0.000000000000000000, 0.000000000000000000, -1.000000000000000000 ) ) ;
#170761=DIRECTION ( 'NONE',  ( 0.000000000000000000, 0.000000000000000000, -1.000000000000000000 ) ) ;
#170785=ORIENTED_EDGE ( 'NONE', *, *, #88689, .F. ) ;
#170789=CARTESIAN_POINT ( 'NONE',  ( -21.05000000000000071, 1.162701749949165642, -108.6000000000000227 ) ) ;
#170810=ORIENTED_EDGE ( 'NONE', *, *, #98760, .T. ) ;
#170832=FACE_OUTER_BOUND ( 'NONE', #110855, .T. ) ;
#170839=LINE ( 'NONE', #93802, #57456 ) ;
#170865=CARTESIAN_POINT ( 'NONE',  ( -21.05000000000000426, 6.270085863700293416, -100.4651319969869263 ) ) ;
#170887=ORIENTED_EDGE ( 'NONE', *, *, #54012, .F. ) ;
#170890=DIRECTION ( 'NONE',  ( 0.000000000000000000, 0.000000000000000000, -1.000000000000000000 ) ) ;
#170894=DIRECTION ( 'NONE',  ( -0.000000000000000000, -0.000000000000000000, 1.000000000000000000 ) ) ;
#170932=CARTESIAN_POINT ( 'NONE',  ( -21.05000000000000426, -0.02103547652895997738, -94.19554417805240121 ) ) ;
#170975=DIRECTION ( 'NONE',  ( 0.000000000000000000, 0.000000000000000000, -1.000000000000000000 ) ) ;
#170990=DIRECTION ( 'NONE',  ( 0.000000000000000000, 0.1568667991644863147, 0.9876197685951252359 ) ) ;
#171012=EDGE_LOOP ( 'NONE', ( #98308, #46345, #238573 ) ) ;
#171075=DIRECTION ( 'NONE',  ( 1.000000000000000000, -0.000000000000000000, -0.000000000000000000 ) ) ;
#171084=AXIS2_PLACEMENT_3D ( 'NONE', #220692, #119031, #101989 ) ;
#171095=AXIS2_PLACEMENT_3D ( 'NONE', #124075, #224433, #165777 ) ;
#171114=ORIENTED_EDGE ( 'NONE', *, *, #121309, .T. ) ;
#171145=EDGE_CURVE ( 'NONE', #204523, #148718, #248079, .T. ) ;
#171185=LINE ( 'NONE', #69486, #158052 ) ;
#171188=CYLINDRICAL_SURFACE ( 'NONE', #108843, 0.09999999999999939493 ) ;
#171195=DIRECTION ( 'NONE',  ( -1.000000000000000000, 0.000000000000000000, 0.000000000000000000 ) ) ;
#171220=EDGE_CURVE ( 'NONE', #200879, #154355, #123187, .T. ) ;
#171263=DIRECTION ( 'NONE',  ( 1.000000000000000000, -0.000000000000000000, -0.000000000000000000 ) ) ;
#171289=CIRCLE ( 'NONE', #4610, 0.09999999999999992228 ) ;
#171301=AXIS2_PLACEMENT_3D ( 'NONE', #217349, #103814, #79122 ) ;
#171317=ORIENTED_EDGE ( 'NONE', *, *, #54909, .T. ) ;
#171379=FACE_OUTER_BOUND ( 'NONE', #205566, .T. ) ;
#171480=CARTESIAN_POINT ( 'NONE',  ( 22.47071067811865319, 0.09909245471376171288, -92.77992525550199332 ) ) ;
#171491=CARTESIAN_POINT ( 'NONE',  ( 20.72390388899123792, 10.58996311843359273, -108.0113482957451509 ) ) ;
#171493=CARTESIAN_POINT ( 'NONE',  ( -20.85000000000000142, -1.164121893230052995, -141.9148480855716343 ) ) ;
#171499=CIRCLE ( 'NONE', #50816, 0.1000000000000028644 ) ;
#171503=DIRECTION ( 'NONE',  ( 0.000000000000000000, 0.000000000000000000, 1.000000000000000000 ) ) ;
#171511=TOROIDAL_SURFACE ( 'NONE', #88055, 11.89999999999999858, 0.1000000000000000056 ) ;
#171520=EDGE_CURVE ( 'NONE', #236424, #107194, #27372, .T. ) ;
#171528=ORIENTED_EDGE ( 'NONE', *, *, #90610, .F. ) ;
#171533=ORIENTED_EDGE ( 'NONE', *, *, #77243, .F. ) ;
#171541=EDGE_CURVE ( 'NONE', #217495, #167927, #81452, .T. ) ;
#171546=ADVANCED_FACE ( 'NONE', ( #194593 ), #115027, .T. ) ;
#171558=ORIENTED_EDGE ( 'NONE', *, *, #3752, .F. ) ;
#171582=CARTESIAN_POINT ( 'NONE',  ( 22.60000000000000142, 0.1008583691098682150, -88.75043287651064361 ) ) ;
#171589=DIRECTION ( 'NONE',  ( 0.000000000000000000, 0.000000000000000000, -1.000000000000000000 ) ) ;
#171616=TOROIDAL_SURFACE ( 'NONE', #84038, 0.6000000000000004219, 0.1000000000000000056 ) ;
#171623=ORIENTED_EDGE ( 'NONE', *, *, #82726, .F. ) ;
#171666=CARTESIAN_POINT ( 'NONE',  ( 18.59999999999999076, 6.650000000011155876, -121.8500000000000369 ) ) ;
#171668=CARTESIAN_POINT ( 'NONE',  ( -18.59999999999999787, 11.65000000001115232, -112.6500000000000341 ) ) ;
#171669=ADVANCED_FACE ( 'NONE', ( #2763 ), #238829, .T. ) ;
#171690=CARTESIAN_POINT ( 'NONE',  ( 21.04999999999999716, 8.871279686006802834, -109.0586289951409498 ) ) ;
#171703=CIRCLE ( 'NONE', #59195, 0.1000000000000028644 ) ;
#171706=CARTESIAN_POINT ( 'NONE',  ( 18.59999999999999076, 11.75000000001115907, -88.75000000000004263 ) ) ;
#171708=CARTESIAN_POINT ( 'NONE',  ( -21.05000000000000071, -1.162701749926853712, -108.6000000000000227 ) ) ;
#171718=CYLINDRICAL_SURFACE ( 'NONE', #22048, 0.09999999999999939493 ) ;
#171720=CARTESIAN_POINT ( 'NONE',  ( 23.14999999999999858, 5.900000000011162093, -123.7809002353436654 ) ) ;
#171766=TOROIDAL_SURFACE ( 'NONE', #205022, 3.899999999999999467, 0.1000000000000000056 ) ;
#171773=EDGE_CURVE ( 'NONE', #43551, #234552, #48352, .T. ) ;
#171776=AXIS2_PLACEMENT_3D ( 'NONE', #147361, #89943, #209919 ) ;
#171798=AXIS2_PLACEMENT_3D ( 'NONE', #92609, #169647, #249153 ) ;
#171805=CIRCLE ( 'NONE', #17629, 0.1000000000000000472 ) ;
#171841=CARTESIAN_POINT ( 'NONE',  ( 18.59999999999998721, 19.85039924724470950, -102.7803030578013903 ) ) ;
#171893=CARTESIAN_POINT ( 'NONE',  ( 23.14999999999999503, 11.65000000001116298, -121.8500000000000369 ) ) ;
#171899=CARTESIAN_POINT ( 'NONE',  ( -18.60000000000000853, -9.364240527579751117, -107.6802485818408002 ) ) ;
#171901=DIRECTION ( 'NONE',  ( 0.000000000000000000, 0.000000000000000000, 1.000000000000000000 ) ) ;
#171912=CARTESIAN_POINT ( 'NONE',  ( -20.64999999999999858, 1.115625160336667635E-11, -136.0000000000000284 ) ) ;
#171950=DIRECTION ( 'NONE',  ( -1.000000000000000000, -0.000000000000000000, -0.000000000000000000 ) ) ;
#171978=SURFACE_SIDE_STYLE ('',( #110676 ) ) ;
#172007=CYLINDRICAL_SURFACE ( 'NONE', #22765, 0.1000000000000101918 ) ;
#172023=DIRECTION ( 'NONE',  ( 0.000000000000000000, -0.8068669527897506244, -0.5907332058516622242 ) ) ;
#172025=CARTESIAN_POINT ( 'NONE',  ( -22.50000000000000000, 1.115600667400684642E-11, -100.4000000000000341 ) ) ;
#172064=CYLINDRICAL_SURFACE ( 'NONE', #10734, 7.899999999999990585 ) ;
#172068=CARTESIAN_POINT ( 'NONE',  ( 20.95512820512820440, 8.876151316299271343, -109.0586289951409924 ) ) ;
#172069=CARTESIAN_POINT ( 'NONE',  ( -18.50000000000000000, -1.162701749926853712, -108.6000000000000227 ) ) ;
#172072=FACE_OUTER_BOUND ( 'NONE', #89179, .T. ) ;
#172118=AXIS2_PLACEMENT_3D ( 'NONE', #177962, #116683, #196219 ) ;
#172133=CARTESIAN_POINT ( 'NONE',  ( 18.43466021071414929, -9.494190690445382330, -140.6170615601278939 ) ) ;
#172143=ORIENTED_EDGE ( 'NONE', *, *, #181352, .T. ) ;
#172152=EDGE_CURVE ( 'NONE', #90910, #26647, #160299, .T. ) ;
#172177=CARTESIAN_POINT ( 'NONE',  ( 22.60000000000000142, 0.1008583691098682150, -88.75043287651064361 ) ) ;
#172197=ORIENTED_EDGE ( 'NONE', *, *, #64632, .T. ) ;
#172211=CIRCLE ( 'NONE', #163786, 0.1000000000000002554 ) ;
#172268=AXIS2_PLACEMENT_3D ( 'NONE', #37272, #54234, #38541 ) ;
#172271=AXIS2_PLACEMENT_3D ( 'NONE', #53777, #132031, #211579 ) ;
#172291=VERTEX_POINT ( 'NONE', #29782 ) ;
#172324=CIRCLE ( 'NONE', #218043, 0.1000000000000028644 ) ;
#172343=ORIENTED_EDGE ( 'NONE', *, *, #73923, .T. ) ;
#172421=VERTEX_POINT ( 'NONE', #34915 ) ;
#172427=DIRECTION ( 'NONE',  ( 0.000000000000000000, -0.8660254037844411501, -0.4999999999999956701 ) ) ;
#172458=DIRECTION ( 'NONE',  ( -1.000000000000000000, 0.000000000000000000, 0.000000000000000000 ) ) ;
#172474=EDGE_CURVE ( 'NONE', #208598, #101037, #120865, .T. ) ;
#172489=DIRECTION ( 'NONE',  ( -0.000000000000000000, 0.000000000000000000, -1.000000000000000000 ) ) ;
#172577=CARTESIAN_POINT ( 'NONE',  ( 20.85000000000000142, 6.933893972137497030, -137.7856458343736108 ) ) ;
#172593=DIRECTION ( 'NONE',  ( -1.000000000000000000, -3.265361837132813093E-16, 0.000000000000000000 ) ) ;
#172644=CARTESIAN_POINT ( 'NONE',  ( 21.00000000000000000, 9.750000000011153745, -112.8500000000000369 ) ) ;
#172652=DIRECTION ( 'NONE',  ( 0.000000000000000000, 0.000000000000000000, 1.000000000000000000 ) ) ;
#172664=CARTESIAN_POINT ( 'NONE',  ( 21.14999999999999858, 11.65000000001116298, -88.75000000000004263 ) ) ;
#172681=EDGE_LOOP ( 'NONE', ( #117367, #98429, #29006, #181252 ) ) ;
#172685=EDGE_CURVE ( 'NONE', #234219, #168502, #198180, .T. ) ;
#172696=VERTEX_POINT ( 'NONE', #39414 ) ;
#172704=EDGE_CURVE ( 'NONE', #95681, #254324, #55065, .T. ) ;
#172706=DIRECTION ( 'NONE',  ( -1.000000000000000000, 0.000000000000000000, 0.000000000000000000 ) ) ;
#172710=DIRECTION ( 'NONE',  ( 0.000000000000000000, 0.9998779222360096863, -0.01562500000001061998 ) ) ;
#172711=AXIS2_PLACEMENT_3D ( 'NONE', #197238, #177712, #90735 ) ;
#172714=VERTEX_POINT ( 'NONE', #198451 ) ;
#172737=DIRECTION ( 'NONE',  ( -0.000000000000000000, -0.000000000000000000, -1.000000000000000000 ) ) ;
#172784=DIRECTION ( 'NONE',  ( -0.000000000000000000, -1.000000000000000000, 6.308085367188393199E-16 ) ) ;
#172785=CARTESIAN_POINT ( 'NONE',  ( 20.44999100639894962, 10.43971070322319683, -108.2590757259705612 ) ) ;
#172789=CARTESIAN_POINT ( 'NONE',  ( 18.49999999999998934, 6.550000000011156231, -121.6500000000000341 ) ) ;
#172822=VERTEX_POINT ( 'NONE', #35196 ) ;
#172839=CARTESIAN_POINT ( 'NONE',  ( -21.64999999999999858, 7.250000000011148416, -112.7500000000000284 ) ) ;
#172840=CARTESIAN_POINT ( 'NONE',  ( -21.05000000000000071, 1.115600667400684642E-11, -134.0000000000000284 ) ) ;
#172864=FACE_OUTER_BOUND ( 'NONE', #94062, .T. ) ;
#172899=LINE ( 'NONE', #30799, #5429 ) ;
#172903=ORIENTED_EDGE ( 'NONE', *, *, #69103, .T. ) ;
#172910=CARTESIAN_POINT ( 'NONE',  ( -18.50000000000000000, 11.65000000001115232, -112.6500000000000341 ) ) ;
#172920=EDGE_CURVE ( 'NONE', #102643, #204472, #152422, .T. ) ;
#172960=DIRECTION ( 'NONE',  ( 0.000000000000000000, -1.000000000000000000, -0.000000000000000000 ) ) ;
#172974=CARTESIAN_POINT ( 'NONE',  ( -23.15000000000000213, 4.350000000011156054, -121.8500000000000369 ) ) ;
#173015=CARTESIAN_POINT ( 'NONE',  ( -23.15000000000000213, 11.65000000001115588, -112.6500000000000341 ) ) ;
#173079=ORIENTED_EDGE ( 'NONE', *, *, #158867, .F. ) ;
#173084=FACE_OUTER_BOUND ( 'NONE', #34972, .T. ) ;
#173112=ORIENTED_EDGE ( 'NONE', *, *, #64866, .T. ) ;
#173147=DIRECTION ( 'NONE',  ( -3.265361837132813093E-16, 1.000000000000000000, -0.000000000000000000 ) ) ;
#173160=CARTESIAN_POINT ( 'NONE',  ( 23.15000000000000213, -11.48912529306489994, -130.9000000000000341 ) ) ;
#173164=VERTEX_POINT ( 'NONE', #192642 ) ;
#173181=CARTESIAN_POINT ( 'NONE',  ( -20.54999999999999716, 1.115600667400684642E-11, -134.0000000000000284 ) ) ;
#173201=CIRCLE ( 'NONE', #206458, 4.099999999999992539 ) ;
#173205=CIRCLE ( 'NONE', #42755, 0.1000000000000028644 ) ;
#173216=CARTESIAN_POINT ( 'NONE',  ( 21.04116576186302368, 10.62466307876251292, -112.8285817686274299 ) ) ;
#173234=CARTESIAN_POINT ( 'NONE',  ( -21.64999999999999858, 7.350000000011155166, -121.6500000000000341 ) ) ;
#173256=CARTESIAN_POINT ( 'NONE',  ( 21.05000000000000071, -11.39257802169451139, -130.9260504201681101 ) ) ;
#173258=UNCERTAINTY_MEASURE_WITH_UNIT (LENGTH_MEASURE( 1.000000000000000082E-05 ), #7251, 'distance_accuracy_value', 'NONE');
#173350=ORIENTED_EDGE ( 'NONE', *, *, #54012, .T. ) ;
#173364=CARTESIAN_POINT ( 'NONE',  ( 21.08750232978087524, 10.72486338602132250, -112.7288581729996224 ) ) ;
#173366=DIRECTION ( 'NONE',  ( 1.000000000000000000, 0.000000000000000000, 0.000000000000000000 ) ) ;
#173371=VERTEX_POINT ( 'NONE', #55647 ) ;
#173372=ORIENTED_EDGE ( 'NONE', *, *, #46095, .F. ) ;
#173413=ADVANCED_FACE ( 'NONE', ( #82918 ), #166377, .T. ) ;
#173425=FACE_OUTER_BOUND ( 'NONE', #99491, .T. ) ;
#173431=CARTESIAN_POINT ( 'NONE',  ( -23.25000000000000000, 1.910280373842936141, -113.1313678551989739 ) ) ;
#173463=CARTESIAN_POINT ( 'NONE',  ( -21.05000000000000071, 1.250000000011155299, -108.5000000000000426 ) ) ;
#173478=DIRECTION ( 'NONE',  ( -1.000000000000000000, 0.000000000000000000, 0.000000000000000000 ) ) ;
#173486=CARTESIAN_POINT ( 'NONE',  ( 20.94999999999999929, 10.29288807859936838, -139.4580020160122160 ) ) ;
#173505=CARTESIAN_POINT ( 'NONE',  ( 21.05000000000000071, 1.115625160336667635E-11, -132.0000000000000284 ) ) ;
#173525=ORIENTED_EDGE ( 'NONE', *, *, #148579, .T. ) ;
#173551=VERTEX_POINT ( 'NONE', #129774 ) ;
#173583=AXIS2_PLACEMENT_3D ( 'NONE', #115282, #155732, #138663 ) ;
#173587=EDGE_CURVE ( 'NONE', #141245, #154382, #19502, .T. ) ;
#173626=EDGE_CURVE ( 'NONE', #46494, #120853, #61492, .T. ) ;
#173635=AXIS2_PLACEMENT_3D ( 'NONE', #193590, #194887, #14963 ) ;
#173650=VERTEX_POINT ( 'NONE', #142299 ) ;
#173651=DIRECTION ( 'NONE',  ( 1.000000000000000000, 0.000000000000000000, 0.000000000000000000 ) ) ;
#173660=DIRECTION ( 'NONE',  ( 0.000000000000000000, 0.000000000000000000, -1.000000000000000000 ) ) ;
#173670=VERTEX_POINT ( 'NONE', #94494 ) ;
#173681=CIRCLE ( 'NONE', #215309, 0.1999999999999996503 ) ;
#173720=CARTESIAN_POINT ( 'NONE',  ( 21.05000000000000071, 8.826429739528350638, -108.9140547129437380 ) ) ;
#173725=VECTOR ( 'NONE', #90993, 1000.000000000000000 ) ;
#173739=VECTOR ( 'NONE', #60236, 1000.000000000000000 ) ;
#173746=VERTEX_POINT ( 'NONE', #104435 ) ;
#173773=ADVANCED_FACE ( 'NONE', ( #207438 ), #189140, .F. ) ;
#173785=EDGE_CURVE ( 'NONE', #23430, #94061, #184001, .T. ) ;
#173790=VERTEX_POINT ( 'NONE', #153921 ) ;
#173843=DIRECTION ( 'NONE',  ( -1.000000000000000000, -1.836970198721029934E-16, 0.000000000000000000 ) ) ;
#173864=CARTESIAN_POINT ( 'NONE',  ( -20.85000000000000142, 1.115600667400684642E-11, -134.0000000000000284 ) ) ;
#173893=CIRCLE ( 'NONE', #223696, 0.1000000000000028644 ) ;
#173908=CIRCLE ( 'NONE', #23854, 4.099999999999992539 ) ;
#173923=ORIENTED_EDGE ( 'NONE', *, *, #22318, .F. ) ;
#173953=DIRECTION ( 'NONE',  ( 0.000000000000000000, 0.000000000000000000, -1.000000000000000000 ) ) ;
#173975=ORIENTED_EDGE ( 'NONE', *, *, #167549, .T. ) ;
#174008=ORIENTED_EDGE ( 'NONE', *, *, #26756, .T. ) ;
#174009=FACE_OUTER_BOUND ( 'NONE', #252610, .T. ) ;
#174029=CARTESIAN_POINT ( 'NONE',  ( -21.05000000000000071, -11.64999999998884483, -103.4000000000000341 ) ) ;
#174049=ORIENTED_EDGE ( 'NONE', *, *, #54348, .F. ) ;
#174055=ORIENTED_EDGE ( 'NONE', *, *, #58797, .T. ) ;
#174074=DIRECTION ( 'NONE',  ( -1.000000000000000000, 0.000000000000000000, 0.000000000000000000 ) ) ;
#174082=EDGE_LOOP ( 'NONE', ( #68748, #33282, #78295, #87028 ) ) ;
#174093=ORIENTED_EDGE ( 'NONE', *, *, #13256, .F. ) ;
#174117=AXIS2_PLACEMENT_3D ( 'NONE', #175332, #254785, #198712 ) ;
#174118=FACE_OUTER_BOUND ( 'NONE', #205086, .T. ) ;
#174141=DIRECTION ( 'NONE',  ( 0.000000000000000000, 0.000000000000000000, -1.000000000000000000 ) ) ;
#174172=DIRECTION ( 'NONE',  ( 1.000000000000000000, 2.952720810173289112E-16, -0.000000000000000000 ) ) ;
#174185=ORIENTED_EDGE ( 'NONE', *, *, #101413, .F. ) ;
#174218=ORIENTED_EDGE ( 'NONE', *, *, #22678, .F. ) ;
#174246=EDGE_CURVE ( 'NONE', #200055, #72387, #219742, .T. ) ;
#174301=CARTESIAN_POINT ( 'NONE',  ( 18.57399277249656322, 10.33112638556969820, -139.5901228926975080 ) ) ;
#174302=EDGE_LOOP ( 'NONE', ( #61113, #196742, #94204, #2593 ) ) ;
#174317=CIRCLE ( 'NONE', #220057, 0.09999999999999967248 ) ;
#174326=ORIENTED_EDGE ( 'NONE', *, *, #17536, .T. ) ;
#174327=AXIS2_PLACEMENT_3D ( 'NONE', #165036, #86760, #248428 ) ;
#174363=ORIENTED_EDGE ( 'NONE', *, *, #227037, .F. ) ;
#174372=ORIENTED_EDGE ( 'NONE', *, *, #1658, .T. ) ;
#174459=ORIENTED_EDGE ( 'NONE', *, *, #161251, .F. ) ;
#174472=EDGE_CURVE ( 'NONE', #173790, #27558, #103212, .T. ) ;
#174478=AXIS2_PLACEMENT_3D ( 'NONE', #44554, #204883, #225719 ) ;
#174490=EDGE_LOOP ( 'NONE', ( #55648, #163135, #63708, #183047, #94364, #208828, #104181, #249923, #13695 ) ) ;
#174505=CARTESIAN_POINT ( 'NONE',  ( -18.59999999999999787, -1.851028230129704522, -112.1539132694225316 ) ) ;
#174517=DIRECTION ( 'NONE',  ( 0.000000000000000000, 0.000000000000000000, 1.000000000000000000 ) ) ;
#174582=EDGE_CURVE ( 'NONE', #144465, #208590, #53349, .T. ) ;
#174591=ORIENTED_EDGE ( 'NONE', *, *, #208411, .F. ) ;
#174609=CARTESIAN_POINT ( 'NONE',  ( 18.59999999999999076, 11.75000000001115907, -125.3500000000000512 ) ) ;
#174652=CARTESIAN_POINT ( 'NONE',  ( 21.13507111622890022, 10.71768338700954537, -112.7491685863608382 ) ) ;
#174655=CIRCLE ( 'NONE', #12311, 0.6000000000000033085 ) ;
#174659=ORIENTED_EDGE ( 'NONE', *, *, #213451, .F. ) ;
#174691=CIRCLE ( 'NONE', #128867, 12.87499999999999822 ) ;
#174701=ORIENTED_EDGE ( 'NONE', *, *, #118809, .F. ) ;
#174717=AXIS2_PLACEMENT_3D ( 'NONE', #156669, #234898, #56226 ) ;
#174740=CYLINDRICAL_SURFACE ( 'NONE', #119073, 0.09999999999999939493 ) ;
#174770=AXIS2_PLACEMENT_3D ( 'NONE', #257722, #116993, #42583 ) ;
#174781=VERTEX_POINT ( 'NONE', #61848 ) ;
#174794=CARTESIAN_POINT ( 'NONE',  ( 21.05000000000000071, 10.72371710471867701, -112.6500000000000341 ) ) ;
#174798=CARTESIAN_POINT ( 'NONE',  ( -18.59999999999999787, 11.65000000001115232, -121.8500000000000369 ) ) ;
#174841=CIRCLE ( 'NONE', #216282, 11.74999999999999645 ) ;
#174889=ORIENTED_EDGE ( 'NONE', *, *, #42676, .T. ) ;
#174925=DIRECTION ( 'NONE',  ( 0.000000000000000000, 0.000000000000000000, -1.000000000000000000 ) ) ;
#174953=DIRECTION ( 'NONE',  ( 0.000000000000000000, 0.000000000000000000, -1.000000000000000000 ) ) ;
#174957=EDGE_LOOP ( 'NONE', ( #155290, #151359, #211375 ) ) ;
#174958=DIRECTION ( 'NONE',  ( -0.000000000000000000, -0.000000000000000000, 1.000000000000000000 ) ) ;
#174970=DIRECTION ( 'NONE',  ( 1.000000000000000000, 0.000000000000000000, 0.000000000000000000 ) ) ;
#175000=ORIENTED_EDGE ( 'NONE', *, *, #37645, .F. ) ;
#175012=TOROIDAL_SURFACE ( 'NONE', #16761, 7.791421356237316687, 0.1000000000000000056 ) ;
#175026=CIRCLE ( 'NONE', #179281, 0.1000000000000002554 ) ;
#175030=EDGE_LOOP ( 'NONE', ( #75805, #99115, #58986, #141639, #69160 ) ) ;
#175033=CARTESIAN_POINT ( 'NONE',  ( -21.08035267497491816, 0.08268862478717949049, -94.16829316021699015 ) ) ;
#175052=DIRECTION ( 'NONE',  ( 1.000000000000000000, 0.000000000000000000, 0.000000000000000000 ) ) ;
#175060=DIRECTION ( 'NONE',  ( 0.000000000000000000, -0.000000000000000000, 1.000000000000000000 ) ) ;
#175104=CARTESIAN_POINT ( 'NONE',  ( -2.995603634470891112E-16, -11.74999999998884448, -112.7500000000000284 ) ) ;
#175119=DIRECTION ( 'NONE',  ( 0.000000000000000000, 0.000000000000000000, -1.000000000000000000 ) ) ;
#175142=CARTESIAN_POINT ( 'NONE',  ( -18.50000000000000000, 10.29270135741298375, -139.4573618871519614 ) ) ;
#175148=FACE_OUTER_BOUND ( 'NONE', #6475, .T. ) ;
#175163=ADVANCED_FACE ( 'NONE', ( #18564 ), #98053, .F. ) ;
#175184=DIRECTION ( 'NONE',  ( 2.952720810173289112E-16, -1.000000000000000000, 0.000000000000000000 ) ) ;
#175200=EDGE_CURVE ( 'NONE', #104969, #163802, #121543, .T. ) ;
#175201=CIRCLE ( 'NONE', #162690, 0.2000000000000057288 ) ;
#175215=DIRECTION ( 'NONE',  ( 0.000000000000000000, -2.428612866367527723E-14, -1.000000000000000000 ) ) ;
#175250=ORIENTED_EDGE ( 'NONE', *, *, #182284, .F. ) ;
#175267=DIRECTION ( 'NONE',  ( 0.000000000000000000, 0.000000000000000000, -1.000000000000000000 ) ) ;
#175285=AXIS2_PLACEMENT_3D ( 'NONE', #250826, #232595, #55169 ) ;
#175293=DIRECTION ( 'NONE',  ( 0.000000000000000000, -1.000000000000000000, 0.000000000000000000 ) ) ;
#175332=CARTESIAN_POINT ( 'NONE',  ( -20.64999999999999858, 4.350000000011156054, -112.8500000000000369 ) ) ;
#175372=CARTESIAN_POINT ( 'NONE',  ( -20.86777300164945004, 10.33200063080771969, -139.5931674956643462 ) ) ;
#175384=DIRECTION ( 'NONE',  ( -1.000000000000000000, -0.000000000000000000, -0.000000000000000000 ) ) ;
#175386=LINE ( 'NONE', #155815, #185897 ) ;
#175398=ADVANCED_FACE ( 'NONE', ( #17918 ), #133029, .T. ) ;
#175444=CARTESIAN_POINT ( 'NONE',  ( -21.14999999999999858, 6.540656951712399803, -100.5000000000000284 ) ) ;
#175445=DIRECTION ( 'NONE',  ( 1.000000000000000000, 0.000000000000000000, 0.000000000000000000 ) ) ;
#175450=DIRECTION ( 'NONE',  ( -0.000000000000000000, 1.000000000000000000, -0.000000000000000000 ) ) ;
#175455=CIRCLE ( 'NONE', #92213, 0.09999999999999939493 ) ;
#175462=FACE_OUTER_BOUND ( 'NONE', #202200, .T. ) ;
#175535=ORIENTED_EDGE ( 'NONE', *, *, #200275, .T. ) ;
#175536=LINE ( 'NONE', #73880, #77662 ) ;
#175552=VERTEX_POINT ( 'NONE', #127298 ) ;
#175642=ORIENTED_EDGE ( 'NONE', *, *, #176756, .F. ) ;
#175647=AXIS2_PLACEMENT_3D ( 'NONE', #80425, #101258, #77888 ) ;
#175656=DIRECTION ( 'NONE',  ( -0.000000000000000000, 0.1350103645451626311, 0.9908441862701635738 ) ) ;
#175671=EDGE_CURVE ( 'NONE', #132129, #234753, #24709, .T. ) ;
#175711=EDGE_CURVE ( 'NONE', #51418, #208604, #116456, .T. ) ;
#175743=CARTESIAN_POINT ( 'NONE',  ( -23.25000000000000000, 7.021664781911246322, -137.8335654018973457 ) ) ;
#175765=EDGE_CURVE ( 'NONE', #153726, #66771, #62270, .T. ) ;
#175768=AXIS2_PLACEMENT_3D ( 'NONE', #129209, #190488, #146186 ) ;
#175786=( BOUNDED_SURFACE ( )  B_SPLINE_SURFACE ( 3, 2, ( 
 ( #85328, #67082, #187054 ),
 ( #164899, #127056, #147915 ),
 ( #207902, #50079, #25404 ),
 ( #166216, #84018, #227431 ),
 ( #48794, #209149, #146588 ),
 ( #65793, #47496, #103607 ),
 ( #145317, #7096, #183188 ),
 ( #206589, #128352, #46220 ) ),
 .UNSPECIFIED., .F., .F., .F. ) 
 B_SPLINE_SURFACE_WITH_KNOTS ( ( 4, 2, 2, 4 ),
 ( 3, 3 ),
 ( 0.0001723339234021411192, 0.0002782939632049912849, 0.0003842540030078414777, 0.0005961740826135418633 ),
 ( 0.000000000000000000, 1.000000000000000000 ),
 .UNSPECIFIED. ) 
 GEOMETRIC_REPRESENTATION_ITEM ( )  RATIONAL_B_SPLINE_SURFACE ( (
 ( 1.000000000000000000, 0.9504532311154628710, 1.000000000000000000),
 ( 1.000000000000000000, 0.9506023220709669541, 1.000000000000000000),
 ( 1.000000000000000000, 0.9395774818181893417, 1.000000000000000000),
 ( 1.000000000000000000, 0.9079328464647246077, 1.000000000000000000),
 ( 1.000000000000000000, 0.8875702416203912204, 1.000000000000000000),
 ( 1.000000000000000000, 0.8205919608043565905, 1.000000000000000000),
 ( 1.000000000000000000, 0.7666842783596220512, 1.000000000000000000),
 ( 1.000000000000000000, 0.7071067811864205632, 1.000000000000000000) ) ) 
 REPRESENTATION_ITEM ( '' )  SURFACE ( )  );
#175787=EDGE_LOOP ( 'NONE', ( #174055, #64787, #89678, #162508 ) ) ;
#175795=AXIS2_PLACEMENT_3D ( 'NONE', #180722, #2051, #41230 ) ;
#175803=CARTESIAN_POINT ( 'NONE',  ( -23.25000000000000000, 1.115600667400684642E-11, -134.0000000000000284 ) ) ;
#175809=DIRECTION ( 'NONE',  ( -0.000000000000000000, 0.6132151058540549204, -0.7899159663865520375 ) ) ;
#175818=CARTESIAN_POINT ( 'NONE',  ( 18.59999999999999787, 1.115600667400684642E-11, -100.5000000000000284 ) ) ;
#175835=EDGE_CURVE ( 'NONE', #217887, #174781, #162249, .T. ) ;
#175855=CARTESIAN_POINT ( 'NONE',  ( -23.15000000000000213, 2.000000000011154189, -120.7753780772379315 ) ) ;
#175888=EDGE_CURVE ( 'NONE', #109188, #201244, #145641, .T. ) ;
#175909=CARTESIAN_POINT ( 'NONE',  ( -20.94999999999999929, 1.115600667400684642E-11, -134.0000000000000284 ) ) ;
#175912=TOROIDAL_SURFACE ( 'NONE', #205087, 4.099999999999999645, 0.1000000000000000056 ) ;
#175955=EDGE_LOOP ( 'NONE', ( #58458, #124301, #225865, #168562 ) ) ;
#175957=AXIS2_PLACEMENT_3D ( 'NONE', #232827, #114128, #193685 ) ;
#175976=TOROIDAL_SURFACE ( 'NONE', #63499, 0.2000000000000000111, 0.1000000000000000056 ) ;
#176070=CARTESIAN_POINT ( 'NONE',  ( -20.94999999999999929, 11.70000000001115126, -127.2450018504814295 ) ) ;
#176082=EDGE_CURVE ( 'NONE', #133593, #81511, #249715, .T. ) ;
#176177=ORIENTED_EDGE ( 'NONE', *, *, #136041, .F. ) ;
#176182=DIRECTION ( 'NONE',  ( -0.000000000000000000, 0.000000000000000000, -1.000000000000000000 ) ) ;
#176216=AXIS2_PLACEMENT_3D ( 'NONE', #6887, #86394, #143818 ) ;
#176233=DIRECTION ( 'NONE',  ( 0.000000000000000000, 0.000000000000000000, -1.000000000000000000 ) ) ;
#176246=EDGE_CURVE ( 'NONE', #54036, #34960, #137447, .T. ) ;
#176250=AXIS2_PLACEMENT_3D ( 'NONE', #39850, #60648, #240591 ) ;
#176255=ORIENTED_EDGE ( 'NONE', *, *, #232207, .T. ) ;
#176322=AXIS2_PLACEMENT_3D ( 'NONE', #241243, #26046, #202108 ) ;
#176351=ORIENTED_EDGE ( 'NONE', *, *, #239012, .T. ) ;
#176358=ORIENTED_EDGE ( 'NONE', *, *, #250503, .F. ) ;
#176364=ORIENTED_EDGE ( 'NONE', *, *, #113272, .T. ) ;
#176395=CARTESIAN_POINT ( 'NONE',  ( -18.59117750673696889, 10.33248238083634796, -139.5948465439131780 ) ) ;
#176397=FACE_OUTER_BOUND ( 'NONE', #233337, .T. ) ;
#176429=DIRECTION ( 'NONE',  ( 0.000000000000000000, 0.000000000000000000, -1.000000000000000000 ) ) ;
#176435=DIRECTION ( 'NONE',  ( 0.000000000000000000, 0.9908441862701596881, -0.1350103645451904977 ) ) ;
#176440=FACE_OUTER_BOUND ( 'NONE', #85085, .T. ) ;
#176442=CARTESIAN_POINT ( 'NONE',  ( 21.33487959338958362, 6.725558151922348848, -100.5000000000000284 ) ) ;
#176464=CARTESIAN_POINT ( 'NONE',  ( -18.59999999999999787, -1.164121893230052995, -141.9148480855716343 ) ) ;
#176491=AXIS2_PLACEMENT_3D ( 'NONE', #228034, #149806, #248889 ) ;
#176535=VECTOR ( 'NONE', #61289, 1000.000000000000000 ) ;
#176565=DIRECTION ( 'NONE',  ( -3.265361837132813093E-16, 1.000000000000000000, 0.000000000000000000 ) ) ;
#176605=CARTESIAN_POINT ( 'NONE',  ( -20.54999999999999716, 1.115600667400684642E-11, -132.0000000000000284 ) ) ;
#176614=EDGE_CURVE ( 'NONE', #243325, #61948, #197104, .T. ) ;
#176617=CARTESIAN_POINT ( 'NONE',  ( 20.94999999999999929, 1.115649653272650466E-11, -130.0000000000000284 ) ) ;
#176626=ORIENTED_EDGE ( 'NONE', *, *, #175888, .T. ) ;
#176631=ORIENTED_EDGE ( 'NONE', *, *, #5272, .F. ) ;
#176635=TOROIDAL_SURFACE ( 'NONE', #22519, 0.4000000000000009104, 0.1000000000000000056 ) ;
#176642=DIRECTION ( 'NONE',  ( -1.000000000000000000, -0.000000000000000000, 0.000000000000000000 ) ) ;
#176694=CYLINDRICAL_SURFACE ( 'NONE', #225372, 0.1000000000000028644 ) ;
#176703=CARTESIAN_POINT ( 'NONE',  ( 21.05000000000000071, 1.115600667400684642E-11, -134.0000000000000284 ) ) ;
#176709=AXIS2_PLACEMENT_3D ( 'NONE', #119200, #63056, #121779 ) ;
#176710=AXIS2_PLACEMENT_3D ( 'NONE', #81445, #197561, #217108 ) ;
#176732=DIRECTION ( 'NONE',  ( -1.000000000000000000, -0.000000000000000000, 0.000000000000000000 ) ) ;
#176756=EDGE_CURVE ( 'NONE', #189704, #140720, #42436, .T. ) ;
#176820=DIRECTION ( 'NONE',  ( 0.000000000000000000, 0.9274965247785529332, 0.3738317757009255171 ) ) ;
#176830=ORIENTED_EDGE ( 'NONE', *, *, #54816, .F. ) ;
#176832=LINE ( 'NONE', #236771, #106902 ) ;
#176835=ADVANCED_FACE ( 'NONE', ( #7921 ), #253457, .T. ) ;
#176853=ORIENTED_EDGE ( 'NONE', *, *, #146274, .T. ) ;
#176862=VERTEX_POINT ( 'NONE', #194274 ) ;
#176890=ORIENTED_EDGE ( 'NONE', *, *, #123252, .T. ) ;
#176962=DIRECTION ( 'NONE',  ( 1.000000000000000000, 0.000000000000000000, 0.000000000000000000 ) ) ;
#176967=CYLINDRICAL_SURFACE ( 'NONE', #81407, 0.09999999999999693856 ) ;
#176975=CIRCLE ( 'NONE', #247678, 0.09999999999999939493 ) ;
#176979=EDGE_CURVE ( 'NONE', #35530, #210115, #167554, .T. ) ;
#176999=EDGE_CURVE ( 'NONE', #108506, #64218, #96763, .T. ) ;
#177002=VERTEX_POINT ( 'NONE', #157736 ) ;
#177043=DIRECTION ( 'NONE',  ( -1.000000000000000000, 0.000000000000000000, 0.000000000000000000 ) ) ;
#177063=DIRECTION ( 'NONE',  ( 1.000000000000000000, 6.938893903907222067E-15, 0.000000000000000000 ) ) ;
#177066=DIRECTION ( 'NONE',  ( 1.000000000000000000, 0.000000000000000000, 0.000000000000000000 ) ) ;
#177111=DIRECTION ( 'NONE',  ( 0.000000000000000000, 1.000000000000000000, 0.000000000000000000 ) ) ;
#177120=FACE_OUTER_BOUND ( 'NONE', #166054, .T. ) ;
#177123=FACE_OUTER_BOUND ( 'NONE', #170582, .T. ) ;
#177144=ORIENTED_EDGE ( 'NONE', *, *, #39106, .F. ) ;
#177165=EDGE_CURVE ( 'NONE', #4043, #255700, #227929, .T. ) ;
#177186=CYLINDRICAL_SURFACE ( 'NONE', #112649, 2.000000000000001776 ) ;
#177191=CARTESIAN_POINT ( 'NONE',  ( -20.54999999999999716, -8.999999999988846255, -110.3939691226524786 ) ) ;
#177199=DIRECTION ( 'NONE',  ( 0.000000000000000000, 0.000000000000000000, -1.000000000000000000 ) ) ;
#177222=DIRECTION ( 'NONE',  ( -1.000000000000000000, 0.000000000000000000, 0.000000000000000000 ) ) ;
#177258=DIRECTION ( 'NONE',  ( 0.7071067811865388020, -0.7071067811865561215, 0.000000000000000000 ) ) ;
#177264=VECTOR ( 'NONE', #20333, 1000.000000000000000 ) ;
#177287=CARTESIAN_POINT ( 'NONE',  ( -22.44366136229477249, 0.009341569497225227225, -88.85028144252612492 ) ) ;
#177312=DIRECTION ( 'NONE',  ( 0.000000000000000000, -1.000000000000000000, 0.000000000000000000 ) ) ;
#177319=DIRECTION ( 'NONE',  ( 0.000000000000000000, 0.000000000000000000, 1.000000000000000000 ) ) ;
#177345=ORIENTED_EDGE ( 'NONE', *, *, #152182, .T. ) ;
#177351=VERTEX_POINT ( 'NONE', #101203 ) ;
#177362=CARTESIAN_POINT ( 'NONE',  ( 18.49999999999999289, 10.37342005529114886, -125.2657881246251037 ) ) ;
#177380=DIRECTION ( 'NONE',  ( 1.000000000000000000, 0.000000000000000000, 0.000000000000000000 ) ) ;
#177385=EDGE_CURVE ( 'NONE', #203793, #256334, #115582, .T. ) ;
#177405=DIRECTION ( 'NONE',  ( 0.000000000000000000, 0.000000000000000000, -1.000000000000000000 ) ) ;
#177420=CARTESIAN_POINT ( 'NONE',  ( 21.04105312098514347, 8.875332623054768888, -112.8285067472120602 ) ) ;
#177453=VERTEX_POINT ( 'NONE', #165076 ) ;
#177460=CARTESIAN_POINT ( 'NONE',  ( -23.15000000000000213, -11.41227409413852811, -131.0000000000000284 ) ) ;
#177469=CARTESIAN_POINT ( 'NONE',  ( 20.94999999999999929, 1.835341550235569663, -112.0551512925630249 ) ) ;
#177477=EDGE_LOOP ( 'NONE', ( #166448, #52440, #211877, #103073 ) ) ;
#177485=ADVANCED_FACE ( 'NONE', ( #107663 ), #77979, .F. ) ;
#177495=ORIENTED_EDGE ( 'NONE', *, *, #100397, .F. ) ;
#177508=ORIENTED_EDGE ( 'NONE', *, *, #55907, .T. ) ;
#177524=VERTEX_POINT ( 'NONE', #5984 ) ;
#177529=AXIS2_PLACEMENT_3D ( 'NONE', #61862, #64431, #141383 ) ;
#177543=FACE_OUTER_BOUND ( 'NONE', #132531, .T. ) ;
#177643=DIRECTION ( 'NONE',  ( -1.000000000000000000, -0.000000000000000000, -0.000000000000000000 ) ) ;
#177646=LINE ( 'NONE', #55067, #4241 ) ;
#177667=CARTESIAN_POINT ( 'NONE',  ( -20.85000000000000142, 7.021664781911246322, -137.8335654018973457 ) ) ;
#177672=DIRECTION ( 'NONE',  ( 0.000000000000000000, 4.440892098500570153E-15, -1.000000000000000000 ) ) ;
#177687=CARTESIAN_POINT ( 'NONE',  ( -18.54148534481894472, 10.32532329027886320, -139.5699343018359855 ) ) ;
#177692=ORIENTED_EDGE ( 'NONE', *, *, #166379, .F. ) ;
#177703=VERTEX_POINT ( 'NONE', #228906 ) ;
#177712=DIRECTION ( 'NONE',  ( -0.000000000000000000, 0.1350103645451649625, -0.9908441862701631297 ) ) ;
#177750=ORIENTED_EDGE ( 'NONE', *, *, #181352, .F. ) ;
#177762=ADVANCED_FACE ( 'NONE', ( #116653 ), #159639, .T. ) ;
#177901=CARTESIAN_POINT ( 'NONE',  ( 21.05000000000000071, -0.09999993529482512078, -94.02192177890532321 ) ) ;
#177910=( NAMED_UNIT ( * ) PLANE_ANGLE_UNIT ( ) SI_UNIT ( $, .RADIAN. ) );
#177916=CARTESIAN_POINT ( 'NONE',  ( -23.25000000000000000, 11.65000000001115588, -88.75000000000004263 ) ) ;
#177946=EDGE_CURVE ( 'NONE', #247064, #79682, #190627, .T. ) ;
#177947=LINE ( 'NONE', #97064, #117079 ) ;
#177948=CIRCLE ( 'NONE', #236194, 0.09999999999999939493 ) ;
#177958=FACE_OUTER_BOUND ( 'NONE', #24356, .T. ) ;
#177962=CARTESIAN_POINT ( 'NONE',  ( 23.14999999999999147, 1.115600667400684642E-11, -100.5000000000000284 ) ) ;
#177979=CARTESIAN_POINT ( 'NONE',  ( 23.14999999999999503, 6.450000000011156587, -112.8500000000000369 ) ) ;
#177986=VECTOR ( 'NONE', #160454, 1000.000000000000000 ) ;
#178020=DIRECTION ( 'NONE',  ( 1.000000000000000000, -0.000000000000000000, -0.000000000000000000 ) ) ;
#178024=AXIS2_PLACEMENT_3D ( 'NONE', #25202, #125562, #162144 ) ;
#178068=CARTESIAN_POINT ( 'NONE',  ( 20.04142135623730070, 11.65000000001115943, -88.75000000000004263 ) ) ;
#178080=ORIENTED_EDGE ( 'NONE', *, *, #27298, .F. ) ;
#178097=CIRCLE ( 'NONE', #69768, 12.97499999999998721 ) ;
#178099=CARTESIAN_POINT ( 'NONE',  ( -22.01447462590972748, 7.263800201241075172, -100.4009629999405036 ) ) ;
#178116=EDGE_CURVE ( 'NONE', #195772, #46245, #38114, .T. ) ;
#178126=ORIENTED_EDGE ( 'NONE', *, *, #80610, .T. ) ;
#178154=ADVANCED_FACE ( 'NONE', ( #120243 ), #115069, .F. ) ;
#178164=CARTESIAN_POINT ( 'NONE',  ( -20.54999999999999716, 2.500000000011154633, -120.7753780772379315 ) ) ;
#178172=AXIS2_PLACEMENT_3D ( 'NONE', #65543, #164663, #125526 ) ;
#178178=ORIENTED_EDGE ( 'NONE', *, *, #158772, .T. ) ;
#178187=ORIENTED_EDGE ( 'NONE', *, *, #46954, .T. ) ;
#178207=EDGE_CURVE ( 'NONE', #172822, #242007, #240299, .T. ) ;
#178226=CARTESIAN_POINT ( 'NONE',  ( -20.94999999999999929, 1.115600667400684642E-11, -134.0000000000000284 ) ) ;
#178230=AXIS2_PLACEMENT_3D ( 'NONE', #193320, #73397, #248148 ) ;
#178245=FACE_OUTER_BOUND ( 'NONE', #155973, .T. ) ;
#178249=ORIENTED_EDGE ( 'NONE', *, *, #256873, .T. ) ;
#178258=FACE_OUTER_BOUND ( 'NONE', #165436, .T. ) ;
#178264=ORIENTED_EDGE ( 'NONE', *, *, #249532, .F. ) ;
#178269=CARTESIAN_POINT ( 'NONE',  ( 19.99999999999998934, 11.75000000001115552, -121.8500000000000369 ) ) ;
#178271=DIRECTION ( 'NONE',  ( 1.000000000000000000, 0.000000000000000000, 0.000000000000000000 ) ) ;
#178277=DIRECTION ( 'NONE',  ( 0.000000000000000000, 0.000000000000000000, -1.000000000000000000 ) ) ;
#178287=CARTESIAN_POINT ( 'NONE',  ( -22.47071067811865319, 1.115600667400684642E-11, -100.5000000000000284 ) ) ;
#178295=CIRCLE ( 'NONE', #224226, 4.049999999999998046 ) ;
#178353=AXIS2_PLACEMENT_3D ( 'NONE', #98582, #233034, #217268 ) ;
#178357=ORIENTED_EDGE ( 'NONE', *, *, #20206, .F. ) ;
#178369=PLANE ( 'NONE',  #221660 ) ;
#178377=ORIENTED_EDGE ( 'NONE', *, *, #150224, .F. ) ;
#178398=ORIENTED_EDGE ( 'NONE', *, *, #30896, .T. ) ;
#178439=FACE_OUTER_BOUND ( 'NONE', #105150, .T. ) ;
#178454=EDGE_LOOP ( 'NONE', ( #96875, #41015, #1118, #110233 ) ) ;
#178457=CARTESIAN_POINT ( 'NONE',  ( -20.05000000000000426, 9.250000000011157297, -121.6500000000000341 ) ) ;
#178513=CARTESIAN_POINT ( 'NONE',  ( 20.94999999999999929, 1.115600667400684642E-11, -134.0000000000000284 ) ) ;
#178514=DIRECTION ( 'NONE',  ( -1.000000000000000000, 0.000000000000000000, 0.000000000000000000 ) ) ;
#178531=FACE_OUTER_BOUND ( 'NONE', #135249, .T. ) ;
#178546=AXIS2_PLACEMENT_3D ( 'NONE', #148709, #49595, #202252 ) ;
#178547=ORIENTED_EDGE ( 'NONE', *, *, #186812, .F. ) ;
#178550=CIRCLE ( 'NONE', #61998, 0.1000000000000008937 ) ;
#178557=DIRECTION ( 'NONE',  ( 0.000000000000000000, 0.000000000000000000, -1.000000000000000000 ) ) ;
#178590=ADVANCED_FACE ( 'NONE', ( #137832 ), #30768, .F. ) ;
#178626=CARTESIAN_POINT ( 'NONE',  ( 20.84999999999998721, -11.74999999998884448, -134.0000000000000284 ) ) ;
#178642=CARTESIAN_POINT ( 'NONE',  ( 20.94999999999999574, -11.64999999998883595, -103.4000000000000341 ) ) ;
#178682=CARTESIAN_POINT ( 'NONE',  ( -1.739115166359751801E-14, 11.65000000001114699, -112.7500000000000284 ) ) ;
#178683=ORIENTED_EDGE ( 'NONE', *, *, #86576, .F. ) ;
#178707=CARTESIAN_POINT ( 'NONE',  ( 18.49999999999999289, 10.20857864377384239, -125.2671572875254071 ) ) ;
#178712=EDGE_CURVE ( 'NONE', #254860, #54914, #173893, .T. ) ;
#178722=AXIS2_PLACEMENT_3D ( 'NONE', #44893, #243082, #47436 ) ;
#178759=CARTESIAN_POINT ( 'NONE',  ( 18.59999999999999787, 1.851028230152016674, -112.1539132694225316 ) ) ;
#178781=DIRECTION ( 'NONE',  ( -1.000000000000000000, 0.000000000000000000, 0.000000000000000000 ) ) ;
#178813=FACE_OUTER_BOUND ( 'NONE', #201894, .T. ) ;
#178830=EDGE_LOOP ( 'NONE', ( #81790, #132942, #42773, #234331 ) ) ;
#178849=CARTESIAN_POINT ( 'NONE',  ( -23.25000000000000000, -1.835859311432481045, -145.6044391687985637 ) ) ;
#178863=CARTESIAN_POINT ( 'NONE',  ( -20.54999999999999716, 1.115600667400684642E-11, -100.5000000000000284 ) ) ;
#178871=CARTESIAN_POINT ( 'NONE',  ( -18.59999999999999787, 9.250000000011157297, -121.6500000000000341 ) ) ;
#178882=DIRECTION ( 'NONE',  ( 1.000000000000000000, 0.000000000000000000, 0.000000000000000000 ) ) ;
#178884=CIRCLE ( 'NONE', #62316, 7.800000000000001599 ) ;
#178885=DIRECTION ( 'NONE',  ( 0.000000000000000000, 0.000000000000000000, -1.000000000000000000 ) ) ;
#178899=DIRECTION ( 'NONE',  ( 0.000000000000000000, 0.000000000000000000, -1.000000000000000000 ) ) ;
#178917=AXIS2_PLACEMENT_3D ( 'NONE', #28158, #129787, #11135 ) ;
#178918=DIRECTION ( 'NONE',  ( 0.000000000000000000, 1.000000000000000000, 0.000000000000000000 ) ) ;
#178931=CARTESIAN_POINT ( 'NONE',  ( -18.50000000000000000, -26.43935341558978891, -118.6415086075074896 ) ) ;
#178932=CARTESIAN_POINT ( 'NONE',  ( -20.00857864376270001, 9.250000000011157297, -121.7500000000000426 ) ) ;
#178937=CARTESIAN_POINT ( 'NONE',  ( 22.47071067811865319, 0.09909245471376171288, -92.77992525550199332 ) ) ;
#178952=CARTESIAN_POINT ( 'NONE',  ( 20.95512820512820795, 8.876151316299273120, -112.7001728591287844 ) ) ;
#178997=ORIENTED_EDGE ( 'NONE', *, *, #243975, .T. ) ;
#179014=DIRECTION ( 'NONE',  ( -1.000000000000000000, -0.000000000000000000, -0.000000000000000000 ) ) ;
#179025=VECTOR ( 'NONE', #23954, 1000.000000000000000 ) ;
#179040=AXIS2_PLACEMENT_3D ( 'NONE', #168027, #6326, #165424 ) ;
#179077=EDGE_CURVE ( 'NONE', #175552, #24921, #49106, .T. ) ;
#179085=ADVANCED_FACE ( 'NONE', ( #194686 ), #82413, .T. ) ;
#179089=DIRECTION ( 'NONE',  ( 7.304098846218134667E-16, -1.000000000000000000, 0.000000000000000000 ) ) ;
#179115=ORIENTED_EDGE ( 'NONE', *, *, #207845, .F. ) ;
#179127=DIRECTION ( 'NONE',  ( 1.000000000000000000, -0.000000000000000000, -0.000000000000000000 ) ) ;
#179189=AXIS2_PLACEMENT_3D ( 'NONE', #58876, #81014, #139707 ) ;
#179196=CYLINDRICAL_SURFACE ( 'NONE', #93554, 0.09999999999999939493 ) ;
#179211=ORIENTED_EDGE ( 'NONE', *, *, #203750, .T. ) ;
#179243=CYLINDRICAL_SURFACE ( 'NONE', #104570, 0.09999999999999781286 ) ;
#179253=DIRECTION ( 'NONE',  ( 0.7071067811865474617, 0.7071067811865474617, -0.000000000000000000 ) ) ;
#179257=AXIS2_PLACEMENT_3D ( 'NONE', #62799, #4105, #220596 ) ;
#179281=AXIS2_PLACEMENT_3D ( 'NONE', #112763, #37101, #157038 ) ;
#179285=CARTESIAN_POINT ( 'NONE',  ( -20.54999999999999716, 1.940186915899009490, -113.3291192110533672 ) ) ;
#179293=CARTESIAN_POINT ( 'NONE',  ( 20.95496329884391784, 10.56743320610419445, -108.0743099322848479 ) ) ;
#179305=CARTESIAN_POINT ( 'NONE',  ( -23.25000000000000000, 11.65000000001115588, -100.5000000000000284 ) ) ;
#179308=CARTESIAN_POINT ( 'NONE',  ( 22.49999999999999645, 11.74956712350054744, -100.3991416309013402 ) ) ;
#179320=ORIENTED_EDGE ( 'NONE', *, *, #141105, .T. ) ;
#179338=CARTESIAN_POINT ( 'NONE',  ( -21.05000000000000071, -11.41227409413852989, -103.5000000000000426 ) ) ;
#179368=AXIS2_PLACEMENT_3D ( 'NONE', #13740, #213204, #174141 ) ;
#179371=VERTEX_POINT ( 'NONE', #120288 ) ;
#179407=CARTESIAN_POINT ( 'NONE',  ( 23.14999999999999503, 11.65000000001116298, -126.9851942293460922 ) ) ;
#179422=EDGE_LOOP ( 'NONE', ( #239738, #4115, #98624, #102610 ) ) ;
#179505=DIRECTION ( 'NONE',  ( 0.000000000000000000, 0.000000000000000000, 1.000000000000000000 ) ) ;
#179536=EDGE_CURVE ( 'NONE', #157888, #197596, #16194, .T. ) ;
#179537=CARTESIAN_POINT ( 'NONE',  ( -23.15000000000000213, -11.64999999998884483, -130.9000000000000341 ) ) ;
#179539=ORIENTED_EDGE ( 'NONE', *, *, #195915, .T. ) ;
#179554=DIRECTION ( 'NONE',  ( 0.000000000000000000, 0.000000000000000000, -1.000000000000000000 ) ) ;
#179569=CARTESIAN_POINT ( 'NONE',  ( 20.94999999999999929, 5.400000000011154988, -112.9052660189131245 ) ) ;
#179600=DIRECTION ( 'NONE',  ( 2.952720810173289112E-16, -1.000000000000000000, -0.000000000000000000 ) ) ;
#179604=AXIS2_PLACEMENT_3D ( 'NONE', #211868, #127181, #8518 ) ;
#179613=CARTESIAN_POINT ( 'NONE',  ( -20.54999999999999716, 1.115600667400684642E-11, -134.0000000000000284 ) ) ;
#179618=EDGE_CURVE ( 'NONE', #196505, #37339, #207721, .T. ) ;
#179625=DIRECTION ( 'NONE',  ( 1.000000000000000000, 0.000000000000000000, 0.000000000000000000 ) ) ;
#179649=CYLINDRICAL_SURFACE ( 'NONE', #85474, 0.09999999999999939493 ) ;
#179683=EDGE_LOOP ( 'NONE', ( #57175, #186614, #74386, #34339 ) ) ;
#179703=ORIENTED_EDGE ( 'NONE', *, *, #169526, .F. ) ;
#179721=AXIS2_PLACEMENT_3D ( 'NONE', #93282, #210668, #208125 ) ;
#179813=DIRECTION ( 'NONE',  ( 0.000000000000000000, 0.000000000000000000, -1.000000000000000000 ) ) ;
#179827=CARTESIAN_POINT ( 'NONE',  ( 18.49999999999999645, -1.164121893230052995, -141.9148480855716343 ) ) ;
#179841=EDGE_CURVE ( 'NONE', #187769, #85468, #28692, .T. ) ;
#179860=CARTESIAN_POINT ( 'NONE',  ( -21.05000000000000071, 1.115600667400684642E-11, -122.3000000000000398 ) ) ;
#179863=EDGE_CURVE ( 'NONE', #139652, #105004, #20445, .T. ) ;
#179874=DIRECTION ( 'NONE',  ( 0.000000000000000000, 1.776356839400306474E-15, 1.000000000000000000 ) ) ;
#179876=CIRCLE ( 'NONE', #246494, 11.65000000000000036 ) ;
#179881=CARTESIAN_POINT ( 'NONE',  ( 23.14999999999999858, 1.115600667400684642E-11, -134.0000000000000284 ) ) ;
#179888=DIRECTION ( 'NONE',  ( 0.000000000000000000, 3.552713678800413366E-15, -1.000000000000000000 ) ) ;
#179948=FACE_OUTER_BOUND ( 'NONE', #92208, .T. ) ;
#179950=AXIS2_PLACEMENT_3D ( 'NONE', #41681, #40417, #56065 ) ;
#179972=AXIS2_PLACEMENT_3D ( 'NONE', #35260, #133053, #70531 ) ;
#179984=CIRCLE ( 'NONE', #5149, 0.09999999999998898659 ) ;
#179995=VERTEX_POINT ( 'NONE', #227550 ) ;
#180001=( BOUNDED_CURVE ( )  B_SPLINE_CURVE ( 3, ( #123521, #84332, #58378, #197910 ),
 .UNSPECIFIED., .F., .T. ) 
 B_SPLINE_CURVE_WITH_KNOTS ( ( 4, 4 ),
 ( 3.192897208853993085, 4.712388980384689674 ),
 .UNSPECIFIED. ) 
 CURVE ( )  GEOMETRIC_REPRESENTATION_ITEM ( )  RATIONAL_B_SPLINE_CURVE ( ( 1.000000000000000000, 0.8166740347213228279, 0.8166740347213228279, 1.000000000000000000 ) ) 
 REPRESENTATION_ITEM ( '' )  );
#180006=CARTESIAN_POINT ( 'NONE',  ( -18.59999999999999787, -1.164121893230052995, -141.9148480855716343 ) ) ;
#180015=ADVANCED_FACE ( 'NONE', ( #114015 ), #90595, .F. ) ;
#180028=CARTESIAN_POINT ( 'NONE',  ( 21.00000000000000000, 9.750000000011153745, -112.8500000000000369 ) ) ;
#180042=ORIENTED_EDGE ( 'NONE', *, *, #114312, .T. ) ;
#180047=CIRCLE ( 'NONE', #121790, 0.09999999999999363565 ) ;
#180095=AXIS2_PLACEMENT_3D ( 'NONE', #37718, #178514, #134209 ) ;
#180146=CARTESIAN_POINT ( 'NONE',  ( -21.04999999999999716, -0.01465611850212083199, -94.00331341423238030 ) ) ;
#180160=FACE_OUTER_BOUND ( 'NONE', #61800, .T. ) ;
#180175=CIRCLE ( 'NONE', #179604, 0.09999999999999939493 ) ;
#180183=CARTESIAN_POINT ( 'NONE',  ( 20.94999999999999929, 5.000000000011153745, -112.9052660189131245 ) ) ;
#180203=EDGE_LOOP ( 'NONE', ( #100895, #184194, #89567, #233572, #24685, #32773, #196770, #187391, #171317, #149536, #212302 ) ) ;
#180206=DIRECTION ( 'NONE',  ( 0.000000000000000000, -0.1298341882520022694, -0.9915357197604852679 ) ) ;
#180216=DIRECTION ( 'NONE',  ( 0.000000000000000000, 0.000000000000000000, 1.000000000000000000 ) ) ;
#180236=DIRECTION ( 'NONE',  ( 1.000000000000000000, 3.265361837132813093E-16, -0.000000000000000000 ) ) ;
#180240=EDGE_CURVE ( 'NONE', #174781, #61278, #171185, .T. ) ;
#180278=CARTESIAN_POINT ( 'NONE',  ( 21.93642651522410603, 7.327166239336949438, -100.5000000000000284 ) ) ;
#180316=EDGE_CURVE ( 'NONE', #205348, #256826, #212178, .T. ) ;
#180319=CARTESIAN_POINT ( 'NONE',  ( -21.06715728752537942, 11.75000000001115019, -107.5148057706540357 ) ) ;
#180330=CIRCLE ( 'NONE', #117780, 0.09999999999999939493 ) ;
#180342=ORIENTED_EDGE ( 'NONE', *, *, #229000, .F. ) ;
#180346=ORIENTED_EDGE ( 'NONE', *, *, #203898, .F. ) ;
#180377=ORIENTED_EDGE ( 'NONE', *, *, #81118, .F. ) ;
#180380=ADVANCED_FACE ( 'NONE', ( #74648 ), #87249, .F. ) ;
#180382=ORIENTED_EDGE ( 'NONE', *, *, #29377, .T. ) ;
#180446=AXIS2_PLACEMENT_3D ( 'NONE', #20169, #60553, #99663 ) ;
#180474=EDGE_CURVE ( 'NONE', #25563, #163036, #208092, .T. ) ;
#180482=DIRECTION ( 'NONE',  ( 0.000000000000000000, 0.000000000000000000, 1.000000000000000000 ) ) ;
#180516=AXIS2_PLACEMENT_3D ( 'NONE', #237129, #21941, #200562 ) ;
#180521=VERTEX_POINT ( 'NONE', #161873 ) ;
#180532=EDGE_CURVE ( 'NONE', #164528, #90248, #101844, .T. ) ;
#180548=DIRECTION ( 'NONE',  ( 0.000000000000000000, 0.000000000000000000, -1.000000000000000000 ) ) ;
#180554=DIRECTION ( 'NONE',  ( 0.000000000000000000, -0.000000000000000000, 1.000000000000000000 ) ) ;
#180556=CARTESIAN_POINT ( 'NONE',  ( 20.95568717954149562, 10.60199405390297400, -108.1025083682686869 ) ) ;
#180614=DIRECTION ( 'NONE',  ( 1.000000000000000000, -0.000000000000000000, -0.000000000000000000 ) ) ;
#180621=DIRECTION ( 'NONE',  ( 1.000000000000000000, 0.000000000000000000, -0.000000000000000000 ) ) ;
#180659=ORIENTED_EDGE ( 'NONE', *, *, #184566, .T. ) ;
#180667=CARTESIAN_POINT ( 'NONE',  ( -23.25000000000000000, 1.115600667400684642E-11, -100.5000000000000284 ) ) ;
#180701=AXIS2_PLACEMENT_3D ( 'NONE', #239392, #3316, #181987 ) ;
#180722=CARTESIAN_POINT ( 'NONE',  ( 23.14999999999999858, 5.600000000011153389, -121.5947339810869465 ) ) ;
#180730=ADVANCED_FACE ( 'NONE', ( #232111 ), #99876, .F. ) ;
#180742=ORIENTED_EDGE ( 'NONE', *, *, #122673, .F. ) ;
#180805=VECTOR ( 'NONE', #61265, 1000.000000000000000 ) ;
#180875=DIRECTION ( 'NONE',  ( 0.000000000000000000, 0.9998779222360102414, 0.01562499999996356907 ) ) ;
#180909=PRODUCT_DEFINITION_CONTEXT ( 'detailed design', #250762, 'design' ) ;
#180923=ORIENTED_EDGE ( 'NONE', *, *, #250813, .F. ) ;
#180931=EDGE_CURVE ( 'NONE', #142111, #102643, #84521, .T. ) ;
#180957=ADVANCED_FACE ( 'NONE', ( #50552 ), #167999, .F. ) ;
#180977=DIRECTION ( 'NONE',  ( 0.000000000000000000, 0.000000000000000000, -1.000000000000000000 ) ) ;
#180990=CARTESIAN_POINT ( 'NONE',  ( -18.39999999999999503, -9.499999999988849808, -140.9221498493304239 ) ) ;
#181017=ORIENTED_EDGE ( 'NONE', *, *, #111469, .F. ) ;
#181020=EDGE_CURVE ( 'NONE', #258105, #22177, #71077, .T. ) ;
#181030=DIRECTION ( 'NONE',  ( 0.000000000000000000, -0.3738317757009718689, 0.9274965247785342815 ) ) ;
#181063=DIRECTION ( 'NONE',  ( 0.000000000000000000, 0.000000000000000000, -1.000000000000000000 ) ) ;
#181071=DIRECTION ( 'NONE',  ( 0.000000000000000000, 0.000000000000000000, -1.000000000000000000 ) ) ;
#181074=ORIENTED_EDGE ( 'NONE', *, *, #17392, .F. ) ;
#181129=ORIENTED_EDGE ( 'NONE', *, *, #239546, .F. ) ;
#181132=ORIENTED_EDGE ( 'NONE', *, *, #17536, .F. ) ;
#181137=DIRECTION ( 'NONE',  ( 1.000000000000000000, 0.000000000000000000, 0.000000000000000000 ) ) ;
#181151=CARTESIAN_POINT ( 'NONE',  ( 21.07928932188134397, 6.328516656404459262, -100.4011048543456468 ) ) ;
#181188=DIRECTION ( 'NONE',  ( -1.000000000000000000, -0.000000000000000000, 0.000000000000000000 ) ) ;
#181252=ORIENTED_EDGE ( 'NONE', *, *, #67045, .T. ) ;
#181274=ORIENTED_EDGE ( 'NONE', *, *, #218512, .F. ) ;
#181307=ORIENTED_EDGE ( 'NONE', *, *, #202985, .F. ) ;
#181311=AXIS2_PLACEMENT_3D ( 'NONE', #161605, #139424, #179874 ) ;
#181335=DIRECTION ( 'NONE',  ( -1.000000000000000000, -0.000000000000000000, 0.000000000000000000 ) ) ;
#181352=EDGE_CURVE ( 'NONE', #256334, #61689, #75371, .T. ) ;
#181411=VECTOR ( 'NONE', #111390, 1000.000000000000000 ) ;
#181415=ORIENTED_EDGE ( 'NONE', *, *, #143286, .T. ) ;
#181416=AXIS2_PLACEMENT_3D ( 'NONE', #164323, #200866, #183874 ) ;
#181427=ORIENTED_EDGE ( 'NONE', *, *, #231860, .F. ) ;
#181443=FACE_OUTER_BOUND ( 'NONE', #82658, .T. ) ;
#181462=LINE ( 'NONE', #120228, #29862 ) ;
#181500=CARTESIAN_POINT ( 'NONE',  ( -20.94999999999999929, 1.115600667400684642E-11, -122.2000000000000313 ) ) ;
#181501=DIRECTION ( 'NONE',  ( 0.000000000000000000, 1.000000000000000000, 0.000000000000000000 ) ) ;
#181509=AXIS2_PLACEMENT_3D ( 'NONE', #53182, #36210, #234377 ) ;
#181513=PLANE ( 'NONE',  #232174 ) ;
#181574=ORIENTED_EDGE ( 'NONE', *, *, #96556, .T. ) ;
#181579=LINE ( 'NONE', #64186, #117061 ) ;
#181612=AXIS2_PLACEMENT_3D ( 'NONE', #46611, #145718, #70078 ) ;
#181637=ORIENTED_EDGE ( 'NONE', *, *, #71151, .F. ) ;
#181658=CARTESIAN_POINT ( 'NONE',  ( -22.39999999999999858, 1.115600667400684642E-11, -100.5000000000000284 ) ) ;
#181687=DIRECTION ( 'NONE',  ( -1.000000000000000000, -2.952720810173289112E-16, 0.000000000000000000 ) ) ;
#181688=CARTESIAN_POINT ( 'NONE',  ( -21.05000000000000071, 11.60000000001115339, -127.0717967697245427 ) ) ;
#181693=CARTESIAN_POINT ( 'NONE',  ( 21.08376601933332495, 6.341947271286812793, -100.4362239890700437 ) ) ;
#181694=CARTESIAN_POINT ( 'NONE',  ( -23.15000000000000213, 11.65000000001115588, -121.7500000000000426 ) ) ;
#181701=CARTESIAN_POINT ( 'NONE',  ( 21.05000000000000071, 10.72371710471867701, -108.1649135690876449 ) ) ;
#181724=CARTESIAN_POINT ( 'NONE',  ( 23.25000000000000000, -8.999999999988844479, -110.3939691226524786 ) ) ;
#181763=FACE_OUTER_BOUND ( 'NONE', #126233, .T. ) ;
#181802=CARTESIAN_POINT ( 'NONE',  ( 18.59999999999999787, 1.866714910068465239, -112.2526752462820525 ) ) ;
#181823=DIRECTION ( 'NONE',  ( 0.000000000000000000, -1.000000000000000000, 0.000000000000000000 ) ) ;
#181837=EDGE_CURVE ( 'NONE', #154355, #110815, #4757, .T. ) ;
#181848=CARTESIAN_POINT ( 'NONE',  ( -21.04999999999999716, 6.344723404101477726, -100.4852821434760415 ) ) ;
#181913=ORIENTED_EDGE ( 'NONE', *, *, #55272, .T. ) ;
#181946=DIRECTION ( 'NONE',  ( -0.000000000000000000, -1.000000000000000000, 6.308085367188393199E-16 ) ) ;
#181956=CARTESIAN_POINT ( 'NONE',  ( 21.09096482362048164, 6.363544365415576110, -100.4605517212259969 ) ) ;
#181959=ORIENTED_EDGE ( 'NONE', *, *, #101487, .T. ) ;
#181961=CARTESIAN_POINT ( 'NONE',  ( -20.64999999999999858, 4.250000000011156409, -112.7500000000000284 ) ) ;
#181969=ORIENTED_EDGE ( 'NONE', *, *, #41052, .F. ) ;
#181987=DIRECTION ( 'NONE',  ( 1.000000000000000000, 0.000000000000000000, 0.000000000000000000 ) ) ;
#181989=ADVANCED_FACE ( 'NONE', ( #162892, #221524 ), #42920, .F. ) ;
#182032=VERTEX_POINT ( 'NONE', #201993 ) ;
#182036=AXIS2_PLACEMENT_3D ( 'NONE', #126996, #149149, #203957 ) ;
#182071=LINE ( 'NONE', #3407, #165565 ) ;
#182101=CARTESIAN_POINT ( 'NONE',  ( -23.25000000000000000, -1.835859311432481045, -145.5044391687985694 ) ) ;
#182121=EDGE_LOOP ( 'NONE', ( #122476, #169845, #156550, #162673 ) ) ;
#182133=ORIENTED_EDGE ( 'NONE', *, *, #244913, .T. ) ;
#182146=CARTESIAN_POINT ( 'NONE',  ( 23.14999999999999858, 1.115600667400684642E-11, -100.5000000000000284 ) ) ;
#182162=CARTESIAN_POINT ( 'NONE',  ( 21.53699400384337181, -8.054621614985864327E-12, -93.71228820675614202 ) ) ;
#182177=ORIENTED_EDGE ( 'NONE', *, *, #239164, .T. ) ;
#182179=CARTESIAN_POINT ( 'NONE',  ( 20.94999999999999929, 1.115600667400684642E-11, -134.0000000000000284 ) ) ;
#182214=CIRCLE ( 'NONE', #165656, 12.87500000000000000 ) ;
#182218=AXIS2_PLACEMENT_3D ( 'NONE', #232519, #95544, #74747 ) ;
#182260=AXIS2_PLACEMENT_3D ( 'NONE', #117817, #241621, #20029 ) ;
#182264=CARTESIAN_POINT ( 'NONE',  ( -20.94999999999999929, 1.115600667400684642E-11, -130.0000000000000284 ) ) ;
#182269=LINE ( 'NONE', #222646, #44208 ) ;
#182271=CARTESIAN_POINT ( 'NONE',  ( -18.43634282235125710, -9.679787199916876972, -140.6606518854538592 ) ) ;
#182284=EDGE_CURVE ( 'NONE', #126005, #170174, #104888, .T. ) ;
#182294=VERTEX_POINT ( 'NONE', #132744 ) ;
#182333=ORIENTED_EDGE ( 'NONE', *, *, #165090, .F. ) ;
#182363=ORIENTED_EDGE ( 'NONE', *, *, #25419, .T. ) ;
#182370=DIRECTION ( 'NONE',  ( 1.000000000000000000, 7.304098846218135653E-16, 0.000000000000000000 ) ) ;
#182450=ORIENTED_EDGE ( 'NONE', *, *, #145357, .T. ) ;
#182476=CARTESIAN_POINT ( 'NONE',  ( 20.85000000000000142, -1.164121893230052995, -141.9148480855716343 ) ) ;
#182477=DIRECTION ( 'NONE',  ( 0.000000000000000000, 0.8660254037844352659, -0.5000000000000058842 ) ) ;
#182492=CARTESIAN_POINT ( 'NONE',  ( -23.25000000000000000, 6.982009704867601307, -137.6961521182563217 ) ) ;
#182502=ORIENTED_EDGE ( 'NONE', *, *, #227856, .T. ) ;
#182507=VECTOR ( 'NONE', #40701, 1000.000000000000000 ) ;
#182526=DIRECTION ( 'NONE',  ( -3.265361837132813093E-16, 1.000000000000000000, 0.000000000000000000 ) ) ;
#182538=DIRECTION ( 'NONE',  ( 0.000000000000000000, 0.000000000000000000, -1.000000000000000000 ) ) ;
#182584=LINE ( 'NONE', #84704, #82080 ) ;
#182595=CYLINDRICAL_SURFACE ( 'NONE', #5059, 11.75000000000001066 ) ;
#182614=DIRECTION ( 'NONE',  ( -0.000000000000000000, 1.000000000000000000, -0.000000000000000000 ) ) ;
#182621=VERTEX_POINT ( 'NONE', #29501 ) ;
#182660=CARTESIAN_POINT ( 'NONE',  ( 18.40000000000000213, -9.519327731081279609, -107.4729763765593731 ) ) ;
#182733=CIRCLE ( 'NONE', #70314, 0.1000000000000028644 ) ;
#182787=DIRECTION ( 'NONE',  ( 0.000000000000000000, 0.000000000000000000, -1.000000000000000000 ) ) ;
#182808=CARTESIAN_POINT ( 'NONE',  ( -23.25000000000000000, 2.000000000011154189, -121.3753780772379258 ) ) ;
#182829=AXIS2_PLACEMENT_3D ( 'NONE', #237211, #42853, #179813 ) ;
#182839=CARTESIAN_POINT ( 'NONE',  ( 21.14999999999999858, 6.550000000011156231, -112.6500000000000341 ) ) ;
#182849=VERTEX_POINT ( 'NONE', #64440 ) ;
#182865=CARTESIAN_POINT ( 'NONE',  ( 18.59999999999999076, 10.20857864377385127, -121.8500000000000369 ) ) ;
#182880=AXIS2_PLACEMENT_3D ( 'NONE', #85015, #148889, #190592 ) ;
#182913=EDGE_LOOP ( 'NONE', ( #186750, #219634, #137850, #70672 ) ) ;
#182919=CARTESIAN_POINT ( 'NONE',  ( 21.00000000000000000, 9.750000000011153745, -112.8500000000000369 ) ) ;
#182924=CARTESIAN_POINT ( 'NONE',  ( -22.39999999999999503, 1.115541036281197940E-11, -92.70922040162662370 ) ) ;
#182933=EDGE_LOOP ( 'NONE', ( #80166, #42551, #72944, #220827 ) ) ;
#182935=AXIS2_PLACEMENT_3D ( 'NONE', #13361, #18496, #77169 ) ;
#183003=EDGE_CURVE ( 'NONE', #61667, #173551, #153161, .T. ) ;
#183009=AXIS2_PLACEMENT_3D ( 'NONE', #146527, #184381, #46160 ) ;
#183039=CARTESIAN_POINT ( 'NONE',  ( -23.25000000000000000, 7.021664781911246322, -137.8335654018973457 ) ) ;
#183047=ORIENTED_EDGE ( 'NONE', *, *, #4953, .T. ) ;
#183062=DIRECTION ( 'NONE',  ( 1.000000000000000000, 0.000000000000000000, 0.000000000000000000 ) ) ;
#183119=VERTEX_POINT ( 'NONE', #186329 ) ;
#183153=DIRECTION ( 'NONE',  ( 1.000000000000000000, -0.000000000000000000, 0.000000000000000000 ) ) ;
#183160=CARTESIAN_POINT ( 'NONE',  ( -18.59999999999999787, 11.65000000001115232, -107.5148057706540357 ) ) ;
#183163=AXIS2_PLACEMENT_3D ( 'NONE', #23033, #102503, #162536 ) ;
#183188=CARTESIAN_POINT ( 'NONE',  ( -18.59999996769639097, -9.363273769819080883, -107.6814939154659783 ) ) ;
#183205=ORIENTED_EDGE ( 'NONE', *, *, #94238, .F. ) ;
#183222=CARTESIAN_POINT ( 'NONE',  ( -21.12642695952773764, 6.375659922046319927, -100.4010967168106703 ) ) ;
#183225=AXIS2_PLACEMENT_3D ( 'NONE', #48607, #207706, #89010 ) ;
#183230=CARTESIAN_POINT ( 'NONE',  ( -23.15000000000000213, 4.350000000011156054, -121.6500000000000341 ) ) ;
#183248=CARTESIAN_POINT ( 'NONE',  ( 22.39999999999999503, 7.790779598384535376, -100.4000000000000341 ) ) ;
#183278=CARTESIAN_POINT ( 'NONE',  ( 20.95595012432476523, 10.60417921308733469, -108.0957693302181895 ) ) ;
#183291=ORIENTED_EDGE ( 'NONE', *, *, #27775, .F. ) ;
#183294=AXIS2_PLACEMENT_3D ( 'NONE', #86909, #166502, #226418 ) ;
#183302=DIRECTION ( 'NONE',  ( 0.000000000000000000, -1.000000000000000000, 0.000000000000000000 ) ) ;
#183330=ORIENTED_EDGE ( 'NONE', *, *, #220280, .F. ) ;
#183331=EDGE_LOOP ( 'NONE', ( #182177, #64140, #210241, #221166 ) ) ;
#183338=ORIENTED_EDGE ( 'NONE', *, *, #225967, .F. ) ;
#183402=DIRECTION ( 'NONE',  ( -3.469446951953604722E-14, -0.9999176327611370985, -0.01283462868040260302 ) ) ;
#183403=FACE_OUTER_BOUND ( 'NONE', #103377, .T. ) ;
#183516=AXIS2_PLACEMENT_3D ( 'NONE', #188197, #186937, #89080 ) ;
#183527=CARTESIAN_POINT ( 'NONE',  ( -21.05000000000000071, 1.851028230152016674, -112.1539132694225316 ) ) ;
#183542=ADVANCED_FACE ( 'NONE', ( #129369 ), #113653, .F. ) ;
#183543=CARTESIAN_POINT ( 'NONE',  ( -20.94999999999999929, 5.850000000011160495, -123.8675027757221017 ) ) ;
#183544=CARTESIAN_POINT ( 'NONE',  ( 20.94999999999999929, -11.48912529306489994, -130.9000000000000341 ) ) ;
#183585=CARTESIAN_POINT ( 'NONE',  ( 22.43288208788031568, 0.004899854896538679595, -88.85034815628095828 ) ) ;
#183591=CARTESIAN_POINT ( 'NONE',  ( 20.94999999999999574, 8.926614585098251453, -108.9716830192231498 ) ) ;
#183599=ORIENTED_EDGE ( 'NONE', *, *, #232618, .T. ) ;
#183600=CARTESIAN_POINT ( 'NONE',  ( 20.94999999999999574, -1.261786168553869603, -108.5864989635455089 ) ) ;
#183605=ORIENTED_EDGE ( 'NONE', *, *, #114615, .T. ) ;
#183609=EDGE_CURVE ( 'NONE', #234753, #257268, #188121, .T. ) ;
#183613=FACE_OUTER_BOUND ( 'NONE', #234924, .T. ) ;
#183616=VERTEX_POINT ( 'NONE', #18406 ) ;
#183618=CARTESIAN_POINT ( 'NONE',  ( -20.94999999999999929, 1.835341550235569663, -112.0551512925630249 ) ) ;
#183624=CARTESIAN_POINT ( 'NONE',  ( -22.39999999999999858, 0.1000000000111554016, -92.70922040162662370 ) ) ;
#183655=CARTESIAN_POINT ( 'NONE',  ( 20.94999999999999574, -11.64999999998883595, -103.6000000000000369 ) ) ;
#183662=ORIENTED_EDGE ( 'NONE', *, *, #244913, .F. ) ;
#183687=CARTESIAN_POINT ( 'NONE',  ( 18.59999999999999076, 1.115600667400684642E-11, -134.0000000000000284 ) ) ;
#183693=CARTESIAN_POINT ( 'NONE',  ( -20.85000000000000497, 11.75000000001115019, -127.0808527540413166 ) ) ;
#183726=CIRCLE ( 'NONE', #88004, 0.1000000000000028644 ) ;
#183734=VERTEX_POINT ( 'NONE', #156672 ) ;
#183741=EDGE_LOOP ( 'NONE', ( #158252, #98751, #159537, #141060 ) ) ;
#183748=LINE ( 'NONE', #22122, #3154 ) ;
#183755=DIRECTION ( 'NONE',  ( -1.000000000000000000, -0.000000000000000000, -0.000000000000000000 ) ) ;
#183760=DIRECTION ( 'NONE',  ( 1.000000000000000000, 0.000000000000000000, 0.000000000000000000 ) ) ;
#183852=AXIS2_PLACEMENT_3D ( 'NONE', #57296, #173478, #232124 ) ;
#183857=CARTESIAN_POINT ( 'NONE',  ( -20.64999999999999858, 4.350000000011156054, -112.7500000000000284 ) ) ;
#183865=DIRECTION ( 'NONE',  ( 1.000000000000000000, 0.000000000000000000, 0.000000000000000000 ) ) ;
#183872=ADVANCED_FACE ( 'NONE', ( #31290 ), #67490, .T. ) ;
#183874=DIRECTION ( 'NONE',  ( 0.000000000000000000, 0.000000000000000000, 1.000000000000000000 ) ) ;
#183878=CIRCLE ( 'NONE', #96373, 0.09999999999999939493 ) ;
#183882=DIRECTION ( 'NONE',  ( 0.000000000000000000, 0.000000000000000000, -1.000000000000000000 ) ) ;
#183883=ORIENTED_EDGE ( 'NONE', *, *, #192488, .T. ) ;
#183894=LINE ( 'NONE', #5224, #238775 ) ;
#183902=ORIENTED_EDGE ( 'NONE', *, *, #154948, .F. ) ;
#183926=DIRECTION ( 'NONE',  ( 0.000000000000000000, 0.000000000000000000, -1.000000000000000000 ) ) ;
#183990=DIRECTION ( 'NONE',  ( 0.7071067811865474617, 0.7071067811865474617, 0.000000000000000000 ) ) ;
#184001=LINE ( 'NONE', #69219, #119447 ) ;
#184014=DIRECTION ( 'NONE',  ( -1.000000000000000000, 0.000000000000000000, 0.000000000000000000 ) ) ;
#184082=DIRECTION ( 'NONE',  ( -1.000000000000000000, -0.000000000000000000, -0.000000000000000000 ) ) ;
#184106=CARTESIAN_POINT ( 'NONE',  ( 21.05000000000000071, 11.65000000001116298, -100.5000000000000284 ) ) ;
#184157=ADVANCED_FACE ( 'NONE', ( #125843 ), #163544, .T. ) ;
#184178=CARTESIAN_POINT ( 'NONE',  ( 22.49999999999999645, 0.1008583691098678403, -88.75043287651062940 ) ) ;
#184192=ORIENTED_EDGE ( 'NONE', *, *, #254176, .T. ) ;
#184194=ORIENTED_EDGE ( 'NONE', *, *, #211385, .T. ) ;
#184214=EDGE_LOOP ( 'NONE', ( #91002, #236742, #93045, #52334, #2717, #24795, #82644 ) ) ;
#184224=VECTOR ( 'NONE', #190473, 1000.000000000000000 ) ;
#184235=( BOUNDED_SURFACE ( )  B_SPLINE_SURFACE ( 3, 2, ( 
 ( #199320, #20695, #100175 ),
 ( #194197, #16839, #54651 ),
 ( #213733, #15565, #95068 ),
 ( #62373, #85737, #225262 ) ),
 .UNSPECIFIED., .F., .F., .F. ) 
 B_SPLINE_SURFACE_WITH_KNOTS ( ( 4, 4 ),
 ( 3, 3 ),
 ( 0.04058434257139475337, 0.04256401539001600232 ),
 ( 0.000000000000000000, 1.000000000000000000 ),
 .UNSPECIFIED. ) 
 GEOMETRIC_REPRESENTATION_ITEM ( )  RATIONAL_B_SPLINE_SURFACE ( (
 ( 1.000000000000000000, 0.7103081912008297749, 1.000000000000000000),
 ( 1.000000000000000000, 0.7104998333555460066, 1.000000000000000000),
 ( 1.000000000000000000, 0.7107238315755025626, 1.000000000000000000),
 ( 1.000000000000000000, 0.7110073749539292942, 1.000000000000000000) ) ) 
 REPRESENTATION_ITEM ( '' )  SURFACE ( )  );
#184246=DIRECTION ( 'NONE',  ( 1.296989514748957922E-15, -0.9887567792719341719, 0.1495327102803664099 ) ) ;
#184261=EDGE_CURVE ( 'NONE', #188649, #239049, #17770, .T. ) ;
#184285=LINE ( 'NONE', #121774, #24204 ) ;
#184294=AXIS2_PLACEMENT_3D ( 'NONE', #177979, #78841, #75047 ) ;
#184328=DIRECTION ( 'NONE',  ( 0.000000000000000000, 2.891205793294679805E-16, -1.000000000000000000 ) ) ;
#184368=CARTESIAN_POINT ( 'NONE',  ( 22.59080734064467677, 11.75000000001115552, -100.4692502919029664 ) ) ;
#184381=DIRECTION ( 'NONE',  ( -1.000000000000000000, -7.304098846218134667E-16, 0.000000000000000000 ) ) ;
#184410=CARTESIAN_POINT ( 'NONE',  ( 22.57320508075688892, 11.75000000001115552, -100.5000000000000284 ) ) ;
#184455=ORIENTED_EDGE ( 'NONE', *, *, #52488, .F. ) ;
#184472=ADVANCED_FACE ( 'NONE', ( #240375 ), #171766, .T. ) ;
#184488=CIRCLE ( 'NONE', #72097, 0.09999999999999939493 ) ;
#184503=CARTESIAN_POINT ( 'NONE',  ( -20.07928932188135107, 9.220710678129810489, -121.7500000000000426 ) ) ;
#184536=ORIENTED_EDGE ( 'NONE', *, *, #235601, .T. ) ;
#184552=ORIENTED_EDGE ( 'NONE', *, *, #234624, .F. ) ;
#184555=CARTESIAN_POINT ( 'NONE',  ( -21.05000000000000071, 1.115600667400684642E-11, -100.5000000000000284 ) ) ;
#184565=AXIS2_PLACEMENT_3D ( 'NONE', #183618, #4937, #199337 ) ;
#184566=EDGE_CURVE ( 'NONE', #89986, #110564, #17962, .T. ) ;
#184570=ORIENTED_EDGE ( 'NONE', *, *, #163722, .T. ) ;
#184574=CYLINDRICAL_SURFACE ( 'NONE', #46292, 0.09999999999999939493 ) ;
#184578=DIRECTION ( 'NONE',  ( 1.000000000000000000, 7.304098846218134667E-16, 0.000000000000000000 ) ) ;
#184581=CARTESIAN_POINT ( 'NONE',  ( 21.05000000000000071, -11.64999999998883595, -131.1000000000000227 ) ) ;
#184609=EDGE_CURVE ( 'NONE', #66896, #186169, #101117, .T. ) ;
#184621=ORIENTED_EDGE ( 'NONE', *, *, #23856, .T. ) ;
#184632=ORIENTED_EDGE ( 'NONE', *, *, #172920, .T. ) ;
#184639=EDGE_LOOP ( 'NONE', ( #18175, #74024, #65273, #37097 ) ) ;
#184663=CARTESIAN_POINT ( 'NONE',  ( -21.14999999999999858, 1.115600667400684642E-11, -93.95934304829879125 ) ) ;
#184666=CARTESIAN_POINT ( 'NONE',  ( 20.94999999999999929, -8.663551401857999323, -124.4758988819327215 ) ) ;
#184723=AXIS2_PLACEMENT_3D ( 'NONE', #188578, #208168, #6084 ) ;
#184765=FACE_OUTER_BOUND ( 'NONE', #215941, .T. ) ;
#184772=VECTOR ( 'NONE', #235843, 1000.000000000000000 ) ;
#184814=ORIENTED_EDGE ( 'NONE', *, *, #88734, .F. ) ;
#184834=EDGE_CURVE ( 'NONE', #164528, #146084, #101302, .T. ) ;
#184842=DIRECTION ( 'NONE',  ( 1.000000000000000000, -0.000000000000000000, -0.000000000000000000 ) ) ;
#184843=DIRECTION ( 'NONE',  ( 2.557131231893036985E-16, -0.8660254037844383745, 0.5000000000000003331 ) ) ;
#184866=SPHERICAL_SURFACE ( 'NONE', #45, 0.1000000000000000056 ) ;
#184895=CARTESIAN_POINT ( 'NONE',  ( 19.58285714285715073, 9.015001489659738354, -108.9206528160817555 ) ) ;
#184993=ADVANCED_FACE ( 'NONE', ( #143525 ), #18889, .T. ) ;
#184996=CARTESIAN_POINT ( 'NONE',  ( 23.14999999999999503, 6.550000000011156231, -121.7500000000000426 ) ) ;
#185000=AXIS2_PLACEMENT_3D ( 'NONE', #43453, #64300, #143819 ) ;
#185011=ORIENTED_EDGE ( 'NONE', *, *, #135493, .F. ) ;
#185017=DIRECTION ( 'NONE',  ( 0.000000000000000000, 0.000000000000000000, -1.000000000000000000 ) ) ;
#185040=CARTESIAN_POINT ( 'NONE',  ( -23.15000000000000213, 11.65000000001115588, -121.8500000000000369 ) ) ;
#185072=VERTEX_POINT ( 'NONE', #83523 ) ;
#185080=ORIENTED_EDGE ( 'NONE', *, *, #69602, .T. ) ;
#185138=CIRCLE ( 'NONE', #172711, 0.1000000000000002692 ) ;
#185146=EDGE_LOOP ( 'NONE', ( #176351, #101758, #185641, #143893 ) ) ;
#185160=VERTEX_POINT ( 'NONE', #153862 ) ;
#185171=EDGE_LOOP ( 'NONE', ( #240090, #9052, #222813, #146939, #191721 ) ) ;
#185176=DIRECTION ( 'NONE',  ( 0.000000000000000000, 0.000000000000000000, 1.000000000000000000 ) ) ;
#185195=CARTESIAN_POINT ( 'NONE',  ( 21.05000000000000071, 6.350000000011161383, -110.3438220896831581 ) ) ;
#185218=DIRECTION ( 'NONE',  ( 0.000000000000000000, 0.000000000000000000, -1.000000000000000000 ) ) ;
#185220=ORIENTED_EDGE ( 'NONE', *, *, #190234, .F. ) ;
#185248=ORIENTED_EDGE ( 'NONE', *, *, #186894, .F. ) ;
#185268=AXIS2_PLACEMENT_3D ( 'NONE', #165257, #106543, #186108 ) ;
#185297=EDGE_CURVE ( 'NONE', #159714, #40953, #147336, .T. ) ;
#185303=CARTESIAN_POINT ( 'NONE',  ( 23.15000000000000213, -9.599999999988842347, -124.1060308773475924 ) ) ;
#185305=CIRCLE ( 'NONE', #14637, 3.999999999999999112 ) ;
#185311=CARTESIAN_POINT ( 'NONE',  ( 23.14999999999998437, -4.049999999988842525, -100.5000000000000284 ) ) ;
#185345=CARTESIAN_POINT ( 'NONE',  ( 18.49999999999998934, 11.65000000001115943, -125.2500000000000284 ) ) ;
#185386=ORIENTED_EDGE ( 'NONE', *, *, #100054, .F. ) ;
#185389=ORIENTED_EDGE ( 'NONE', *, *, #233955, .T. ) ;
#185395=DIRECTION ( 'NONE',  ( 0.000000000000000000, 1.000000000000000000, 0.000000000000000000 ) ) ;
#185421=EDGE_CURVE ( 'NONE', #24871, #138064, #51616, .T. ) ;
#185455=CARTESIAN_POINT ( 'NONE',  ( -20.54999999999999716, 4.350000000011156054, -121.7500000000000426 ) ) ;
#185461=CARTESIAN_POINT ( 'NONE',  ( 18.59999999999999076, 6.550000000011156231, -121.6500000000000341 ) ) ;
#185502=DIRECTION ( 'NONE',  ( 0.000000000000000000, 0.000000000000000000, 1.000000000000000000 ) ) ;
#185528=DIRECTION ( 'NONE',  ( -3.469446951953612296E-14, -0.9908441862701596881, -0.1350103645451904977 ) ) ;
#185535=CARTESIAN_POINT ( 'NONE',  ( -20.94999999999999574, 11.63687328911503371, -127.1782407866755307 ) ) ;
#185559=ORIENTED_EDGE ( 'NONE', *, *, #235601, .F. ) ;
#185561=DIRECTION ( 'NONE',  ( 1.000000000000000000, 0.000000000000000000, -0.000000000000000000 ) ) ;
#185572=ORIENTED_EDGE ( 'NONE', *, *, #103790, .T. ) ;
#185623=CARTESIAN_POINT ( 'NONE',  ( -21.05000000000000071, -0.09999999998884338825, -88.85042919245522341 ) ) ;
#185636=EDGE_CURVE ( 'NONE', #226146, #162071, #218582, .T. ) ;
#185641=ORIENTED_EDGE ( 'NONE', *, *, #233033, .F. ) ;
#185658=DIRECTION ( 'NONE',  ( 0.000000000000000000, 0.000000000000000000, -1.000000000000000000 ) ) ;
#185695=EDGE_LOOP ( 'NONE', ( #163538, #31690, #57673, #57435 ) ) ;
#185716=AXIS2_PLACEMENT_3D ( 'NONE', #6268, #242322, #182370 ) ;
#185743=FACE_OUTER_BOUND ( 'NONE', #124324, .T. ) ;
#185750=DIRECTION ( 'NONE',  ( -1.000000000000000000, 0.000000000000000000, 0.000000000000000000 ) ) ;
#185755=FACE_OUTER_BOUND ( 'NONE', #195994, .T. ) ;
#185766=( BOUNDED_CURVE ( )  B_SPLINE_CURVE ( 3, ( #43055, #238678, #82143, #22218 ),
 .UNSPECIFIED., .F., .F. ) 
 B_SPLINE_CURVE_WITH_KNOTS ( ( 4, 4 ),
 ( 3.141592653589793116, 4.712388980384689674 ),
 .UNSPECIFIED. ) 
 CURVE ( )  GEOMETRIC_REPRESENTATION_ITEM ( )  RATIONAL_B_SPLINE_CURVE ( ( 1.000000000000000000, 0.8047378541243649375, 0.8047378541243649375, 1.000000000000000000 ) ) 
 REPRESENTATION_ITEM ( '' )  );
#185770=EDGE_CURVE ( 'NONE', #255048, #211247, #189230, .T. ) ;
#185796=EDGE_LOOP ( 'NONE', ( #156954, #182363, #254712, #223511 ) ) ;
#185806=DIRECTION ( 'NONE',  ( -0.7070776581708965169, -0.7071359030027827286, -0.000000000000000000 ) ) ;
#185811=VERTEX_POINT ( 'NONE', #226279 ) ;
#185844=ORIENTED_EDGE ( 'NONE', *, *, #158321, .F. ) ;
#185897=VECTOR ( 'NONE', #12451, 1000.000000000000000 ) ;
#185917=CARTESIAN_POINT ( 'NONE',  ( -20.91682497891423154, 10.32263460347359185, -139.5605957968672328 ) ) ;
#185932=VERTEX_POINT ( 'NONE', #123364 ) ;
#185966=SPHERICAL_SURFACE ( 'NONE', #38766, 0.1000000000000000056 ) ;
#186000=DIRECTION ( 'NONE',  ( 1.000000000000000000, 0.000000000000000000, 0.000000000000000000 ) ) ;
#186059=DIRECTION ( 'NONE',  ( 1.000000000000000000, 0.000000000000000000, -0.000000000000000000 ) ) ;
#186069=EDGE_LOOP ( 'NONE', ( #219233, #166774, #55887, #141456 ) ) ;
#186085=ORIENTED_EDGE ( 'NONE', *, *, #120594, .T. ) ;
#186108=DIRECTION ( 'NONE',  ( 0.000000000000000000, 0.000000000000000000, -1.000000000000000000 ) ) ;
#186116=LINE ( 'NONE', #146968, #231241 ) ;
#186123=CARTESIAN_POINT ( 'NONE',  ( -20.94999999999999929, 1.250000000011155299, -108.5000000000000426 ) ) ;
#186134=VERTEX_POINT ( 'NONE', #2762 ) ;
#186147=CARTESIAN_POINT ( 'NONE',  ( 22.39999999999999503, 1.115600667400684642E-11, -92.75000000000002842 ) ) ;
#186157=CIRCLE ( 'NONE', #215371, 0.8750000000000007772 ) ;
#186169=VERTEX_POINT ( 'NONE', #41932 ) ;
#186193=CARTESIAN_POINT ( 'NONE',  ( 21.14999999999999503, -0.09999999998884338825, -88.85042919245522341 ) ) ;
#186209=EDGE_CURVE ( 'NONE', #245711, #101037, #135214, .T. ) ;
#186222=AXIS2_PLACEMENT_3D ( 'NONE', #88380, #205782, #83242 ) ;
#186233=DIRECTION ( 'NONE',  ( -1.000000000000000000, -0.000000000000000000, 0.000000000000000000 ) ) ;
#186244=ORIENTED_EDGE ( 'NONE', *, *, #180316, .T. ) ;
#186259=DIRECTION ( 'NONE',  ( -1.000000000000000000, 0.000000000000000000, 0.000000000000000000 ) ) ;
#186263=CARTESIAN_POINT ( 'NONE',  ( 21.05000000000000071, -11.48912529306490349, -103.6000000000000369 ) ) ;
#186301=CARTESIAN_POINT ( 'NONE',  ( -23.25000000000000000, -11.74999999998884448, -130.9000000000000341 ) ) ;
#186329=CARTESIAN_POINT ( 'NONE',  ( -20.94999999999999929, -11.64999999998884483, -131.1000000000000227 ) ) ;
#186335=LINE ( 'NONE', #207186, #56618 ) ;
#186384=DIRECTION ( 'NONE',  ( -1.000000000000000000, -0.000000000000000000, -0.000000000000000000 ) ) ;
#186395=ADVANCED_FACE ( 'NONE', ( #13078 ), #73072, .T. ) ;
#186397=EDGE_LOOP ( 'NONE', ( #180346, #142405, #48130, #225788 ) ) ;
#186401=VERTEX_POINT ( 'NONE', #52166 ) ;
#186441=ORIENTED_EDGE ( 'NONE', *, *, #183609, .F. ) ;
#186443=FACE_OUTER_BOUND ( 'NONE', #111060, .T. ) ;
#186466=CARTESIAN_POINT ( 'NONE',  ( -18.59999999999999787, 1.115600667400684642E-11, -134.0000000000000284 ) ) ;
#186586=VECTOR ( 'NONE', #96791, 1000.000000000000000 ) ;
#186614=ORIENTED_EDGE ( 'NONE', *, *, #217935, .F. ) ;
#186634=CARTESIAN_POINT ( 'NONE',  ( 21.14999999999999503, -11.64999999998883595, -88.75000000000004263 ) ) ;
#186655=DIRECTION ( 'NONE',  ( 0.000000000000000000, 0.000000000000000000, -1.000000000000000000 ) ) ;
#186700=EDGE_CURVE ( 'NONE', #136780, #75197, #243566, .T. ) ;
#186703=ADVANCED_FACE ( 'NONE', ( #105388 ), #94547, .T. ) ;
#186704=VECTOR ( 'NONE', #47200, 1000.000000000000000 ) ;
#186729=EDGE_LOOP ( 'NONE', ( #210225, #217206, #243900, #135896 ) ) ;
#186750=ORIENTED_EDGE ( 'NONE', *, *, #111925, .T. ) ;
#186781=CARTESIAN_POINT ( 'NONE',  ( 20.94999999999999574, -1.360870587180885716, -108.5729979270909951 ) ) ;
#186812=EDGE_CURVE ( 'NONE', #129441, #247064, #12770, .T. ) ;
#186831=DIRECTION ( 'NONE',  ( -1.000000000000000000, 0.000000000000000000, 0.000000000000000000 ) ) ;
#186842=AXIS2_PLACEMENT_3D ( 'NONE', #121294, #161685, #177405 ) ;
#186855=EDGE_CURVE ( 'NONE', #219593, #2430, #14047, .T. ) ;
#186866=CARTESIAN_POINT ( 'NONE',  ( -23.15000000000000213, 1.115600667400684642E-11, -134.0000000000000284 ) ) ;
#186890=CIRCLE ( 'NONE', #78518, 11.90000000000000391 ) ;
#186891=AXIS2_PLACEMENT_3D ( 'NONE', #58585, #18197, #138121 ) ;
#186893=CARTESIAN_POINT ( 'NONE',  ( 18.49999999999999645, 5.699452464332751767, -87.95772604343019907 ) ) ;
#186894=EDGE_CURVE ( 'NONE', #169135, #136780, #111128, .T. ) ;
#186907=VECTOR ( 'NONE', #247567, 1000.000000000000000 ) ;
#186916=DIRECTION ( 'NONE',  ( 0.000000000000000000, -1.000000000000000000, 0.000000000000000000 ) ) ;
#186937=DIRECTION ( 'NONE',  ( -1.000000000000000000, 0.000000000000000000, 0.000000000000000000 ) ) ;
#186950=CYLINDRICAL_SURFACE ( 'NONE', #231773, 0.1000000000000028644 ) ;
#186955=AXIS2_PLACEMENT_3D ( 'NONE', #140780, #204592, #23434 ) ;
#187010=CARTESIAN_POINT ( 'NONE',  ( 18.43709777086141344, -9.682403433465239573, -140.6568433774128550 ) ) ;
#187016=DIRECTION ( 'NONE',  ( 0.000000000000000000, 0.000000000000000000, 1.000000000000000000 ) ) ;
#187029=EDGE_LOOP ( 'NONE', ( #112306, #197692, #87957, #72280 ) ) ;
#187052=DIRECTION ( 'NONE',  ( 0.7071067811865474617, 0.7071067811865474617, 0.000000000000000000 ) ) ;
#187054=CARTESIAN_POINT ( 'NONE',  ( -18.40000000000000213, -9.519327731081286714, -107.4729763765593589 ) ) ;
#187102=ADVANCED_FACE ( 'NONE', ( #120422 ), #199941, .T. ) ;
#187118=CARTESIAN_POINT ( 'NONE',  ( 20.94999999999999929, 5.500000000011153745, -121.5947339810869465 ) ) ;
#187196=EDGE_LOOP ( 'NONE', ( #152836, #41188, #213299, #21989, #207503, #120088 ) ) ;
#187225=CARTESIAN_POINT ( 'NONE',  ( -20.92356734117541706, 10.31973158071402175, -139.5505334713354841 ) ) ;
#187252=DIRECTION ( 'NONE',  ( -2.952720810173288619E-16, 1.000000000000000000, 0.000000000000000000 ) ) ;
#187303=VECTOR ( 'NONE', #38885, 1000.000000000000000 ) ;
#187345=DIRECTION ( 'NONE',  ( 2.915501640297155269E-16, -1.000000000000000000, 0.000000000000000000 ) ) ;
#187391=ORIENTED_EDGE ( 'NONE', *, *, #173626, .T. ) ;
#187433=FACE_OUTER_BOUND ( 'NONE', #114842, .T. ) ;
#187435=EDGE_CURVE ( 'NONE', #241950, #232157, #52163, .T. ) ;
#187440=DIRECTION ( 'NONE',  ( 1.000000000000000000, 0.000000000000000000, 0.000000000000000000 ) ) ;
#187454=AXIS2_PLACEMENT_3D ( 'NONE', #37219, #176732, #114167 ) ;
#187466=EDGE_LOOP ( 'NONE', ( #61878, #31499, #189023, #26619 ) ) ;
#187495=ORIENTED_EDGE ( 'NONE', *, *, #179618, .T. ) ;
#187565=ORIENTED_EDGE ( 'NONE', *, *, #176979, .F. ) ;
#187566=CARTESIAN_POINT ( 'NONE',  ( 21.05000000000000071, 1.162701749949165642, -108.4000000000000341 ) ) ;
#187571=VECTOR ( 'NONE', #143692, 1000.000000000000000 ) ;
#187605=CIRCLE ( 'NONE', #220885, 0.09999999999999939493 ) ;
#187612=CARTESIAN_POINT ( 'NONE',  ( 21.05000000000000071, 10.72371710471867701, -112.6500000000000341 ) ) ;
#187631=CARTESIAN_POINT ( 'NONE',  ( -23.15000000000000213, 4.250000000011156409, -112.7500000000000284 ) ) ;
#187651=EDGE_CURVE ( 'NONE', #67239, #169135, #158125, .T. ) ;
#187660=FACE_OUTER_BOUND ( 'NONE', #116934, .T. ) ;
#187670=DIRECTION ( 'NONE',  ( 0.000000000000000000, 0.000000000000000000, -1.000000000000000000 ) ) ;
#187691=ORIENTED_EDGE ( 'NONE', *, *, #113155, .T. ) ;
#187740=CIRCLE ( 'NONE', #4539, 0.1000000000000028644 ) ;
#187769=VERTEX_POINT ( 'NONE', #171912 ) ;
#187783=EDGE_LOOP ( 'NONE', ( #166953, #252446, #116635, #54544 ) ) ;
#187828=DIRECTION ( 'NONE',  ( 0.000000000000000000, -1.000000000000000000, 0.000000000000000000 ) ) ;
#187875=CARTESIAN_POINT ( 'NONE',  ( 20.91682497891423154, 10.32263460347359185, -139.5605957968672328 ) ) ;
#187952=CARTESIAN_POINT ( 'NONE',  ( 21.14999999999999503, -0.09999999998884338825, -88.85042919245522341 ) ) ;
#187962=ORIENTED_EDGE ( 'NONE', *, *, #216663, .T. ) ;
#187963=DIRECTION ( 'NONE',  ( 0.000000000000000000, 0.000000000000000000, -1.000000000000000000 ) ) ;
#187985=ORIENTED_EDGE ( 'NONE', *, *, #229853, .T. ) ;
#187988=CARTESIAN_POINT ( 'NONE',  ( 20.85000000000000142, -1.835859311432481045, -145.5044391687985694 ) ) ;
#188030=CARTESIAN_POINT ( 'NONE',  ( -23.25000000000000000, -11.64999999998884483, -88.75000000000004263 ) ) ;
#188059=ORIENTED_EDGE ( 'NONE', *, *, #204232, .T. ) ;
#188075=DIRECTION ( 'NONE',  ( -1.000000000000000000, 0.000000000000000000, 0.000000000000000000 ) ) ;
#188110=FACE_OUTER_BOUND ( 'NONE', #135357, .T. ) ;
#188121=CIRCLE ( 'NONE', #221409, 0.5000000000000013323 ) ;
#188163=AXIS2_PLACEMENT_3D ( 'NONE', #234179, #114249, #217179 ) ;
#188174=EDGE_CURVE ( 'NONE', #40304, #19526, #48440, .T. ) ;
#188180=VERTEX_POINT ( 'NONE', #32080 ) ;
#188186=CARTESIAN_POINT ( 'NONE',  ( 18.59999999999999076, -1.835859311432481045, -145.6044391687985637 ) ) ;
#188197=CARTESIAN_POINT ( 'NONE',  ( -20.85000000000000142, 7.021664781911246322, -137.8335654018973457 ) ) ;
#188211=EDGE_CURVE ( 'NONE', #122312, #182621, #11029, .T. ) ;
#188212=DIRECTION ( 'NONE',  ( 0.000000000000000000, 0.000000000000000000, -1.000000000000000000 ) ) ;
#188232=ORIENTED_EDGE ( 'NONE', *, *, #30708, .T. ) ;
#188241=CARTESIAN_POINT ( 'NONE',  ( -20.85000000000000142, -1.263275465206102233, -141.9018646667464338 ) ) ;
#188253=FACE_OUTER_BOUND ( 'NONE', #49207, .T. ) ;
#188267=CARTESIAN_POINT ( 'NONE',  ( 18.52351027002948669, -9.642162904684020930, -140.7150469505098158 ) ) ;
#188275=EDGE_CURVE ( 'NONE', #128415, #28381, #115261, .T. ) ;
#188286=ORIENTED_EDGE ( 'NONE', *, *, #123192, .F. ) ;
#188302=CARTESIAN_POINT ( 'NONE',  ( 18.49999999999998934, 10.25000000001115552, -125.2500000000000284 ) ) ;
#188307=VERTEX_POINT ( 'NONE', #217083 ) ;
#188325=CIRCLE ( 'NONE', #179972, 0.09999999999999939493 ) ;
#188337=ORIENTED_EDGE ( 'NONE', *, *, #74313, .F. ) ;
#188353=CIRCLE ( 'NONE', #134355, 3.999999999999999112 ) ;
#188403=DIRECTION ( 'NONE',  ( 0.000000000000000000, 0.000000000000000000, -1.000000000000000000 ) ) ;
#188482=ORIENTED_EDGE ( 'NONE', *, *, #105061, .T. ) ;
#188517=AXIS2_PLACEMENT_3D ( 'NONE', #40562, #220455, #183882 ) ;
#188548=CYLINDRICAL_SURFACE ( 'NONE', #109232, 0.1000000000000028644 ) ;
#188578=CARTESIAN_POINT ( 'NONE',  ( -21.44999999999999929, 7.350000000011155166, -112.8500000000000369 ) ) ;
#188589=ORIENTED_EDGE ( 'NONE', *, *, #168100, .F. ) ;
#188597=EDGE_CURVE ( 'NONE', #155920, #88045, #253365, .T. ) ;
#188625=DIRECTION ( 'NONE',  ( -1.000000000000000000, 0.000000000000000000, 0.000000000000000000 ) ) ;
#188629=ORIENTED_EDGE ( 'NONE', *, *, #216333, .T. ) ;
#188649=VERTEX_POINT ( 'NONE', #216800 ) ;
#188658=FACE_OUTER_BOUND ( 'NONE', #207670, .T. ) ;
#188660=CIRCLE ( 'NONE', #221952, 0.09999999999999939493 ) ;
#188703=EDGE_LOOP ( 'NONE', ( #182502, #220568, #183902, #226107 ) ) ;
#188712=DIRECTION ( 'NONE',  ( 0.000000000000000000, 1.000000000000000000, 0.000000000000000000 ) ) ;
#188715=CARTESIAN_POINT ( 'NONE',  ( -23.25000000000000000, 11.75000000001115552, -134.0000000000000284 ) ) ;
#188729=FACE_OUTER_BOUND ( 'NONE', #252569, .T. ) ;
#188732=ORIENTED_EDGE ( 'NONE', *, *, #154440, .T. ) ;
#188734=ORIENTED_EDGE ( 'NONE', *, *, #211279, .F. ) ;
#188768=VERTEX_POINT ( 'NONE', #99407 ) ;
#188771=EDGE_CURVE ( 'NONE', #192673, #193662, #173201, .T. ) ;
#188798=DIRECTION ( 'NONE',  ( 0.000000000000000000, 0.000000000000000000, -1.000000000000000000 ) ) ;
#188850=VERTEX_POINT ( 'NONE', #206236 ) ;
#188878=CARTESIAN_POINT ( 'NONE',  ( 21.11344571971228490, 10.61787902352632962, -112.7460208923997840 ) ) ;
#188918=CARTESIAN_POINT ( 'NONE',  ( 18.59999999999999432, -1.261786168553869603, -108.5864989635455089 ) ) ;
#188940=VECTOR ( 'NONE', #257173, 1000.000000000000000 ) ;
#188945=CARTESIAN_POINT ( 'NONE',  ( 18.59999999999999076, 10.49142135624846439, -125.2500000000000284 ) ) ;
#188953=ADVANCED_FACE ( 'NONE', ( #88827 ), #81517, .T. ) ;
#188954=VERTEX_POINT ( 'NONE', #28932 ) ;
#189007=AXIS2_PLACEMENT_3D ( 'NONE', #177469, #133175, #174925 ) ;
#189023=ORIENTED_EDGE ( 'NONE', *, *, #203900, .F. ) ;
#189054=ORIENTED_EDGE ( 'NONE', *, *, #64632, .F. ) ;
#189080=EDGE_LOOP ( 'NONE', ( #56774, #200321, #163356 ) ) ;
#189088=CARTESIAN_POINT ( 'NONE',  ( 18.41815437325347204, -9.498709853130273828, -140.6039458388020194 ) ) ;
#189102=ORIENTED_EDGE ( 'NONE', *, *, #245561, .T. ) ;
#189111=ORIENTED_EDGE ( 'NONE', *, *, #189774, .T. ) ;
#189138=CARTESIAN_POINT ( 'NONE',  ( 20.94999675878240808, 10.29307482169071442, -139.4586421466940465 ) ) ;
#189140=CYLINDRICAL_SURFACE ( 'NONE', #131909, 11.80000000000000426 ) ;
#189217=VERTEX_POINT ( 'NONE', #83378 ) ;
#189230=CIRCLE ( 'NONE', #164295, 0.09999999999999939493 ) ;
#189254=DIRECTION ( 'NONE',  ( 0.000000000000000000, 0.1575844902526560010, 0.9875055080513781558 ) ) ;
#189279=DIRECTION ( 'NONE',  ( -1.000000000000000000, -3.265361837132813093E-16, 0.000000000000000000 ) ) ;
#189287=EDGE_LOOP ( 'NONE', ( #139414, #10425, #60591, #248883 ) ) ;
#189319=AXIS2_PLACEMENT_3D ( 'NONE', #229417, #67767, #92452 ) ;
#189335=DIRECTION ( 'NONE',  ( 0.000000000000000000, 1.000000000000000000, 0.000000000000000000 ) ) ;
#189375=VERTEX_POINT ( 'NONE', #126386 ) ;
#189391=EDGE_CURVE ( 'NONE', #229099, #160408, #11201, .T. ) ;
#189400=EDGE_CURVE ( 'NONE', #74892, #36453, #94381, .T. ) ;
#189415=VERTEX_POINT ( 'NONE', #51963 ) ;
#189422=DIRECTION ( 'NONE',  ( -0.000000000000000000, 0.000000000000000000, -1.000000000000000000 ) ) ;
#189426=FACE_OUTER_BOUND ( 'NONE', #97284, .T. ) ;
#189441=EDGE_CURVE ( 'NONE', #125538, #83513, #165137, .T. ) ;
#189505=MANIFOLD_SOLID_BREP ( 'Stock-MAS-200-1', #7473 ) ;
#189508=DIRECTION ( 'NONE',  ( 0.000000000000000000, 0.000000000000000000, -1.000000000000000000 ) ) ;
#189529=B_SPLINE_CURVE_WITH_KNOTS ( 'NONE', 3,
 ( #228222, #89968, #170865, #10455, #134229, #229504, #31333, #110821 ),
 .UNSPECIFIED., .F., .F.,
 ( 4, 2, 2, 4 ),
 ( 0.000000000000000000, 9.550056980124721853E-05, 0.0001910011396024944371, 0.0003820022792050102329 ),
 .UNSPECIFIED. ) ;
#189530=B_SPLINE_CURVE_WITH_KNOTS ( 'NONE', 3,
 ( #95142, #6294, #106669, #105368, #45438, #63709, #161555 ),
 .UNSPECIFIED., .F., .F.,
 ( 4, 3, 4 ),
 ( 0.000000000000000000, 1.860045280646151707E-05, 5.251155757303908953E-05 ),
 .UNSPECIFIED. ) ;
#189538=ORIENTED_EDGE ( 'NONE', *, *, #213436, .T. ) ;
#189540=CARTESIAN_POINT ( 'NONE',  ( 22.60000000000000142, 1.115600667400684642E-11, -100.5000000000000284 ) ) ;
#189554=DIRECTION ( 'NONE',  ( -1.000000000000000000, 0.000000000000000000, 0.000000000000000000 ) ) ;
#189574=CARTESIAN_POINT ( 'NONE',  ( -23.25000000000000000, 1.115650265596050101E-11, -96.45000000000003126 ) ) ;
#189576=EDGE_CURVE ( 'NONE', #46245, #255159, #65174, .T. ) ;
#189584=ADVANCED_FACE ( 'NONE', ( #40155 ), #237043, .T. ) ;
#189593=ADVANCED_FACE ( 'NONE', ( #58369 ), #243126, .F. ) ;
#189606=DIRECTION ( 'NONE',  ( -1.000000000000000000, 0.000000000000000000, 0.000000000000000000 ) ) ;
#189607=DIRECTION ( 'NONE',  ( 2.952720810173289112E-16, -1.000000000000000000, 0.000000000000000000 ) ) ;
#189648=DIRECTION ( 'NONE',  ( 0.000000000000000000, -1.000000000000000000, 0.000000000000000000 ) ) ;
#189695=CARTESIAN_POINT ( 'NONE',  ( -18.54270223418606633, -9.624105502871751483, -140.7409350504075007 ) ) ;
#189704=VERTEX_POINT ( 'NONE', #89186 ) ;
#189707=EDGE_CURVE ( 'NONE', #164361, #149886, #243759, .T. ) ;
#189728=LINE ( 'NONE', #46346, #145852 ) ;
#189746=ORIENTED_EDGE ( 'NONE', *, *, #111279, .T. ) ;
#189750=CARTESIAN_POINT ( 'NONE',  ( -20.54999999999999716, 1.115600667400684642E-11, -134.0000000000000284 ) ) ;
#189770=CARTESIAN_POINT ( 'NONE',  ( -20.93975676684922504, 10.31104185824063002, -139.5204516983105805 ) ) ;
#189774=EDGE_CURVE ( 'NONE', #140474, #24921, #123810, .T. ) ;
#189782=CARTESIAN_POINT ( 'NONE',  ( -20.94999999999999929, -11.48912529306489994, -130.9000000000000341 ) ) ;
#189786=DIRECTION ( 'NONE',  ( 0.000000000000000000, 0.000000000000000000, -1.000000000000000000 ) ) ;
#189789=DIRECTION ( 'NONE',  ( -1.000000000000000000, 0.000000000000000000, 0.000000000000000000 ) ) ;
#189790=EDGE_CURVE ( 'NONE', #224679, #60113, #240339, .T. ) ;
#189804=DIRECTION ( 'NONE',  ( 0.000000000000000000, 0.000000000000000000, -1.000000000000000000 ) ) ;
#189857=DIRECTION ( 'NONE',  ( 0.000000000000000000, 0.000000000000000000, -1.000000000000000000 ) ) ;
#189873=DIRECTION ( 'NONE',  ( 0.000000000000000000, 0.9999631594459056361, -0.008583690987128059571 ) ) ;
#189930=DIRECTION ( 'NONE',  ( 0.000000000000000000, 0.000000000000000000, -1.000000000000000000 ) ) ;
#189940=CARTESIAN_POINT ( 'NONE',  ( 21.05000000000000071, 8.926614585098253229, -108.9716830192231640 ) ) ;
#189966=CARTESIAN_POINT ( 'NONE',  ( 18.53317502108576775, 10.32263460347359896, -139.5605957968672328 ) ) ;
#190015=ORIENTED_EDGE ( 'NONE', *, *, #62339, .T. ) ;
#190029=ORIENTED_EDGE ( 'NONE', *, *, #164779, .T. ) ;
#190034=ORIENTED_EDGE ( 'NONE', *, *, #31823, .T. ) ;
#190035=EDGE_CURVE ( 'NONE', #40759, #238428, #246671, .T. ) ;
#190042=ORIENTED_EDGE ( 'NONE', *, *, #207365, .F. ) ;
#190043=DIRECTION ( 'NONE',  ( 0.000000000000000000, 0.000000000000000000, -1.000000000000000000 ) ) ;
#190055=DIRECTION ( 'NONE',  ( 0.000000000000000000, -0.000000000000000000, -1.000000000000000000 ) ) ;
#190077=DIRECTION ( 'NONE',  ( 1.000000000000000000, -0.000000000000000000, -0.000000000000000000 ) ) ;
#190098=CARTESIAN_POINT ( 'NONE',  ( -21.05000000000000071, -1.249999999988843369, -108.5000000000000426 ) ) ;
#190108=CARTESIAN_POINT ( 'NONE',  ( 21.14999999999999858, -11.74999999998884448, -112.7500000000000284 ) ) ;
#190119=PLANE ( 'NONE',  #129181 ) ;
#190123=DIRECTION ( 'NONE',  ( 0.000000000000000000, 0.000000000000000000, 1.000000000000000000 ) ) ;
#190127=EDGE_CURVE ( 'NONE', #122312, #8209, #155321, .T. ) ;
#190145=LINE ( 'NONE', #14076, #160076 ) ;
#190188=ORIENTED_EDGE ( 'NONE', *, *, #32785, .F. ) ;
#190215=CARTESIAN_POINT ( 'NONE',  ( -23.25000000000000000, 11.75000000001115552, -88.75000000000004263 ) ) ;
#190234=EDGE_CURVE ( 'NONE', #54914, #100676, #138266, .T. ) ;
#190250=B_SPLINE_CURVE_WITH_KNOTS ( 'NONE', 3,
 ( #72192, #52601, #153039, #207863, #188267, #132148, #187010, #50039 ),
 .UNSPECIFIED., .F., .F.,
 ( 4, 2, 2, 4 ),
 ( 0.000000000000000000, 0.0002181133598168738638, 0.0003271700397253405300, 0.0004362267196338071962 ),
 .UNSPECIFIED. ) ;
#190303=VECTOR ( 'NONE', #198680, 1000.000000000000000 ) ;
#190308=ORIENTED_EDGE ( 'NONE', *, *, #128700, .F. ) ;
#190324=CIRCLE ( 'NONE', #65410, 0.09999999999998898659 ) ;
#190333=ORIENTED_EDGE ( 'NONE', *, *, #220280, .T. ) ;
#190345=AXIS2_PLACEMENT_3D ( 'NONE', #148668, #208647, #155106 ) ;
#190356=CARTESIAN_POINT ( 'NONE',  ( 20.85000000000000142, -1.851617760457748618, -145.6031897196037050 ) ) ;
#190391=DIRECTION ( 'NONE',  ( 0.000000000000000000, 0.000000000000000000, -1.000000000000000000 ) ) ;
#190397=CARTESIAN_POINT ( 'NONE',  ( -20.94999999999999929, 1.115600667400684642E-11, -134.0000000000000284 ) ) ;
#190426=CARTESIAN_POINT ( 'NONE',  ( -18.59999999999999787, 7.021664781911246322, -137.8335654018973457 ) ) ;
#190433=DIRECTION ( 'NONE',  ( 1.000000000000000000, 0.000000000000000000, 0.000000000000000000 ) ) ;
#190470=VERTEX_POINT ( 'NONE', #57132 ) ;
#190473=DIRECTION ( 'NONE',  ( -1.000000000000000000, 7.304098846218134667E-16, 2.111765289898285610E-31 ) ) ;
#190480=CYLINDRICAL_SURFACE ( 'NONE', #146956, 0.5000000000000004441 ) ;
#190488=DIRECTION ( 'NONE',  ( -0.000000000000000000, -0.1350103645451928291, -0.9908441862701594660 ) ) ;
#190510=DIRECTION ( 'NONE',  ( 1.000000000000000000, -0.000000000000000000, -0.000000000000000000 ) ) ;
#190529=DIRECTION ( 'NONE',  ( -0.8660254037843878594, 0.000000000000000000, -0.5000000000000880407 ) ) ;
#190531=CARTESIAN_POINT ( 'NONE',  ( 18.59999999999999432, -1.866714910046153308, -112.2526752462820525 ) ) ;
#190534=ORIENTED_EDGE ( 'NONE', *, *, #197340, .F. ) ;
#190571=FACE_OUTER_BOUND ( 'NONE', #110644, .T. ) ;
#190592=DIRECTION ( 'NONE',  ( 0.000000000000000000, 0.9908441862701596881, 0.1350103645451904977 ) ) ;
#190603=DIRECTION ( 'NONE',  ( -1.000000000000000000, 0.000000000000000000, 0.000000000000000000 ) ) ;
#190615=AXIS2_PLACEMENT_3D ( 'NONE', #209160, #87909, #10971 ) ;
#190627=CIRCLE ( 'NONE', #223898, 0.9750000000000036415 ) ;
#190650=ADVANCED_FACE ( 'NONE', ( #115855 ), #86543, .F. ) ;
#190652=EDGE_LOOP ( 'NONE', ( #112836, #169062, #75273, #252775 ) ) ;
#190661=FACE_OUTER_BOUND ( 'NONE', #149096, .T. ) ;
#190694=ORIENTED_EDGE ( 'NONE', *, *, #161459, .T. ) ;
#190695=EDGE_CURVE ( 'NONE', #168502, #234219, #61630, .T. ) ;
#190712=CARTESIAN_POINT ( 'NONE',  ( 22.39999999999999503, 11.65000000001116298, -100.4000000000000483 ) ) ;
#190714=ORIENTED_EDGE ( 'NONE', *, *, #171520, .T. ) ;
#190715=ORIENTED_EDGE ( 'NONE', *, *, #16079, .F. ) ;
#190716=ORIENTED_EDGE ( 'NONE', *, *, #189441, .F. ) ;
#190717=VERTEX_POINT ( 'NONE', #83096 ) ;
#190731=EDGE_LOOP ( 'NONE', ( #158855, #94690, #10626, #56014 ) ) ;
#190740=ORIENTED_EDGE ( 'NONE', *, *, #22746, .F. ) ;
#190758=AXIS2_PLACEMENT_3D ( 'NONE', #212261, #91011, #170608 ) ;
#190809=EDGE_CURVE ( 'NONE', #75064, #148820, #226474, .T. ) ;
#190813=LINE ( 'NONE', #49978, #159326 ) ;
#190831=DIRECTION ( 'NONE',  ( 0.000000000000000000, 0.000000000000000000, -1.000000000000000000 ) ) ;
#190856=DIRECTION ( 'NONE',  ( 0.000000000000000000, 0.000000000000000000, -1.000000000000000000 ) ) ;
#190870=CARTESIAN_POINT ( 'NONE',  ( 21.05000000000000071, -1.249999999988843369, -108.4000000000000341 ) ) ;
#190880=TOROIDAL_SURFACE ( 'NONE', #153474, 0.9750000000000019762, 0.1000000000000000056 ) ;
#190899=CARTESIAN_POINT ( 'NONE',  ( 21.07946286933444924, 0.07668384326756245983, -94.17096268099238898 ) ) ;
#190904=DIRECTION ( 'NONE',  ( 0.000000000000000000, 0.000000000000000000, -1.000000000000000000 ) ) ;
#190908=DIRECTION ( 'NONE',  ( -0.000000000000000000, -0.000000000000000000, 1.000000000000000000 ) ) ;
#190909=ADVANCED_FACE ( 'NONE', ( #154694 ), #71300, .T. ) ;
#190915=DIRECTION ( 'NONE',  ( -0.000000000000000000, -1.265107689135680095E-16, 1.000000000000000000 ) ) ;
#190922=CYLINDRICAL_SURFACE ( 'NONE', #105521, 0.09999999999999939493 ) ;
#190925=CARTESIAN_POINT ( 'NONE',  ( 20.85000000000000142, 0.1610488207298751417, -133.7158101556398151 ) ) ;
#190954=LINE ( 'NONE', #245770, #245026 ) ;
#190964=DIRECTION ( 'NONE',  ( 0.000000000000000000, 0.01562500000001045344, 0.9998779222360096863 ) ) ;
#190980=VERTEX_POINT ( 'NONE', #49987 ) ;
#190996=DIRECTION ( 'NONE',  ( 1.000000000000000000, -0.000000000000000000, -0.000000000000000000 ) ) ;
#191052=CARTESIAN_POINT ( 'NONE',  ( -20.54999999999999716, 7.250000000011155521, -112.7500000000000284 ) ) ;
#191065=ORIENTED_EDGE ( 'NONE', *, *, #187435, .T. ) ;
#191072=DIRECTION ( 'NONE',  ( 0.000000000000000000, 0.9875055080513743810, -0.1575844902526802316 ) ) ;
#191128=ORIENTED_EDGE ( 'NONE', *, *, #82631, .T. ) ;
#191177=VERTEX_POINT ( 'NONE', #78400 ) ;
#191202=CARTESIAN_POINT ( 'NONE',  ( 22.59999999999999432, 0.1000000000111554016, -88.85042919245522341 ) ) ;
#191206=DIRECTION ( 'NONE',  ( -0.000000000000000000, -0.1298341882520022694, -0.9915357197604853789 ) ) ;
#191215=EDGE_CURVE ( 'NONE', #135831, #21528, #103656, .T. ) ;
#191232=ORIENTED_EDGE ( 'NONE', *, *, #21670, .T. ) ;
#191268=FACE_OUTER_BOUND ( 'NONE', #195956, .T. ) ;
#191278=FACE_OUTER_BOUND ( 'NONE', #104437, .T. ) ;
#191302=CARTESIAN_POINT ( 'NONE',  ( 20.94999999999999929, 5.000000000011153745, -121.5947339810869465 ) ) ;
#191327=CARTESIAN_POINT ( 'NONE',  ( 18.59999999999999076, 7.070967871809997973, -137.7465642218683399 ) ) ;
#191348=DIRECTION ( 'NONE',  ( 0.000000000000000000, 0.000000000000000000, -1.000000000000000000 ) ) ;
#191354=CARTESIAN_POINT ( 'NONE',  ( 20.94999999999999929, 11.65000000001115943, -127.2161343370219413 ) ) ;
#191451=AXIS2_PLACEMENT_3D ( 'NONE', #141889, #37689, #18093 ) ;
#191464=CARTESIAN_POINT ( 'NONE',  ( -20.64999999999999858, 4.350000000011156054, -112.8500000000000369 ) ) ;
#191473=ORIENTED_EDGE ( 'NONE', *, *, #253659, .T. ) ;
#191477=CARTESIAN_POINT ( 'NONE',  ( 21.06089410995848255, 10.72529553213474429, -112.7023807310433625 ) ) ;
#191483=DIRECTION ( 'NONE',  ( -1.000000000000000000, -0.000000000000000000, -0.000000000000000000 ) ) ;
#191491=EDGE_LOOP ( 'NONE', ( #234754, #25307, #56535, #94054 ) ) ;
#191499=ORIENTED_EDGE ( 'NONE', *, *, #107291, .T. ) ;
#191520=DIRECTION ( 'NONE',  ( 1.000000000000000000, 0.000000000000000000, -0.000000000000000000 ) ) ;
#191528=FILL_AREA_STYLE_COLOUR ( '', #11004 ) ;
#191542=EDGE_CURVE ( 'NONE', #71456, #213068, #76816, .T. ) ;
#191577=EDGE_CURVE ( 'NONE', #240390, #208327, #8031, .T. ) ;
#191631=CYLINDRICAL_SURFACE ( 'NONE', #245030, 0.1000000000000028644 ) ;
#191633=SPHERICAL_SURFACE ( 'NONE', #163940, 0.1000000000000000056 ) ;
#191688=ORIENTED_EDGE ( 'NONE', *, *, #71062, .T. ) ;
#191691=CARTESIAN_POINT ( 'NONE',  ( 18.33683296300430854, -9.511149971121708901, -140.9057074127098304 ) ) ;
#191702=ORIENTED_EDGE ( 'NONE', *, *, #92103, .F. ) ;
#191721=ORIENTED_EDGE ( 'NONE', *, *, #215972, .T. ) ;
#191785=CARTESIAN_POINT ( 'NONE',  ( 21.05000000000000071, -11.64999999998883595, -100.5000000000000284 ) ) ;
#191831=CYLINDRICAL_SURFACE ( 'NONE', #103085, 0.8750000000000007772 ) ;
#191854=CIRCLE ( 'NONE', #125188, 0.09999999999999439892 ) ;
#191859=VERTEX_POINT ( 'NONE', #214732 ) ;
#191883=DIRECTION ( 'NONE',  ( 0.000000000000000000, 0.000000000000000000, -1.000000000000000000 ) ) ;
#191886=ORIENTED_EDGE ( 'NONE', *, *, #238403, .T. ) ;
#191919=ORIENTED_EDGE ( 'NONE', *, *, #170342, .T. ) ;
#191969=CARTESIAN_POINT ( 'NONE',  ( -23.25000000000000000, -11.74999999998884448, -103.6000000000000369 ) ) ;
#192012=FACE_OUTER_BOUND ( 'NONE', #93011, .T. ) ;
#192032=CARTESIAN_POINT ( 'NONE',  ( -23.25000000000000000, 1.115600667400684642E-11, -100.5000000000000284 ) ) ;
#192106=EDGE_CURVE ( 'NONE', #238459, #137271, #88030, .T. ) ;
#192108=SPHERICAL_SURFACE ( 'NONE', #230478, 0.1000000000000000056 ) ;
#192151=EDGE_LOOP ( 'NONE', ( #152211, #185386, #111756, #227869 ) ) ;
#192165=DIRECTION ( 'NONE',  ( 0.000000000000000000, 0.9915357197604973694, -0.1298341882519105928 ) ) ;
#192191=EDGE_CURVE ( 'NONE', #85468, #74786, #116609, .T. ) ;
#192194=EDGE_CURVE ( 'NONE', #190470, #93357, #175026, .T. ) ;
#192200=DIRECTION ( 'NONE',  ( 0.000000000000000000, -0.8660254037844383745, 0.5000000000000003331 ) ) ;
#192219=ORIENTED_EDGE ( 'NONE', *, *, #116265, .T. ) ;
#192249=CARTESIAN_POINT ( 'NONE',  ( 20.85000000000000142, -1.835859311432481045, -145.5044391687985694 ) ) ;
#192253=CARTESIAN_POINT ( 'NONE',  ( 20.94999999999999929, 4.813084112160684214, -122.0584822434762060 ) ) ;
#192262=VECTOR ( 'NONE', #219062, 1000.000000000000000 ) ;
#192266=AXIS2_PLACEMENT_3D ( 'NONE', #129834, #232821, #209379 ) ;
#192271=DIRECTION ( 'NONE',  ( 0.000000000000000000, 0.000000000000000000, -1.000000000000000000 ) ) ;
#192294=ORIENTED_EDGE ( 'NONE', *, *, #22204, .F. ) ;
#192298=CARTESIAN_POINT ( 'NONE',  ( 22.24259225415828567, 0.09906588346399246292, -93.00806212943462015 ) ) ;
#192299=DIRECTION ( 'NONE',  ( 3.469446951953635015E-14, -0.000000000000000000, 1.000000000000000000 ) ) ;
#192310=CARTESIAN_POINT ( 'NONE',  ( 20.13684514579998464, 9.495855392759668945, -108.6430316856869922 ) ) ;
#192378=FACE_OUTER_BOUND ( 'NONE', #79513, .T. ) ;
#192401=DIRECTION ( 'NONE',  ( 0.000000000000000000, 0.000000000000000000, -1.000000000000000000 ) ) ;
#192402=ADVANCED_FACE ( 'NONE', ( #27819 ), #62551, .T. ) ;
#192427=ORIENTED_EDGE ( 'NONE', *, *, #158069, .T. ) ;
#192436=ORIENTED_EDGE ( 'NONE', *, *, #162827, .T. ) ;
#192437=AXIS2_PLACEMENT_3D ( 'NONE', #243360, #25613, #106399 ) ;
#192450=ORIENTED_EDGE ( 'NONE', *, *, #152095, .T. ) ;
#192465=DIRECTION ( 'NONE',  ( 0.000000000000000000, -1.000000000000000000, 0.000000000000000000 ) ) ;
#192488=EDGE_CURVE ( 'NONE', #77303, #68117, #129192, .T. ) ;
#192495=CIRCLE ( 'NONE', #175957, 0.09999999999999907574 ) ;
#192538=CARTESIAN_POINT ( 'NONE',  ( 23.15000000000000213, -12.41227409413852811, -130.9000000000000341 ) ) ;
#192543=DIRECTION ( 'NONE',  ( 1.000000000000000000, -0.000000000000000000, -0.000000000000000000 ) ) ;
#192573=CIRCLE ( 'NONE', #255037, 0.09999999999999907574 ) ;
#192588=ORIENTED_EDGE ( 'NONE', *, *, #213592, .T. ) ;
#192608=ORIENTED_EDGE ( 'NONE', *, *, #189790, .T. ) ;
#192620=CARTESIAN_POINT ( 'NONE',  ( -18.47690164073607022, -9.464844538001084828, -140.7013809398361275 ) ) ;
#192625=TOROIDAL_SURFACE ( 'NONE', #218104, 0.9750000000000019762, 0.1000000000000000056 ) ;
#192642=CARTESIAN_POINT ( 'NONE',  ( 21.05000000000000071, -0.09999999998884338825, -88.85042919245522341 ) ) ;
#192653=DIRECTION ( 'NONE',  ( -0.000000000000000000, 1.000000000000000000, -1.224646799147352961E-16 ) ) ;
#192658=FACE_OUTER_BOUND ( 'NONE', #11394, .T. ) ;
#192673=VERTEX_POINT ( 'NONE', #101529 ) ;
#192689=DIRECTION ( 'NONE',  ( -1.000000000000000000, 0.000000000000000000, 0.000000000000000000 ) ) ;
#192711=ORIENTED_EDGE ( 'NONE', *, *, #23608, .F. ) ;
#192717=EDGE_CURVE ( 'NONE', #14082, #245837, #10179, .T. ) ;
#192719=ORIENTED_EDGE ( 'NONE', *, *, #21302, .F. ) ;
#192725=CIRCLE ( 'NONE', #225995, 0.1000000000000028644 ) ;
#192747=CARTESIAN_POINT ( 'NONE',  ( 20.95378194480896639, 10.53491199155394220, -108.0650541481478939 ) ) ;
#192755=CARTESIAN_POINT ( 'NONE',  ( 21.14999999999999858, -0.09999999998884338825, -100.5000000000000284 ) ) ;
#192777=CARTESIAN_POINT ( 'NONE',  ( 22.39999999999999858, 1.115600667400684642E-11, -100.5000000000000284 ) ) ;
#192779=DIRECTION ( 'NONE',  ( -0.000000000000000000, 0.000000000000000000, -1.000000000000000000 ) ) ;
#192797=DIRECTION ( 'NONE',  ( 0.000000000000000000, -1.000000000000000000, -1.734723475976807292E-15 ) ) ;
#192798=CARTESIAN_POINT ( 'NONE',  ( 23.14999999999999858, 3.900000000011155432, -134.0000000000000284 ) ) ;
#192807=ORIENTED_EDGE ( 'NONE', *, *, #145437, .T. ) ;
#192821=CARTESIAN_POINT ( 'NONE',  ( -20.85000000000000142, 0.1610488207298751417, -133.7158101556398151 ) ) ;
#192865=EDGE_CURVE ( 'NONE', #177524, #112449, #212764, .T. ) ;
#192872=AXIS2_PLACEMENT_3D ( 'NONE', #146225, #52248, #190529 ) ;
#192884=CIRCLE ( 'NONE', #76325, 0.2000000000000000944 ) ;
#192887=CARTESIAN_POINT ( 'NONE',  ( 18.49999999999999289, 10.20857864377385127, -88.75000000000004263 ) ) ;
#192912=ORIENTED_EDGE ( 'NONE', *, *, #147310, .F. ) ;
#192979=AXIS2_PLACEMENT_3D ( 'NONE', #252224, #78715, #34502 ) ;
#192986=CARTESIAN_POINT ( 'NONE',  ( 22.57856590037848576, -0.004128330053175016841, -88.74994153732457391 ) ) ;
#193004=AXIS2_PLACEMENT_3D ( 'NONE', #156199, #36248, #177043 ) ;
#193021=EDGE_CURVE ( 'NONE', #168971, #224344, #170731, .T. ) ;
#193030=ADVANCED_FACE ( 'NONE', ( #65981 ), #9855, .T. ) ;
#193041=ADVANCED_FACE ( 'NONE', ( #127243 ), #233611, .F. ) ;
#193049=LINE ( 'NONE', #191785, #144139 ) ;
#193060=EDGE_CURVE ( 'NONE', #11869, #40953, #24958, .T. ) ;
#193110=CARTESIAN_POINT ( 'NONE',  ( 21.12400222705968389, 8.778511907088480726, -112.7500000000000284 ) ) ;
#193124=LINE ( 'NONE', #53604, #254670 ) ;
#193144=ORIENTED_EDGE ( 'NONE', *, *, #241275, .T. ) ;
#193187=CIRCLE ( 'NONE', #18381, 0.1000000000000028644 ) ;
#193239=EDGE_LOOP ( 'NONE', ( #199022, #12807, #203740, #148177, #147341, #57148, #131397, #254701, #75280, #245275, #18273, #211041, #112120, #55143, #142288, #139607, #161974, #133768, #50003, #236688, #244266, #130071, #122681, #37286, #164335, #11213, #79964 ) ) ;
#193242=EDGE_CURVE ( 'NONE', #24198, #68117, #134906, .T. ) ;
#193253=DIRECTION ( 'NONE',  ( 0.000000000000000000, 1.000000000000000000, 0.000000000000000000 ) ) ;
#193296=CARTESIAN_POINT ( 'NONE',  ( 20.94999999999999929, -1.835341550213257733, -112.0551512925630249 ) ) ;
#193300=DIRECTION ( 'NONE',  ( -1.000000000000000000, 0.000000000000000000, 0.000000000000000000 ) ) ;
#193308=CARTESIAN_POINT ( 'NONE',  ( 20.94999999999999574, 1.115600667400684642E-11, -100.5000000000000284 ) ) ;
#193320=CARTESIAN_POINT ( 'NONE',  ( 18.59999999999999787, 1.115600667400684642E-11, -100.5000000000000284 ) ) ;
#193385=DIRECTION ( 'NONE',  ( -1.000000000000000000, -0.000000000000000000, -0.000000000000000000 ) ) ;
#193389=CARTESIAN_POINT ( 'NONE',  ( -18.50016250449483479, 10.29766095125289738, -139.4743663933276139 ) ) ;
#193417=ORIENTED_EDGE ( 'NONE', *, *, #130190, .T. ) ;
#193432=DIRECTION ( 'NONE',  ( 0.000000000000000000, 0.7397360091702755991, -0.6728971962616832059 ) ) ;
#193507=ORIENTED_EDGE ( 'NONE', *, *, #88206, .F. ) ;
#193525=CIRCLE ( 'NONE', #60224, 0.09999999999998898659 ) ;
#193553=CARTESIAN_POINT ( 'NONE',  ( -20.94999999999999929, -11.39257802169451317, -130.9260504201681101 ) ) ;
#193557=CARTESIAN_POINT ( 'NONE',  ( 22.47071067811865319, 7.720074744509199505, -100.4009075452974287 ) ) ;
#193564=CARTESIAN_POINT ( 'NONE',  ( -18.59999999999999787, 3.912899247244609580, -111.9818229730110062 ) ) ;
#193584=EDGE_CURVE ( 'NONE', #224935, #15812, #177646, .T. ) ;
#193590=CARTESIAN_POINT ( 'NONE',  ( -21.65000000000000213, 7.708578643773852157, -112.8500000000000369 ) ) ;
#193598=FACE_OUTER_BOUND ( 'NONE', #2237, .T. ) ;
#193635=VERTEX_POINT ( 'NONE', #195911 ) ;
#193637=CARTESIAN_POINT ( 'NONE',  ( 23.14999999999999503, 11.75000000001116263, -88.75000000000004263 ) ) ;
#193639=LINE ( 'NONE', #172839, #40189 ) ;
#193662=VERTEX_POINT ( 'NONE', #95502 ) ;
#193670=VERTEX_POINT ( 'NONE', #155517 ) ;
#193678=DIRECTION ( 'NONE',  ( -1.000000000000000000, 0.000000000000000000, 0.000000000000000000 ) ) ;
#193685=DIRECTION ( 'NONE',  ( 0.000000000000000000, 0.9915357197604973694, -0.1298341882519105928 ) ) ;
#193688=VECTOR ( 'NONE', #53655, 1000.000000000000000 ) ;
#193692=CARTESIAN_POINT ( 'NONE',  ( -21.05000000000000071, 1.115600667400684642E-11, -100.5000000000000284 ) ) ;
#193703=ORIENTED_EDGE ( 'NONE', *, *, #154257, .F. ) ;
#193783=ADVANCED_FACE ( 'NONE', ( #82326 ), #145903, .T. ) ;
#193785=LINE ( 'NONE', #13864, #148381 ) ;
#193786=EDGE_LOOP ( 'NONE', ( #168878, #27401, #15778 ) ) ;
#193811=CYLINDRICAL_SURFACE ( 'NONE', #249240, 7.899999999999990585 ) ;
#193815=VECTOR ( 'NONE', #76137, 1000.000000000000000 ) ;
#193824=CARTESIAN_POINT ( 'NONE',  ( -20.64999999999999858, 4.350000000011156054, -121.6500000000000341 ) ) ;
#193826=AXIS2_PLACEMENT_3D ( 'NONE', #107532, #87948, #172706 ) ;
#193869=ORIENTED_EDGE ( 'NONE', *, *, #4826, .F. ) ;
#193903=CARTESIAN_POINT ( 'NONE',  ( 21.05000000000000071, 11.60000000001116227, -127.0717967697245143 ) ) ;
#193912=AXIS2_PLACEMENT_3D ( 'NONE', #175104, #132075, #232479 ) ;
#193929=EDGE_CURVE ( 'NONE', #20965, #58429, #48364, .T. ) ;
#193944=DIRECTION ( 'NONE',  ( 2.952720810173289112E-16, -1.000000000000000000, 0.000000000000000000 ) ) ;
#193976=EDGE_CURVE ( 'NONE', #229941, #188850, #216993, .T. ) ;
#194001=EDGE_CURVE ( 'NONE', #92189, #252923, #73107, .T. ) ;
#194045=DIRECTION ( 'NONE',  ( 0.000000000000000000, 0.008583690987128059571, -0.9999631594459056361 ) ) ;
#194055=ORIENTED_EDGE ( 'NONE', *, *, #142777, .F. ) ;
#194066=VERTEX_POINT ( 'NONE', #151345 ) ;
#194137=CIRCLE ( 'NONE', #40020, 0.09999999999998807065 ) ;
#194140=DIRECTION ( 'NONE',  ( 1.000000000000000000, 0.000000000000000000, -0.000000000000000000 ) ) ;
#194160=ORIENTED_EDGE ( 'NONE', *, *, #206696, .T. ) ;
#194186=DIRECTION ( 'NONE',  ( 2.952720810173289112E-16, -1.000000000000000000, 0.000000000000000000 ) ) ;
#194197=CARTESIAN_POINT ( 'NONE',  ( 22.00411653962177638, 7.253442868381098307, -100.4009618941994404 ) ) ;
#194229=ORIENTED_EDGE ( 'NONE', *, *, #256873, .F. ) ;
#194268=CARTESIAN_POINT ( 'NONE',  ( -18.45068461519105796, -9.486506529077932015, -107.5687771689047452 ) ) ;
#194274=CARTESIAN_POINT ( 'NONE',  ( 21.14999999999999503, -0.1008583690875562017, -88.75043287651064361 ) ) ;
#194305=ORIENTED_EDGE ( 'NONE', *, *, #92215, .F. ) ;
#194319=ADVANCED_FACE ( 'NONE', ( #49019 ), #153300, .T. ) ;
#194328=ORIENTED_EDGE ( 'NONE', *, *, #175200, .F. ) ;
#194361=ORIENTED_EDGE ( 'NONE', *, *, #46044, .T. ) ;
#194407=DIRECTION ( 'NONE',  ( 1.000000000000000000, 0.000000000000000000, -0.000000000000000000 ) ) ;
#194427=ADVANCED_FACE ( 'NONE', ( #114122 ), #176694, .F. ) ;
#194461=ADVANCED_BREP_SHAPE_REPRESENTATION ( '', ( #189505, #2425 ), #119141 ) ;
#194475=LINE ( 'NONE', #73253, #193688 ) ;
#194480=CARTESIAN_POINT ( 'NONE',  ( 23.14999999999999503, 11.75000000001116263, -88.75000000000004263 ) ) ;
#194486=CARTESIAN_POINT ( 'NONE',  ( 18.49999999999999645, -1.162701749926855266, -108.6000000000000227 ) ) ;
#194495=EDGE_CURVE ( 'NONE', #32249, #177703, #183878, .T. ) ;
#194503=CARTESIAN_POINT ( 'NONE',  ( 20.94999999999999929, 1.835341550235569663, -112.0551512925630249 ) ) ;
#194513=EDGE_CURVE ( 'NONE', #2430, #34898, #131961, .T. ) ;
#194515=EDGE_CURVE ( 'NONE', #114911, #253025, #112414, .T. ) ;
#194574=VECTOR ( 'NONE', #32944, 1000.000000000000000 ) ;
#194588=DIRECTION ( 'NONE',  ( 0.000000000000000000, 0.000000000000000000, -1.000000000000000000 ) ) ;
#194593=FACE_OUTER_BOUND ( 'NONE', #224029, .T. ) ;
#194641=CIRCLE ( 'NONE', #11467, 0.1000000000000001027 ) ;
#194658=CARTESIAN_POINT ( 'NONE',  ( 23.24999999999999289, 11.65000000001116298, -112.6500000000000341 ) ) ;
#194666=DIRECTION ( 'NONE',  ( 0.000000000000000000, 0.000000000000000000, -1.000000000000000000 ) ) ;
#194672=CARTESIAN_POINT ( 'NONE',  ( 21.00000000000000000, 9.750000000011153745, -121.7500000000000426 ) ) ;
#194686=FACE_OUTER_BOUND ( 'NONE', #246740, .T. ) ;
#194739=EDGE_CURVE ( 'NONE', #235011, #85365, #229856, .T. ) ;
#194745=CIRCLE ( 'NONE', #182260, 2.100000000000002309 ) ;
#194797=EDGE_LOOP ( 'NONE', ( #241230, #59696, #149546, #244490 ) ) ;
#194847=CARTESIAN_POINT ( 'NONE',  ( -20.94999999999999929, 11.65000000001115232, -134.0000000000000284 ) ) ;
#194864=EDGE_CURVE ( 'NONE', #104969, #161165, #21571, .T. ) ;
#194887=DIRECTION ( 'NONE',  ( 0.000000000000000000, -1.000000000000000000, 0.000000000000000000 ) ) ;
#194897=CARTESIAN_POINT ( 'NONE',  ( 21.30000000000002558, 1.115600667400684642E-11, -100.5000000000000284 ) ) ;
#194898=VECTOR ( 'NONE', #128644, 1000.000000000000000 ) ;
#194942=ORIENTED_EDGE ( 'NONE', *, *, #42173, .T. ) ;
#194986=ORIENTED_EDGE ( 'NONE', *, *, #253019, .T. ) ;
#195002=ORIENTED_EDGE ( 'NONE', *, *, #33233, .F. ) ;
#195006=PLANE ( 'NONE',  #45701 ) ;
#195032=LINE ( 'NONE', #92051, #129637 ) ;
#195045=CARTESIAN_POINT ( 'NONE',  ( 18.49999999999999289, 10.20857864377385127, -125.1500000000000341 ) ) ;
#195062=ORIENTED_EDGE ( 'NONE', *, *, #216663, .F. ) ;
#195133=LINE ( 'NONE', #153461, #6327 ) ;
#195141=AXIS2_PLACEMENT_3D ( 'NONE', #91620, #229845, #108612 ) ;
#195153=B_SPLINE_CURVE_WITH_KNOTS ( 'NONE', 3,
 ( #134245, #97675, #139374, #35206, #194268, #135529, #15636, #95138, #234648, #116002 ),
 .UNSPECIFIED., .F., .F.,
 ( 4, 2, 2, 2, 4 ),
 ( 0.000000000000000000, 3.990160268012661246E-05, 7.980320536025322493E-05, 0.0001596064107205033328, 0.0003192128214409992930 ),
 .UNSPECIFIED. ) ;
#195158=TOROIDAL_SURFACE ( 'NONE', #224167, 0.2000000000000000111, 0.1000000000000000056 ) ;
#195160=CIRCLE ( 'NONE', #3586, 2.000000000000002665 ) ;
#195167=LINE ( 'NONE', #178164, #123469 ) ;
#195170=CARTESIAN_POINT ( 'NONE',  ( 20.94999999999999574, 1.162701749949165642, -108.4000000000000341 ) ) ;
#195172=EDGE_LOOP ( 'NONE', ( #44525, #52055, #94795 ) ) ;
#195233=EDGE_CURVE ( 'NONE', #123531, #196984, #179984, .T. ) ;
#195240=CARTESIAN_POINT ( 'NONE',  ( 21.05000000000000071, 11.75000000001116263, -126.9851942293460922 ) ) ;
#195241=DIRECTION ( 'NONE',  ( 0.000000000000000000, 0.000000000000000000, -1.000000000000000000 ) ) ;
#195256=AXIS2_PLACEMENT_3D ( 'NONE', #43305, #139813, #202371 ) ;
#195270=CARTESIAN_POINT ( 'NONE',  ( -21.14999999999999858, -11.74999999998884448, -100.5000000000000284 ) ) ;
#195315=VECTOR ( 'NONE', #65845, 1000.000000000000000 ) ;
#195322=CARTESIAN_POINT ( 'NONE',  ( 23.24999999999999289, 6.550000000011156231, -121.8500000000000369 ) ) ;
#195365=DIRECTION ( 'NONE',  ( 1.000000000000000000, 0.000000000000000000, -0.000000000000000000 ) ) ;
#195369=ORIENTED_EDGE ( 'NONE', *, *, #143286, .F. ) ;
#195400=FACE_OUTER_BOUND ( 'NONE', #76893, .T. ) ;
#195416=CARTESIAN_POINT ( 'NONE',  ( 20.94999999999999929, 6.450000000011156587, -110.5170271704400591 ) ) ;
#195469=CARTESIAN_POINT ( 'NONE',  ( -23.25000000000000000, 1.115600667400684642E-11, -134.0000000000000284 ) ) ;
#195473=FACE_OUTER_BOUND ( 'NONE', #9555, .T. ) ;
#195480=AXIS2_PLACEMENT_3D ( 'NONE', #55951, #156396, #15597 ) ;
#195488=FACE_OUTER_BOUND ( 'NONE', #127803, .T. ) ;
#195533=FACE_OUTER_BOUND ( 'NONE', #13579, .T. ) ;
#195557=CARTESIAN_POINT ( 'NONE',  ( -22.43310005002225438, 0.005636942152031573783, -88.85033787286563722 ) ) ;
#195589=ADVANCED_FACE ( 'NONE', ( #167407 ), #91697, .T. ) ;
#195590=CARTESIAN_POINT ( 'NONE',  ( -21.53551880898957904, 0.09896973458281840830, -93.71520223858368581 ) ) ;
#195619=ORIENTED_EDGE ( 'NONE', *, *, #211675, .F. ) ;
#195645=CARTESIAN_POINT ( 'NONE',  ( -23.15000000000000213, 1.115600667400684642E-11, -100.5000000000000284 ) ) ;
#195658=CARTESIAN_POINT ( 'NONE',  ( 18.49999999999999645, -1.299733671219632791, -90.52812952286942050 ) ) ;
#195662=TOROIDAL_SURFACE ( 'NONE', #24802, 0.6000000000000009770, 0.1000000000000000056 ) ;
#195672=FACE_OUTER_BOUND ( 'NONE', #94141, .T. ) ;
#195695=CARTESIAN_POINT ( 'NONE',  ( 18.49999999999999289, 10.32573593129922607, -125.3500000000000512 ) ) ;
#195697=ORIENTED_EDGE ( 'NONE', *, *, #215812, .F. ) ;
#195741=ORIENTED_EDGE ( 'NONE', *, *, #160379, .F. ) ;
#195747=EDGE_LOOP ( 'NONE', ( #44000, #37416, #174049 ) ) ;
#195752=CARTESIAN_POINT ( 'NONE',  ( 23.14999999999999503, 11.65000000001116298, -121.8500000000000369 ) ) ;
#195756=VECTOR ( 'NONE', #195991, 1000.000000000000000 ) ;
#195771=CARTESIAN_POINT ( 'NONE',  ( 18.59999999999999432, -1.135018845899022466, -141.7169768834323520 ) ) ;
#195772=VERTEX_POINT ( 'NONE', #160693 ) ;
#195837=FACE_OUTER_BOUND ( 'NONE', #248532, .T. ) ;
#195844=CIRCLE ( 'NONE', #75046, 0.1000000000000053069 ) ;
#195845=AXIS2_PLACEMENT_3D ( 'NONE', #118018, #95874, #94595 ) ;
#195856=EDGE_LOOP ( 'NONE', ( #167025, #212444, #231724, #62384 ) ) ;
#195862=VERTEX_POINT ( 'NONE', #60263 ) ;
#195907=CARTESIAN_POINT ( 'NONE',  ( -18.50000000000000000, 1.115600667400684642E-11, -134.0000000000000284 ) ) ;
#195911=CARTESIAN_POINT ( 'NONE',  ( 23.14999999999999503, 11.75000000001116263, -126.9851942293460922 ) ) ;
#195915=EDGE_CURVE ( 'NONE', #38481, #246420, #197063, .T. ) ;
#195928=CARTESIAN_POINT ( 'NONE',  ( 21.08489247129320887, 8.877675190881227252, -112.8500000000000654 ) ) ;
#195930=TOROIDAL_SURFACE ( 'NONE', #158516, 4.099999999999999645, 0.1000000000000000056 ) ;
#195931=DIRECTION ( 'NONE',  ( -0.000000000000000000, -0.000000000000000000, 1.000000000000000000 ) ) ;
#195945=DIRECTION ( 'NONE',  ( 1.000000000000000000, 0.000000000000000000, 0.000000000000000000 ) ) ;
#195946=LINE ( 'NONE', #17302, #186586 ) ;
#195956=EDGE_LOOP ( 'NONE', ( #190740, #34053, #52988 ) ) ;
#195991=DIRECTION ( 'NONE',  ( -1.000000000000000000, -0.000000000000000000, -0.000000000000000000 ) ) ;
#195994=EDGE_LOOP ( 'NONE', ( #190333, #58286, #52751, #95030 ) ) ;
#196014=AXIS2_PLACEMENT_3D ( 'NONE', #245410, #103298, #26361 ) ;
#196016=VERTEX_POINT ( 'NONE', #240848 ) ;
#196043=VERTEX_POINT ( 'NONE', #17930 ) ;
#196047=EDGE_CURVE ( 'NONE', #251571, #48720, #126348, .T. ) ;
#196068=AXIS2_PLACEMENT_3D ( 'NONE', #150940, #72710, #149674 ) ;
#196097=ADVANCED_FACE ( 'NONE', ( #219987 ), #96177, .F. ) ;
#196118=FACE_OUTER_BOUND ( 'NONE', #250112, .T. ) ;
#196127=CYLINDRICAL_SURFACE ( 'NONE', #132165, 0.09999999999999781286 ) ;
#196145=ORIENTED_EDGE ( 'NONE', *, *, #143760, .T. ) ;
#196160=CARTESIAN_POINT ( 'NONE',  ( 21.13435531349810148, 1.115513965377477154E-11, -94.00627893640816524 ) ) ;
#196202=ORIENTED_EDGE ( 'NONE', *, *, #135893, .T. ) ;
#196211=EDGE_CURVE ( 'NONE', #239723, #34485, #72875, .T. ) ;
#196214=FACE_OUTER_BOUND ( 'NONE', #109119, .T. ) ;
#196219=DIRECTION ( 'NONE',  ( 2.952720810173289112E-16, -1.000000000000000000, 0.000000000000000000 ) ) ;
#196222=ORIENTED_EDGE ( 'NONE', *, *, #17679, .T. ) ;
#196245=ADVANCED_FACE ( 'NONE', ( #126014 ), #123463, .T. ) ;
#196254=EDGE_CURVE ( 'NONE', #53303, #113518, #218553, .T. ) ;
#196289=AXIS2_PLACEMENT_3D ( 'NONE', #79165, #161309, #120908 ) ;
#196299=DIRECTION ( 'NONE',  ( 0.000000000000000000, 1.734723475976807292E-15, -1.000000000000000000 ) ) ;
#196301=CARTESIAN_POINT ( 'NONE',  ( -18.50000000000000000, 1.637172712981535883, -112.0821533654720525 ) ) ;
#196387=EDGE_LOOP ( 'NONE', ( #214908, #196145, #117928, #54291 ) ) ;
#196392=ORIENTED_EDGE ( 'NONE', *, *, #114734, .F. ) ;
#196436=VERTEX_POINT ( 'NONE', #179305 ) ;
#196443=CARTESIAN_POINT ( 'NONE',  ( 20.94999999999999929, 1.115600667400684642E-11, -100.5000000000000284 ) ) ;
#196448=CIRCLE ( 'NONE', #200548, 7.791421356237310469 ) ;
#196452=ORIENTED_EDGE ( 'NONE', *, *, #157491, .F. ) ;
#196463=CARTESIAN_POINT ( 'NONE',  ( -18.50000000000000000, 9.250000000011157297, -121.8500000000000369 ) ) ;
#196467=CARTESIAN_POINT ( 'NONE',  ( -23.15000000000000213, -11.48912529306489816, -130.9000000000000341 ) ) ;
#196477=DIRECTION ( 'NONE',  ( 0.000000000000000000, 0.8700118002898322711, -0.4930308989875231696 ) ) ;
#196483=CARTESIAN_POINT ( 'NONE',  ( 21.05000000000000071, -9.399999999988844834, -124.1060308773475924 ) ) ;
#196505=VERTEX_POINT ( 'NONE', #65751 ) ;
#196510=CARTESIAN_POINT ( 'NONE',  ( 20.94999999999999929, -1.835341550213257733, -112.0551512925630249 ) ) ;
#196540=CIRCLE ( 'NONE', #117450, 0.1000000000000002554 ) ;
#196547=LINE ( 'NONE', #96150, #26889 ) ;
#196560=ADVANCED_FACE ( 'NONE', ( #104835 ), #107444, .F. ) ;
#196569=DIRECTION ( 'NONE',  ( 1.000000000000000000, -0.000000000000000000, -0.000000000000000000 ) ) ;
#196581=FACE_OUTER_BOUND ( 'NONE', #231569, .T. ) ;
#196591=ADVANCED_FACE ( 'NONE', ( #110008 ), #93016, .F. ) ;
#196600=ORIENTED_EDGE ( 'NONE', *, *, #46739, .F. ) ;
#196621=ORIENTED_EDGE ( 'NONE', *, *, #143546, .F. ) ;
#196646=ORIENTED_EDGE ( 'NONE', *, *, #15626, .F. ) ;
#196742=ORIENTED_EDGE ( 'NONE', *, *, #211255, .F. ) ;
#196767=CARTESIAN_POINT ( 'NONE',  ( 20.85000000000000142, 7.021664781911246322, -137.8335654018973457 ) ) ;
#196770=ORIENTED_EDGE ( 'NONE', *, *, #169046, .T. ) ;
#196780=ADVANCED_FACE ( 'NONE', ( #16084 ), #26447, .T. ) ;
#196797=EDGE_CURVE ( 'NONE', #102643, #161835, #117716, .T. ) ;
#196819=CARTESIAN_POINT ( 'NONE',  ( -21.05000000000000071, 1.261786168576181755, -108.5864989635455089 ) ) ;
#196839=DIRECTION ( 'NONE',  ( -1.000000000000000000, 0.000000000000000000, 0.000000000000000000 ) ) ;
#196843=CYLINDRICAL_SURFACE ( 'NONE', #14111, 0.1000000000000000472 ) ;
#196847=CARTESIAN_POINT ( 'NONE',  ( -18.59999999999999787, 1.851028230152016674, -112.1539132694225316 ) ) ;
#196861=CIRCLE ( 'NONE', #234264, 0.2000000000000057288 ) ;
#196862=ORIENTED_EDGE ( 'NONE', *, *, #101413, .T. ) ;
#196881=CARTESIAN_POINT ( 'NONE',  ( 18.49999999999999289, 10.23906162413259402, -125.2543974345976778 ) ) ;
#196920=CARTESIAN_POINT ( 'NONE',  ( -23.15000000000000213, -11.48912529306489994, -130.9000000000000341 ) ) ;
#196948=ORIENTED_EDGE ( 'NONE', *, *, #84117, .F. ) ;
#196951=DIRECTION ( 'NONE',  ( 0.000000000000000000, 0.000000000000000000, 1.000000000000000000 ) ) ;
#196955=CARTESIAN_POINT ( 'NONE',  ( -23.15000000000000213, 1.115600667400684642E-11, -132.0000000000000284 ) ) ;
#196984=VERTEX_POINT ( 'NONE', #84976 ) ;
#196993=ORIENTED_EDGE ( 'NONE', *, *, #94440, .T. ) ;
#197016=CIRCLE ( 'NONE', #230339, 0.09999999999998898659 ) ;
#197055=AXIS2_PLACEMENT_3D ( 'NONE', #77639, #172960, #212058 ) ;
#197063=CIRCLE ( 'NONE', #159671, 0.09999999999999939493 ) ;
#197087=CIRCLE ( 'NONE', #163784, 2.000000000000001776 ) ;
#197096=CARTESIAN_POINT ( 'NONE',  ( -21.11927991906891577, 0.009083679485028806067, -94.05150688150853000 ) ) ;
#197099=CARTESIAN_POINT ( 'NONE',  ( -20.64999999999999858, 4.350000000011156054, -112.7500000000000284 ) ) ;
#197104=LINE ( 'NONE', #156739, #30004 ) ;
#197110=CARTESIAN_POINT ( 'NONE',  ( -23.25000000000000000, 1.115600667400684642E-11, -134.0000000000000284 ) ) ;
#197127=CARTESIAN_POINT ( 'NONE',  ( 23.25000000000000000, -11.74999999998883560, -88.75000000000004263 ) ) ;
#197141=CARTESIAN_POINT ( 'NONE',  ( -23.25000000000000000, -9.599999999988838795, -124.1060308773475924 ) ) ;
#197147=CIRCLE ( 'NONE', #26484, 0.09999999999999939493 ) ;
#197179=EDGE_CURVE ( 'NONE', #249334, #222623, #133885, .T. ) ;
#197181=AXIS2_PLACEMENT_3D ( 'NONE', #88170, #193432, #233833 ) ;
#197199=CARTESIAN_POINT ( 'NONE',  ( 22.39999999999999503, -0.09999999998884338825, -88.85042919245522341 ) ) ;
#197201=ADVANCED_FACE ( 'NONE', ( #34065 ), #160582, .F. ) ;
#197238=CARTESIAN_POINT ( 'NONE',  ( -20.94999999999999929, 1.835341550235569663, -112.0551512925630249 ) ) ;
#197275=FACE_OUTER_BOUND ( 'NONE', #184639, .T. ) ;
#197292=DIRECTION ( 'NONE',  ( 7.304098846218134667E-16, 1.000000000000000000, -0.000000000000000000 ) ) ;
#197299=DIRECTION ( 'NONE',  ( -1.836970198721029934E-16, 1.000000000000000000, 0.000000000000000000 ) ) ;
#197314=ORIENTED_EDGE ( 'NONE', *, *, #188771, .F. ) ;
#197340=EDGE_CURVE ( 'NONE', #133593, #64097, #91119, .T. ) ;
#197357=EDGE_LOOP ( 'NONE', ( #226130, #129831, #213384, #254226 ) ) ;
#197367=CARTESIAN_POINT ( 'NONE',  ( -21.05000000000000071, 0.2561057921033771945, -100.4651035583277405 ) ) ;
#197402=EDGE_LOOP ( 'NONE', ( #187985, #4524, #20642, #243652, #143446 ) ) ;
#197420=CARTESIAN_POINT ( 'NONE',  ( -18.59999999999999787, 1.115600667400684642E-11, -100.5000000000000284 ) ) ;
#197472=CARTESIAN_POINT ( 'NONE',  ( -20.94999999999999929, -11.48912529306489994, -131.0000000000000284 ) ) ;
#197483=EDGE_CURVE ( 'NONE', #32589, #32249, #74162, .T. ) ;
#197536=DIRECTION ( 'NONE',  ( 0.000000000000000000, 2.891205793294679805E-16, -1.000000000000000000 ) ) ;
#197552=CARTESIAN_POINT ( 'NONE',  ( 20.12500000000000000, 9.750000000011153745, -121.6500000000000341 ) ) ;
#197559=DIRECTION ( 'NONE',  ( 0.000000000000000000, 0.000000000000000000, -1.000000000000000000 ) ) ;
#197561=DIRECTION ( 'NONE',  ( 1.000000000000000000, -0.000000000000000000, -0.000000000000000000 ) ) ;
#197569=CIRCLE ( 'NONE', #110087, 0.09999999999998898659 ) ;
#197578=VERTEX_POINT ( 'NONE', #65787 ) ;
#197589=VERTEX_POINT ( 'NONE', #245714 ) ;
#197596=VERTEX_POINT ( 'NONE', #59663 ) ;
#197619=ADVANCED_FACE ( 'NONE', ( #961 ), #160102, .T. ) ;
#197635=ADVANCED_FACE ( 'NONE', ( #226116 ), #214252, .F. ) ;
#197646=VERTEX_POINT ( 'NONE', #60965 ) ;
#197665=CARTESIAN_POINT ( 'NONE',  ( -23.25000000000000000, 1.115600667400684642E-11, -100.5000000000000284 ) ) ;
#197670=DIRECTION ( 'NONE',  ( 1.000000000000000000, -0.000000000000000000, -0.000000000000000000 ) ) ;
#197679=CARTESIAN_POINT ( 'NONE',  ( -21.05000000000000071, 1.115600667400684642E-11, -134.0000000000000284 ) ) ;
#197692=ORIENTED_EDGE ( 'NONE', *, *, #213592, .F. ) ;
#197762=AXIS2_PLACEMENT_3D ( 'NONE', #227427, #207900, #189607 ) ;
#197771=DIRECTION ( 'NONE',  ( 0.000000000000000000, 0.000000000000000000, -1.000000000000000000 ) ) ;
#197772=DIRECTION ( 'NONE',  ( 0.000000000000000000, 1.000000000000000000, 0.000000000000000000 ) ) ;
#197786=VECTOR ( 'NONE', #48632, 1000.000000000000000 ) ;
#197793=FACE_OUTER_BOUND ( 'NONE', #189080, .T. ) ;
#197800=CARTESIAN_POINT ( 'NONE',  ( -18.59999999999999787, 11.65000000001115232, -107.5148057706540357 ) ) ;
#197805=AXIS2_PLACEMENT_3D ( 'NONE', #11892, #167122, #70586 ) ;
#197811=DIRECTION ( 'NONE',  ( 0.000000000000000000, 0.000000000000000000, -1.000000000000000000 ) ) ;
#197837=ORIENTED_EDGE ( 'NONE', *, *, #235357, .F. ) ;
#197838=SPHERICAL_SURFACE ( 'NONE', #196289, 0.1000000000000000056 ) ;
#197860=CARTESIAN_POINT ( 'NONE',  ( -20.54999999999999716, 9.350000000011156942, -121.7500000000000426 ) ) ;
#197892=DIRECTION ( 'NONE',  ( 0.000000000000000000, -1.265107689135680095E-16, 1.000000000000000000 ) ) ;
#197907=AXIS2_PLACEMENT_3D ( 'NONE', #194672, #215477, #33046 ) ;
#197909=CARTESIAN_POINT ( 'NONE',  ( 18.59999999999999076, 6.450000000011156587, -121.7500000000000426 ) ) ;
#197910=CARTESIAN_POINT ( 'NONE',  ( 20.12500000000000000, 9.750000000011153745, -108.6117712821143186 ) ) ;
#197937=DIRECTION ( 'NONE',  ( -2.978066053179067751E-16, 1.000000000000000000, 0.000000000000000000 ) ) ;
#198020=EDGE_CURVE ( 'NONE', #100043, #116896, #224551, .T. ) ;
#198028=ORIENTED_EDGE ( 'NONE', *, *, #135079, .F. ) ;
#198058=CARTESIAN_POINT ( 'NONE',  ( -20.94999999999999929, -1.835341550213257733, -112.0551512925630249 ) ) ;
#198110=DIRECTION ( 'NONE',  ( 1.000000000000000000, 0.000000000000000000, 0.000000000000000000 ) ) ;
#198112=DIRECTION ( 'NONE',  ( 1.000000000000000000, 2.952720810173289112E-16, -0.000000000000000000 ) ) ;
#198113=LINE ( 'NONE', #196819, #17599 ) ;
#198116=DIRECTION ( 'NONE',  ( 0.000000000000000000, 1.000000000000000000, 0.000000000000000000 ) ) ;
#198122=VERTEX_POINT ( 'NONE', #116046 ) ;
#198130=AXIS2_PLACEMENT_3D ( 'NONE', #56517, #136052, #155682 ) ;
#198138=CARTESIAN_POINT ( 'NONE',  ( -22.50000000000000000, 11.75000000001115552, -100.5000000000000284 ) ) ;
#198166=DIRECTION ( 'NONE',  ( 2.840903330521631775E-16, -0.8700118002898321601, 0.4930308989875230585 ) ) ;
#198177=ORIENTED_EDGE ( 'NONE', *, *, #84449, .T. ) ;
#198180=CIRCLE ( 'NONE', #69224, 4.299999999999956302 ) ;
#198196=ORIENTED_EDGE ( 'NONE', *, *, #248772, .F. ) ;
#198205=DIRECTION ( 'NONE',  ( 0.000000000000000000, 1.000000000000000000, 0.000000000000000000 ) ) ;
#198226=DIRECTION ( 'NONE',  ( 0.000000000000000000, 0.000000000000000000, 1.000000000000000000 ) ) ;
#198236=AXIS2_PLACEMENT_3D ( 'NONE', #30958, #90892, #11365 ) ;
#198248=CARTESIAN_POINT ( 'NONE',  ( -22.45354308602489013, 2.198879698723710744E-07, -88.74956710954123196 ) ) ;
#198261=VECTOR ( 'NONE', #119702, 1000.000000000000000 ) ;
#198319=EDGE_CURVE ( 'NONE', #245768, #162687, #247921, .T. ) ;
#198332=EDGE_CURVE ( 'NONE', #213681, #239657, #241139, .T. ) ;
#198379=EDGE_CURVE ( 'NONE', #239723, #224903, #258066, .T. ) ;
#198393=FACE_OUTER_BOUND ( 'NONE', #241552, .T. ) ;
#198402=CARTESIAN_POINT ( 'NONE',  ( -23.25000000000000000, 4.350000000011156054, -112.7500000000000284 ) ) ;
#198433=DIRECTION ( 'NONE',  ( -0.000000000000000000, 1.265107689135680095E-16, -1.000000000000000000 ) ) ;
#198447=EDGE_LOOP ( 'NONE', ( #200657, #123330, #100149, #112526, #248358, #55360, #16566, #212590, #84886, #52985 ) ) ;
#198451=CARTESIAN_POINT ( 'NONE',  ( -18.50000000000000000, 9.150000000011157653, -121.6500000000000341 ) ) ;
#198499=ORIENTED_EDGE ( 'NONE', *, *, #93278, .F. ) ;
#198501=CIRCLE ( 'NONE', #148441, 0.09999999999999999167 ) ;
#198537=CYLINDRICAL_SURFACE ( 'NONE', #56233, 0.09999999999999939493 ) ;
#198547=AXIS2_PLACEMENT_3D ( 'NONE', #58064, #137601, #217135 ) ;
#198561=VERTEX_POINT ( 'NONE', #128885 ) ;
#198578=CIRCLE ( 'NONE', #44484, 0.1000000000000028644 ) ;
#198608=VERTEX_POINT ( 'NONE', #15364 ) ;
#198621=ORIENTED_EDGE ( 'NONE', *, *, #49259, .T. ) ;
#198629=ORIENTED_EDGE ( 'NONE', *, *, #132217, .F. ) ;
#198648=EDGE_CURVE ( 'NONE', #104317, #217495, #190145, .T. ) ;
#198680=DIRECTION ( 'NONE',  ( 4.408576920032447355E-17, -0.1350103645451876666, -0.9908441862701600211 ) ) ;
#198688=DIRECTION ( 'NONE',  ( 1.000000000000000000, 2.952720810173289112E-16, -0.000000000000000000 ) ) ;
#198690=CARTESIAN_POINT ( 'NONE',  ( 22.39999999999999858, 7.790779598384538929, -100.4000000000000341 ) ) ;
#198693=AXIS2_PLACEMENT_3D ( 'NONE', #178513, #257968, #181071 ) ;
#198696=ORIENTED_EDGE ( 'NONE', *, *, #64035, .T. ) ;
#198712=DIRECTION ( 'NONE',  ( -1.000000000000000000, 0.000000000000000000, 0.000000000000000000 ) ) ;
#198725=ORIENTED_EDGE ( 'NONE', *, *, #123903, .T. ) ;
#198727=VERTEX_POINT ( 'NONE', #81690 ) ;
#198734=ORIENTED_EDGE ( 'NONE', *, *, #174582, .F. ) ;
#198736=AXIS2_PLACEMENT_3D ( 'NONE', #68267, #125660, #86504 ) ;
#198739=ORIENTED_EDGE ( 'NONE', *, *, #199471, .F. ) ;
#198775=VECTOR ( 'NONE', #66252, 1000.000000000000000 ) ;
#198785=CARTESIAN_POINT ( 'NONE',  ( 21.05000000000000426, 0.03486800302426329434, -94.22991413631089586 ) ) ;
#198789=CARTESIAN_POINT ( 'NONE',  ( -18.39999999999999858, -9.599999999988845900, -140.7001893912220680 ) ) ;
#198792=DIRECTION ( 'NONE',  ( 0.000000000000000000, 0.000000000000000000, -1.000000000000000000 ) ) ;
#198820=CARTESIAN_POINT ( 'NONE',  ( 20.95265033839679347, 10.51225083247831371, -108.0657637560299946 ) ) ;
#198899=AXIS2_PLACEMENT_3D ( 'NONE', #252044, #94249, #232510 ) ;
#198918=DIRECTION ( 'NONE',  ( 0.000000000000000000, -1.000000000000000000, 0.000000000000000000 ) ) ;
#198920=EDGE_LOOP ( 'NONE', ( #44545, #152920, #39235, #103072 ) ) ;
#198933=CARTESIAN_POINT ( 'NONE',  ( 21.07954763557417621, 6.329290990048651366, -100.4341240813815261 ) ) ;
#199003=CARTESIAN_POINT ( 'NONE',  ( 20.94999999999999929, 11.65000000001115943, -127.1583993101029790 ) ) ;
#199010=ORIENTED_EDGE ( 'NONE', *, *, #172685, .T. ) ;
#199022=ORIENTED_EDGE ( 'NONE', *, *, #61335, .T. ) ;
#199054=EDGE_LOOP ( 'NONE', ( #107998, #48975, #75449, #18186 ) ) ;
#199072=DIRECTION ( 'NONE',  ( -0.7071067811865388020, 0.7071067811865561215, 0.000000000000000000 ) ) ;
#199090=DIRECTION ( 'NONE',  ( 1.000000000000000000, -0.000000000000000000, -0.000000000000000000 ) ) ;
#199148=DIRECTION ( 'NONE',  ( 0.000000000000000000, -0.000000000000000000, -1.000000000000000000 ) ) ;
#199149=DIRECTION ( 'NONE',  ( 0.000000000000000000, 0.000000000000000000, -1.000000000000000000 ) ) ;
#199153=CARTESIAN_POINT ( 'NONE',  ( 21.14999999999999858, 1.115600667400684642E-11, -112.6500000000000341 ) ) ;
#199156=VECTOR ( 'NONE', #20970, 1000.000000000000000 ) ;
#199206=ORIENTED_EDGE ( 'NONE', *, *, #47715, .T. ) ;
#199250=ORIENTED_EDGE ( 'NONE', *, *, #175765, .T. ) ;
#199270=ORIENTED_EDGE ( 'NONE', *, *, #123303, .F. ) ;
#199278=DIRECTION ( 'NONE',  ( 0.7071067811865474617, 0.7071067811865474617, 2.044391222244499837E-16 ) ) ;
#199285=ORIENTED_EDGE ( 'NONE', *, *, #147757, .T. ) ;
#199300=VECTOR ( 'NONE', #65538, 1000.000000000000000 ) ;
#199301=AXIS2_PLACEMENT_3D ( 'NONE', #197099, #215380, #116306 ) ;
#199306=FACE_OUTER_BOUND ( 'NONE', #125039, .T. ) ;
#199319=ORIENTED_EDGE ( 'NONE', *, *, #223415, .F. ) ;
#199320=CARTESIAN_POINT ( 'NONE',  ( 22.47071067811865319, 7.720074744509197728, -100.4009075452974429 ) ) ;
#199322=CARTESIAN_POINT ( 'NONE',  ( -21.64999999999999858, 7.250000000011148416, -121.6500000000000341 ) ) ;
#199337=DIRECTION ( 'NONE',  ( 1.000000000000000000, 0.000000000000000000, 0.000000000000000000 ) ) ;
#199375=AXIS2_PLACEMENT_3D ( 'NONE', #101914, #181501, #2826 ) ;
#199383=AXIS2_PLACEMENT_3D ( 'NONE', #245237, #163139, #84829 ) ;
#199388=CIRCLE ( 'NONE', #182829, 4.000000000000003553 ) ;
#199414=CYLINDRICAL_SURFACE ( 'NONE', #78047, 0.09999999999999939493 ) ;
#199418=DIRECTION ( 'NONE',  ( 0.000000000000000000, 0.000000000000000000, -1.000000000000000000 ) ) ;
#199445=LINE ( 'NONE', #20805, #50837 ) ;
#199448=DIRECTION ( 'NONE',  ( 1.000000000000000000, 2.952720810173289112E-16, -0.000000000000000000 ) ) ;
#199471=EDGE_CURVE ( 'NONE', #185811, #20386, #123783, .T. ) ;
#199482=AXIS2_PLACEMENT_3D ( 'NONE', #179613, #38812, #58334 ) ;
#199483=AXIS2_PLACEMENT_3D ( 'NONE', #210250, #26473, #109833 ) ;
#199508=CARTESIAN_POINT ( 'NONE',  ( 20.94999999999999929, -8.999999999988842703, -124.5060308773475839 ) ) ;
#199552=CIRCLE ( 'NONE', #7999, 0.1000000000000028644 ) ;
#199553=DIRECTION ( 'NONE',  ( -4.336808689941752679E-15, 0.8660254037844482555, 0.4999999999999837907 ) ) ;
#199580=AXIS2_PLACEMENT_3D ( 'NONE', #196483, #235608, #197772 ) ;
#199582=SPHERICAL_SURFACE ( 'NONE', #76769, 0.1000000000000000056 ) ;
#199588=ORIENTED_EDGE ( 'NONE', *, *, #142671, .F. ) ;
#199602=DIRECTION ( 'NONE',  ( 1.000000000000000000, 0.000000000000000000, 0.000000000000000000 ) ) ;
#199639=ORIENTED_EDGE ( 'NONE', *, *, #23856, .F. ) ;
#199648=CARTESIAN_POINT ( 'NONE',  ( 20.94999999999999929, 5.000000000011153745, -121.9947339810869380 ) ) ;
#199649=DIRECTION ( 'NONE',  ( 0.000000000000000000, 0.000000000000000000, -1.000000000000000000 ) ) ;
#199655=ORIENTED_EDGE ( 'NONE', *, *, #135513, .T. ) ;
#199679=ORIENTED_EDGE ( 'NONE', *, *, #139375, .F. ) ;
#199699=AXIS2_PLACEMENT_3D ( 'NONE', #149031, #70787, #147732 ) ;
#199718=CARTESIAN_POINT ( 'NONE',  ( -21.05000000000000071, -0.09999996528893663472, -94.02244781750655989 ) ) ;
#199721=AXIS2_PLACEMENT_3D ( 'NONE', #70781, #72047, #149023 ) ;
#199725=CARTESIAN_POINT ( 'NONE',  ( -21.55000000000000071, 7.350000000011155166, -112.8500000000000369 ) ) ;
#199727=CARTESIAN_POINT ( 'NONE',  ( 23.24999999999999289, 11.65000000001116298, -100.6000000000000369 ) ) ;
#199732=CARTESIAN_POINT ( 'NONE',  ( -20.85000000000000142, -1.736705739456431807, -145.5174225876237699 ) ) ;
#199753=FACE_OUTER_BOUND ( 'NONE', #133140, .T. ) ;
#199754=AXIS2_PLACEMENT_3D ( 'NONE', #250144, #191483, #117052 ) ;
#199773=LINE ( 'NONE', #220603, #27911 ) ;
#199803=DIRECTION ( 'NONE',  ( 1.000000000000000000, -7.304098846218134667E-16, -4.217023435051625732E-16 ) ) ;
#199808=CARTESIAN_POINT ( 'NONE',  ( 18.59999999999997655, 1.115600667400684642E-11, -134.0000000000000284 ) ) ;
#199812=ORIENTED_EDGE ( 'NONE', *, *, #77922, .T. ) ;
#199819=ORIENTED_EDGE ( 'NONE', *, *, #58559, .T. ) ;
#199857=ORIENTED_EDGE ( 'NONE', *, *, #189790, .F. ) ;
#199867=CYLINDRICAL_SURFACE ( 'NONE', #21885, 0.1000000000000028644 ) ;
#199874=ORIENTED_EDGE ( 'NONE', *, *, #116606, .F. ) ;
#199911=DIRECTION ( 'NONE',  ( 0.000000000000000000, -0.9908441862701600211, -0.1350103645451876666 ) ) ;
#199916=DIRECTION ( 'NONE',  ( 0.000000000000000000, -0.4930308989874653269, -0.8700118002898649117 ) ) ;
#199922=CARTESIAN_POINT ( 'NONE',  ( -21.53699400384214968, 1.542889524662434004E-12, -93.71228820675507620 ) ) ;
#199939=CYLINDRICAL_SURFACE ( 'NONE', #20079, 0.09999999999998898659 ) ;
#199941=CYLINDRICAL_SURFACE ( 'NONE', #64630, 0.09999999999999939493 ) ;
#199947=FACE_OUTER_BOUND ( 'NONE', #142071, .T. ) ;
#199958=ORIENTED_EDGE ( 'NONE', *, *, #101345, .T. ) ;
#199961=FACE_OUTER_BOUND ( 'NONE', #67268, .T. ) ;
#199972=CARTESIAN_POINT ( 'NONE',  ( -20.99780126800919078, 11.60538868788780498, -127.0873525717055657 ) ) ;
#199976=DIRECTION ( 'NONE',  ( 1.000000000000000000, 3.265361837132813093E-16, -0.000000000000000000 ) ) ;
#200049=CARTESIAN_POINT ( 'NONE',  ( -20.94999999999999929, 11.65000000001115588, -107.5148057706540357 ) ) ;
#200055=VERTEX_POINT ( 'NONE', #12530 ) ;
#200058=VECTOR ( 'NONE', #164890, 1000.000000000000000 ) ;
#200061=ORIENTED_EDGE ( 'NONE', *, *, #92103, .T. ) ;
#200066=CARTESIAN_POINT ( 'NONE',  ( 23.15000000000000213, -11.74999999998883737, -112.7500000000000284 ) ) ;
#200109=ORIENTED_EDGE ( 'NONE', *, *, #103968, .F. ) ;
#200111=EDGE_CURVE ( 'NONE', #224306, #68117, #194137, .T. ) ;
#200116=CARTESIAN_POINT ( 'NONE',  ( 20.95203847575071521, 10.50106053928516303, -108.0670713486235996 ) ) ;
#200127=CARTESIAN_POINT ( 'NONE',  ( -21.05000000000000071, 6.304961112695925074, -100.5213855659375639 ) ) ;
#200137=ORIENTED_EDGE ( 'NONE', *, *, #113908, .T. ) ;
#200144=DIRECTION ( 'NONE',  ( 1.000000000000000000, 0.000000000000000000, 0.000000000000000000 ) ) ;
#200149=CYLINDRICAL_SURFACE ( 'NONE', #882, 0.09999999999999939493 ) ;
#200160=EDGE_CURVE ( 'NONE', #229941, #157888, #23453, .T. ) ;
#200168=CARTESIAN_POINT ( 'NONE',  ( 21.02374657821589921, 11.60000000083178406, -127.0717967701983326 ) ) ;
#200270=DIRECTION ( 'NONE',  ( 1.000000000000000000, -0.000000000000000000, -0.000000000000000000 ) ) ;
#200275=EDGE_CURVE ( 'NONE', #239256, #159674, #59290, .T. ) ;
#200303=ORIENTED_EDGE ( 'NONE', *, *, #148795, .T. ) ;
#200321=ORIENTED_EDGE ( 'NONE', *, *, #40568, .T. ) ;
#200336=EDGE_CURVE ( 'NONE', #141039, #195862, #98381, .T. ) ;
#200342=ORIENTED_EDGE ( 'NONE', *, *, #33615, .F. ) ;
#200359=CARTESIAN_POINT ( 'NONE',  ( -20.94999999999999929, -11.64999999998884306, -103.6000000000000369 ) ) ;
#200424=EDGE_CURVE ( 'NONE', #26109, #198727, #77553, .T. ) ;
#200483=FACE_OUTER_BOUND ( 'NONE', #186069, .T. ) ;
#200496=EDGE_CURVE ( 'NONE', #155920, #70151, #91748, .T. ) ;
#200497=EDGE_LOOP ( 'NONE', ( #172343, #204590, #181074, #116933 ) ) ;
#200510=DIRECTION ( 'NONE',  ( -0.000000000000000000, -0.1350103645451876666, 0.9908441862701600211 ) ) ;
#200526=ORIENTED_EDGE ( 'NONE', *, *, #203898, .T. ) ;
#200538=CARTESIAN_POINT ( 'NONE',  ( -18.41809261886922755, -9.682403314745256395, -140.6568435500915086 ) ) ;
#200548=AXIS2_PLACEMENT_3D ( 'NONE', #17359, #344, #236394 ) ;
#200552=ORIENTED_EDGE ( 'NONE', *, *, #68482, .F. ) ;
#200562=DIRECTION ( 'NONE',  ( 0.000000000000000000, 0.000000000000000000, -1.000000000000000000 ) ) ;
#200602=ORIENTED_EDGE ( 'NONE', *, *, #4249, .F. ) ;
#200612=ORIENTED_EDGE ( 'NONE', *, *, #160481, .T. ) ;
#200643=CYLINDRICAL_SURFACE ( 'NONE', #133026, 0.09999999999999892308 ) ;
#200657=ORIENTED_EDGE ( 'NONE', *, *, #43350, .F. ) ;
#200663=CARTESIAN_POINT ( 'NONE',  ( -23.25000000000000000, -8.999999999988844479, -124.1060308773475924 ) ) ;
#200689=SPHERICAL_SURFACE ( 'NONE', #162796, 0.1000000000000000056 ) ;
#200711=AXIS2_PLACEMENT_3D ( 'NONE', #35246, #114752, #16945 ) ;
#200808=AXIS2_PLACEMENT_3D ( 'NONE', #76535, #97352, #234325 ) ;
#200843=ORIENTED_EDGE ( 'NONE', *, *, #239413, .F. ) ;
#200866=DIRECTION ( 'NONE',  ( 1.000000000000000000, 0.000000000000000000, 0.000000000000000000 ) ) ;
#200874=CYLINDRICAL_SURFACE ( 'NONE', #188517, 0.1000000000000028644 ) ;
#200878=CARTESIAN_POINT ( 'NONE',  ( 21.05000000000000071, 5.400000000011154988, -121.5947339810869465 ) ) ;
#200879=VERTEX_POINT ( 'NONE', #106476 ) ;
#200888=CIRCLE ( 'NONE', #25942, 4.300000000000025580 ) ;
#200900=DIRECTION ( 'NONE',  ( 0.000000000000000000, 0.000000000000000000, -1.000000000000000000 ) ) ;
#200901=DIRECTION ( 'NONE',  ( 3.265361837132813093E-16, -1.000000000000000000, -0.000000000000000000 ) ) ;
#200911=CARTESIAN_POINT ( 'NONE',  ( 21.07928932188134397, 0.09889514566555242248, -94.17148334360672379 ) ) ;
#200912=EDGE_CURVE ( 'NONE', #215032, #167562, #102869, .T. ) ;
#200945=CARTESIAN_POINT ( 'NONE',  ( -20.54999999999999716, 2.000000000011154189, -113.7246219227621395 ) ) ;
#200971=EDGE_CURVE ( 'NONE', #142813, #100304, #69597, .T. ) ;
#200997=DIRECTION ( 'NONE',  ( 0.000000000000000000, 1.000000000000000000, 0.000000000000000000 ) ) ;
#201033=DIRECTION ( 'NONE',  ( 1.000000000000000000, 7.304098846218134667E-16, -4.607487905232622991E-31 ) ) ;
#201045=SPHERICAL_SURFACE ( 'NONE', #199375, 0.1000000000000000056 ) ;
#201056=EDGE_LOOP ( 'NONE', ( #217614, #92113, #157598, #75597 ) ) ;
#201150=AXIS2_PLACEMENT_3D ( 'NONE', #65572, #8184, #185528 ) ;
#201174=EDGE_LOOP ( 'NONE', ( #8054, #26443, #128654, #8354 ) ) ;
#201194=AXIS2_PLACEMENT_3D ( 'NONE', #40241, #100152, #16817 ) ;
#201202=ORIENTED_EDGE ( 'NONE', *, *, #9110, .F. ) ;
#201228=TOROIDAL_SURFACE ( 'NONE', #234550, 11.65000000000000036, 0.1000000000000000056 ) ;
#201231=CARTESIAN_POINT ( 'NONE',  ( -20.99551997958415583, 11.75000000001124434, -127.1516591376888954 ) ) ;
#201233=LINE ( 'NONE', #22630, #40278 ) ;
#201241=CARTESIAN_POINT ( 'NONE',  ( -23.15000000000000213, 4.250000000011156409, -112.8500000000000369 ) ) ;
#201244=VERTEX_POINT ( 'NONE', #86614 ) ;
#201283=ADVANCED_FACE ( 'NONE', ( #27990 ), #175786, .T. ) ;
#201288=DIRECTION ( 'NONE',  ( 0.000000000000000000, 0.000000000000000000, 1.000000000000000000 ) ) ;
#201293=ORIENTED_EDGE ( 'NONE', *, *, #22678, .T. ) ;
#201336=AXIS2_PLACEMENT_3D ( 'NONE', #10760, #72027, #126852 ) ;
#201341=CARTESIAN_POINT ( 'NONE',  ( 21.05000000000000071, 1.162701749949165642, -108.6000000000000227 ) ) ;
#201358=CARTESIAN_POINT ( 'NONE',  ( -21.05000000000000071, -11.48912529306490349, -103.6000000000000369 ) ) ;
#201363=ORIENTED_EDGE ( 'NONE', *, *, #150699, .T. ) ;
#201388=DIRECTION ( 'NONE',  ( 0.000000000000000000, 1.000000000000000000, -1.224646799147353207E-16 ) ) ;
#201410=CIRCLE ( 'NONE', #88968, 0.09999999999999939493 ) ;
#201423=EDGE_CURVE ( 'NONE', #140720, #107194, #210460, .T. ) ;
#201480=CARTESIAN_POINT ( 'NONE',  ( -21.59780538579341425, 6.847090529954407145, -100.4010213304020454 ) ) ;
#201520=ADVANCED_FACE ( 'NONE', ( #16947 ), #53496, .F. ) ;
#201528=CARTESIAN_POINT ( 'NONE',  ( -23.15000000000000213, 4.350000000011156054, -112.7500000000000284 ) ) ;
#201534=AXIS2_PLACEMENT_3D ( 'NONE', #130834, #151721, #69598 ) ;
#201554=CARTESIAN_POINT ( 'NONE',  ( 18.59999999999999076, 10.20857864377385127, -121.8500000000000369 ) ) ;
#201573=FACE_OUTER_BOUND ( 'NONE', #25474, .T. ) ;
#201576=CARTESIAN_POINT ( 'NONE',  ( 19.86930884467607328, 11.68691006698174739, -125.2392226389383012 ) ) ;
#201586=CARTESIAN_POINT ( 'NONE',  ( 20.97107704358301916, 8.875478152032441059, -109.0589732293892951 ) ) ;
#201588=AXIS2_PLACEMENT_3D ( 'NONE', #211436, #152782, #208869 ) ;
#201589=FACE_OUTER_BOUND ( 'NONE', #6261, .T. ) ;
#201599=AXIS2_PLACEMENT_3D ( 'NONE', #42839, #257981, #2405 ) ;
#201616=TOROIDAL_SURFACE ( 'NONE', #68358, 0.2000000000000000111, 0.1000000000000000056 ) ;
#201680=CARTESIAN_POINT ( 'NONE',  ( -23.15000000000000213, 2.000000000011154189, -113.7246219227621395 ) ) ;
#201720=PLANE ( 'NONE',  #199482 ) ;
#201730=FACE_OUTER_BOUND ( 'NONE', #62961, .T. ) ;
#201736=VERTEX_POINT ( 'NONE', #229482 ) ;
#201740=EDGE_CURVE ( 'NONE', #234652, #240390, #170839, .T. ) ;
#201753=DIRECTION ( 'NONE',  ( -1.000000000000000000, -0.000000000000000000, 0.000000000000000000 ) ) ;
#201757=EDGE_LOOP ( 'NONE', ( #257028, #66600, #207453, #167226 ) ) ;
#201765=FACE_OUTER_BOUND ( 'NONE', #185171, .T. ) ;
#201770=CIRCLE ( 'NONE', #235119, 11.80000000000000426 ) ;
#201794=ORIENTED_EDGE ( 'NONE', *, *, #3215, .T. ) ;
#201833=EDGE_CURVE ( 'NONE', #240390, #90545, #86473, .T. ) ;
#201836=CARTESIAN_POINT ( 'NONE',  ( 20.94999999999999574, -11.41227409413852989, -103.5000000000000426 ) ) ;
#201845=CARTESIAN_POINT ( 'NONE',  ( -21.05000000000000071, 11.65000000001115232, -107.2838656629781724 ) ) ;
#201848=EDGE_CURVE ( 'NONE', #168409, #22177, #32563, .T. ) ;
#201894=EDGE_LOOP ( 'NONE', ( #211131, #5391, #76562, #123492 ) ) ;
#201899=DIRECTION ( 'NONE',  ( 0.000000000000000000, 1.000000000000000000, 0.000000000000000000 ) ) ;
#201962=CIRCLE ( 'NONE', #72803, 0.09999999999999939493 ) ;
#201985=EDGE_CURVE ( 'NONE', #253683, #85377, #203950, .T. ) ;
#201993=CARTESIAN_POINT ( 'NONE',  ( -22.59999999999999787, 11.74956712350054744, -100.3991416309013260 ) ) ;
#202033=DIRECTION ( 'NONE',  ( 1.000000000000000000, 0.000000000000000000, 0.000000000000000000 ) ) ;
#202059=DIRECTION ( 'NONE',  ( -2.952720810173288619E-16, 1.000000000000000000, 0.000000000000000000 ) ) ;
#202061=ADVANCED_FACE ( 'NONE', ( #81908 ), #107927, .F. ) ;
#202080=LINE ( 'NONE', #61280, #68595 ) ;
#202086=DIRECTION ( 'NONE',  ( 0.000000000000000000, -0.1350103645451876666, 0.9908441862701600211 ) ) ;
#202100=VECTOR ( 'NONE', #78414, 1000.000000000000000 ) ;
#202105=CARTESIAN_POINT ( 'NONE',  ( -20.85000000000000142, 7.021664781911246322, -137.8335654018973457 ) ) ;
#202108=DIRECTION ( 'NONE',  ( 0.000000000000000000, 0.9908441862701596881, -0.1350103645451904977 ) ) ;
#202110=DIRECTION ( 'NONE',  ( 0.000000000000000000, 0.000000000000000000, -1.000000000000000000 ) ) ;
#202139=CARTESIAN_POINT ( 'NONE',  ( -18.59999999999999787, -1.637172712959223952, -112.0821533654720383 ) ) ;
#202143=DIRECTION ( 'NONE',  ( 1.000000000000000000, -0.000000000000000000, -0.000000000000000000 ) ) ;
#202171=ORIENTED_EDGE ( 'NONE', *, *, #213281, .T. ) ;
#202182=AXIS2_PLACEMENT_3D ( 'NONE', #108423, #150134, #187963 ) ;
#202193=ORIENTED_EDGE ( 'NONE', *, *, #71042, .T. ) ;
#202200=EDGE_LOOP ( 'NONE', ( #250791, #67388, #39292, #146665, #209004 ) ) ;
#202232=FACE_OUTER_BOUND ( 'NONE', #83690, .T. ) ;
#202252=DIRECTION ( 'NONE',  ( 0.000000000000000000, 0.9908441862701596881, -0.1350103645451904977 ) ) ;
#202289=CIRCLE ( 'NONE', #206376, 0.09999999999998898659 ) ;
#202291=VECTOR ( 'NONE', #95589, 1000.000000000000000 ) ;
#202298=AXIS2_PLACEMENT_3D ( 'NONE', #181724, #141307, #123037 ) ;
#202345=MECHANICAL_DESIGN_GEOMETRIC_PRESENTATION_REPRESENTATION('',(#23306),#231570);
#202371=DIRECTION ( 'NONE',  ( 0.000000000000000000, 0.000000000000000000, 1.000000000000000000 ) ) ;
#202400=ADVANCED_FACE ( 'NONE', ( #201573 ), #45073, .T. ) ;
#202430=EDGE_LOOP ( 'NONE', ( #247027, #87732, #174459, #16848, #204481 ) ) ;
#202442=ADVANCED_FACE ( 'NONE', ( #230129 ), #149336, .F. ) ;
#202456=EDGE_CURVE ( 'NONE', #149886, #37861, #154012, .T. ) ;
#202506=EDGE_LOOP ( 'NONE', ( #88336, #139277, #86377, #124958 ) ) ;
#202529=DIRECTION ( 'NONE',  ( 1.000000000000000000, -0.000000000000000000, -0.000000000000000000 ) ) ;
#202530=CARTESIAN_POINT ( 'NONE',  ( -18.39999999999999858, -9.519327731081281385, -107.4729763765593589 ) ) ;
#202534=LINE ( 'NONE', #40927, #35353 ) ;
#202539=DIRECTION ( 'NONE',  ( -1.000000000000000000, -2.952720810173289112E-16, 0.000000000000000000 ) ) ;
#202562=ORIENTED_EDGE ( 'NONE', *, *, #148579, .F. ) ;
#202623=DIRECTION ( 'NONE',  ( 0.000000000000000000, 0.000000000000000000, -1.000000000000000000 ) ) ;
#202624=AXIS2_PLACEMENT_3D ( 'NONE', #60735, #200270, #159878 ) ;
#202683=CARTESIAN_POINT ( 'NONE',  ( 20.95512820512820440, 8.876151316299271343, -112.6500000000000341 ) ) ;
#202720=ORIENTED_EDGE ( 'NONE', *, *, #52531, .F. ) ;
#202754=EDGE_LOOP ( 'NONE', ( #220948, #225989, #25435, #29667, #111722, #202193, #125570, #121386, #67577, #166677, #225440, #58481, #212942, #114945, #183599, #234287, #52945, #129664, #244550, #188232, #138406, #67716, #2233, #94044, #249762 ) ) ;
#202763=FACE_OUTER_BOUND ( 'NONE', #10548, .T. ) ;
#202793=DIRECTION ( 'NONE',  ( -0.000000000000000000, -0.000000000000000000, -1.000000000000000000 ) ) ;
#202807=CARTESIAN_POINT ( 'NONE',  ( 18.59999999999999076, -1.149570369564537842, -141.8159124845019790 ) ) ;
#202823=EDGE_CURVE ( 'NONE', #254324, #74301, #12251, .T. ) ;
#202831=CARTESIAN_POINT ( 'NONE',  ( 20.95429693346636313, 10.54330487990688958, -108.0608825383130522 ) ) ;
#202880=ORIENTED_EDGE ( 'NONE', *, *, #37310, .T. ) ;
#202922=ORIENTED_EDGE ( 'NONE', *, *, #193242, .F. ) ;
#202947=DIRECTION ( 'NONE',  ( -0.000000000000000000, 0.01283462868039629209, -0.9999176327611372095 ) ) ;
#202985=EDGE_CURVE ( 'NONE', #39467, #154121, #162091, .T. ) ;
#203060=CIRCLE ( 'NONE', #90624, 0.09999999999999939493 ) ;
#203101=FACE_OUTER_BOUND ( 'NONE', #248717, .T. ) ;
#203106=TOROIDAL_SURFACE ( 'NONE', #61646, 0.4000000000000009104, 0.1000000000000000056 ) ;
#203140=CARTESIAN_POINT ( 'NONE',  ( 22.41477678272288188, 0.0008238657741001872850, -88.85041471548463221 ) ) ;
#203179=ORIENTED_EDGE ( 'NONE', *, *, #83397, .T. ) ;
#203217=DIRECTION ( 'NONE',  ( 0.000000000000000000, -0.8660254037844384856, 0.5000000000000002220 ) ) ;
#203225=ORIENTED_EDGE ( 'NONE', *, *, #74826, .F. ) ;
#203267=CARTESIAN_POINT ( 'NONE',  ( -21.44999999999999929, 7.250000000011155521, -121.6500000000000341 ) ) ;
#203293=DIRECTION ( 'NONE',  ( -7.304098846218134667E-16, -1.000000000000000000, 0.000000000000000000 ) ) ;
#203307=ADVANCED_FACE ( 'NONE', ( #109569 ), #66591, .T. ) ;
#203310=DIRECTION ( 'NONE',  ( 0.000000000000000000, -1.000000000000000000, -0.000000000000000000 ) ) ;
#203320=CARTESIAN_POINT ( 'NONE',  ( -21.05000000000000071, -1.261786168553869603, -108.5864989635455089 ) ) ;
#203323=ORIENTED_EDGE ( 'NONE', *, *, #30866, .T. ) ;
#203402=DIRECTION ( 'NONE',  ( -0.000000000000000000, 1.000000000000000000, 0.000000000000000000 ) ) ;
#203420=CARTESIAN_POINT ( 'NONE',  ( 21.05000000000000071, -11.64999999998883595, -131.0000000000000284 ) ) ;
#203550=FACE_OUTER_BOUND ( 'NONE', #137879, .T. ) ;
#203585=CARTESIAN_POINT ( 'NONE',  ( -18.50000000000000000, 11.75000000001115552, -112.6500000000000341 ) ) ;
#203589=EDGE_CURVE ( 'NONE', #78774, #120951, #233198, .T. ) ;
#203608=DIRECTION ( 'NONE',  ( 1.000000000000000000, 0.000000000000000000, -0.000000000000000000 ) ) ;
#203614=CARTESIAN_POINT ( 'NONE',  ( -23.25000000000000000, 1.115600667400684642E-11, -134.0000000000000284 ) ) ;
#203671=CARTESIAN_POINT ( 'NONE',  ( -20.85000000000000142, -1.149570369564537842, -141.8159124845019790 ) ) ;
#203676=EDGE_LOOP ( 'NONE', ( #71114, #12141 ) ) ;
#203702=CARTESIAN_POINT ( 'NONE',  ( 23.25000000000000000, -11.64999999998883595, -88.75000000000004263 ) ) ;
#203726=EDGE_CURVE ( 'NONE', #116896, #74961, #216018, .T. ) ;
#203729=EDGE_LOOP ( 'NONE', ( #122918, #88899, #216241, #107251 ) ) ;
#203740=ORIENTED_EDGE ( 'NONE', *, *, #216985, .T. ) ;
#203750=EDGE_CURVE ( 'NONE', #173650, #219752, #245076, .T. ) ;
#203753=VERTEX_POINT ( 'NONE', #61819 ) ;
#203755=ORIENTED_EDGE ( 'NONE', *, *, #58285, .F. ) ;
#203756=CARTESIAN_POINT ( 'NONE',  ( -22.00356870069490967, -4.067518095897675031E-12, -93.24575763824979902 ) ) ;
#203774=FACE_OUTER_BOUND ( 'NONE', #49509, .T. ) ;
#203783=ORIENTED_EDGE ( 'NONE', *, *, #100753, .T. ) ;
#203793=VERTEX_POINT ( 'NONE', #222137 ) ;
#203804=CARTESIAN_POINT ( 'NONE',  ( -20.94999999999999929, 11.65000000001115588, -127.2161343370219413 ) ) ;
#203817=AXIS2_PLACEMENT_3D ( 'NONE', #203854, #125603, #201288 ) ;
#203834=CARTESIAN_POINT ( 'NONE',  ( 20.94999999999999929, -11.64999999998883595, -134.0000000000000284 ) ) ;
#203854=CARTESIAN_POINT ( 'NONE',  ( -22.50000000000000000, 1.115600667400684642E-11, -100.5000000000000284 ) ) ;
#203866=ORIENTED_EDGE ( 'NONE', *, *, #250205, .F. ) ;
#203898=EDGE_CURVE ( 'NONE', #191859, #148589, #128212, .T. ) ;
#203900=EDGE_CURVE ( 'NONE', #173746, #54193, #45340, .T. ) ;
#203908=ORIENTED_EDGE ( 'NONE', *, *, #30844, .T. ) ;
#203918=DIRECTION ( 'NONE',  ( 0.000000000000000000, -1.000000000000000000, 0.000000000000000000 ) ) ;
#203924=CARTESIAN_POINT ( 'NONE',  ( -21.07928932188134041, 0.09889514566555068775, -94.17148334360673800 ) ) ;
#203950=( BOUNDED_CURVE ( )  B_SPLINE_CURVE ( 3, ( #207035, #106618, #184895, #122367 ),
 .UNSPECIFIED., .F., .F. ) 
 B_SPLINE_CURVE_WITH_KNOTS ( ( 4, 4 ),
 ( 0.06456096931748307732, 3.077031684272310219 ),
 .UNSPECIFIED. ) 
 CURVE ( )  GEOMETRIC_REPRESENTATION_ITEM ( )  RATIONAL_B_SPLINE_CURVE ( ( 1.000000000000000000, 0.3763440860215093164, 0.3763440860215093164, 1.000000000000000000 ) ) 
 REPRESENTATION_ITEM ( '' )  );
#203957=DIRECTION ( 'NONE',  ( 0.000000000000000000, -0.5000000000000078826, 0.8660254037844340447 ) ) ;
#203958=DIRECTION ( 'NONE',  ( -1.000000000000000000, -0.000000000000000000, 0.000000000000000000 ) ) ;
#203974=CARTESIAN_POINT ( 'NONE',  ( 22.50014994444007499, 11.74971973190324448, -100.4169198432808372 ) ) ;
#203992=CARTESIAN_POINT ( 'NONE',  ( -21.33487959338958362, 6.725558151922345296, -100.5000000000000284 ) ) ;
#204031=CARTESIAN_POINT ( 'NONE',  ( -21.14999999999999858, 6.540656951712397138, -100.5000000000000284 ) ) ;
#204060=CARTESIAN_POINT ( 'NONE',  ( -21.05000000000000071, 6.300000000011169554, -100.6000000000000369 ) ) ;
#204073=ORIENTED_EDGE ( 'NONE', *, *, #232337, .F. ) ;
#204081=DIRECTION ( 'NONE',  ( 5.421010862427554711E-16, -1.000000000000000000, -3.252606517456533024E-15 ) ) ;
#204086=DIRECTION ( 'NONE',  ( -0.000000000000000000, 1.000000000000000000, 1.734723475976807292E-15 ) ) ;
#204106=VECTOR ( 'NONE', #139002, 1000.000000000000000 ) ;
#204119=ORIENTED_EDGE ( 'NONE', *, *, #183003, .F. ) ;
#204131=EDGE_CURVE ( 'NONE', #198561, #214263, #134598, .T. ) ;
#204132=VECTOR ( 'NONE', #124993, 1000.000000000000000 ) ;
#204135=ORIENTED_EDGE ( 'NONE', *, *, #57269, .F. ) ;
#204145=CARTESIAN_POINT ( 'NONE',  ( 20.22483756094572271, 9.501904678882469923, -108.6395391287147305 ) ) ;
#204149=CARTESIAN_POINT ( 'NONE',  ( 21.05000000000000071, 1.115600667400684642E-11, -134.0000000000000284 ) ) ;
#204190=CARTESIAN_POINT ( 'NONE',  ( -21.05000000000000071, 1.115600667400684642E-11, -134.0000000000000284 ) ) ;
#204232=EDGE_CURVE ( 'NONE', #11304, #24198, #41283, .T. ) ;
#204239=DIRECTION ( 'NONE',  ( 0.000000000000000000, 0.000000000000000000, 1.000000000000000000 ) ) ;
#204250=DIRECTION ( 'NONE',  ( 0.000000000000000000, 0.000000000000000000, 1.000000000000000000 ) ) ;
#204311=DIRECTION ( 'NONE',  ( 0.000000000000000000, 0.000000000000000000, -1.000000000000000000 ) ) ;
#204337=EDGE_CURVE ( 'NONE', #63872, #110634, #127909, .T. ) ;
#204342=ORIENTED_EDGE ( 'NONE', *, *, #239268, .F. ) ;
#204352=DIRECTION ( 'NONE',  ( 0.000000000000000000, -1.000000000000000000, 6.308085367188393199E-16 ) ) ;
#204374=ORIENTED_EDGE ( 'NONE', *, *, #59120, .F. ) ;
#204410=CYLINDRICAL_SURFACE ( 'NONE', #181612, 0.09999999999999939493 ) ;
#204417=DIRECTION ( 'NONE',  ( 0.000000000000000000, 1.000000000000000000, 0.000000000000000000 ) ) ;
#204464=DIRECTION ( 'NONE',  ( 0.000000000000000000, 0.000000000000000000, -1.000000000000000000 ) ) ;
#204468=DIRECTION ( 'NONE',  ( 0.000000000000000000, 0.9654727137038726648, -0.2605042016806632943 ) ) ;
#204472=VERTEX_POINT ( 'NONE', #152636 ) ;
#204479=VERTEX_POINT ( 'NONE', #36541 ) ;
#204481=ORIENTED_EDGE ( 'NONE', *, *, #13411, .F. ) ;
#204502=DIRECTION ( 'NONE',  ( 1.000000000000000000, 0.000000000000000000, -0.000000000000000000 ) ) ;
#204513=EDGE_LOOP ( 'NONE', ( #43872, #256411, #104530, #109542, #108218, #110406, #131890 ) ) ;
#204519=CARTESIAN_POINT ( 'NONE',  ( 23.24999999999999645, 5.600000000011153389, -112.9052660189131245 ) ) ;
#204523=VERTEX_POINT ( 'NONE', #196847 ) ;
#204540=AXIS2_PLACEMENT_3D ( 'NONE', #205698, #85720, #23253 ) ;
#204548=DIRECTION ( 'NONE',  ( 0.000000000000000000, 0.000000000000000000, 1.000000000000000000 ) ) ;
#204574=ORIENTED_EDGE ( 'NONE', *, *, #107422, .F. ) ;
#204590=ORIENTED_EDGE ( 'NONE', *, *, #90224, .F. ) ;
#204592=DIRECTION ( 'NONE',  ( 1.000000000000000000, -0.000000000000000000, -0.000000000000000000 ) ) ;
#204629=DIRECTION ( 'NONE',  ( -1.000000000000000000, 0.000000000000000000, 0.000000000000000000 ) ) ;
#204639=EDGE_CURVE ( 'NONE', #173650, #69817, #20604, .T. ) ;
#204700=FACE_OUTER_BOUND ( 'NONE', #206786, .T. ) ;
#204766=ORIENTED_EDGE ( 'NONE', *, *, #96436, .T. ) ;
#204780=CARTESIAN_POINT ( 'NONE',  ( 23.24999999999999645, 4.775700934590584090, -112.3487681040460160 ) ) ;
#204787=EDGE_LOOP ( 'NONE', ( #111391, #200612, #107834, #207960 ) ) ;
#204801=CARTESIAN_POINT ( 'NONE',  ( -20.64999999999999858, -9.399999999988846611, -124.1060308773475924 ) ) ;
#204806=CARTESIAN_POINT ( 'NONE',  ( -23.25000000000000000, -1.835859311432481045, -145.6044391687985637 ) ) ;
#204838=TOROIDAL_SURFACE ( 'NONE', #75697, 0.9750000000000019762, 0.1000000000000000056 ) ;
#204855=AXIS2_PLACEMENT_3D ( 'NONE', #91232, #208618, #152512 ) ;
#204870=CIRCLE ( 'NONE', #38473, 7.899999999999990585 ) ;
#204877=CARTESIAN_POINT ( 'NONE',  ( 23.25000000000000000, 11.75000000001116263, -121.8500000000000369 ) ) ;
#204883=DIRECTION ( 'NONE',  ( 0.000000000000000000, 0.000000000000000000, -1.000000000000000000 ) ) ;
#204925=CARTESIAN_POINT ( 'NONE',  ( -18.59999999999999787, 11.65000000001115232, -121.8500000000000369 ) ) ;
#204938=CARTESIAN_POINT ( 'NONE',  ( 18.59999999999999432, -1.162701749926853712, -108.6000000000000227 ) ) ;
#204964=CIRCLE ( 'NONE', #238289, 12.97499999999999964 ) ;
#204988=CARTESIAN_POINT ( 'NONE',  ( -20.00857864376270001, 9.350000000011156942, -121.6500000000000341 ) ) ;
#204989=ORIENTED_EDGE ( 'NONE', *, *, #98760, .F. ) ;
#205022=AXIS2_PLACEMENT_3D ( 'NONE', #99538, #181687, #242927 ) ;
#205046=ORIENTED_EDGE ( 'NONE', *, *, #18394, .F. ) ;
#205066=ORIENTED_EDGE ( 'NONE', *, *, #232207, .F. ) ;
#205086=EDGE_LOOP ( 'NONE', ( #130161, #48745, #133951, #222029 ) ) ;
#205087=AXIS2_PLACEMENT_3D ( 'NONE', #172840, #189789, #168983 ) ;
#205143=CIRCLE ( 'NONE', #109474, 0.1000000000000028644 ) ;
#205172=CIRCLE ( 'NONE', #163501, 0.09999999999998898659 ) ;
#205221=ORIENTED_EDGE ( 'NONE', *, *, #143768, .F. ) ;
#205232=EDGE_LOOP ( 'NONE', ( #26323, #188734, #11299, #152172 ) ) ;
#205235=AXIS2_PLACEMENT_3D ( 'NONE', #13862, #73867, #153414 ) ;
#205257=AXIS2_PLACEMENT_3D ( 'NONE', #145012, #9355, #5489 ) ;
#205309=ORIENTED_EDGE ( 'NONE', *, *, #161975, .T. ) ;
#205322=ORIENTED_EDGE ( 'NONE', *, *, #184609, .T. ) ;
#205341=ADVANCED_FACE ( 'NONE', ( #192378 ), #133682, .F. ) ;
#205343=CARTESIAN_POINT ( 'NONE',  ( 20.94999999999999929, -11.48912529306489994, -131.0000000000000284 ) ) ;
#205348=VERTEX_POINT ( 'NONE', #80086 ) ;
#205357=EDGE_LOOP ( 'NONE', ( #40594, #118109, #78256, #32198 ) ) ;
#205378=DIRECTION ( 'NONE',  ( 0.000000000000000000, 1.000000000000000000, 0.000000000000000000 ) ) ;
#205381=CARTESIAN_POINT ( 'NONE',  ( -18.60000000000000142, -9.523954320741633950, -140.8820170568273795 ) ) ;
#205448=CARTESIAN_POINT ( 'NONE',  ( -21.53699400380730111, 6.787711793201517629, -100.5000000000000426 ) ) ;
#205449=CARTESIAN_POINT ( 'NONE',  ( 23.14999999999999503, 11.75000000001116263, -121.8500000000000369 ) ) ;
#205476=DIRECTION ( 'NONE',  ( 0.000000000000000000, 0.000000000000000000, -1.000000000000000000 ) ) ;
#205483=CARTESIAN_POINT ( 'NONE',  ( 20.12500000000000000, 9.750000000011153745, -108.6117712821143186 ) ) ;
#205512=DIRECTION ( 'NONE',  ( 0.000000000000000000, 0.5000000000000078826, -0.8660254037844340447 ) ) ;
#205540=DIRECTION ( 'NONE',  ( 0.000000000000000000, 0.000000000000000000, -1.000000000000000000 ) ) ;
#205549=CARTESIAN_POINT ( 'NONE',  ( 22.00411653889210228, 0.09903810579707052197, -93.24655713235962651 ) ) ;
#205566=EDGE_LOOP ( 'NONE', ( #67472, #61868, #157799, #134805 ) ) ;
#205593=ORIENTED_EDGE ( 'NONE', *, *, #34130, .T. ) ;
#205647=EDGE_CURVE ( 'NONE', #250577, #61689, #137822, .T. ) ;
#205675=DIRECTION ( 'NONE',  ( 0.000000000000000000, 0.000000000000000000, -1.000000000000000000 ) ) ;
#205686=LINE ( 'NONE', #248681, #138769 ) ;
#205695=CARTESIAN_POINT ( 'NONE',  ( -20.54999999999999716, -11.74999999998884626, -112.8500000000000369 ) ) ;
#205698=CARTESIAN_POINT ( 'NONE',  ( -20.64999999999999858, 2.000000000011154189, -113.7246219227621395 ) ) ;
#205708=VECTOR ( 'NONE', #41503, 1000.000000000000114 ) ;
#205720=CARTESIAN_POINT ( 'NONE',  ( 21.30000000000002558, 1.115600667400684642E-11, -100.5000000000000284 ) ) ;
#205756=CARTESIAN_POINT ( 'NONE',  ( 18.59999999999996945, 7.021664781911246322, -137.8335654018973457 ) ) ;
#205758=ADVANCED_FACE ( 'NONE', ( #77248 ), #108620, .F. ) ;
#205767=AXIS2_PLACEMENT_3D ( 'NONE', #193296, #55031, #155483 ) ;
#205782=DIRECTION ( 'NONE',  ( -0.000000000000000000, -0.000000000000000000, 1.000000000000000000 ) ) ;
#205791=CARTESIAN_POINT ( 'NONE',  ( -18.59999999999999787, 11.75000000001115552, -121.7500000000000426 ) ) ;
#205826=AXIS2_PLACEMENT_3D ( 'NONE', #70693, #189335, #69397 ) ;
#205833=DIRECTION ( 'NONE',  ( 0.000000000000000000, 0.000000000000000000, 1.000000000000000000 ) ) ;
#205986=VECTOR ( 'NONE', #88037, 1000.000000000000000 ) ;
#205999=ORIENTED_EDGE ( 'NONE', *, *, #210773, .T. ) ;
#206005=CYLINDRICAL_SURFACE ( 'NONE', #123139, 0.1000000000000028644 ) ;
#206009=AXIS2_PLACEMENT_3D ( 'NONE', #58177, #54341, #133884 ) ;
#206057=CARTESIAN_POINT ( 'NONE',  ( -20.54999999999999716, 4.350000000011156054, -121.6500000000000341 ) ) ;
#206080=EDGE_LOOP ( 'NONE', ( #250269, #25440, #219885, #143800 ) ) ;
#206081=CARTESIAN_POINT ( 'NONE',  ( -20.97625342178427843, 11.60000000083146077, -107.4282032298019800 ) ) ;
#206090=DIRECTION ( 'NONE',  ( 0.000000000000000000, 0.000000000000000000, -1.000000000000000000 ) ) ;
#206110=AXIS2_PLACEMENT_3D ( 'NONE', #192032, #95468, #13379 ) ;
#206143=CARTESIAN_POINT ( 'NONE',  ( 21.07928932188134397, 6.328516656404459262, -100.4011048543456468 ) ) ;
#206153=DIRECTION ( 'NONE',  ( 0.000000000000000000, -1.000000000000000000, 0.000000000000000000 ) ) ;
#206185=DIRECTION ( 'NONE',  ( 4.504528286903032433E-15, -0.1298341882520124002, -0.9915357197604841577 ) ) ;
#206204=DIRECTION ( 'NONE',  ( 0.000000000000000000, 0.000000000000000000, -1.000000000000000000 ) ) ;
#206236=CARTESIAN_POINT ( 'NONE',  ( -23.15000000000000213, 1.925233644870972816, -113.2302435331261563 ) ) ;
#206255=VECTOR ( 'NONE', #159226, 1000.000000000000114 ) ;
#206274=CARTESIAN_POINT ( 'NONE',  ( 23.25000000000000000, -11.74999999998883560, -112.6500000000000341 ) ) ;
#206323=ORIENTED_EDGE ( 'NONE', *, *, #190127, .F. ) ;
#206336=CARTESIAN_POINT ( 'NONE',  ( -20.94999999999999929, -11.64999999998884483, -103.4000000000000341 ) ) ;
#206352=AXIS2_PLACEMENT_3D ( 'NONE', #107274, #202529, #46015 ) ;
#206373=ORIENTED_EDGE ( 'NONE', *, *, #116810, .F. ) ;
#206376=AXIS2_PLACEMENT_3D ( 'NONE', #245218, #66578, #142247 ) ;
#206391=CARTESIAN_POINT ( 'NONE',  ( 18.39999999999999858, -9.599999999988845900, -140.7001893912220680 ) ) ;
#206458=AXIS2_PLACEMENT_3D ( 'NONE', #320, #2879, #18612 ) ;
#206483=VECTOR ( 'NONE', #148496, 1000.000000000000000 ) ;
#206518=ORIENTED_EDGE ( 'NONE', *, *, #72317, .F. ) ;
#206553=DIRECTION ( 'NONE',  ( -1.000000000000000000, 0.000000000000000000, 0.000000000000000000 ) ) ;
#206569=CARTESIAN_POINT ( 'NONE',  ( -21.93642651522410247, 7.327166239336959208, -100.5000000000000284 ) ) ;
#206589=CARTESIAN_POINT ( 'NONE',  ( -18.50000000000000355, -9.399999999988814636, -107.7972597596633335 ) ) ;
#206621=CARTESIAN_POINT ( 'NONE',  ( 21.05000000000000071, 11.65000000001116298, -112.6500000000000341 ) ) ;
#206642=DIRECTION ( 'NONE',  ( -1.000000000000000000, 0.000000000000000000, 0.000000000000000000 ) ) ;
#206666=ADVANCED_FACE ( 'NONE', ( #147866 ), #227383, .F. ) ;
#206673=DIRECTION ( 'NONE',  ( 1.000000000000000000, 0.000000000000000000, 0.000000000000000000 ) ) ;
#206691=CARTESIAN_POINT ( 'NONE',  ( 21.05000000000000071, 10.72371710471868056, -108.1649135690876449 ) ) ;
#206696=EDGE_CURVE ( 'NONE', #232157, #241950, #17522, .T. ) ;
#206742=CARTESIAN_POINT ( 'NONE',  ( -23.15000000000000213, -9.599999999988847676, -110.3939691226524786 ) ) ;
#206761=CARTESIAN_POINT ( 'NONE',  ( -23.15000000000000213, 5.900000000011162093, -123.7809002353436654 ) ) ;
#206764=DIRECTION ( 'NONE',  ( 0.000000000000000000, 0.000000000000000000, -1.000000000000000000 ) ) ;
#206767=PLANE ( 'NONE',  #145127 ) ;
#206769=CARTESIAN_POINT ( 'NONE',  ( -20.94999999999999929, 10.29270135741298731, -139.4573618871519614 ) ) ;
#206778=DIRECTION ( 'NONE',  ( 1.000000000000000000, 0.000000000000000000, 0.000000000000000000 ) ) ;
#206786=EDGE_LOOP ( 'NONE', ( #228666, #152764, #231510, #145405 ) ) ;
#206792=ORIENTED_EDGE ( 'NONE', *, *, #227452, .T. ) ;
#206802=ORIENTED_EDGE ( 'NONE', *, *, #99311, .T. ) ;
#206820=DIRECTION ( 'NONE',  ( 1.000000000000000000, 0.000000000000000000, -0.000000000000000000 ) ) ;
#206863=EDGE_CURVE ( 'NONE', #239256, #248313, #159046, .T. ) ;
#206866=DIRECTION ( 'NONE',  ( 0.000000000000000000, 0.008583690987127625890, 0.9999631594459055250 ) ) ;
#206883=AXIS2_PLACEMENT_3D ( 'NONE', #167325, #143867, #142577 ) ;
#206935=CYLINDRICAL_SURFACE ( 'NONE', #3266, 0.1000000000000028644 ) ;
#206945=CARTESIAN_POINT ( 'NONE',  ( -20.94999999999999929, -11.64999999998884483, -134.0000000000000284 ) ) ;
#206961=ORIENTED_EDGE ( 'NONE', *, *, #192488, .F. ) ;
#206979=ORIENTED_EDGE ( 'NONE', *, *, #127447, .T. ) ;
#206997=CARTESIAN_POINT ( 'NONE',  ( 22.47809213839789066, 0.03753706763967752658, -88.85002666521222636 ) ) ;
#207019=DIRECTION ( 'NONE',  ( 0.000000000000000000, 0.000000000000000000, -1.000000000000000000 ) ) ;
#207035=CARTESIAN_POINT ( 'NONE',  ( 20.94999999999999574, 10.47338541492405994, -108.0786544642485865 ) ) ;
#207068=AXIS2_PLACEMENT_3D ( 'NONE', #179827, #1145, #80684 ) ;
#207106=CARTESIAN_POINT ( 'NONE',  ( -20.85000000000000142, 11.75000000001115197, -127.2161343370219413 ) ) ;
#207120=AXIS2_PLACEMENT_3D ( 'NONE', #45488, #165450, #148453 ) ;
#207169=CARTESIAN_POINT ( 'NONE',  ( 18.49505816908823874, -9.437872553199978753, -140.7776572016709054 ) ) ;
#207186=CARTESIAN_POINT ( 'NONE',  ( -18.50000000000000000, -9.499999999988849808, -108.6000000000000227 ) ) ;
#207202=LINE ( 'NONE', #28607, #218142 ) ;
#207203=AXIS2_PLACEMENT_3D ( 'NONE', #258092, #182477, #101594 ) ;
#207206=B_SPLINE_CURVE_WITH_KNOTS ( 'NONE', 3,
 ( #32856, #253130, #112363, #95355, #233591, #229727, #54920, #131912 ),
 .UNSPECIFIED., .F., .F.,
 ( 4, 2, 2, 4 ),
 ( 0.000000000000000000, 0.0002114466876442108679, 0.0003171700314663126563, 0.0004228933752884144175 ),
 .UNSPECIFIED. ) ;
#207218=FACE_OUTER_BOUND ( 'NONE', #239701, .T. ) ;
#207224=ORIENTED_EDGE ( 'NONE', *, *, #93260, .T. ) ;
#207254=ADVANCED_FACE ( 'NONE', ( #241223 ), #175976, .F. ) ;
#207258=DIRECTION ( 'NONE',  ( 1.000000000000000000, 0.000000000000000000, 0.000000000000000000 ) ) ;
#207292=ADVANCED_FACE ( 'NONE', ( #221616 ), #84655, .F. ) ;
#207323=AXIS2_PLACEMENT_3D ( 'NONE', #227376, #26636, #189554 ) ;
#207363=DIRECTION ( 'NONE',  ( 0.000000000000000000, -0.8700118002898359348, 0.4930308989875165082 ) ) ;
#207365=EDGE_CURVE ( 'NONE', #123327, #54036, #204964, .T. ) ;
#207367=CIRCLE ( 'NONE', #19932, 12.87499999999999822 ) ;
#207377=CARTESIAN_POINT ( 'NONE',  ( 21.06600267594171783, 8.775166069211060460, -112.7042627823747694 ) ) ;
#207409=DIRECTION ( 'NONE',  ( -4.239556034732056743E-17, 0.1298341882520022694, 0.9915357197604853789 ) ) ;
#207418=EDGE_LOOP ( 'NONE', ( #93699, #251346, #177495, #213425 ) ) ;
#207425=EDGE_LOOP ( 'NONE', ( #54505, #227008, #71576, #55947 ) ) ;
#207428=CIRCLE ( 'NONE', #128312, 0.09999999999999491240 ) ;
#207438=FACE_OUTER_BOUND ( 'NONE', #125322, .T. ) ;
#207441=CIRCLE ( 'NONE', #82489, 0.09999999999999939493 ) ;
#207442=CIRCLE ( 'NONE', #103169, 0.1000000000000008937 ) ;
#207444=AXIS2_PLACEMENT_3D ( 'NONE', #15678, #112201, #208728 ) ;
#207453=ORIENTED_EDGE ( 'NONE', *, *, #192106, .T. ) ;
#207468=EDGE_CURVE ( 'NONE', #10935, #120254, #205143, .T. ) ;
#207503=ORIENTED_EDGE ( 'NONE', *, *, #110919, .F. ) ;
#207527=LINE ( 'NONE', #28925, #20662 ) ;
#207540=CARTESIAN_POINT ( 'NONE',  ( -18.59999999999999787, -1.835859311432484375, -145.5044391687985694 ) ) ;
#207559=SPHERICAL_SURFACE ( 'NONE', #216990, 0.1000000000000000056 ) ;
#207563=DIRECTION ( 'NONE',  ( 0.000000000000000000, 0.4930308989875230585, 0.8700118002898322711 ) ) ;
#207576=EDGE_CURVE ( 'NONE', #188768, #319, #153718, .T. ) ;
#207589=DIRECTION ( 'NONE',  ( -1.000000000000000000, 0.000000000000000000, 0.000000000000000000 ) ) ;
#207630=ORIENTED_EDGE ( 'NONE', *, *, #201985, .T. ) ;
#207638=ORIENTED_EDGE ( 'NONE', *, *, #24179, .F. ) ;
#207670=EDGE_LOOP ( 'NONE', ( #209311, #48098, #124298 ) ) ;
#207672=AXIS2_PLACEMENT_3D ( 'NONE', #5657, #25271, #146464 ) ;
#207673=CARTESIAN_POINT ( 'NONE',  ( -20.94999999999999929, -11.64999999998884483, -131.0000000000000284 ) ) ;
#207674=EDGE_LOOP ( 'NONE', ( #65068, #128371 ) ) ;
#207691=AXIS2_PLACEMENT_3D ( 'NONE', #127361, #201753, #204311 ) ;
#207706=DIRECTION ( 'NONE',  ( -0.7071067811865475727, -0.7071067811865475727, -0.000000000000000000 ) ) ;
#207721=CIRCLE ( 'NONE', #211814, 0.5000000000000004441 ) ;
#207730=DIRECTION ( 'NONE',  ( 0.000000000000000000, 0.000000000000000000, -1.000000000000000000 ) ) ;
#207740=CARTESIAN_POINT ( 'NONE',  ( 23.14999999999999503, 11.65000000001116298, -127.0851942293460866 ) ) ;
#207773=ORIENTED_EDGE ( 'NONE', *, *, #43348, .T. ) ;
#207785=EDGE_CURVE ( 'NONE', #46619, #14082, #209632, .T. ) ;
#207788=CARTESIAN_POINT ( 'NONE',  ( -18.59999999999999787, 9.250000000011157297, -112.8500000000000369 ) ) ;
#207792=VERTEX_POINT ( 'NONE', #247300 ) ;
#207804=DIRECTION ( 'NONE',  ( 0.000000000000000000, 0.000000000000000000, -1.000000000000000000 ) ) ;
#207845=EDGE_CURVE ( 'NONE', #55613, #101037, #197147, .T. ) ;
#207863=CARTESIAN_POINT ( 'NONE',  ( 18.54286124688534088, -9.623917578786652882, -140.7412023318627234 ) ) ;
#207880=DIRECTION ( 'NONE',  ( 1.000000000000000000, 0.000000000000000000, -0.000000000000000000 ) ) ;
#207900=DIRECTION ( 'NONE',  ( -1.000000000000000000, -2.952720810173289112E-16, 0.000000000000000000 ) ) ;
#207902=CARTESIAN_POINT ( 'NONE',  ( -18.43473496883416729, -9.494952410988140912, -107.5458715722282648 ) ) ;
#207918=VERTEX_POINT ( 'NONE', #215864 ) ;
#207935=EDGE_CURVE ( 'NONE', #135828, #74892, #18084, .T. ) ;
#207951=DIRECTION ( 'NONE',  ( 0.000000000000000000, 0.9654727137038715545, 0.2605042016806676242 ) ) ;
#207960=ORIENTED_EDGE ( 'NONE', *, *, #225427, .T. ) ;
#207964=DIRECTION ( 'NONE',  ( -3.265361837132813093E-16, 1.000000000000000000, 0.000000000000000000 ) ) ;
#207992=EDGE_CURVE ( 'NONE', #10935, #156135, #154662, .T. ) ;
#207995=CARTESIAN_POINT ( 'NONE',  ( 21.05000000000000071, 10.72371681401022592, -108.0943992358844525 ) ) ;
#208035=CARTESIAN_POINT ( 'NONE',  ( 20.86036036209908318, 10.62104277658211693, -108.1663484185050237 ) ) ;
#208039=DIRECTION ( 'NONE',  ( 1.000000000000000000, 3.469446951953704435E-14, -2.003086131649669752E-14 ) ) ;
#208048=ORIENTED_EDGE ( 'NONE', *, *, #170138, .F. ) ;
#208057=( LENGTH_UNIT ( ) NAMED_UNIT ( * ) SI_UNIT ( .MILLI., .METRE. ) );
#208060=ORIENTED_EDGE ( 'NONE', *, *, #44965, .F. ) ;
#208092=CIRCLE ( 'NONE', #78865, 0.1000000000000028644 ) ;
#208108=ORIENTED_EDGE ( 'NONE', *, *, #233925, .F. ) ;
#208117=DIRECTION ( 'NONE',  ( 0.000000000000000000, 0.000000000000000000, -1.000000000000000000 ) ) ;
#208125=DIRECTION ( 'NONE',  ( 0.000000000000000000, 0.000000000000000000, -1.000000000000000000 ) ) ;
#208139=CARTESIAN_POINT ( 'NONE',  ( 18.49999999999998934, 6.450000000011156587, -110.5170271704400591 ) ) ;
#208145=VERTEX_POINT ( 'NONE', #1954 ) ;
#208162=VERTEX_POINT ( 'NONE', #133165 ) ;
#208168=DIRECTION ( 'NONE',  ( -0.000000000000000000, -2.891205793294679805E-16, 1.000000000000000000 ) ) ;
#208170=AXIS2_PLACEMENT_3D ( 'NONE', #61881, #103548, #218356 ) ;
#208192=DIRECTION ( 'NONE',  ( 0.000000000000000000, -0.4999999999999949485, 0.8660254037844415942 ) ) ;
#208234=CARTESIAN_POINT ( 'NONE',  ( 21.05000000000000071, 8.776282648982402179, -108.9875923785189258 ) ) ;
#208242=ORIENTED_EDGE ( 'NONE', *, *, #70623, .T. ) ;
#208248=EDGE_CURVE ( 'NONE', #241028, #124696, #93283, .T. ) ;
#208291=CYLINDRICAL_SURFACE ( 'NONE', #43976, 0.1000000000000028644 ) ;
#208293=CARTESIAN_POINT ( 'NONE',  ( 22.49806830649814060, 0.07746431633666320260, -88.85011034516095663 ) ) ;
#208327=VERTEX_POINT ( 'NONE', #19643 ) ;
#208352=DIRECTION ( 'NONE',  ( -1.000000000000000000, -0.000000000000000000, -0.000000000000000000 ) ) ;
#208404=ORIENTED_EDGE ( 'NONE', *, *, #181837, .T. ) ;
#208408=CARTESIAN_POINT ( 'NONE',  ( 21.05000000000000071, -1.835341550213257733, -112.0551512925630249 ) ) ;
#208411=EDGE_CURVE ( 'NONE', #183734, #146084, #153612, .T. ) ;
#208414=CIRCLE ( 'NONE', #154264, 4.000000000000003553 ) ;
#208464=CARTESIAN_POINT ( 'NONE',  ( 21.04999999999999716, 10.62872031401550466, -112.6500000000000199 ) ) ;
#208492=FACE_OUTER_BOUND ( 'NONE', #49406, .T. ) ;
#208547=CARTESIAN_POINT ( 'NONE',  ( 21.05000000000000071, 1.115600667400684642E-11, -100.5000000000000284 ) ) ;
#208567=( BOUNDED_SURFACE ( )  B_SPLINE_SURFACE ( 3, 2, ( 
 ( #203804, #104669, #5580 ),
 ( #185535, #120456, #121726 ),
 ( #85106, #201231, #242928 ),
 ( #199972, #164690, #241650 ),
 ( #22627, #4308, #102109 ),
 ( #181688, #83816, #3019 ) ),
 .UNSPECIFIED., .F., .F., .F. ) 
 B_SPLINE_SURFACE_WITH_KNOTS ( ( 4, 2, 4 ),
 ( 3, 3 ),
 ( 1.570796326794897668, 2.356194490192346169, 3.141592653589794448 ),
 ( 0.000000000000000000, 1.000000000000000000 ),
 .UNSPECIFIED. ) 
 GEOMETRIC_REPRESENTATION_ITEM ( )  RATIONAL_B_SPLINE_SURFACE ( (
 ( 1.000000000000000000, 0.7071067811865719976, 1.000000000000000000),
 ( 1.000000000000000000, 0.6611148371783983624, 1.000000000000000000),
 ( 1.000000000000000000, 0.6092287576689580098, 1.000000000000000000),
 ( 1.000000000000000000, 0.5278258667064269494, 1.000000000000000000),
 ( 1.000000000000000000, 0.4993418825329443700, 1.000000000000000000),
 ( 1.000000000000000000, 0.5000000000000260902, 1.000000000000000000) ) ) 
 REPRESENTATION_ITEM ( '' )  SURFACE ( )  );
#208590=VERTEX_POINT ( 'NONE', #68587 ) ;
#208591=AXIS2_PLACEMENT_3D ( 'NONE', #217987, #39412, #237587 ) ;
#208598=VERTEX_POINT ( 'NONE', #123420 ) ;
#208604=VERTEX_POINT ( 'NONE', #184663 ) ;
#208605=ORIENTED_EDGE ( 'NONE', *, *, #180532, .T. ) ;
#208615=LINE ( 'NONE', #29992, #129056 ) ;
#208618=DIRECTION ( 'NONE',  ( 1.000000000000000000, 3.265361837132813093E-16, -0.000000000000000000 ) ) ;
#208640=AXIS2_PLACEMENT_3D ( 'NONE', #154230, #228595, #209018 ) ;
#208642=ORIENTED_EDGE ( 'NONE', *, *, #172704, .T. ) ;
#208647=DIRECTION ( 'NONE',  ( -1.000000000000000000, 0.000000000000000000, 0.000000000000000000 ) ) ;
#208664=CARTESIAN_POINT ( 'NONE',  ( -21.14999999893415250, 11.75000000001115197, -107.3444953435264040 ) ) ;
#208670=DIRECTION ( 'NONE',  ( 0.000000000000000000, 1.000000000000000000, 0.000000000000000000 ) ) ;
#208673=CARTESIAN_POINT ( 'NONE',  ( -23.25000000000000000, 1.115600667400684642E-11, -100.5000000000000284 ) ) ;
#208703=LINE ( 'NONE', #209978, #46502 ) ;
#208706=CARTESIAN_POINT ( 'NONE',  ( -23.15000000000000213, 1.115600667400684642E-11, -134.0000000000000284 ) ) ;
#208722=CARTESIAN_POINT ( 'NONE',  ( 20.94403535211772294, 10.30632246271647467, -139.5041836778896140 ) ) ;
#208728=DIRECTION ( 'NONE',  ( 0.000000000000000000, 0.000000000000000000, -1.000000000000000000 ) ) ;
#208749=DIRECTION ( 'NONE',  ( 0.000000000000000000, -0.1568667991644693838, -0.9876197685951279004 ) ) ;
#208756=EDGE_CURVE ( 'NONE', #100676, #18989, #5961, .T. ) ;
#208828=ORIENTED_EDGE ( 'NONE', *, *, #31471, .T. ) ;
#208834=CARTESIAN_POINT ( 'NONE',  ( 18.49999999999999289, 7.021664781911246322, -137.8335654018973457 ) ) ;
#208849=ADVANCED_FACE ( 'NONE', ( #232065 ), #80795, .T. ) ;
#208869=DIRECTION ( 'NONE',  ( 0.000000000000000000, 0.000000000000000000, 1.000000000000000000 ) ) ;
#208873=ADVANCED_FACE ( 'NONE', ( #238462 ), #121116, .F. ) ;
#208893=AXIS2_PLACEMENT_3D ( 'NONE', #200359, #63395, #242041 ) ;
#208903=CARTESIAN_POINT ( 'NONE',  ( 23.14999999999999858, 5.000000000011153745, -112.9052660189131245 ) ) ;
#208919=ADVANCED_FACE ( 'NONE', ( #42833 ), #214283, .T. ) ;
#208920=ORIENTED_EDGE ( 'NONE', *, *, #218512, .T. ) ;
#208926=DIRECTION ( 'NONE',  ( -1.836970198721029934E-16, 1.000000000000000000, 0.000000000000000000 ) ) ;
#208933=CIRCLE ( 'NONE', #254671, 0.09999999999999939493 ) ;
#208949=VECTOR ( 'NONE', #25631, 1000.000000000000000 ) ;
#208951=CARTESIAN_POINT ( 'NONE',  ( -22.39999999999999858, 0.1000000000111554016, -92.70922040162662370 ) ) ;
#208964=CARTESIAN_POINT ( 'NONE',  ( 21.14999999999999858, 6.540656951712400691, -100.5000000000000284 ) ) ;
#208971=CIRCLE ( 'NONE', #104883, 0.6000000000000033085 ) ;
#209004=ORIENTED_EDGE ( 'NONE', *, *, #150503, .F. ) ;
#209018=DIRECTION ( 'NONE',  ( 1.000000000000000000, 0.000000000000000000, 0.000000000000000000 ) ) ;
#209089=DIRECTION ( 'NONE',  ( 0.000000000000000000, 0.000000000000000000, -1.000000000000000000 ) ) ;
#209096=VECTOR ( 'NONE', #118171, 1000.000000000000000 ) ;
#209100=ORIENTED_EDGE ( 'NONE', *, *, #66168, .T. ) ;
#209138=DIRECTION ( 'NONE',  ( 1.000000000000000000, -0.000000000000000000, 0.000000000000000000 ) ) ;
#209140=DIRECTION ( 'NONE',  ( 0.000000000000000000, -0.000000000000000000, 1.000000000000000000 ) ) ;
#209145=CARTESIAN_POINT ( 'NONE',  ( -20.54999999999999716, -8.999999999988846255, -110.3939691226524786 ) ) ;
#209149=CARTESIAN_POINT ( 'NONE',  ( -18.49719636458538830, -9.446365359216949642, -107.5716138698836062 ) ) ;
#209160=CARTESIAN_POINT ( 'NONE',  ( -23.15000000000000213, 1.115600667400684642E-11, -100.5000000000000284 ) ) ;
#209162=B_SPLINE_CURVE_WITH_KNOTS ( 'NONE', 3,
 ( #128894, #230561, #247549, #130155, #209707, #31106, #171899, #12810 ),
 .UNSPECIFIED., .F., .F.,
 ( 4, 2, 2, 4 ),
 ( 0.000000000000000000, 0.0001049670497870067789, 0.0002099340995740135577, 0.0004198681991479925294 ),
 .UNSPECIFIED. ) ;
#209168=DIRECTION ( 'NONE',  ( 0.000000000000000000, 0.1298341882520022694, 0.9915357197604852679 ) ) ;
#209180=LINE ( 'NONE', #48823, #225517 ) ;
#209181=AXIS2_PLACEMENT_3D ( 'NONE', #47830, #248620, #226466 ) ;
#209184=DIRECTION ( 'NONE',  ( 1.000000000000000000, 0.000000000000000000, 0.000000000000000000 ) ) ;
#209208=DIRECTION ( 'NONE',  ( -0.000000000000000000, 0.1350103645451876666, 0.9908441862701600211 ) ) ;
#209248=CARTESIAN_POINT ( 'NONE',  ( -18.59999999999999787, -9.480686695267820596, -140.9411151687578752 ) ) ;
#209263=DIRECTION ( 'NONE',  ( 0.000000000000000000, 0.000000000000000000, 1.000000000000000000 ) ) ;
#209311=ORIENTED_EDGE ( 'NONE', *, *, #89630, .T. ) ;
#209312=ORIENTED_EDGE ( 'NONE', *, *, #22922, .T. ) ;
#209320=CARTESIAN_POINT ( 'NONE',  ( -23.25000000000000000, -1.249999999988843369, -141.8004807544151333 ) ) ;
#209372=DIRECTION ( 'NONE',  ( -1.000000000000000000, -0.000000000000000000, -0.000000000000000000 ) ) ;
#209375=CARTESIAN_POINT ( 'NONE',  ( 21.14999999999999858, 6.540656951712400691, -100.6000000000000369 ) ) ;
#209379=DIRECTION ( 'NONE',  ( 1.000000000000000000, 0.000000000000000000, 0.000000000000000000 ) ) ;
#209395=CARTESIAN_POINT ( 'NONE',  ( 23.24999999999999645, 1.115600667400684642E-11, -134.0000000000000284 ) ) ;
#209397=TOROIDAL_SURFACE ( 'NONE', #126004, 1.900000000000002576, 0.1000000000000000056 ) ;
#209409=DIRECTION ( 'NONE',  ( 0.000000000000000000, 1.000000000000000000, -3.469446951953635015E-14 ) ) ;
#209420=CARTESIAN_POINT ( 'NONE',  ( 23.14999999999999858, 5.000000000011153745, -122.0947339810869465 ) ) ;
#209427=EDGE_CURVE ( 'NONE', #50377, #217484, #30758, .T. ) ;
#209473=CIRCLE ( 'NONE', #84536, 0.1000000000000028644 ) ;
#209483=ORIENTED_EDGE ( 'NONE', *, *, #174472, .F. ) ;
#209492=DIRECTION ( 'NONE',  ( 0.000000000000000000, 0.000000000000000000, -1.000000000000000000 ) ) ;
#209503=DIRECTION ( 'NONE',  ( 0.000000000000000000, 1.000000000000000000, 0.000000000000000000 ) ) ;
#209523=CARTESIAN_POINT ( 'NONE',  ( 18.51024323315077069, 10.31104185824064068, -139.5204516983106089 ) ) ;
#209536=CARTESIAN_POINT ( 'NONE',  ( -18.59999999999999787, 1.835341550235567887, -112.0551512925630249 ) ) ;
#209553=CARTESIAN_POINT ( 'NONE',  ( 22.50000000000000000, 11.64957080755595520, -100.4000000000000483 ) ) ;
#209559=EDGE_LOOP ( 'NONE', ( #578, #205593, #134078, #149577 ) ) ;
#209564=FACE_OUTER_BOUND ( 'NONE', #169160, .T. ) ;
#209573=AXIS2_PLACEMENT_3D ( 'NONE', #230401, #131294, #210841 ) ;
#209632=CIRCLE ( 'NONE', #242939, 0.1000000000000028644 ) ;
#209637=LINE ( 'NONE', #31036, #34152 ) ;
#209686=DIRECTION ( 'NONE',  ( -1.000000000000000000, -0.000000000000000000, -0.000000000000000000 ) ) ;
#209707=CARTESIAN_POINT ( 'NONE',  ( -18.54118089899632693, -9.463537631836942410, -107.5485775978681602 ) ) ;
#209711=ORIENTED_EDGE ( 'NONE', *, *, #162242, .T. ) ;
#209720=PRODUCT ( 'Injection Molded Chain Links 4', 'Injection Molded Chain Links 4', '', ( #151348 ) ) ;
#209817=ADVANCED_FACE ( 'NONE', ( #86123 ), #251484, .F. ) ;
#209835=VERTEX_POINT ( 'NONE', #88700 ) ;
#209889=EDGE_CURVE ( 'NONE', #16939, #111732, #148716, .T. ) ;
#209895=EDGE_CURVE ( 'NONE', #109956, #74961, #97947, .T. ) ;
#209919=DIRECTION ( 'NONE',  ( 0.000000000000000000, 0.000000000000000000, -1.000000000000000000 ) ) ;
#209927=DIRECTION ( 'NONE',  ( -1.000000000000000000, -0.000000000000000000, -0.000000000000000000 ) ) ;
#209939=TOROIDAL_SURFACE ( 'NONE', #72386, 4.099999999999999645, 0.1000000000000000056 ) ;
#209955=CARTESIAN_POINT ( 'NONE',  ( -21.05000000000000071, 1.115600667400684642E-11, -129.9000000000000341 ) ) ;
#209978=CARTESIAN_POINT ( 'NONE',  ( 20.94999999999999574, 6.550000000011159784, -110.3438220896831581 ) ) ;
#210022=DIRECTION ( 'NONE',  ( -3.265361837132813093E-16, 1.000000000000000000, 0.000000000000000000 ) ) ;
#210052=LINE ( 'NONE', #31435, #128433 ) ;
#210099=ORIENTED_EDGE ( 'NONE', *, *, #92914, .T. ) ;
#210115=VERTEX_POINT ( 'NONE', #238505 ) ;
#210195=AXIS2_PLACEMENT_3D ( 'NONE', #162792, #138061, #118541 ) ;
#210225=ORIENTED_EDGE ( 'NONE', *, *, #146693, .T. ) ;
#210241=ORIENTED_EDGE ( 'NONE', *, *, #72850, .F. ) ;
#210250=CARTESIAN_POINT ( 'NONE',  ( -20.85000000000000142, -1.835859311432481045, -145.5044391687985694 ) ) ;
#210261=EDGE_LOOP ( 'NONE', ( #240438, #25735, #88641, #133628 ) ) ;
#210280=DIRECTION ( 'NONE',  ( 1.000000000000000000, 0.000000000000000000, 0.000000000000000000 ) ) ;
#210301=TOROIDAL_SURFACE ( 'NONE', #160432, 0.2000000000000000111, 0.1000000000000000056 ) ;
#210379=ORIENTED_EDGE ( 'NONE', *, *, #72461, .T. ) ;
#210408=ORIENTED_EDGE ( 'NONE', *, *, #149364, .T. ) ;
#210421=CIRCLE ( 'NONE', #123106, 0.09999999999999363565 ) ;
#210445=CARTESIAN_POINT ( 'NONE',  ( 21.08479644141222664, 0.05855444257529220792, -94.15496134226816594 ) ) ;
#210450=DIRECTION ( 'NONE',  ( 1.000000000000000000, 0.000000000000000000, 0.000000000000000000 ) ) ;
#210460=LINE ( 'NONE', #110054, #44814 ) ;
#210470=ADVANCED_FACE ( 'NONE', ( #178258 ), #257699, .F. ) ;
#210488=ORIENTED_EDGE ( 'NONE', *, *, #45395, .T. ) ;
#210505=EDGE_CURVE ( 'NONE', #254324, #8739, #123392, .T. ) ;
#210524=FACE_OUTER_BOUND ( 'NONE', #203729, .T. ) ;
#210542=LINE ( 'NONE', #193553, #64687 ) ;
#210557=CIRCLE ( 'NONE', #118995, 3.999999999999999112 ) ;
#210563=DIRECTION ( 'NONE',  ( -1.000000000000000000, 7.304098846218134667E-16, -4.217023435051678980E-16 ) ) ;
#210583=CARTESIAN_POINT ( 'NONE',  ( 20.77766267348356166, 10.44904239063021123, -108.0927089158775374 ) ) ;
#210586=DIRECTION ( 'NONE',  ( -1.000000000000000000, 0.000000000000000000, 0.000000000000000000 ) ) ;
#210588=FACE_OUTER_BOUND ( 'NONE', #129612, .T. ) ;
#210618=CARTESIAN_POINT ( 'NONE',  ( -22.59999999999999787, 11.74987124438766273, -100.4345704089863602 ) ) ;
#210668=DIRECTION ( 'NONE',  ( 1.000000000000000000, 0.000000000000000000, 0.000000000000000000 ) ) ;
#210689=DIRECTION ( 'NONE',  ( 1.000000000000000000, 0.000000000000000000, 0.000000000000000000 ) ) ;
#210712=COLOUR_RGB ( '', 0.40784314, 0.44705882, 0.49803922) ;
#210726=CIRCLE ( 'NONE', #223193, 0.5000000000000004441 ) ;
#210773=EDGE_CURVE ( 'NONE', #20729, #46619, #114672, .T. ) ;
#210778=VECTOR ( 'NONE', #44010, 1000.000000000000000 ) ;
#210781=CARTESIAN_POINT ( 'NONE',  ( 21.05000000000000071, 8.876614585098257848, -108.8850804788447135 ) ) ;
#210785=DIRECTION ( 'NONE',  ( 1.000000000000000000, 0.000000000000000000, 0.000000000000000000 ) ) ;
#210814=VERTEX_POINT ( 'NONE', #185623 ) ;
#210841=DIRECTION ( 'NONE',  ( 0.000000000000000000, 0.000000000000000000, -1.000000000000000000 ) ) ;
#210867=DIRECTION ( 'NONE',  ( 0.7071067811865475727, 0.7071067811865475727, 2.044391222244500083E-16 ) ) ;
#210878=FACE_OUTER_BOUND ( 'NONE', #97548, .T. ) ;
#210908=DIRECTION ( 'NONE',  ( 0.000000000000000000, -0.1350103645451904977, 0.9908441862701596881 ) ) ;
#210935=AXIS2_PLACEMENT_3D ( 'NONE', #111452, #249687, #93163 ) ;
#210962=CARTESIAN_POINT ( 'NONE',  ( -23.25000000000000000, 2.600000000011156054, -120.7753780772379315 ) ) ;
#210981=CARTESIAN_POINT ( 'NONE',  ( 20.94999999999999929, 5.850000000011160495, -123.8675027757221017 ) ) ;
#211007=EDGE_LOOP ( 'NONE', ( #153273, #169282, #218898, #202562 ) ) ;
#211013=CARTESIAN_POINT ( 'NONE',  ( 21.14999999999999858, 10.71339244341104013, -112.7500000000000284 ) ) ;
#211014=DIRECTION ( 'NONE',  ( 0.000000000000000000, -1.000000000000000000, 0.000000000000000000 ) ) ;
#211041=ORIENTED_EDGE ( 'NONE', *, *, #240835, .T. ) ;
#211057=LINE ( 'NONE', #71569, #225916 ) ;
#211098=CARTESIAN_POINT ( 'NONE',  ( 20.04142135623730070, 11.75000000001115907, -125.1500000000000341 ) ) ;
#211111=CARTESIAN_POINT ( 'NONE',  ( 18.59999999999999076, 11.65000000001115943, -134.0000000000000284 ) ) ;
#211119=CIRCLE ( 'NONE', #131999, 0.2000000000000057288 ) ;
#211131=ORIENTED_EDGE ( 'NONE', *, *, #94548, .F. ) ;
#211153=CIRCLE ( 'NONE', #169697, 0.1000000000000028644 ) ;
#211184=EDGE_LOOP ( 'NONE', ( #123205, #147795, #52483, #136475 ) ) ;
#211204=ADVANCED_FACE ( 'NONE', ( #25930 ), #85582, .F. ) ;
#211214=CARTESIAN_POINT ( 'NONE',  ( 18.48413544395661745, -9.664304033616602396, -140.6831049930383131 ) ) ;
#211218=DIRECTION ( 'NONE',  ( -1.000000000000000000, 0.000000000000000000, 0.000000000000000000 ) ) ;
#211238=LINE ( 'NONE', #53450, #153920 ) ;
#211247=VERTEX_POINT ( 'NONE', #27241 ) ;
#211255=EDGE_CURVE ( 'NONE', #146084, #100999, #147142, .T. ) ;
#211279=EDGE_CURVE ( 'NONE', #142411, #28813, #105415, .T. ) ;
#211300=VERTEX_POINT ( 'NONE', #67607 ) ;
#211302=ADVANCED_FACE ( 'NONE', ( #152316 ), #34942, .T. ) ;
#211305=FACE_OUTER_BOUND ( 'NONE', #197357, .T. ) ;
#211367=DIRECTION ( 'NONE',  ( 0.000000000000000000, 0.008583690987124100932, -0.9999631594459055250 ) ) ;
#211375=ORIENTED_EDGE ( 'NONE', *, *, #186209, .F. ) ;
#211383=DIRECTION ( 'NONE',  ( 1.000000000000000000, 0.000000000000000000, 0.000000000000000000 ) ) ;
#211384=ORIENTED_EDGE ( 'NONE', *, *, #161602, .T. ) ;
#211385=EDGE_CURVE ( 'NONE', #172291, #43551, #117010, .T. ) ;
#211436=CARTESIAN_POINT ( 'NONE',  ( -20.64999999999999858, 7.250000000011155521, -121.6500000000000341 ) ) ;
#211494=ORIENTED_EDGE ( 'NONE', *, *, #125657, .T. ) ;
#211516=CARTESIAN_POINT ( 'NONE',  ( 20.95512820512820440, 8.876151316299271343, -121.7500000000000426 ) ) ;
#211550=EDGE_CURVE ( 'NONE', #70455, #253683, #69081, .T. ) ;
#211579=DIRECTION ( 'NONE',  ( 0.000000000000000000, 0.000000000000000000, -1.000000000000000000 ) ) ;
#211675=EDGE_CURVE ( 'NONE', #131609, #74676, #248305, .T. ) ;
#211723=ADVANCED_FACE ( 'NONE', ( #230226 ), #150695, .T. ) ;
#211736=FACE_OUTER_BOUND ( 'NONE', #126537, .T. ) ;
#211754=CARTESIAN_POINT ( 'NONE',  ( -21.05000000000000071, 5.900000000011162093, -123.7809002353436654 ) ) ;
#211767=ORIENTED_EDGE ( 'NONE', *, *, #44965, .T. ) ;
#211801=ORIENTED_EDGE ( 'NONE', *, *, #120095, .F. ) ;
#211808=LINE ( 'NONE', #111417, #206255 ) ;
#211814=AXIS2_PLACEMENT_3D ( 'NONE', #107933, #88337, #29715 ) ;
#211868=CARTESIAN_POINT ( 'NONE',  ( -23.15000000000000213, 11.65000000001115588, -112.6500000000000483 ) ) ;
#211877=ORIENTED_EDGE ( 'NONE', *, *, #191542, .T. ) ;
#211885=CARTESIAN_POINT ( 'NONE',  ( 20.54374330479337374, 10.50501031423420351, -108.2256836348895632 ) ) ;
#211908=EDGE_LOOP ( 'NONE', ( #155364, #200526, #226938, #243581 ) ) ;
#211914=CARTESIAN_POINT ( 'NONE',  ( -23.15000000000000213, 1.115600667400684642E-11, -134.0000000000000284 ) ) ;
#211989=DIRECTION ( 'NONE',  ( 0.000000000000000000, 0.000000000000000000, -1.000000000000000000 ) ) ;
#212014=FACE_OUTER_BOUND ( 'NONE', #166255, .T. ) ;
#212058=DIRECTION ( 'NONE',  ( 0.000000000000000000, 0.000000000000000000, -1.000000000000000000 ) ) ;
#212121=ORIENTED_EDGE ( 'NONE', *, *, #250503, .T. ) ;
#212143=CYLINDRICAL_SURFACE ( 'NONE', #198236, 0.1000000000000028644 ) ;
#212165=EDGE_CURVE ( 'NONE', #239723, #111333, #77781, .T. ) ;
#212174=CARTESIAN_POINT ( 'NONE',  ( -20.64999999999999858, 2.000000000011154189, -120.7753780772379315 ) ) ;
#212178=CIRCLE ( 'NONE', #199721, 0.1000000000000028644 ) ;
#212192=CARTESIAN_POINT ( 'NONE',  ( -22.59999999999999787, 1.115600667400684642E-11, -100.5000000000000284 ) ) ;
#212234=ORIENTED_EDGE ( 'NONE', *, *, #107408, .T. ) ;
#212261=CARTESIAN_POINT ( 'NONE',  ( 22.39999999999999503, 11.65000000001116298, -100.6000000000000369 ) ) ;
#212285=VERTEX_POINT ( 'NONE', #212374 ) ;
#212302=ORIENTED_EDGE ( 'NONE', *, *, #176246, .T. ) ;
#212307=CARTESIAN_POINT ( 'NONE',  ( 21.09551895715267378, 10.62143732717967382, -112.7371246658993726 ) ) ;
#212321=AXIS2_PLACEMENT_3D ( 'NONE', #160993, #59266, #137549 ) ;
#212336=ORIENTED_EDGE ( 'NONE', *, *, #176979, .T. ) ;
#212337=FACE_OUTER_BOUND ( 'NONE', #170751, .T. ) ;
#212363=CARTESIAN_POINT ( 'NONE',  ( -23.25000000000000000, 1.115600667400684642E-11, -134.0000000000000284 ) ) ;
#212364=EDGE_LOOP ( 'NONE', ( #198177, #169460, #569, #51833 ) ) ;
#212374=CARTESIAN_POINT ( 'NONE',  ( 18.59999999999996945, 10.33248238083634440, -139.5948465439131780 ) ) ;
#212397=DIRECTION ( 'NONE',  ( -1.000000000000000000, 0.000000000000000000, 0.000000000000000000 ) ) ;
#212408=CIRCLE ( 'NONE', #99918, 0.1000000000000029060 ) ;
#212411=DIRECTION ( 'NONE',  ( 0.000000000000000000, -0.1568667991644714932, 0.9876197685951274563 ) ) ;
#212412=ORIENTED_EDGE ( 'NONE', *, *, #150224, .T. ) ;
#212413=CARTESIAN_POINT ( 'NONE',  ( -20.64999999999999858, -8.663551401858004652, -110.0241011180673354 ) ) ;
#212444=ORIENTED_EDGE ( 'NONE', *, *, #71590, .F. ) ;
#212479=ORIENTED_EDGE ( 'NONE', *, *, #57928, .T. ) ;
#212534=EDGE_LOOP ( 'NONE', ( #190034, #96941, #5206, #86197, #84473 ) ) ;
#212548=CARTESIAN_POINT ( 'NONE',  ( 20.94999999999999574, 1.115600667400684642E-11, -100.5000000000000284 ) ) ;
#212549=AXIS2_PLACEMENT_3D ( 'NONE', #52633, #209140, #91773 ) ;
#212578=CARTESIAN_POINT ( 'NONE',  ( 22.49806830649814060, 11.64988965485023620, -100.4225356836745249 ) ) ;
#212582=CIRCLE ( 'NONE', #4450, 7.720710678118678061 ) ;
#212590=ORIENTED_EDGE ( 'NONE', *, *, #238665, .T. ) ;
#212621=DIRECTION ( 'NONE',  ( 0.000000000000000000, 0.000000000000000000, 1.000000000000000000 ) ) ;
#212673=CARTESIAN_POINT ( 'NONE',  ( 18.49999999999999289, 10.20857864377385127, -125.1500000000000341 ) ) ;
#212749=DIRECTION ( 'NONE',  ( 1.000000000000000000, 0.000000000000000000, 0.000000000000000000 ) ) ;
#212753=ORIENTED_EDGE ( 'NONE', *, *, #173626, .F. ) ;
#212761=VECTOR ( 'NONE', #245944, 1000.000000000000000 ) ;
#212764=CIRCLE ( 'NONE', #54332, 11.74999999999999645 ) ;
#212788=ADVANCED_FACE ( 'NONE', ( #251145 ), #219734, .T. ) ;
#212820=EDGE_CURVE ( 'NONE', #213068, #34846, #207367, .T. ) ;
#212827=CIRCLE ( 'NONE', #133702, 0.1000000000000001860 ) ;
#212832=CARTESIAN_POINT ( 'NONE',  ( -21.11101077989000174, 0.01528526892543874242, -94.07631526527390520 ) ) ;
#212846=DIRECTION ( 'NONE',  ( 0.000000000000000000, 0.000000000000000000, -1.000000000000000000 ) ) ;
#212864=DIRECTION ( 'NONE',  ( 1.000000000000000000, 2.952720810173289112E-16, -0.000000000000000000 ) ) ;
#212904=CYLINDRICAL_SURFACE ( 'NONE', #82458, 0.09999999999999939493 ) ;
#212921=ORIENTED_EDGE ( 'NONE', *, *, #229825, .F. ) ;
#212935=CARTESIAN_POINT ( 'NONE',  ( -18.52643265882458579, 10.31973158071402530, -139.5505334713354841 ) ) ;
#212942=ORIENTED_EDGE ( 'NONE', *, *, #95603, .F. ) ;
#212965=DIRECTION ( 'NONE',  ( -1.000000000000000000, -8.673617379884087537E-15, 0.000000000000000000 ) ) ;
#212970=DIRECTION ( 'NONE',  ( 2.342056488767301376E-15, -0.1350103645451904977, -0.9908441862701596881 ) ) ;
#212973=EDGE_CURVE ( 'NONE', #14418, #242494, #90620, .T. ) ;
#213022=CYLINDRICAL_SURFACE ( 'NONE', #122861, 0.1000000000000101918 ) ;
#213045=ORIENTED_EDGE ( 'NONE', *, *, #147066, .F. ) ;
#213054=DIRECTION ( 'NONE',  ( 1.000000000000000000, 0.000000000000000000, 0.000000000000000000 ) ) ;
#213068=VERTEX_POINT ( 'NONE', #233868 ) ;
#213078=CYLINDRICAL_SURFACE ( 'NONE', #235314, 11.80000000000000426 ) ;
#213087=AXIS2_PLACEMENT_3D ( 'NONE', #29610, #229073, #209492 ) ;
#213097=ORIENTED_EDGE ( 'NONE', *, *, #10472, .F. ) ;
#213105=CYLINDRICAL_SURFACE ( 'NONE', #192979, 0.8750000000000007772 ) ;
#213115=DIRECTION ( 'NONE',  ( 0.000000000000000000, -1.000000000000000000, 0.000000000000000000 ) ) ;
#213117=( BOUNDED_SURFACE ( )  B_SPLINE_SURFACE ( 3, 2, ( 
 ( #92337, #208464, #187612 ),
 ( #250138, #54491, #49369 ),
 ( #168076, #33702, #191477 ),
 ( #173216, #212307, #247564 ),
 ( #71521, #188878, #229297 ),
 ( #169355, #131469, #211013 ) ),
 .UNSPECIFIED., .F., .F., .F. ) 
 B_SPLINE_SURFACE_WITH_KNOTS ( ( 4, 2, 4 ),
 ( 3, 3 ),
 ( 0.0001342700090130013644, 0.0002909192928057326741, 0.0004475685765984639838 ),
 ( 0.000000000000000000, 1.000000000000000000 ),
 .UNSPECIFIED. ) 
 GEOMETRIC_REPRESENTATION_ITEM ( )  RATIONAL_B_SPLINE_SURFACE ( (
 ( 1.000000000000000000, 0.7250110520819876836, 1.000000000000000000),
 ( 1.000000000000000000, 0.7257599279127774361, 1.000000000000000000),
 ( 1.000000000000000000, 0.7137594617292282173, 1.000000000000000000),
 ( 1.000000000000000000, 0.6959270178801697515, 1.000000000000000000),
 ( 1.000000000000000000, 0.6919879549344937208, 1.000000000000000000),
 ( 1.000000000000000000, 0.7071067811865966446, 1.000000000000000000) ) ) 
 REPRESENTATION_ITEM ( '' )  SURFACE ( )  );
#213134=CARTESIAN_POINT ( 'NONE',  ( 21.14999999999999858, 0.09779029131994770863, -94.24218538952391100 ) ) ;
#213135=EDGE_CURVE ( 'NONE', #239657, #177002, #213863, .T. ) ;
#213143=DIRECTION ( 'NONE',  ( -3.469446951953515108E-14, 0.000000000000000000, 1.000000000000000000 ) ) ;
#213149=DIRECTION ( 'NONE',  ( 0.000000000000000000, 1.000000000000000000, 2.891205793294679805E-16 ) ) ;
#213161=DIRECTION ( 'NONE',  ( 0.000000000000000000, -0.4791956752371546169, -0.8777080977375152360 ) ) ;
#213204=DIRECTION ( 'NONE',  ( 1.000000000000000000, -0.000000000000000000, -0.000000000000000000 ) ) ;
#213232=CARTESIAN_POINT ( 'NONE',  ( -18.59999999999999787, -1.835341550213255957, -112.0551512925630107 ) ) ;
#213248=CARTESIAN_POINT ( 'NONE',  ( -21.05000000000000071, 6.540656951712400691, -100.6000000000000369 ) ) ;
#213250=DIRECTION ( 'NONE',  ( 1.000000000000000000, 0.000000000000000000, 0.000000000000000000 ) ) ;
#213281=EDGE_CURVE ( 'NONE', #86438, #253135, #30248, .T. ) ;
#213295=CARTESIAN_POINT ( 'NONE',  ( 23.14999999999999503, 6.650000000011155876, -121.6500000000000341 ) ) ;
#213299=ORIENTED_EDGE ( 'NONE', *, *, #101345, .F. ) ;
#213307=EDGE_CURVE ( 'NONE', #110957, #124745, #168505, .T. ) ;
#213318=ORIENTED_EDGE ( 'NONE', *, *, #120095, .T. ) ;
#213336=CARTESIAN_POINT ( 'NONE',  ( -21.14999999999999858, -0.09999999998884338825, -88.85042919245522341 ) ) ;
#213339=CARTESIAN_POINT ( 'NONE',  ( 23.24999999999999289, 11.65000000001116298, -126.9851942293460922 ) ) ;
#213350=DIRECTION ( 'NONE',  ( 0.000000000000000000, 0.000000000000000000, -1.000000000000000000 ) ) ;
#213384=ORIENTED_EDGE ( 'NONE', *, *, #137976, .F. ) ;
#213395=DIRECTION ( 'NONE',  ( -1.000000000000000000, -0.000000000000000000, 0.000000000000000000 ) ) ;
#213399=CARTESIAN_POINT ( 'NONE',  ( 22.39999999999999503, 11.75000000001116263, -100.6000000000000369 ) ) ;
#213425=ORIENTED_EDGE ( 'NONE', *, *, #88220, .F. ) ;
#213433=CARTESIAN_POINT ( 'NONE',  ( -22.50000000000000000, 1.115600667400684642E-11, -100.5000000000000284 ) ) ;
#213436=EDGE_CURVE ( 'NONE', #242494, #246420, #97873, .T. ) ;
#213444=CARTESIAN_POINT ( 'NONE',  ( 21.09706851349342216, 8.775842513484549912, -112.7355662163996755 ) ) ;
#213451=EDGE_CURVE ( 'NONE', #236931, #18989, #257529, .T. ) ;
#213547=ADVANCED_FACE ( 'NONE', ( #161760 ), #79608, .F. ) ;
#213572=CARTESIAN_POINT ( 'NONE',  ( 20.95325940946048249, 10.52339007070744437, -108.0644621292401126 ) ) ;
#213592=EDGE_CURVE ( 'NONE', #209835, #163148, #186890, .T. ) ;
#213604=DIRECTION ( 'NONE',  ( 1.000000000000000000, 0.000000000000000000, 0.000000000000000000 ) ) ;
#213611=DIRECTION ( 'NONE',  ( 1.000000000000000000, 0.000000000000000000, 0.000000000000000000 ) ) ;
#213616=CARTESIAN_POINT ( 'NONE',  ( 20.94999999999999929, 1.115600667400684642E-11, -134.0000000000000284 ) ) ;
#213639=ORIENTED_EDGE ( 'NONE', *, *, #124270, .F. ) ;
#213659=ADVANCED_FACE ( 'NONE', ( #186443 ), #92133, .T. ) ;
#213660=CARTESIAN_POINT ( 'NONE',  ( 23.14999999999999503, 11.75000000001116263, -112.6500000000000341 ) ) ;
#213676=DIRECTION ( 'NONE',  ( 1.000000000000000000, 0.000000000000000000, 0.000000000000000000 ) ) ;
#213681=VERTEX_POINT ( 'NONE', #44371 ) ;
#213699=ADVANCED_FACE ( 'NONE', ( #6500 ), #245126, .T. ) ;
#213709=ORIENTED_EDGE ( 'NONE', *, *, #116810, .T. ) ;
#213713=ORIENTED_EDGE ( 'NONE', *, *, #31383, .T. ) ;
#213726=EDGE_LOOP ( 'NONE', ( #139191, #78625, #181274, #32226, #170424 ) ) ;
#213733=CARTESIAN_POINT ( 'NONE',  ( 21.53752568617672836, 6.786807874515049299, -100.4010255387293427 ) ) ;
#213742=ADVANCED_FACE ( 'NONE', ( #133825 ), #193811, .T. ) ;
#213790=AXIS2_PLACEMENT_3D ( 'NONE', #257047, #78447, #240112 ) ;
#213795=VERTEX_POINT ( 'NONE', #155986 ) ;
#213800=FACE_OUTER_BOUND ( 'NONE', #91467, .T. ) ;
#213803=FACE_OUTER_BOUND ( 'NONE', #250121, .T. ) ;
#213821=CARTESIAN_POINT ( 'NONE',  ( 22.45305468355010703, -0.1008583690885486023, -88.75043287651031676 ) ) ;
#213839=AXIS2_PLACEMENT_3D ( 'NONE', #6484, #245108, #166891 ) ;
#213863=( BOUNDED_CURVE ( )  B_SPLINE_CURVE ( 3, ( #42110, #43376, #180319, #83737 ),
 .UNSPECIFIED., .F., .F. ) 
 B_SPLINE_CURVE_WITH_KNOTS ( ( 4, 4 ),
 ( 1.570796326794955622, 3.141592653589791784 ),
 .UNSPECIFIED. ) 
 CURVE ( )  GEOMETRIC_REPRESENTATION_ITEM ( )  RATIONAL_B_SPLINE_CURVE ( ( 1.000000000000000000, 0.8047378541243791483, 0.8047378541243791483, 1.000000000000000000 ) ) 
 REPRESENTATION_ITEM ( '' )  );
#213876=EDGE_LOOP ( 'NONE', ( #227049, #213713, #231137 ) ) ;
#213918=EDGE_CURVE ( 'NONE', #149981, #246634, #22892, .T. ) ;
#213938=VERTEX_POINT ( 'NONE', #81520 ) ;
#214017=EDGE_CURVE ( 'NONE', #175552, #54821, #182214, .T. ) ;
#214023=ORIENTED_EDGE ( 'NONE', *, *, #242095, .T. ) ;
#214088=DIRECTION ( 'NONE',  ( 1.000000000000000000, 0.000000000000000000, 0.000000000000000000 ) ) ;
#214090=DIRECTION ( 'NONE',  ( 0.000000000000000000, -1.265107689135680095E-16, 1.000000000000000000 ) ) ;
#214098=AXIS2_PLACEMENT_3D ( 'NONE', #59797, #158956, #117238 ) ;
#214103=ORIENTED_EDGE ( 'NONE', *, *, #50472, .F. ) ;
#214252=TOROIDAL_SURFACE ( 'NONE', #80943, 0.2000000000000000111, 0.1000000000000000056 ) ;
#214259=CARTESIAN_POINT ( 'NONE',  ( -18.50000000000000000, 11.65000000001115232, -112.7500000000000284 ) ) ;
#214263=VERTEX_POINT ( 'NONE', #1701 ) ;
#214265=CARTESIAN_POINT ( 'NONE',  ( 18.50000000000000000, -9.399999999988843058, -107.4992856778388841 ) ) ;
#214279=DIRECTION ( 'NONE',  ( 0.000000000000000000, -0.4999999999999949485, 0.8660254037844415942 ) ) ;
#214283=TOROIDAL_SURFACE ( 'NONE', #210195, 4.149999999999999467, 0.1000000000000000056 ) ;
#214295=DIRECTION ( 'NONE',  ( -1.000000000000000000, -0.000000000000000000, 0.000000000000000000 ) ) ;
#214325=DIRECTION ( 'NONE',  ( 0.000000000000000000, -1.000000000000000000, 0.000000000000000000 ) ) ;
#214329=ORIENTED_EDGE ( 'NONE', *, *, #58559, .F. ) ;
#214336=LINE ( 'NONE', #155680, #115280 ) ;
#214360=EDGE_LOOP ( 'NONE', ( #242562, #251720, #133359, #62078, #147582 ) ) ;
#214365=LINE ( 'NONE', #192253, #244769 ) ;
#214379=ADVANCED_FACE ( 'NONE', ( #222020 ), #199939, .T. ) ;
#214410=DIRECTION ( 'NONE',  ( 1.000000000000000000, 0.000000000000000000, 0.000000000000000000 ) ) ;
#214412=DIRECTION ( 'NONE',  ( 0.000000000000000000, 0.1350103645451904977, -0.9908441862701596881 ) ) ;
#214426=FACE_OUTER_BOUND ( 'NONE', #214775, .T. ) ;
#214461=CARTESIAN_POINT ( 'NONE',  ( -23.25000000000000000, -1.149570369564537842, -141.8159124845019790 ) ) ;
#214492=CARTESIAN_POINT ( 'NONE',  ( -23.15000000000000213, 1.115600667400684642E-11, -100.5000000000000284 ) ) ;
#214537=FACE_BOUND ( 'NONE', #142851, .T. ) ;
#214550=CIRCLE ( 'NONE', #35541, 11.70000000000000284 ) ;
#214593=AXIS2_PLACEMENT_3D ( 'NONE', #48871, #125834, #127128 ) ;
#214612=DIRECTION ( 'NONE',  ( 0.000000000000000000, 0.000000000000000000, -1.000000000000000000 ) ) ;
#214640=VECTOR ( 'NONE', #144969, 1000.000000000000000 ) ;
#214647=CARTESIAN_POINT ( 'NONE',  ( 18.55807992284871588, 10.32898536001801659, -139.5826683222764757 ) ) ;
#214652=ORIENTED_EDGE ( 'NONE', *, *, #106827, .F. ) ;
#214662=AXIS2_PLACEMENT_3D ( 'NONE', #231623, #133786, #253721 ) ;
#214673=( BOUNDED_SURFACE ( )  B_SPLINE_SURFACE ( 3, 2, ( 
 ( #84788, #164373, #63982 ),
 ( #161825, #65259, #140964 ),
 ( #144777, #66554, #163100 ),
 ( #26151, #143508, #224333 ),
 ( #43143, #24881, #220496 ),
 ( #104364, #105644, #240056 ),
 ( #241347, #121423, #83507 ),
 ( #62702, #5256, #182660 ) ),
 .UNSPECIFIED., .F., .F., .F. ) 
 B_SPLINE_SURFACE_WITH_KNOTS ( ( 4, 2, 2, 4 ),
 ( 3, 3 ),
 ( 0.0001704874539069910233, 0.0003809798300636633517, 0.0004862260181419994888, 0.0005914722062203356260 ),
 ( 0.000000000000000000, 1.000000000000000000 ),
 .UNSPECIFIED. ) 
 GEOMETRIC_REPRESENTATION_ITEM ( )  RATIONAL_B_SPLINE_SURFACE ( (
 ( 1.000000000000000000, 0.7071067811864942820, 1.000000000000000000),
 ( 1.000000000000000000, 0.7670648383574680818, 1.000000000000000000),
 ( 1.000000000000000000, 0.8204820770254317441, 1.000000000000000000),
 ( 1.000000000000000000, 0.8877218296112791007, 1.000000000000000000),
 ( 1.000000000000000000, 0.9080815932666936874, 1.000000000000000000),
 ( 1.000000000000000000, 0.9395541505860436349, 1.000000000000000000),
 ( 1.000000000000000000, 0.9506520335379957665, 1.000000000000000000),
 ( 1.000000000000000000, 0.9504532311154669788, 1.000000000000000000) ) ) 
 REPRESENTATION_ITEM ( '' )  SURFACE ( )  );
#214679=ORIENTED_EDGE ( 'NONE', *, *, #245428, .F. ) ;
#214716=DIRECTION ( 'NONE',  ( -1.000000000000000000, 0.000000000000000000, 0.000000000000000000 ) ) ;
#214732=CARTESIAN_POINT ( 'NONE',  ( -20.94999999999999929, 1.835341550235567887, -112.1551512925630192 ) ) ;
#214747=DIRECTION ( 'NONE',  ( 0.000000000000000000, 0.9887567792719341719, -0.1495327102803664099 ) ) ;
#214751=CYLINDRICAL_SURFACE ( 'NONE', #69220, 0.1000000000000028644 ) ;
#214756=AXIS2_PLACEMENT_3D ( 'NONE', #58875, #216690, #116327 ) ;
#214758=VERTEX_POINT ( 'NONE', #2679 ) ;
#214775=EDGE_LOOP ( 'NONE', ( #232872, #38379, #119619, #92506 ) ) ;
#214849=CARTESIAN_POINT ( 'NONE',  ( 23.14999999999999503, 6.650000000011155876, -112.6500000000000341 ) ) ;
#214862=DIRECTION ( 'NONE',  ( 0.000000000000000000, 0.9999631594459053030, 0.008583690987162899758 ) ) ;
#214908=ORIENTED_EDGE ( 'NONE', *, *, #136770, .T. ) ;
#214952=ORIENTED_EDGE ( 'NONE', *, *, #75201, .T. ) ;
#214972=DIRECTION ( 'NONE',  ( 0.000000000000000000, 0.6728971962616792091, -0.7397360091702790408 ) ) ;
#214982=CIRCLE ( 'NONE', #35943, 0.1000000000000008937 ) ;
#214997=CARTESIAN_POINT ( 'NONE',  ( 21.12769345151713196, 10.71928767695172624, -112.7474803461975199 ) ) ;
#215030=CIRCLE ( 'NONE', #23545, 0.09999999999998898659 ) ;
#215032=VERTEX_POINT ( 'NONE', #92494 ) ;
#215034=EDGE_LOOP ( 'NONE', ( #211767, #199250 ) ) ;
#215058=DIRECTION ( 'NONE',  ( -1.000000000000000000, -0.000000000000000000, -0.000000000000000000 ) ) ;
#215059=DIRECTION ( 'NONE',  ( 1.000000000000000000, 0.000000000000000000, 0.000000000000000000 ) ) ;
#215069=CIRCLE ( 'NONE', #73459, 4.049999999999998934 ) ;
#215083=AXIS2_PLACEMENT_3D ( 'NONE', #236860, #161190, #120800 ) ;
#215094=CARTESIAN_POINT ( 'NONE',  ( -22.49510344025093644, 0.06712767820541533370, -88.85002989488579317 ) ) ;
#215096=DIRECTION ( 'NONE',  ( 1.000000000000000000, 0.000000000000000000, 0.000000000000000000 ) ) ;
#215129=CARTESIAN_POINT ( 'NONE',  ( -22.47071067811865319, 0.09909245471376171288, -92.77992525550196490 ) ) ;
#215197=AXIS2_PLACEMENT_3D ( 'NONE', #99479, #199911, #257243 ) ;
#215221=CIRCLE ( 'NONE', #161062, 11.64999999999999325 ) ;
#215226=AXIS2_PLACEMENT_3D ( 'NONE', #33377, #197536, #158451 ) ;
#215240=EDGE_LOOP ( 'NONE', ( #228220, #144344, #227283, #216517 ) ) ;
#215247=CARTESIAN_POINT ( 'NONE',  ( 23.25000000000000000, -11.74999999998883560, -130.9000000000000341 ) ) ;
#215250=DIRECTION ( 'NONE',  ( 0.000000000000000000, 0.000000000000000000, -1.000000000000000000 ) ) ;
#215262=DIRECTION ( 'NONE',  ( 0.000000000000000000, 0.000000000000000000, -1.000000000000000000 ) ) ;
#215309=AXIS2_PLACEMENT_3D ( 'NONE', #26572, #184328, #108655 ) ;
#215319=CARTESIAN_POINT ( 'NONE',  ( -20.64999999999999858, 2.400000000011155432, -120.7753780772379315 ) ) ;
#215334=ORIENTED_EDGE ( 'NONE', *, *, #119828, .T. ) ;
#215339=VERTEX_POINT ( 'NONE', #44084 ) ;
#215371=AXIS2_PLACEMENT_3D ( 'NONE', #45950, #29003, #164626 ) ;
#215378=CARTESIAN_POINT ( 'NONE',  ( -21.14250536705909411, 1.115600667400684642E-11, -93.98182782311928918 ) ) ;
#215380=DIRECTION ( 'NONE',  ( 0.000000000000000000, 0.000000000000000000, -1.000000000000000000 ) ) ;
#215392=ORIENTED_EDGE ( 'NONE', *, *, #216985, .F. ) ;
#215426=ORIENTED_EDGE ( 'NONE', *, *, #141105, .F. ) ;
#215432=CIRCLE ( 'NONE', #244648, 0.5000000000000004441 ) ;
#215437=B_SPLINE_CURVE_WITH_KNOTS ( 'NONE', 3,
 ( #72817, #166786, #67647, #147182, #253972, #200116, #198820, #213572, #192747, #54498, #100955, #179293, #240524, #42324, #119297, #180556, #233169, #21495, #94902, #1886, #234413, #20202 ),
 .UNSPECIFIED., .F., .F.,
 ( 4, 3, 3, 3, 3, 3, 3, 4 ),
 ( 0.000000000000000000, 7.307836821080901168E-06, 4.161455748548376624E-05, 7.576591810647682044E-05, 0.0001098090429817505560, 0.0001438003617351163335, 0.0001777914035423660871, 0.0002117966137403033873 ),
 .UNSPECIFIED. ) ;
#215449=ORIENTED_EDGE ( 'NONE', *, *, #159742, .T. ) ;
#215477=DIRECTION ( 'NONE',  ( -0.000000000000000000, 0.000000000000000000, -1.000000000000000000 ) ) ;
#215550=DIRECTION ( 'NONE',  ( 0.000000000000000000, 0.000000000000000000, -1.000000000000000000 ) ) ;
#215557=EDGE_LOOP ( 'NONE', ( #82812, #229427, #29734, #165315 ) ) ;
#215581=AXIS2_PLACEMENT_3D ( 'NONE', #25869, #31024, #165371 ) ;
#215590=ORIENTED_EDGE ( 'NONE', *, *, #6621, .F. ) ;
#215645=CIRCLE ( 'NONE', #65628, 0.2000000000000057288 ) ;
#215649=FACE_OUTER_BOUND ( 'NONE', #80688, .T. ) ;
#215707=AXIS2_PLACEMENT_3D ( 'NONE', #177667, #218018, #180216 ) ;
#215731=CARTESIAN_POINT ( 'NONE',  ( -22.39999999999999858, -0.09999999998884338825, -88.85042919245522341 ) ) ;
#215737=CIRCLE ( 'NONE', #78189, 0.09999999999999749367 ) ;
#215745=LINE ( 'NONE', #197472, #116689 ) ;
#215801=ORIENTED_EDGE ( 'NONE', *, *, #97431, .T. ) ;
#215807=FACE_OUTER_BOUND ( 'NONE', #130571, .T. ) ;
#215812=EDGE_CURVE ( 'NONE', #23430, #241950, #410, .T. ) ;
#215816=ORIENTED_EDGE ( 'NONE', *, *, #196254, .T. ) ;
#215830=CARTESIAN_POINT ( 'NONE',  ( -20.64999999999999858, 4.350000000011156054, -112.8500000000000369 ) ) ;
#215852=CARTESIAN_POINT ( 'NONE',  ( 20.94999999999999929, -8.663551401858002876, -110.0241011180673354 ) ) ;
#215864=CARTESIAN_POINT ( 'NONE',  ( 23.24999999999999645, 2.100000000011158274, -134.0000000000000284 ) ) ;
#215896=CIRCLE ( 'NONE', #136810, 0.1000000000000043493 ) ;
#215941=EDGE_LOOP ( 'NONE', ( #204135, #132015, #20364, #147109 ) ) ;
#215965=CARTESIAN_POINT ( 'NONE',  ( -18.59999999999999787, 7.070967871809997973, -137.7465642218683399 ) ) ;
#215972=EDGE_CURVE ( 'NONE', #46505, #80843, #212827, .T. ) ;
#215990=ORIENTED_EDGE ( 'NONE', *, *, #18776, .F. ) ;
#216018=CIRCLE ( 'NONE', #24517, 0.1000000000000028644 ) ;
#216020=ORIENTED_EDGE ( 'NONE', *, *, #254850, .F. ) ;
#216033=ADVANCED_FACE ( 'NONE', ( #222649 ), #222204, .T. ) ;
#216046=FACE_OUTER_BOUND ( 'NONE', #236564, .T. ) ;
#216100=AXIS2_PLACEMENT_3D ( 'NONE', #83551, #243932, #105683 ) ;
#216109=CARTESIAN_POINT ( 'NONE',  ( 18.49999999999998934, 6.550000000011156231, -121.7500000000000426 ) ) ;
#216115=DIRECTION ( 'NONE',  ( 1.000000000000000000, -0.000000000000000000, -0.000000000000000000 ) ) ;
#216128=DIRECTION ( 'NONE',  ( 1.000000000000000000, -0.000000000000000000, -0.000000000000000000 ) ) ;
#216152=DIRECTION ( 'NONE',  ( 0.000000000000000000, 0.000000000000000000, 1.000000000000000000 ) ) ;
#216170=EDGE_CURVE ( 'NONE', #189375, #212285, #152234, .T. ) ;
#216241=ORIENTED_EDGE ( 'NONE', *, *, #13208, .T. ) ;
#216254=CARTESIAN_POINT ( 'NONE',  ( -2.995603634470891112E-16, -11.74999999998884448, -121.7500000000000426 ) ) ;
#216278=DIRECTION ( 'NONE',  ( -1.000000000000000000, -0.000000000000000000, -0.000000000000000000 ) ) ;
#216282=AXIS2_PLACEMENT_3D ( 'NONE', #235700, #137870, #174517 ) ;
#216302=EDGE_LOOP ( 'NONE', ( #63829, #4816, #172903, #210379, #257288, #99494 ) ) ;
#216333=EDGE_CURVE ( 'NONE', #74301, #124743, #123261, .T. ) ;
#216340=EDGE_LOOP ( 'NONE', ( #41319, #38855, #29294 ) ) ;
#216362=CARTESIAN_POINT ( 'NONE',  ( 21.05000000000000071, 1.115600667400684642E-11, -134.0000000000000284 ) ) ;
#216371=CARTESIAN_POINT ( 'NONE',  ( -22.46246831459151494, 0.02191216695058596786, -88.85013543879007614 ) ) ;
#216398=VECTOR ( 'NONE', #64992, 1000.000000000000000 ) ;
#216403=EDGE_CURVE ( 'NONE', #92189, #34456, #163585, .T. ) ;
#216462=CARTESIAN_POINT ( 'NONE',  ( -23.25000000000000000, 11.65000000001115588, -126.9851942293460922 ) ) ;
#216469=ORIENTED_EDGE ( 'NONE', *, *, #115449, .F. ) ;
#216488=CARTESIAN_POINT ( 'NONE',  ( -21.05000000000000071, 1.115600667400684642E-11, -100.5000000000000284 ) ) ;
#216504=CARTESIAN_POINT ( 'NONE',  ( -23.15000000000000213, 1.115600667400684642E-11, -134.0000000000000284 ) ) ;
#216514=AXIS2_PLACEMENT_3D ( 'NONE', #101739, #181335, #1368 ) ;
#216517=ORIENTED_EDGE ( 'NONE', *, *, #228999, .F. ) ;
#216544=DIRECTION ( 'NONE',  ( -1.000000000000000000, 0.000000000000000000, 0.000000000000000000 ) ) ;
#216559=AXIS2_PLACEMENT_3D ( 'NONE', #77325, #137302, #60334 ) ;
#216565=CARTESIAN_POINT ( 'NONE',  ( 21.05000000000000071, -11.48912529306489994, -130.9000000000000341 ) ) ;
#216585=CARTESIAN_POINT ( 'NONE',  ( -18.59999999999999787, 9.250000000011157297, -112.7500000000000284 ) ) ;
#216586=ORIENTED_EDGE ( 'NONE', *, *, #221318, .T. ) ;
#216624=AXIS2_PLACEMENT_3D ( 'NONE', #212548, #215096, #134255 ) ;
#216631=ORIENTED_EDGE ( 'NONE', *, *, #154094, .F. ) ;
#216636=AXIS2_PLACEMENT_3D ( 'NONE', #2565, #7729, #182526 ) ;
#216654=CYLINDRICAL_SURFACE ( 'NONE', #139869, 0.09999999999999939493 ) ;
#216663=EDGE_CURVE ( 'NONE', #256334, #258105, #183894, .T. ) ;
#216672=CARTESIAN_POINT ( 'NONE',  ( -21.07971444708686093, 0.08782343632898161057, -94.17020791837347815 ) ) ;
#216687=LINE ( 'NONE', #39371, #11058 ) ;
#216690=DIRECTION ( 'NONE',  ( -0.000000000000000000, 0.000000000000000000, 1.000000000000000000 ) ) ;
#216700=VECTOR ( 'NONE', #184842, 1000.000000000000000 ) ;
#216705=AXIS2_PLACEMENT_3D ( 'NONE', #62468, #68898, #251358 ) ;
#216708=DIRECTION ( 'NONE',  ( 0.000000000000000000, 0.000000000000000000, -1.000000000000000000 ) ) ;
#216762=SPHERICAL_SURFACE ( 'NONE', #168633, 0.1000000000000000056 ) ;
#216763=CARTESIAN_POINT ( 'NONE',  ( 21.00000000000000000, 9.750000000011153745, -121.6500000000000341 ) ) ;
#216790=FACE_OUTER_BOUND ( 'NONE', #202754, .T. ) ;
#216795=AXIS2_PLACEMENT_3D ( 'NONE', #59321, #20249, #17652 ) ;
#216800=CARTESIAN_POINT ( 'NONE',  ( 23.14999999999999858, 2.000000000011158630, -134.0000000000000284 ) ) ;
#216802=ORIENTED_EDGE ( 'NONE', *, *, #237472, .F. ) ;
#216826=DIRECTION ( 'NONE',  ( 1.000000000000000000, 0.000000000000000000, 0.000000000000000000 ) ) ;
#216837=EDGE_CURVE ( 'NONE', #191177, #223255, #72966, .T. ) ;
#216851=DIRECTION ( 'NONE',  ( 0.000000000000000000, -1.000000000000000000, 0.000000000000000000 ) ) ;
#216859=ADVANCED_FACE ( 'NONE', ( #233314 ), #191633, .T. ) ;
#216889=ORIENTED_EDGE ( 'NONE', *, *, #147786, .F. ) ;
#216892=VERTEX_POINT ( 'NONE', #172069 ) ;
#216934=CARTESIAN_POINT ( 'NONE',  ( 23.14999999999999858, 1.115600667400684642E-11, -134.0000000000000284 ) ) ;
#216949=EDGE_CURVE ( 'NONE', #90248, #183734, #14120, .T. ) ;
#216971=ADVANCED_FACE ( 'NONE', ( #195473 ), #38953, .T. ) ;
#216977=EDGE_CURVE ( 'NONE', #105004, #50700, #255358, .T. ) ;
#216985=EDGE_CURVE ( 'NONE', #114076, #37949, #89099, .T. ) ;
#216990=AXIS2_PLACEMENT_3D ( 'NONE', #187988, #88854, #168473 ) ;
#216993=CIRCLE ( 'NONE', #29600, 0.1000000000000053069 ) ;
#216995=ORIENTED_EDGE ( 'NONE', *, *, #189391, .F. ) ;
#217071=DIRECTION ( 'NONE',  ( 1.000000000000000000, 0.000000000000000000, 0.000000000000000000 ) ) ;
#217083=CARTESIAN_POINT ( 'NONE',  ( -18.50000000000000000, -1.135018845899022466, -141.7169768834323520 ) ) ;
#217088=CARTESIAN_POINT ( 'NONE',  ( -21.09107601085560901, 6.363877975371195816, -100.4606928352827850 ) ) ;
#217108=DIRECTION ( 'NONE',  ( 0.000000000000000000, 1.810617628050740656E-13, 1.000000000000000000 ) ) ;
#217115=EDGE_LOOP ( 'NONE', ( #249644, #187495, #150172, #35743 ) ) ;
#217135=DIRECTION ( 'NONE',  ( 0.000000000000000000, 0.000000000000000000, 1.000000000000000000 ) ) ;
#217143=CARTESIAN_POINT ( 'NONE',  ( -20.64999999999999858, 2.000000000011154189, -120.7753780772379315 ) ) ;
#217155=CYLINDRICAL_SURFACE ( 'NONE', #214662, 0.1000000000000000472 ) ;
#217179=DIRECTION ( 'NONE',  ( 0.000000000000000000, 5.204170427930272346E-14, -1.000000000000000000 ) ) ;
#217200=CARTESIAN_POINT ( 'NONE',  ( -20.64999999999999858, 1.925233644870967487, -121.2697564668739005 ) ) ;
#217201=CARTESIAN_POINT ( 'NONE',  ( 21.04999999999879634, 6.496686585778748579, -100.5146561185119225 ) ) ;
#217206=ORIENTED_EDGE ( 'NONE', *, *, #213281, .F. ) ;
#217233=ORIENTED_EDGE ( 'NONE', *, *, #223594, .F. ) ;
#217237=CYLINDRICAL_SURFACE ( 'NONE', #235827, 11.80000000000000426 ) ;
#217264=CARTESIAN_POINT ( 'NONE',  ( -18.59999999999999787, -1.164121893230052995, -141.8148480855716684 ) ) ;
#217268=DIRECTION ( 'NONE',  ( 0.000000000000000000, 0.000000000000000000, 1.000000000000000000 ) ) ;
#217288=CARTESIAN_POINT ( 'NONE',  ( -22.50000000000000000, 11.65000000001113278, -100.5000000000000284 ) ) ;
#217312=CARTESIAN_POINT ( 'NONE',  ( -18.59999999999999787, -26.43935341558978891, -118.6415086075074896 ) ) ;
#217344=CARTESIAN_POINT ( 'NONE',  ( -18.39999999999999858, -9.682403433465239573, -140.6568433774128266 ) ) ;
#217349=CARTESIAN_POINT ( 'NONE',  ( -23.15000000000000213, 1.115600667400684642E-11, -100.5000000000000284 ) ) ;
#217376=CIRCLE ( 'NONE', #104919, 11.90000000000000746 ) ;
#217378=AXIS2_PLACEMENT_3D ( 'NONE', #183687, #70176, #5010 ) ;
#217390=FACE_OUTER_BOUND ( 'NONE', #187196, .T. ) ;
#217392=CARTESIAN_POINT ( 'NONE',  ( -18.59999999999999787, -9.499999999988842703, -112.6500000000000483 ) ) ;
#217395=VECTOR ( 'NONE', #88389, 1000.000000000000000 ) ;
#217396=ORIENTED_EDGE ( 'NONE', *, *, #157163, .T. ) ;
#217406=FACE_OUTER_BOUND ( 'NONE', #53828, .T. ) ;
#217429=EDGE_LOOP ( 'NONE', ( #238288, #13910, #122804, #105830 ) ) ;
#217456=CARTESIAN_POINT ( 'NONE',  ( 23.14999999999999503, 6.650000000011155876, -121.6500000000000341 ) ) ;
#217483=CARTESIAN_POINT ( 'NONE',  ( -20.85000000000000142, 11.75000000001115197, -127.2161343370219413 ) ) ;
#217484=VERTEX_POINT ( 'NONE', #223670 ) ;
#217495=VERTEX_POINT ( 'NONE', #243236 ) ;
#217518=ORIENTED_EDGE ( 'NONE', *, *, #11813, .T. ) ;
#217562=ORIENTED_EDGE ( 'NONE', *, *, #166125, .F. ) ;
#217575=CARTESIAN_POINT ( 'NONE',  ( -20.94999999999999929, 1.115600667400684642E-11, -134.0000000000000284 ) ) ;
#217598=ORIENTED_EDGE ( 'NONE', *, *, #8179, .T. ) ;
#217614=ORIENTED_EDGE ( 'NONE', *, *, #245428, .T. ) ;
#217625=DIRECTION ( 'NONE',  ( 0.000000000000000000, 0.000000000000000000, -1.000000000000000000 ) ) ;
#217629=CARTESIAN_POINT ( 'NONE',  ( -23.15000000000000213, -8.999999999988844479, -124.7060308773475867 ) ) ;
#217672=DIRECTION ( 'NONE',  ( -0.000000000000000000, -0.000000000000000000, -1.000000000000000000 ) ) ;
#217701=AXIS2_PLACEMENT_3D ( 'NONE', #226457, #246056, #123538 ) ;
#217715=DIRECTION ( 'NONE',  ( 2.952720810173288619E-16, -1.000000000000000000, 0.000000000000000000 ) ) ;
#217740=ORIENTED_EDGE ( 'NONE', *, *, #188597, .F. ) ;
#217747=CARTESIAN_POINT ( 'NONE',  ( -20.85000000000000142, 6.933893972137497030, -137.7856458343736108 ) ) ;
#217750=ADVANCED_FACE ( 'NONE', ( #235238 ), #213105, .T. ) ;
#217766=EDGE_CURVE ( 'NONE', #55645, #109188, #168641, .T. ) ;
#217830=ADVANCED_FACE ( 'NONE', ( #163418 ), #106011, .F. ) ;
#217887=VERTEX_POINT ( 'NONE', #201241 ) ;
#217908=CARTESIAN_POINT ( 'NONE',  ( 22.39999999999999503, 0.1000000000111554016, -92.70922040162665212 ) ) ;
#217920=DIRECTION ( 'NONE',  ( 1.000000000000000000, 0.000000000000000000, 0.000000000000000000 ) ) ;
#217935=EDGE_CURVE ( 'NONE', #217887, #163256, #202534, .T. ) ;
#217956=PLANE ( 'NONE',  #108999 ) ;
#217960=FACE_BOUND ( 'NONE', #229211, .T. ) ;
#217971=DIRECTION ( 'NONE',  ( -1.000000000000000000, -0.000000000000000000, -0.000000000000000000 ) ) ;
#217972=ORIENTED_EDGE ( 'NONE', *, *, #169768, .T. ) ;
#217987=CARTESIAN_POINT ( 'NONE',  ( 18.59999999999999076, 1.835341550235567887, -112.0551512925630249 ) ) ;
#217988=DIRECTION ( 'NONE',  ( 0.000000000000000000, -2.664535259100396996E-15, 1.000000000000000000 ) ) ;
#217989=EDGE_CURVE ( 'NONE', #213795, #200055, #97230, .T. ) ;
#218018=DIRECTION ( 'NONE',  ( -1.000000000000000000, 0.000000000000000000, 0.000000000000000000 ) ) ;
#218023=EDGE_LOOP ( 'NONE', ( #127997, #99035, #255654, #17963 ) ) ;
#218028=DIRECTION ( 'NONE',  ( 0.000000000000000000, -1.000000000000000000, 0.000000000000000000 ) ) ;
#218039=CARTESIAN_POINT ( 'NONE',  ( -18.50596464788227635, 10.30632246271647112, -139.5041836778896140 ) ) ;
#218043=AXIS2_PLACEMENT_3D ( 'NONE', #215830, #37234, #56741 ) ;
#218047=ORIENTED_EDGE ( 'NONE', *, *, #2174, .F. ) ;
#218104=AXIS2_PLACEMENT_3D ( 'NONE', #182919, #69393, #130628 ) ;
#218108=ADVANCED_FACE ( 'NONE', ( #49876 ), #129418, .T. ) ;
#218142=VECTOR ( 'NONE', #108096, 1000.000000000000000 ) ;
#218209=DIRECTION ( 'NONE',  ( -1.000000000000000000, -0.000000000000000000, -0.000000000000000000 ) ) ;
#218242=AXIS2_PLACEMENT_3D ( 'NONE', #226179, #63283, #26763 ) ;
#218270=CARTESIAN_POINT ( 'NONE',  ( 21.07954640115298162, 0.06600770715069002870, -94.17071230397618820 ) ) ;
#218307=EDGE_CURVE ( 'NONE', #151151, #145162, #9981, .T. ) ;
#218356=DIRECTION ( 'NONE',  ( 0.000000000000000000, 0.000000000000000000, -1.000000000000000000 ) ) ;
#218363=CARTESIAN_POINT ( 'NONE',  ( 21.00000000000000000, 9.750000000011153745, -121.6500000000000341 ) ) ;
#218374=ORIENTED_EDGE ( 'NONE', *, *, #254850, .T. ) ;
#218377=DIRECTION ( 'NONE',  ( 0.000000000000000000, 0.000000000000000000, -1.000000000000000000 ) ) ;
#218393=DIRECTION ( 'NONE',  ( 0.000000000000000000, 0.000000000000000000, -1.000000000000000000 ) ) ;
#218448=DIRECTION ( 'NONE',  ( 0.000000000000000000, 0.000000000000000000, -1.000000000000000000 ) ) ;
#218462=FACE_OUTER_BOUND ( 'NONE', #27349, .T. ) ;
#218512=EDGE_CURVE ( 'NONE', #257268, #123284, #118327, .T. ) ;
#218520=DIRECTION ( 'NONE',  ( -1.000000000000000000, 0.000000000000000000, 0.000000000000000000 ) ) ;
#218553=CIRCLE ( 'NONE', #47871, 0.09999999999999939493 ) ;
#218579=VERTEX_POINT ( 'NONE', #19104 ) ;
#218582=LINE ( 'NONE', #196463, #226616 ) ;
#218585=FACE_OUTER_BOUND ( 'NONE', #206080, .T. ) ;
#218590=AXIS2_PLACEMENT_3D ( 'NONE', #92417, #169443, #109409 ) ;
#218594=AXIS2_PLACEMENT_3D ( 'NONE', #137045, #159198, #178781 ) ;
#218616=DIRECTION ( 'NONE',  ( 1.000000000000000000, -0.000000000000000000, -0.000000000000000000 ) ) ;
#218620=ADVANCED_FACE ( 'NONE', ( #38680 ), #14286, .T. ) ;
#218623=EDGE_CURVE ( 'NONE', #200055, #236931, #234297, .T. ) ;
#218634=ADVANCED_FACE ( 'NONE', ( #201589 ), #161197, .T. ) ;
#218658=CARTESIAN_POINT ( 'NONE',  ( 20.94999999999999929, -9.399999999988844834, -124.1060308773475924 ) ) ;
#218667=DIRECTION ( 'NONE',  ( 0.000000000000000000, -0.4999999999999949485, 0.8660254037844415942 ) ) ;
#218668=DIRECTION ( 'NONE',  ( -1.000000000000000000, -2.952720810173289112E-16, 0.000000000000000000 ) ) ;
#218679=VECTOR ( 'NONE', #217672, 1000.000000000000000 ) ;
#218686=DIRECTION ( 'NONE',  ( -1.000000000000000000, 0.000000000000000000, 0.000000000000000000 ) ) ;
#218695=AXIS2_PLACEMENT_3D ( 'NONE', #192249, #17152, #160517 ) ;
#218697=AXIS2_PLACEMENT_3D ( 'NONE', #3893, #199553, #164267 ) ;
#218714=AXIS2_PLACEMENT_3D ( 'NONE', #115882, #31252, #95021 ) ;
#218728=DIRECTION ( 'NONE',  ( -0.000000000000000000, -0.000000000000000000, -1.000000000000000000 ) ) ;
#218741=DIRECTION ( 'NONE',  ( 0.000000000000000000, -0.000000000000000000, 1.000000000000000000 ) ) ;
#218753=EDGE_CURVE ( 'NONE', #100999, #77303, #193525, .T. ) ;
#218763=EDGE_CURVE ( 'NONE', #28813, #20729, #128483, .T. ) ;
#218768=LINE ( 'NONE', #137949, #187303 ) ;
#218804=CARTESIAN_POINT ( 'NONE',  ( -20.94999999999999929, 1.115600667400684642E-11, -134.0000000000000284 ) ) ;
#218806=ORIENTED_EDGE ( 'NONE', *, *, #137376, .F. ) ;
#218820=VERTEX_POINT ( 'NONE', #228871 ) ;
#218853=EDGE_CURVE ( 'NONE', #40869, #218579, #64331, .T. ) ;
#218861=ORIENTED_EDGE ( 'NONE', *, *, #94440, .F. ) ;
#218885=LINE ( 'NONE', #58525, #65336 ) ;
#218891=ORIENTED_EDGE ( 'NONE', *, *, #148020, .F. ) ;
#218898=ORIENTED_EDGE ( 'NONE', *, *, #66261, .F. ) ;
#218937=ADVANCED_FACE ( 'NONE', ( #16267 ), #179196, .T. ) ;
#218942=ORIENTED_EDGE ( 'NONE', *, *, #216403, .T. ) ;
#218944=DIRECTION ( 'NONE',  ( 1.000000000000000000, 0.000000000000000000, 0.000000000000000000 ) ) ;
#218959=DIRECTION ( 'NONE',  ( 0.000000000000000000, 0.000000000000000000, -1.000000000000000000 ) ) ;
#218978=DIRECTION ( 'NONE',  ( 0.000000000000000000, 0.5000000000000144329, 0.8660254037844302699 ) ) ;
#219005=DIRECTION ( 'NONE',  ( 0.000000000000000000, 0.000000000000000000, -1.000000000000000000 ) ) ;
#219006=CARTESIAN_POINT ( 'NONE',  ( 21.14999999999998082, -11.74999999998884448, -100.5000000000000284 ) ) ;
#219062=DIRECTION ( 'NONE',  ( -0.000000000000000000, -0.000000000000000000, -1.000000000000000000 ) ) ;
#219087=CARTESIAN_POINT ( 'NONE',  ( -22.45437739390953524, 1.115486826172573664E-11, -88.85042918840584036 ) ) ;
#219120=CARTESIAN_POINT ( 'NONE',  ( -20.85000000000000142, 11.65000000001115232, -127.2161343370219413 ) ) ;
#219147=EDGE_CURVE ( 'NONE', #56434, #215032, #90320, .T. ) ;
#219148=CIRCLE ( 'NONE', #106721, 0.09999999999999939493 ) ;
#219163=EDGE_CURVE ( 'NONE', #197646, #152480, #43674, .T. ) ;
#219169=CIRCLE ( 'NONE', #235931, 7.899999999999990585 ) ;
#219174=VERTEX_POINT ( 'NONE', #9506 ) ;
#219205=ORIENTED_EDGE ( 'NONE', *, *, #21879, .F. ) ;
#219233=ORIENTED_EDGE ( 'NONE', *, *, #224780, .T. ) ;
#219244=CARTESIAN_POINT ( 'NONE',  ( -21.05000000000000071, -0.02110330804789880416, -94.19548367073602435 ) ) ;
#219261=AXIS2_PLACEMENT_3D ( 'NONE', #79495, #41689, #16990 ) ;
#219266=ORIENTED_EDGE ( 'NONE', *, *, #71151, .T. ) ;
#219295=AXIS2_PLACEMENT_3D ( 'NONE', #42389, #240590, #661 ) ;
#219344=AXIS2_PLACEMENT_3D ( 'NONE', #99484, #179089, #239028 ) ;
#219345=CARTESIAN_POINT ( 'NONE',  ( -21.45000000000000284, 7.708578643773852157, -121.7500000000000426 ) ) ;
#219349=EDGE_LOOP ( 'NONE', ( #216802, #225883, #227594 ) ) ;
#219356=DIRECTION ( 'NONE',  ( -1.000000000000000000, 0.000000000000000000, 0.000000000000000000 ) ) ;
#219427=CIRCLE ( 'NONE', #57109, 0.1000000000000053069 ) ;
#219445=CARTESIAN_POINT ( 'NONE',  ( -21.46681500597866332, 1.115542391533913547E-11, -93.64248884057226974 ) ) ;
#219450=ORIENTED_EDGE ( 'NONE', *, *, #73468, .T. ) ;
#219454=ORIENTED_EDGE ( 'NONE', *, *, #177165, .F. ) ;
#219509=AXIS2_PLACEMENT_3D ( 'NONE', #181658, #145075, #2993 ) ;
#219585=CARTESIAN_POINT ( 'NONE',  ( -20.64999999999999858, 1.940186915899009490, -113.3291192110533672 ) ) ;
#219588=ORIENTED_EDGE ( 'NONE', *, *, #258058, .T. ) ;
#219593=VERTEX_POINT ( 'NONE', #83290 ) ;
#219634=ORIENTED_EDGE ( 'NONE', *, *, #180240, .F. ) ;
#219658=FACE_OUTER_BOUND ( 'NONE', #13832, .T. ) ;
#219678=CARTESIAN_POINT ( 'NONE',  ( 22.59999985501178799, 11.74986979301414181, -100.4344013302006005 ) ) ;
#219683=CARTESIAN_POINT ( 'NONE',  ( -23.25000000000000000, 1.115600667400684642E-11, -100.5000000000000284 ) ) ;
#219684=CIRCLE ( 'NONE', #44735, 0.1000000000000028644 ) ;
#219699=AXIS2_PLACEMENT_3D ( 'NONE', #126261, #166717, #186259 ) ;
#219734=SPHERICAL_SURFACE ( 'NONE', #169788, 0.1000000000000000056 ) ;
#219742=CIRCLE ( 'NONE', #190758, 0.1000000000000028644 ) ;
#219746=CARTESIAN_POINT ( 'NONE',  ( 18.49999999999999289, 6.450000000011156587, -110.5170271704400591 ) ) ;
#219752=VERTEX_POINT ( 'NONE', #233130 ) ;
#219753=CARTESIAN_POINT ( 'NONE',  ( 23.14999999999999503, 11.75000000001115552, -121.7500000000000426 ) ) ;
#219766=DIRECTION ( 'NONE',  ( -1.000000000000000000, 0.000000000000000000, 0.000000000000000000 ) ) ;
#219790=ORIENTED_EDGE ( 'NONE', *, *, #171541, .T. ) ;
#219798=ORIENTED_EDGE ( 'NONE', *, *, #35537, .F. ) ;
#219803=ORIENTED_EDGE ( 'NONE', *, *, #126166, .T. ) ;
#219876=ORIENTED_EDGE ( 'NONE', *, *, #112567, .F. ) ;
#219885=ORIENTED_EDGE ( 'NONE', *, *, #1587, .T. ) ;
#219904=DIRECTION ( 'NONE',  ( -1.000000000000000000, -0.000000000000000000, 0.000000000000000000 ) ) ;
#219928=ORIENTED_EDGE ( 'NONE', *, *, #34622, .T. ) ;
#219972=DIRECTION ( 'NONE',  ( -1.000000000000000000, 0.000000000000000000, 0.000000000000000000 ) ) ;
#219973=FACE_OUTER_BOUND ( 'NONE', #219349, .T. ) ;
#219986=FACE_OUTER_BOUND ( 'NONE', #103964, .T. ) ;
#219987=FACE_OUTER_BOUND ( 'NONE', #250463, .T. ) ;
#219999=CARTESIAN_POINT ( 'NONE',  ( 20.94999999999999574, -1.835341550213255957, -112.1551512925630050 ) ) ;
#220043=CARTESIAN_POINT ( 'NONE',  ( 20.94999999999999574, 8.926614585098251453, -108.9716830192231498 ) ) ;
#220057=AXIS2_PLACEMENT_3D ( 'NONE', #14004, #93521, #80021 ) ;
#220108=CARTESIAN_POINT ( 'NONE',  ( -18.50000000000000000, -9.421290279512383847, -140.8238821790260999 ) ) ;
#220114=ADVANCED_FACE ( 'NONE', ( #229901 ), #51232, .F. ) ;
#220142=CARTESIAN_POINT ( 'NONE',  ( -21.05000000000000071, 11.60000000001115517, -127.0717967697245143 ) ) ;
#220150=VECTOR ( 'NONE', #101649, 1000.000000000000114 ) ;
#220193=AXIS2_PLACEMENT_3D ( 'NONE', #19668, #137037, #80893 ) ;
#220242=DIRECTION ( 'NONE',  ( 0.000000000000000000, 0.000000000000000000, -1.000000000000000000 ) ) ;
#220243=ORIENTED_EDGE ( 'NONE', *, *, #200160, .F. ) ;
#220280=EDGE_CURVE ( 'NONE', #81295, #70011, #40148, .T. ) ;
#220297=ORIENTED_EDGE ( 'NONE', *, *, #164779, .F. ) ;
#220301=ORIENTED_EDGE ( 'NONE', *, *, #219147, .F. ) ;
#220305=VERTEX_POINT ( 'NONE', #79786 ) ;
#220386=AXIS2_PLACEMENT_3D ( 'NONE', #167676, #54111, #247174 ) ;
#220402=DIRECTION ( 'NONE',  ( 0.000000000000000000, 0.000000000000000000, 1.000000000000000000 ) ) ;
#220409=VECTOR ( 'NONE', #232102, 1000.000000000000000 ) ;
#220418=EDGE_LOOP ( 'NONE', ( #180382, #228177, #2892 ) ) ;
#220423=DIRECTION ( 'NONE',  ( 0.000000000000000000, -0.9915357197604853789, 0.1298341882520022694 ) ) ;
#220432=EDGE_CURVE ( 'NONE', #141245, #11304, #219169, .T. ) ;
#220445=ADVANCED_FACE ( 'NONE', ( #88775 ), #240041, .T. ) ;
#220455=DIRECTION ( 'NONE',  ( 1.000000000000000000, -0.000000000000000000, -0.000000000000000000 ) ) ;
#220478=EDGE_CURVE ( 'NONE', #32249, #257642, #193049, .T. ) ;
#220496=CARTESIAN_POINT ( 'NONE',  ( 18.52165635395179066, -9.481150711270972309, -107.5248375828625740 ) ) ;
#220515=DIRECTION ( 'NONE',  ( 1.000000000000000000, -0.000000000000000000, 0.000000000000000000 ) ) ;
#220532=ORIENTED_EDGE ( 'NONE', *, *, #161341, .F. ) ;
#220551=CARTESIAN_POINT ( 'NONE',  ( 18.59999999999999076, 10.20857864377385127, -121.8500000000000369 ) ) ;
#220568=ORIENTED_EDGE ( 'NONE', *, *, #131970, .T. ) ;
#220574=CONICAL_SURFACE ( 'NONE', #108146, 4.299999999999956302, 0.7853981633974466137 ) ;
#220581=CARTESIAN_POINT ( 'NONE',  ( -20.94999999999999929, -11.41227409413852989, -103.5000000000000426 ) ) ;
#220594=EDGE_CURVE ( 'NONE', #62956, #90545, #31434, .T. ) ;
#220596=DIRECTION ( 'NONE',  ( 0.000000000000000000, 0.000000000000000000, -1.000000000000000000 ) ) ;
#220603=CARTESIAN_POINT ( 'NONE',  ( 23.24999999999999289, 11.75000000001116263, -100.6000000000000369 ) ) ;
#220631=CARTESIAN_POINT ( 'NONE',  ( 20.85000000000000142, 1.115600667400684642E-11, -134.0000000000000284 ) ) ;
#220671=CARTESIAN_POINT ( 'NONE',  ( -18.59999999999999787, -1.835341550213255957, -112.1551512925630050 ) ) ;
#220692=CARTESIAN_POINT ( 'NONE',  ( 18.59999999999999787, -10.35479209691423996, -127.7565409830737906 ) ) ;
#220697=AXIS2_PLACEMENT_3D ( 'NONE', #197800, #178277, #79123 ) ;
#220723=EDGE_CURVE ( 'NONE', #189375, #38731, #97756, .T. ) ;
#220724=ORIENTED_EDGE ( 'NONE', *, *, #123563, .F. ) ;
#220750=CARTESIAN_POINT ( 'NONE',  ( -22.47071067811865319, 0.09909245471376178227, -92.77992525550196490 ) ) ;
#220772=DIRECTION ( 'NONE',  ( 1.000000000000000000, 0.000000000000000000, 0.000000000000000000 ) ) ;
#220775=DIRECTION ( 'NONE',  ( -1.000000000000000000, 0.000000000000000000, 0.000000000000000000 ) ) ;
#220782=ORIENTED_EDGE ( 'NONE', *, *, #108909, .F. ) ;
#220806=CARTESIAN_POINT ( 'NONE',  ( 21.10320863425824811, 6.400277386470322405, -100.4749777487729006 ) ) ;
#220809=CARTESIAN_POINT ( 'NONE',  ( 21.05000000000000071, 1.115600667400684642E-11, -134.0000000000000284 ) ) ;
#220818=DIRECTION ( 'NONE',  ( -0.000000000000000000, -1.000000000000000000, 0.000000000000000000 ) ) ;
#220819=CARTESIAN_POINT ( 'NONE',  ( -23.15000000000000213, 2.600000000011156054, -88.75000000000004263 ) ) ;
#220827=ORIENTED_EDGE ( 'NONE', *, *, #113908, .F. ) ;
#220854=EDGE_LOOP ( 'NONE', ( #83872, #104105, #60744, #208920 ) ) ;
#220885=AXIS2_PLACEMENT_3D ( 'NONE', #132183, #228734, #29278 ) ;
#220939=DIRECTION ( 'NONE',  ( -1.000000000000000000, -0.000000000000000000, -0.000000000000000000 ) ) ;
#220948=ORIENTED_EDGE ( 'NONE', *, *, #33615, .T. ) ;
#220974=ORIENTED_EDGE ( 'NONE', *, *, #88734, .T. ) ;
#220986=ORIENTED_EDGE ( 'NONE', *, *, #96503, .F. ) ;
#221021=CIRCLE ( 'NONE', #208591, 0.1000000000000000472 ) ;
#221027=ADVANCED_FACE ( 'NONE', ( #217406 ), #101269, .F. ) ;
#221028=EDGE_CURVE ( 'NONE', #37949, #18904, #194641, .T. ) ;
#221030=EDGE_LOOP ( 'NONE', ( #82437, #89050, #18171, #223968 ) ) ;
#221047=EDGE_CURVE ( 'NONE', #124745, #183616, #135303, .T. ) ;
#221074=ADVANCED_FACE ( 'NONE', ( #219986 ), #236995, .T. ) ;
#221114=DIRECTION ( 'NONE',  ( 0.000000000000000000, 0.000000000000000000, 1.000000000000000000 ) ) ;
#221166=ORIENTED_EDGE ( 'NONE', *, *, #28086, .F. ) ;
#221173=DIRECTION ( 'NONE',  ( 0.000000000000000000, 2.664535259100315349E-15, -1.000000000000000000 ) ) ;
#221197=ORIENTED_EDGE ( 'NONE', *, *, #134778, .T. ) ;
#221229=VERTEX_POINT ( 'NONE', #142993 ) ;
#221316=ORIENTED_EDGE ( 'NONE', *, *, #154609, .F. ) ;
#221318=EDGE_CURVE ( 'NONE', #213795, #61667, #69915, .T. ) ;
#221335=DIRECTION ( 'NONE',  ( 0.000000000000000000, -0.8777080977375715243, 0.4791956752370512551 ) ) ;
#221348=EDGE_LOOP ( 'NONE', ( #220301, #66821, #26470, #87464 ) ) ;
#221409=AXIS2_PLACEMENT_3D ( 'NONE', #208903, #36723, #159225 ) ;
#221468=ORIENTED_EDGE ( 'NONE', *, *, #207785, .F. ) ;
#221496=CARTESIAN_POINT ( 'NONE',  ( 23.24999999999999289, 11.75000000001116263, -112.6500000000000341 ) ) ;
#221499=VERTEX_POINT ( 'NONE', #236666 ) ;
#221524=FACE_BOUND ( 'NONE', #227132, .T. ) ;
#221531=DIRECTION ( 'NONE',  ( 1.000000000000000000, 0.000000000000000000, 0.000000000000000000 ) ) ;
#221558=CARTESIAN_POINT ( 'NONE',  ( 18.49999999999999645, 10.28015861706802347, -125.2245720712022319 ) ) ;
#221561=CIRCLE ( 'NONE', #180095, 4.049999999999998046 ) ;
#221616=FACE_OUTER_BOUND ( 'NONE', #104475, .T. ) ;
#221643=CARTESIAN_POINT ( 'NONE',  ( 20.94999999999999574, 1.835341550235567887, -112.0551512925630249 ) ) ;
#221647=ORIENTED_EDGE ( 'NONE', *, *, #42305, .F. ) ;
#221660=AXIS2_PLACEMENT_3D ( 'NONE', #119665, #94942, #195365 ) ;
#221690=CARTESIAN_POINT ( 'NONE',  ( -21.04999999999999716, -9.599999999988844124, -107.5320693966997112 ) ) ;
#221741=AXIS2_PLACEMENT_3D ( 'NONE', #37362, #39937, #15229 ) ;
#221755=DIRECTION ( 'NONE',  ( 0.000000000000000000, 0.000000000000000000, 1.000000000000000000 ) ) ;
#221762=CYLINDRICAL_SURFACE ( 'NONE', #156498, 0.5000000000000004441 ) ;
#221791=CIRCLE ( 'NONE', #26021, 0.09999999999999693856 ) ;
#221805=DIRECTION ( 'NONE',  ( -1.000000000000000000, 0.000000000000000000, 0.000000000000000000 ) ) ;
#221809=SPHERICAL_SURFACE ( 'NONE', #241248, 0.1000000000000000056 ) ;
#221813=VECTOR ( 'NONE', #202793, 1000.000000000000000 ) ;
#221829=CARTESIAN_POINT ( 'NONE',  ( 20.12500000000000000, 9.750000000011153745, -108.6117712821143186 ) ) ;
#221883=FACE_OUTER_BOUND ( 'NONE', #189287, .T. ) ;
#221910=DIRECTION ( 'NONE',  ( 0.000000000000000000, 0.9999631594459053030, 0.008583690987162899758 ) ) ;
#221952=AXIS2_PLACEMENT_3D ( 'NONE', #179407, #98516, #238069 ) ;
#221955=AXIS2_PLACEMENT_3D ( 'NONE', #128133, #64299, #164689 ) ;
#221975=DIRECTION ( 'NONE',  ( 0.000000000000000000, 0.000000000000000000, -1.000000000000000000 ) ) ;
#221982=FACE_OUTER_BOUND ( 'NONE', #13955, .T. ) ;
#222004=CARTESIAN_POINT ( 'NONE',  ( 22.50046968638162781, 0.04516984715002460293, -88.74995484552745495 ) ) ;
#222020=FACE_OUTER_BOUND ( 'NONE', #98949, .T. ) ;
#222029=ORIENTED_EDGE ( 'NONE', *, *, #229825, .T. ) ;
#222044=AXIS2_PLACEMENT_3D ( 'NONE', #221643, #122582, #44325 ) ;
#222100=CARTESIAN_POINT ( 'NONE',  ( -23.25000000000000000, 11.65000000001115588, -88.75000000000004263 ) ) ;
#222103=CYLINDRICAL_SURFACE ( 'NONE', #152765, 0.1000000000000028644 ) ;
#222128=DIRECTION ( 'NONE',  ( 0.000000000000000000, -0.1350103645451876944, 0.9908441862701601321 ) ) ;
#222137=CARTESIAN_POINT ( 'NONE',  ( -21.59142135623730852, 7.850000000011158718, -121.7500000000000426 ) ) ;
#222172=CIRCLE ( 'NONE', #180701, 0.09999999999999939493 ) ;
#222200=CIRCLE ( 'NONE', #97101, 0.09999999999999736877 ) ;
#222204=( BOUNDED_SURFACE ( )  B_SPLINE_SURFACE ( 3, 2, ( 
 ( #240955, #64871, #80560 ),
 ( #220108, #141840, #144384 ),
 ( #44036, #27069, #239674 ),
 ( #21914, #84385, #63589 ),
 ( #145684, #223934, #122292 ),
 ( #45317, #163990, #83114 ),
 ( #126117, #244785, #160161 ),
 ( #106550, #123573, #182271 ),
 ( #121038, #101385, #200538 ),
 ( #66163, #180990, #124857 ) ),
 .UNSPECIFIED., .F., .F., .F. ) 
 B_SPLINE_SURFACE_WITH_KNOTS ( ( 4, 2, 2, 2, 4 ),
 ( 3, 3 ),
 ( 0.0001836757140119083063, 0.0004000170051583593783, 0.0005081876507315849414, 0.0005622729735181976416, 0.0006163582963048104503 ),
 ( 0.000000000000000000, 1.000000000000000000 ),
 .UNSPECIFIED. ) 
 GEOMETRIC_REPRESENTATION_ITEM ( )  RATIONAL_B_SPLINE_SURFACE ( (
 ( 1.000000000000000000, 0.7071067811865425767, 1.000000000000000000),
 ( 1.000000000000000000, 0.6461995200031245279, 1.000000000000000000),
 ( 1.000000000000000000, 0.5776453529547745935, 1.000000000000000000),
 ( 1.000000000000000000, 0.4585233068352737584, 1.000000000000000000),
 ( 1.000000000000000000, 0.4154092989937730462, 1.000000000000000000),
 ( 1.000000000000000000, 0.3550093145837215358, 1.000000000000000000),
 ( 1.000000000000000000, 0.3354498651689109545, 1.000000000000000000),
 ( 1.000000000000000000, 0.3060347992252169802, 1.000000000000000000),
 ( 1.000000000000000000, 0.2963555829629179739, 1.000000000000000000),
 ( 1.000000000000000000, 0.2966190024560962923, 1.000000000000000000) ) ) 
 REPRESENTATION_ITEM ( '' )  SURFACE ( )  );
#222207=EDGE_LOOP ( 'NONE', ( #191128, #154734, #15651, #198629 ) ) ;
#222231=CARTESIAN_POINT ( 'NONE',  ( 22.48660254037844197, 11.65000000001115588, -100.4500000000000455 ) ) ;
#222236=AXIS2_PLACEMENT_3D ( 'NONE', #245734, #67091, #25414 ) ;
#222260=CARTESIAN_POINT ( 'NONE',  ( -20.94999999999999929, 5.900000000011102586, -110.7190997646564483 ) ) ;
#222320=AXIS2_PLACEMENT_3D ( 'NONE', #234280, #76489, #250007 ) ;
#222325=CARTESIAN_POINT ( 'NONE',  ( 21.07928932188134397, 6.328516656404468144, -100.4011048543456468 ) ) ;
#222334=FACE_OUTER_BOUND ( 'NONE', #245173, .T. ) ;
#222340=ORIENTED_EDGE ( 'NONE', *, *, #140296, .F. ) ;
#222359=CYLINDRICAL_SURFACE ( 'NONE', #256474, 0.09999999999999939493 ) ;
#222406=CARTESIAN_POINT ( 'NONE',  ( 20.30466543256828160, 9.304236939266628426, -108.7536626513920197 ) ) ;
#222428=DIRECTION ( 'NONE',  ( 0.000000000000000000, 0.000000000000000000, -1.000000000000000000 ) ) ;
#222439=AXIS2_PLACEMENT_3D ( 'NONE', #120284, #199803, #100644 ) ;
#222445=DIRECTION ( 'NONE',  ( 0.000000000000000000, 0.000000000000000000, -1.000000000000000000 ) ) ;
#222457=CIRCLE ( 'NONE', #176710, 0.2000000000000057288 ) ;
#222491=LINE ( 'NONE', #184666, #212761 ) ;
#222495=VERTEX_POINT ( 'NONE', #229027 ) ;
#222509=AXIS2_PLACEMENT_3D ( 'NONE', #80857, #203402, #220402 ) ;
#222520=DIRECTION ( 'NONE',  ( 0.000000000000000000, -3.729655473350132098E-14, -1.000000000000000000 ) ) ;
#222529=ORIENTED_EDGE ( 'NONE', *, *, #117676, .F. ) ;
#222623=VERTEX_POINT ( 'NONE', #195045 ) ;
#222646=CARTESIAN_POINT ( 'NONE',  ( -21.05000000000000071, -1.261786168553869603, -108.5864989635455089 ) ) ;
#222649=FACE_OUTER_BOUND ( 'NONE', #130682, .T. ) ;
#222664=CARTESIAN_POINT ( 'NONE',  ( -20.94999999999999929, -11.74999999998884448, -103.6000000000000369 ) ) ;
#222666=ORIENTED_EDGE ( 'NONE', *, *, #142418, .T. ) ;
#222681=DIRECTION ( 'NONE',  ( 0.000000000000000000, 0.000000000000000000, -1.000000000000000000 ) ) ;
#222696=DIRECTION ( 'NONE',  ( 0.000000000000000000, 1.000000000000000000, 0.000000000000000000 ) ) ;
#222727=DIRECTION ( 'NONE',  ( 0.000000000000000000, 0.000000000000000000, 1.000000000000000000 ) ) ;
#222791=CARTESIAN_POINT ( 'NONE',  ( -18.50000000000000000, 1.115600667400684642E-11, -100.5000000000000284 ) ) ;
#222807=EDGE_CURVE ( 'NONE', #52329, #4150, #245604, .T. ) ;
#222813=ORIENTED_EDGE ( 'NONE', *, *, #165099, .F. ) ;
#222814=LINE ( 'NONE', #65033, #58609 ) ;
#222827=CIRCLE ( 'NONE', #10466, 0.5000000000000004441 ) ;
#222832=VERTEX_POINT ( 'NONE', #222260 ) ;
#222854=FACE_OUTER_BOUND ( 'NONE', #8154, .T. ) ;
#222877=CARTESIAN_POINT ( 'NONE',  ( -20.94999999999999929, 10.29270135741298731, -139.4573618871519614 ) ) ;
#222894=DIRECTION ( 'NONE',  ( -1.000000000000000000, 0.000000000000000000, 0.000000000000000000 ) ) ;
#222913=DIRECTION ( 'NONE',  ( 0.000000000000000000, -8.881784197001832136E-16, -1.000000000000000000 ) ) ;
#222933=CARTESIAN_POINT ( 'NONE',  ( -18.59999999999999787, 11.65000000001115232, -107.5148057706540357 ) ) ;
#222982=FACE_OUTER_BOUND ( 'NONE', #236148, .T. ) ;
#222988=TOROIDAL_SURFACE ( 'NONE', #23111, 11.65000000000000036, 0.1000000000000000056 ) ;
#222994=DIRECTION ( 'NONE',  ( 1.000000000000000000, 0.000000000000000000, 0.000000000000000000 ) ) ;
#223001=ORIENTED_EDGE ( 'NONE', *, *, #51077, .F. ) ;
#223006=AXIS2_PLACEMENT_3D ( 'NONE', #166866, #246369, #67728 ) ;
#223022=CIRCLE ( 'NONE', #127351, 0.6000000000000033085 ) ;
#223023=EDGE_CURVE ( 'NONE', #214758, #97941, #244824, .T. ) ;
#223042=ORIENTED_EDGE ( 'NONE', *, *, #57315, .F. ) ;
#223045=CYLINDRICAL_SURFACE ( 'NONE', #128085, 0.1000000000000028644 ) ;
#223054=EDGE_CURVE ( 'NONE', #168030, #108506, #74194, .T. ) ;
#223061=CARTESIAN_POINT ( 'NONE',  ( -20.94684162601830124, 11.75000000001115374, -107.3416439990470224 ) ) ;
#223069=DIRECTION ( 'NONE',  ( -2.252264143451594314E-15, -0.1298341882520124002, -0.9915357197604841577 ) ) ;
#223100=DIRECTION ( 'NONE',  ( 0.000000000000000000, 0.000000000000000000, -1.000000000000000000 ) ) ;
#223107=CARTESIAN_POINT ( 'NONE',  ( -20.54999999999999716, 1.115600667400684642E-11, -121.1250000000000426 ) ) ;
#223156=EDGE_CURVE ( 'NONE', #255700, #144708, #233857, .T. ) ;
#223174=DIRECTION ( 'NONE',  ( 0.000000000000000000, -0.8660254037844383745, 0.5000000000000003331 ) ) ;
#223193=AXIS2_PLACEMENT_3D ( 'NONE', #104514, #184082, #44583 ) ;
#223196=AXIS2_PLACEMENT_3D ( 'NONE', #84348, #161397, #41456 ) ;
#223233=DIRECTION ( 'NONE',  ( 0.000000000000000000, 0.000000000000000000, -1.000000000000000000 ) ) ;
#223244=EDGE_CURVE ( 'NONE', #168568, #189415, #61682, .T. ) ;
#223255=VERTEX_POINT ( 'NONE', #91342 ) ;
#223264=VECTOR ( 'NONE', #224979, 1000.000000000000114 ) ;
#223286=DIRECTION ( 'NONE',  ( -1.000000000000000000, -2.952720810173289112E-16, 0.000000000000000000 ) ) ;
#223291=CARTESIAN_POINT ( 'NONE',  ( -18.59999999999999787, 1.835341550235567887, -112.1551512925630192 ) ) ;
#223298=ORIENTED_EDGE ( 'NONE', *, *, #42790, .F. ) ;
#223300=CARTESIAN_POINT ( 'NONE',  ( 22.40000000000010516, 1.019545479467800000E-11, -88.74956710754109679 ) ) ;
#223307=AXIS2_PLACEMENT_3D ( 'NONE', #220551, #142286, #139705 ) ;
#223319=CARTESIAN_POINT ( 'NONE',  ( 18.59999999999999076, 6.550000000011156231, -110.5170271704400591 ) ) ;
#223325=EDGE_CURVE ( 'NONE', #114232, #55645, #58979, .T. ) ;
#223344=ORIENTED_EDGE ( 'NONE', *, *, #27298, .T. ) ;
#223364=CARTESIAN_POINT ( 'NONE',  ( 21.11101077988997332, 6.423684734737197921, -100.4847147310857167 ) ) ;
#223378=LINE ( 'NONE', #8216, #157092 ) ;
#223382=VERTEX_POINT ( 'NONE', #60686 ) ;
#223415=EDGE_CURVE ( 'NONE', #172696, #242555, #90891, .T. ) ;
#223443=CIRCLE ( 'NONE', #173635, 0.1000000000000028644 ) ;
#223473=EDGE_CURVE ( 'NONE', #58429, #110957, #53495, .T. ) ;
#223506=DIRECTION ( 'NONE',  ( 0.000000000000000000, 0.9998779222360102414, 0.01562499999996356907 ) ) ;
#223511=ORIENTED_EDGE ( 'NONE', *, *, #72639, .T. ) ;
#223541=EDGE_CURVE ( 'NONE', #106114, #54036, #170065, .T. ) ;
#223545=VECTOR ( 'NONE', #15850, 1000.000000000000000 ) ;
#223594=EDGE_CURVE ( 'NONE', #95316, #35530, #190954, .T. ) ;
#223606=ORIENTED_EDGE ( 'NONE', *, *, #15830, .T. ) ;
#223612=TOROIDAL_SURFACE ( 'NONE', #127402, 0.2000000000000000111, 0.1000000000000000056 ) ;
#223632=LINE ( 'NONE', #78971, #168701 ) ;
#223643=FACE_OUTER_BOUND ( 'NONE', #126463, .T. ) ;
#223670=CARTESIAN_POINT ( 'NONE',  ( -21.05000000000000071, -11.29603075032412995, -103.5478991596638991 ) ) ;
#223672=ORIENTED_EDGE ( 'NONE', *, *, #242095, .F. ) ;
#223694=CARTESIAN_POINT ( 'NONE',  ( 19.97071067811865674, 11.72071067812981937, -125.1500000000000341 ) ) ;
#223696=AXIS2_PLACEMENT_3D ( 'NONE', #209375, #170300, #54144 ) ;
#223700=CARTESIAN_POINT ( 'NONE',  ( -20.94999999999999929, -11.29603075032412995, -103.5478991596638991 ) ) ;
#223717=VERTEX_POINT ( 'NONE', #154412 ) ;
#223724=AXIS2_PLACEMENT_3D ( 'NONE', #77822, #122107, #199072 ) ;
#223729=CIRCLE ( 'NONE', #257023, 0.09999999999998898659 ) ;
#223744=CARTESIAN_POINT ( 'NONE',  ( -20.94788355080264353, 10.30207779525983192, -139.4895520716782755 ) ) ;
#223745=ORIENTED_EDGE ( 'NONE', *, *, #197483, .F. ) ;
#223791=AXIS2_PLACEMENT_3D ( 'NONE', #159229, #244828, #165303 ) ;
#223841=CARTESIAN_POINT ( 'NONE',  ( -21.05000000000000071, -1.162701749926853712, -108.6000000000000227 ) ) ;
#223866=DIRECTION ( 'NONE',  ( -1.000000000000000000, -2.952720810173289112E-16, 0.000000000000000000 ) ) ;
#223868=ORIENTED_EDGE ( 'NONE', *, *, #15905, .F. ) ;
#223898=AXIS2_PLACEMENT_3D ( 'NONE', #103488, #225988, #183062 ) ;
#223910=LINE ( 'NONE', #183527, #210778 ) ;
#223934=CARTESIAN_POINT ( 'NONE',  ( -18.33981767444297972, -9.569575789792892806, -140.8191618437252259 ) ) ;
#223967=DIRECTION ( 'NONE',  ( 0.000000000000000000, 0.5000000000000014433, -0.8660254037844378194 ) ) ;
#223968=ORIENTED_EDGE ( 'NONE', *, *, #186855, .F. ) ;
#223975=DIRECTION ( 'NONE',  ( -0.000000000000000000, 1.000000000000000000, 2.891205793294679805E-16 ) ) ;
#223987=EDGE_CURVE ( 'NONE', #61689, #23723, #145065, .T. ) ;
#224003=ORIENTED_EDGE ( 'NONE', *, *, #126834, .T. ) ;
#224029=EDGE_LOOP ( 'NONE', ( #237087, #128118, #21823 ) ) ;
#224068=AXIS2_PLACEMENT_3D ( 'NONE', #234329, #54414, #36156 ) ;
#224097=ADVANCED_FACE ( 'NONE', ( #91528 ), #52377, .F. ) ;
#224110=CIRCLE ( 'NONE', #128272, 0.2000000000000000944 ) ;
#224140=ADVANCED_FACE ( 'NONE', ( #77089 ), #132988, .T. ) ;
#224141=CARTESIAN_POINT ( 'NONE',  ( 23.14999999999999858, 1.115625160336667635E-11, -132.0000000000000284 ) ) ;
#224167=AXIS2_PLACEMENT_3D ( 'NONE', #42275, #142628, #117946 ) ;
#224202=LINE ( 'NONE', #45581, #106468 ) ;
#224226=AXIS2_PLACEMENT_3D ( 'NONE', #231211, #115096, #194666 ) ;
#224278=EDGE_LOOP ( 'NONE', ( #32511, #12620, #37457, #4649 ) ) ;
#224306=VERTEX_POINT ( 'NONE', #241319 ) ;
#224333=CARTESIAN_POINT ( 'NONE',  ( 18.54147908293623459, -9.463261657916778091, -107.5489488967560305 ) ) ;
#224344=VERTEX_POINT ( 'NONE', #108220 ) ;
#224349=CARTESIAN_POINT ( 'NONE',  ( -21.05000000000000426, 11.75000000001115374, -107.2838656629781866 ) ) ;
#224356=DIRECTION ( 'NONE',  ( 0.000000000000000000, 0.000000000000000000, 1.000000000000000000 ) ) ;
#224357=DIRECTION ( 'NONE',  ( 1.000000000000000000, 0.000000000000000000, 0.000000000000000000 ) ) ;
#224398=AXIS2_PLACEMENT_3D ( 'NONE', #80976, #117550, #103104 ) ;
#224405=AXIS2_PLACEMENT_3D ( 'NONE', #51202, #130768, #250712 ) ;
#224415=EDGE_LOOP ( 'NONE', ( #242009, #5307, #101083, #171114 ) ) ;
#224433=DIRECTION ( 'NONE',  ( 1.000000000000000000, -0.000000000000000000, -0.000000000000000000 ) ) ;
#224446=DIRECTION ( 'NONE',  ( 0.000000000000000000, 0.000000000000000000, -1.000000000000000000 ) ) ;
#224447=EDGE_CURVE ( 'NONE', #193670, #61689, #208615, .T. ) ;
#224460=CARTESIAN_POINT ( 'NONE',  ( 20.94999999999999929, 14.05000000001115623, -128.4863049292391395 ) ) ;
#224542=ORIENTED_EDGE ( 'NONE', *, *, #39688, .F. ) ;
#224544=DIRECTION ( 'NONE',  ( 0.000000000000000000, 0.8660254037844309360, -0.5000000000000134337 ) ) ;
#224551=LINE ( 'NONE', #244113, #18773 ) ;
#224572=EDGE_LOOP ( 'NONE', ( #164526, #49328, #57454, #49837, #147917, #90200, #245917, #3177, #118506, #138917, #2056 ) ) ;
#224609=ORIENTED_EDGE ( 'NONE', *, *, #64441, .T. ) ;
#224645=CARTESIAN_POINT ( 'NONE',  ( -22.39999999999999858, 0.1000000000111554016, -92.70922040162662370 ) ) ;
#224657=ORIENTED_EDGE ( 'NONE', *, *, #246469, .F. ) ;
#224669=ORIENTED_EDGE ( 'NONE', *, *, #187651, .F. ) ;
#224679=VERTEX_POINT ( 'NONE', #237153 ) ;
#224699=ORIENTED_EDGE ( 'NONE', *, *, #34622, .F. ) ;
#224774=CIRCLE ( 'NONE', #112371, 0.09999999999998898659 ) ;
#224779=EDGE_LOOP ( 'NONE', ( #165376, #28525, #217598, #160502 ) ) ;
#224780=EDGE_CURVE ( 'NONE', #138314, #238428, #124965, .T. ) ;
#224788=ADVANCED_FACE ( 'NONE', ( #27119 ), #154227, .T. ) ;
#224790=ADVANCED_FACE ( 'NONE', ( #106595 ), #184866, .T. ) ;
#224799=ORIENTED_EDGE ( 'NONE', *, *, #175835, .T. ) ;
#224824=TOROIDAL_SURFACE ( 'NONE', #216636, 11.65000000000000036, 0.1000000000000000056 ) ;
#224849=CARTESIAN_POINT ( 'NONE',  ( 20.96428641294275863, 11.75000000001150013, -127.1748931779422946 ) ) ;
#224903=VERTEX_POINT ( 'NONE', #191327 ) ;
#224934=EDGE_CURVE ( 'NONE', #144062, #160208, #71367, .T. ) ;
#224935=VERTEX_POINT ( 'NONE', #152195 ) ;
#224940=CARTESIAN_POINT ( 'NONE',  ( 20.94999999999999929, -8.999999999988842703, -124.1060308773475924 ) ) ;
#224957=ORIENTED_EDGE ( 'NONE', *, *, #148020, .T. ) ;
#224979=DIRECTION ( 'NONE',  ( -0.7071067811865474617, -0.7071067811865474617, -2.044391222244499837E-16 ) ) ;
#224987=ORIENTED_EDGE ( 'NONE', *, *, #72461, .F. ) ;
#225084=CARTESIAN_POINT ( 'NONE',  ( -22.47071067811865319, 0.09909245471376171288, -92.77992525550196490 ) ) ;
#225090=ORIENTED_EDGE ( 'NONE', *, *, #186855, .T. ) ;
#225102=CARTESIAN_POINT ( 'NONE',  ( 22.47071067811864964, 0.09909245471376176839, -92.77992525550199332 ) ) ;
#225109=CIRCLE ( 'NONE', #133553, 0.09999999999999939493 ) ;
#225112=DIRECTION ( 'NONE',  ( 0.000000000000000000, 2.891205793294679805E-16, -1.000000000000000000 ) ) ;
#225126=ORIENTED_EDGE ( 'NONE', *, *, #166144, .F. ) ;
#225145=CARTESIAN_POINT ( 'NONE',  ( 23.24999999999999645, 1.115600667400684642E-11, -134.0000000000000284 ) ) ;
#225150=CARTESIAN_POINT ( 'NONE',  ( 20.95346350065193519, 8.887177249185651107, -109.0117319470354289 ) ) ;
#225156=CARTESIAN_POINT ( 'NONE',  ( -23.15000000000000213, -8.999999999988844479, -124.1060308773475924 ) ) ;
#225161=CARTESIAN_POINT ( 'NONE',  ( 18.59999999999999787, 1.115600667400684642E-11, -100.5000000000000284 ) ) ;
#225166=TOROIDAL_SURFACE ( 'NONE', #112771, 1.900000000000002576, 0.1000000000000000056 ) ;
#225218=ORIENTED_EDGE ( 'NONE', *, *, #180931, .T. ) ;
#225247=DIRECTION ( 'NONE',  ( -0.000000000000000000, 0.9274965247785350586, 0.3738317757009704811 ) ) ;
#225253=DIRECTION ( 'NONE',  ( 1.000000000000000000, 0.000000000000000000, 0.000000000000000000 ) ) ;
#225262=CARTESIAN_POINT ( 'NONE',  ( 21.00023020733438273, 6.390869245278871347, -100.5000000000000426 ) ) ;
#225274=VERTEX_POINT ( 'NONE', #116280 ) ;
#225315=EDGE_CURVE ( 'NONE', #46937, #143803, #97953, .T. ) ;
#225324=DIRECTION ( 'NONE',  ( -1.000000000000000000, 0.000000000000000000, 0.000000000000000000 ) ) ;
#225371=VERTEX_POINT ( 'NONE', #41888 ) ;
#225372=AXIS2_PLACEMENT_3D ( 'NONE', #136230, #193678, #157135 ) ;
#225427=EDGE_CURVE ( 'NONE', #222832, #148718, #101803, .T. ) ;
#225440=ORIENTED_EDGE ( 'NONE', *, *, #178207, .T. ) ;
#225450=CARTESIAN_POINT ( 'NONE',  ( -20.94999999999999929, 1.115600667400684642E-11, -134.0000000000000284 ) ) ;
#225484=ORIENTED_EDGE ( 'NONE', *, *, #46044, .F. ) ;
#225517=VECTOR ( 'NONE', #108793, 1000.000000000000000 ) ;
#225670=CARTESIAN_POINT ( 'NONE',  ( 21.76363531954645936, 7.012936547882880234, -100.4009981257005819 ) ) ;
#225689=EDGE_CURVE ( 'NONE', #170174, #163726, #252896, .T. ) ;
#225693=FACE_OUTER_BOUND ( 'NONE', #58221, .T. ) ;
#225715=DIRECTION ( 'NONE',  ( 0.000000000000000000, 0.000000000000000000, 1.000000000000000000 ) ) ;
#225719=DIRECTION ( 'NONE',  ( -1.000000000000000000, 0.000000000000000000, 0.000000000000000000 ) ) ;
#225786=ADVANCED_FACE ( 'NONE', ( #178531 ), #37734, .F. ) ;
#225788=ORIENTED_EDGE ( 'NONE', *, *, #91435, .T. ) ;
#225800=DIRECTION ( 'NONE',  ( 0.000000000000000000, 0.000000000000000000, 1.000000000000000000 ) ) ;
#225806=DIRECTION ( 'NONE',  ( -2.952720810173289112E-16, 1.000000000000000000, 0.000000000000000000 ) ) ;
#225807=FACE_OUTER_BOUND ( 'NONE', #152829, .T. ) ;
#225815=CYLINDRICAL_SURFACE ( 'NONE', #182880, 0.1000000000000000472 ) ;
#225849=ORIENTED_EDGE ( 'NONE', *, *, #117024, .F. ) ;
#225857=AXIS2_PLACEMENT_3D ( 'NONE', #250329, #139347, #255412 ) ;
#225860=ORIENTED_EDGE ( 'NONE', *, *, #133818, .T. ) ;
#225865=ORIENTED_EDGE ( 'NONE', *, *, #58797, .F. ) ;
#225883=ORIENTED_EDGE ( 'NONE', *, *, #252259, .T. ) ;
#225913=DIRECTION ( 'NONE',  ( 1.000000000000000000, 0.000000000000000000, 0.000000000000000000 ) ) ;
#225916=VECTOR ( 'NONE', #9002, 1000.000000000000000 ) ;
#225935=ORIENTED_EDGE ( 'NONE', *, *, #255971, .T. ) ;
#225967=EDGE_CURVE ( 'NONE', #224903, #74036, #251143, .T. ) ;
#225988=DIRECTION ( 'NONE',  ( 0.000000000000000000, -0.000000000000000000, 1.000000000000000000 ) ) ;
#225989=ORIENTED_EDGE ( 'NONE', *, *, #285, .T. ) ;
#225995=AXIS2_PLACEMENT_3D ( 'NONE', #173015, #107853, #131268 ) ;
#226002=VECTOR ( 'NONE', #71899, 1000.000000000000000 ) ;
#226009=EDGE_CURVE ( 'NONE', #182849, #27184, #142802, .T. ) ;
#226016=DIRECTION ( 'NONE',  ( 1.000000000000000000, 0.000000000000000000, 0.000000000000000000 ) ) ;
#226017=DIRECTION ( 'NONE',  ( 0.000000000000000000, 0.000000000000000000, -1.000000000000000000 ) ) ;
#226051=CARTESIAN_POINT ( 'NONE',  ( 23.24999999999999289, 6.650000000011155876, -121.8500000000000369 ) ) ;
#226079=AXIS2_PLACEMENT_3D ( 'NONE', #71122, #13687, #151948 ) ;
#226107=ORIENTED_EDGE ( 'NONE', *, *, #66396, .T. ) ;
#226115=CARTESIAN_POINT ( 'NONE',  ( 21.03670563405602678, 10.62482368933940258, -112.8255468862091817 ) ) ;
#226116=FACE_OUTER_BOUND ( 'NONE', #131959, .T. ) ;
#226130=ORIENTED_EDGE ( 'NONE', *, *, #147574, .F. ) ;
#226146=VERTEX_POINT ( 'NONE', #230468 ) ;
#226171=EDGE_CURVE ( 'NONE', #245888, #77303, #59592, .T. ) ;
#226179=CARTESIAN_POINT ( 'NONE',  ( -23.15000000000000213, -8.596261682231835621, -109.9501275171503210 ) ) ;
#226202=CARTESIAN_POINT ( 'NONE',  ( -20.64999999999999858, 2.000000000011154189, -120.7753780772379315 ) ) ;
#226205=DIRECTION ( 'NONE',  ( 1.000000000000000000, -7.304098846218133681E-16, 4.607487905232622991E-31 ) ) ;
#226228=AXIS2_PLACEMENT_3D ( 'NONE', #18709, #39597, #121686 ) ;
#226231=AXIS2_PLACEMENT_3D ( 'NONE', #216934, #16208, #57853 ) ;
#226249=DIRECTION ( 'NONE',  ( -7.304098846218201720E-16, 1.000000000000000000, 0.000000000000000000 ) ) ;
#226267=CARTESIAN_POINT ( 'NONE',  ( 23.14999999999999858, 11.65000000001116298, -126.9851942293460922 ) ) ;
#226279=CARTESIAN_POINT ( 'NONE',  ( -18.59999999999999787, -1.261786168553869603, -108.5864989635455089 ) ) ;
#226286=DIRECTION ( 'NONE',  ( 1.000000000000000000, -0.000000000000000000, -0.000000000000000000 ) ) ;
#226312=VERTEX_POINT ( 'NONE', #227581 ) ;
#226314=CARTESIAN_POINT ( 'NONE',  ( 21.05000000000000071, 1.115600667400684642E-11, -96.20000000000000284 ) ) ;
#226332=AXIS2_PLACEMENT_3D ( 'NONE', #204988, #163330, #221975 ) ;
#226345=DIRECTION ( 'NONE',  ( 0.000000000000000000, 0.000000000000000000, -1.000000000000000000 ) ) ;
#226380=AXIS2_PLACEMENT_3D ( 'NONE', #50938, #251735, #212621 ) ;
#226418=DIRECTION ( 'NONE',  ( -1.000000000000000000, 0.000000000000000000, 0.000000000000000000 ) ) ;
#226451=CARTESIAN_POINT ( 'NONE',  ( 20.94999999999999574, -1.736257131586239844, -112.0686523290175245 ) ) ;
#226457=CARTESIAN_POINT ( 'NONE',  ( -23.15000000000000213, -8.999999999988846255, -110.3939691226524786 ) ) ;
#226466=DIRECTION ( 'NONE',  ( 0.000000000000000000, 0.000000000000000000, -1.000000000000000000 ) ) ;
#226470=DIRECTION ( 'NONE',  ( 0.000000000000000000, 0.000000000000000000, -1.000000000000000000 ) ) ;
#226474=LINE ( 'NONE', #28339, #28550 ) ;
#226516=VECTOR ( 'NONE', #207409, 999.9999999999998863 ) ;
#226525=DIRECTION ( 'NONE',  ( 1.734723475976817507E-14, 0.000000000000000000, -1.000000000000000000 ) ) ;
#226532=AXIS2_PLACEMENT_3D ( 'NONE', #119821, #19423, #40300 ) ;
#226575=FACE_OUTER_BOUND ( 'NONE', #112151, .T. ) ;
#226587=ADVANCED_FACE ( 'NONE', ( #240430 ), #256071, .F. ) ;
#226616=VECTOR ( 'NONE', #99906, 1000.000000000000000 ) ;
#226636=DIRECTION ( 'NONE',  ( -0.7071067811865475727, -0.7071067811865475727, 0.000000000000000000 ) ) ;
#226637=VECTOR ( 'NONE', #36125, 1000.000000000000000 ) ;
#226647=DIRECTION ( 'NONE',  ( -0.1538461538461510236, 0.9880948137434718559, 0.000000000000000000 ) ) ;
#226657=ADVANCED_FACE ( 'NONE', ( #76199 ), #111031, .T. ) ;
#226703=DIRECTION ( 'NONE',  ( 0.000000000000000000, -0.9893560106964500722, 0.1455152366551550613 ) ) ;
#226707=LINE ( 'NONE', #29837, #186907 ) ;
#226712=DIRECTION ( 'NONE',  ( 0.000000000000000000, 0.000000000000000000, -1.000000000000000000 ) ) ;
#226719=TOROIDAL_SURFACE ( 'NONE', #47817, 11.65000000000000036, 0.1000000000000000056 ) ;
#226794=ORIENTED_EDGE ( 'NONE', *, *, #188275, .F. ) ;
#226800=CARTESIAN_POINT ( 'NONE',  ( -20.64999999999999858, 7.150000000011155876, -121.6500000000000341 ) ) ;
#226821=CARTESIAN_POINT ( 'NONE',  ( 20.94999999999999929, -1.362429037182151470, -141.8888812479212334 ) ) ;
#226884=EDGE_CURVE ( 'NONE', #194066, #75197, #51579, .T. ) ;
#226890=DIRECTION ( 'NONE',  ( 0.000000000000000000, -1.000000000000000000, 0.000000000000000000 ) ) ;
#226891=EDGE_CURVE ( 'NONE', #52329, #233201, #35099, .T. ) ;
#226938=ORIENTED_EDGE ( 'NONE', *, *, #76503, .T. ) ;
#226954=AXIS2_PLACEMENT_3D ( 'NONE', #172644, #8390, #30533 ) ;
#226970=CARTESIAN_POINT ( 'NONE',  ( 20.94999999999999929, -8.730841121484166578, -124.4019252810156928 ) ) ;
#227008=ORIENTED_EDGE ( 'NONE', *, *, #148607, .F. ) ;
#227037=EDGE_CURVE ( 'NONE', #173670, #69817, #23548, .T. ) ;
#227047=CARTESIAN_POINT ( 'NONE',  ( 21.05000000000000071, 6.540656951712400691, -100.6000000000000369 ) ) ;
#227049=ORIENTED_EDGE ( 'NONE', *, *, #180474, .F. ) ;
#227099=CARTESIAN_POINT ( 'NONE',  ( -20.54999999999999716, 1.115600667400684642E-11, -134.0000000000000284 ) ) ;
#227132=EDGE_LOOP ( 'NONE', ( #217972, #106670 ) ) ;
#227161=ORIENTED_EDGE ( 'NONE', *, *, #239546, .T. ) ;
#227166=ADVANCED_FACE ( 'NONE', ( #54277 ), #133821, .T. ) ;
#227200=DIRECTION ( 'NONE',  ( 0.000000000000000000, 0.000000000000000000, -1.000000000000000000 ) ) ;
#227283=ORIENTED_EDGE ( 'NONE', *, *, #152182, .F. ) ;
#227302=DIRECTION ( 'NONE',  ( -1.000000000000000000, 0.000000000000000000, 0.000000000000000000 ) ) ;
#227376=CARTESIAN_POINT ( 'NONE',  ( 21.14999999999999858, -0.09999999998884338825, -93.95934304829877703 ) ) ;
#227383=CYLINDRICAL_SURFACE ( 'NONE', #5045, 0.09999999999999939493 ) ;
#227427=CARTESIAN_POINT ( 'NONE',  ( 23.25000000000000000, -11.74999999998883560, -88.75000000000004263 ) ) ;
#227431=CARTESIAN_POINT ( 'NONE',  ( -18.52186455168981993, -9.481018481431380707, -107.5250164779145194 ) ) ;
#227437=DIRECTION ( 'NONE',  ( -1.000000000000000000, 0.000000000000000000, 0.000000000000000000 ) ) ;
#227447=CIRCLE ( 'NONE', #106633, 1.900000000000012790 ) ;
#227452=EDGE_CURVE ( 'NONE', #148820, #191859, #10317, .T. ) ;
#227457=DIRECTION ( 'NONE',  ( -0.000000000000000000, -0.000000000000000000, -1.000000000000000000 ) ) ;
#227467=AXIS2_PLACEMENT_3D ( 'NONE', #112965, #231637, #154683 ) ;
#227485=VERTEX_POINT ( 'NONE', #149570 ) ;
#227550=CARTESIAN_POINT ( 'NONE',  ( -20.54999999999999716, 4.350000000011156054, -112.8500000000000369 ) ) ;
#227558=CARTESIAN_POINT ( 'NONE',  ( 21.78635804494511419, 0.09900506551883611617, -93.46433851484685817 ) ) ;
#227581=CARTESIAN_POINT ( 'NONE',  ( 18.59999999999997655, 1.115600667400684642E-11, -141.9000000000000341 ) ) ;
#227594=ORIENTED_EDGE ( 'NONE', *, *, #141366, .F. ) ;
#227628=ADVANCED_FACE ( 'NONE', ( #234200 ), #110241, .T. ) ;
#227649=CARTESIAN_POINT ( 'NONE',  ( -23.25000000000000000, 1.115600667400684642E-11, -136.1000000000000227 ) ) ;
#227650=DIRECTION ( 'NONE',  ( -0.000000000000000000, 0.8660254037844502539, 0.4999999999999799605 ) ) ;
#227685=ORIENTED_EDGE ( 'NONE', *, *, #161602, .F. ) ;
#227695=DIRECTION ( 'NONE',  ( -1.000000000000000000, 0.000000000000000000, 0.000000000000000000 ) ) ;
#227738=ORIENTED_EDGE ( 'NONE', *, *, #225689, .F. ) ;
#227739=DIRECTION ( 'NONE',  ( -1.000000000000000000, 0.000000000000000000, 0.000000000000000000 ) ) ;
#227744=ADVANCED_FACE ( 'NONE', ( #3282 ), #164947, .F. ) ;
#227774=VECTOR ( 'NONE', #244294, 1000.000000000000114 ) ;
#227781=CARTESIAN_POINT ( 'NONE',  ( 21.05000000000000071, 1.115600667400684642E-11, -100.5000000000000284 ) ) ;
#227787=DIRECTION ( 'NONE',  ( -0.000000000000000000, -0.000000000000000000, -1.000000000000000000 ) ) ;
#227824=CARTESIAN_POINT ( 'NONE',  ( -18.59999999999999787, 7.250000000011155521, -121.8500000000000369 ) ) ;
#227827=FACE_OUTER_BOUND ( 'NONE', #52004, .T. ) ;
#227830=DIRECTION ( 'NONE',  ( 0.000000000000000000, 2.664535259100339804E-15, -1.000000000000000000 ) ) ;
#227842=EDGE_CURVE ( 'NONE', #190980, #43551, #48068, .T. ) ;
#227849=AXIS2_PLACEMENT_3D ( 'NONE', #94320, #13521, #117744 ) ;
#227856=EDGE_CURVE ( 'NONE', #180521, #116815, #127179, .T. ) ;
#227869=ORIENTED_EDGE ( 'NONE', *, *, #207576, .F. ) ;
#227912=VERTEX_POINT ( 'NONE', #138628 ) ;
#227929=LINE ( 'NONE', #205791, #217395 ) ;
#227961=AXIS2_PLACEMENT_3D ( 'NONE', #11965, #31544, #91482 ) ;
#227974=CARTESIAN_POINT ( 'NONE',  ( -20.64999999999999858, -8.999999999988844479, -124.1060308773475924 ) ) ;
#228005=CARTESIAN_POINT ( 'NONE',  ( 18.44444291854882323, -9.490101180932068559, -140.6289039648909807 ) ) ;
#228012=DIRECTION ( 'NONE',  ( 0.000000000000000000, -2.428612866367797514E-13, 1.000000000000000000 ) ) ;
#228030=ORIENTED_EDGE ( 'NONE', *, *, #1497, .F. ) ;
#228034=CARTESIAN_POINT ( 'NONE',  ( 23.15000000000000213, -8.999999999988844479, -110.3939691226524786 ) ) ;
#228037=DIRECTION ( 'NONE',  ( 1.000000000000000000, 0.000000000000000000, 0.000000000000000000 ) ) ;
#228038=ADVANCED_FACE ( 'NONE', ( #203774 ), #148027, .F. ) ;
#228105=CYLINDRICAL_SURFACE ( 'NONE', #246242, 2.000000000000001776 ) ;
#228140=ORIENTED_EDGE ( 'NONE', *, *, #209889, .F. ) ;
#228158=AXIS2_PLACEMENT_3D ( 'NONE', #101357, #157588, #197937 ) ;
#228177=ORIENTED_EDGE ( 'NONE', *, *, #81118, .T. ) ;
#228199=EDGE_CURVE ( 'NONE', #34898, #196043, #250594, .T. ) ;
#228220=ORIENTED_EDGE ( 'NONE', *, *, #240851, .T. ) ;
#228222=CARTESIAN_POINT ( 'NONE',  ( -21.05000000000000071, 6.257814610487270279, -100.4022097086912311 ) ) ;
#228223=CARTESIAN_POINT ( 'NONE',  ( -20.54999999999999716, 2.400000000011155432, -120.7753780772379315 ) ) ;
#228226=CARTESIAN_POINT ( 'NONE',  ( 21.05000000000000071, 14.05000000001115623, -128.4863049292391395 ) ) ;
#228251=CARTESIAN_POINT ( 'NONE',  ( 18.59999999999999787, -1.249999999988843369, -141.8004807544151333 ) ) ;
#228256=DIRECTION ( 'NONE',  ( -1.000000000000000000, 0.000000000000000000, 0.000000000000000000 ) ) ;
#228277=CARTESIAN_POINT ( 'NONE',  ( 20.94788355080264353, 10.30207779525983192, -139.4895520716782755 ) ) ;
#228302=CARTESIAN_POINT ( 'NONE',  ( -23.25000000000000000, 4.250000000011156409, -121.6500000000000341 ) ) ;
#228346=ADVANCED_FACE ( 'NONE', ( #25787 ), #148306, .F. ) ;
#228364=FACE_OUTER_BOUND ( 'NONE', #8541, .T. ) ;
#228419=ORIENTED_EDGE ( 'NONE', *, *, #57050, .T. ) ;
#228425=DIRECTION ( 'NONE',  ( -0.000000000000000000, -0.000000000000000000, 1.000000000000000000 ) ) ;
#228437=DIRECTION ( 'NONE',  ( 0.000000000000000000, 0.000000000000000000, 1.000000000000000000 ) ) ;
#228449=DIRECTION ( 'NONE',  ( -0.000000000000000000, -0.000000000000000000, -1.000000000000000000 ) ) ;
#228456=EDGE_LOOP ( 'NONE', ( #125394, #233627, #206518 ) ) ;
#228467=ORIENTED_EDGE ( 'NONE', *, *, #115052, .T. ) ;
#228479=ADVANCED_FACE ( 'NONE', ( #93446 ), #208291, .F. ) ;
#228495=ORIENTED_EDGE ( 'NONE', *, *, #111469, .T. ) ;
#228510=EDGE_CURVE ( 'NONE', #51418, #210814, #49196, .T. ) ;
#228541=ORIENTED_EDGE ( 'NONE', *, *, #237402, .F. ) ;
#228566=DIRECTION ( 'NONE',  ( 1.000000000000000000, 0.000000000000000000, -0.000000000000000000 ) ) ;
#228594=ORIENTED_EDGE ( 'NONE', *, *, #186894, .T. ) ;
#228595=DIRECTION ( 'NONE',  ( 0.000000000000000000, 0.000000000000000000, 1.000000000000000000 ) ) ;
#228624=AXIS2_PLACEMENT_3D ( 'NONE', #77557, #3165, #141406 ) ;
#228637=AXIS2_PLACEMENT_3D ( 'NONE', #208834, #189279, #10638 ) ;
#228664=ORIENTED_EDGE ( 'NONE', *, *, #32032, .T. ) ;
#228666=ORIENTED_EDGE ( 'NONE', *, *, #24891, .T. ) ;
#228709=AXIS2_PLACEMENT_3D ( 'NONE', #241391, #27512, #167015 ) ;
#228734=DIRECTION ( 'NONE',  ( -0.000000000000000000, -0.000000000000000000, -1.000000000000000000 ) ) ;
#228751=DIRECTION ( 'NONE',  ( -0.000000000000000000, 0.000000000000000000, 1.000000000000000000 ) ) ;
#228752=ORIENTED_EDGE ( 'NONE', *, *, #122605, .F. ) ;
#228760=ADVANCED_FACE ( 'NONE', ( #86707 ), #222359, .T. ) ;
#228795=DIRECTION ( 'NONE',  ( 1.000000000000000000, 0.000000000000000000, 0.000000000000000000 ) ) ;
#228796=DIRECTION ( 'NONE',  ( 0.000000000000000000, 0.000000000000000000, -1.000000000000000000 ) ) ;
#228797=ORIENTED_EDGE ( 'NONE', *, *, #226171, .T. ) ;
#228814=CARTESIAN_POINT ( 'NONE',  ( -20.94999999999999929, 1.116121084443477685E-11, -103.4000000000000199 ) ) ;
#228817=LINE ( 'NONE', #28064, #132590 ) ;
#228844=DIRECTION ( 'NONE',  ( 0.000000000000000000, 0.000000000000000000, -1.000000000000000000 ) ) ;
#228848=DIRECTION ( 'NONE',  ( 0.000000000000000000, 0.8660254037844384856, -0.5000000000000003331 ) ) ;
#228854=CARTESIAN_POINT ( 'NONE',  ( -20.64999999999999858, 7.150000000011155876, -121.6500000000000341 ) ) ;
#228863=CARTESIAN_POINT ( 'NONE',  ( -21.37071067811865532, 8.070710678129811910, -112.7500000000000284 ) ) ;
#228870=CIRCLE ( 'NONE', #4009, 0.09999999999998898659 ) ;
#228871=CARTESIAN_POINT ( 'NONE',  ( 23.24999999999999289, -4.149999999988843058, -100.5000000000000284 ) ) ;
#228873=VERTEX_POINT ( 'NONE', #133566 ) ;
#228880=ORIENTED_EDGE ( 'NONE', *, *, #179536, .T. ) ;
#228891=AXIS2_PLACEMENT_3D ( 'NONE', #208706, #110866, #31371 ) ;
#228896=FACE_OUTER_BOUND ( 'NONE', #65031, .T. ) ;
#228902=CARTESIAN_POINT ( 'NONE',  ( -20.94999999999999929, 10.29288807859936661, -139.4580020160122160 ) ) ;
#228906=CARTESIAN_POINT ( 'NONE',  ( 20.94999999999999574, -11.64999999998883595, -103.5000000000000426 ) ) ;
#228910=CARTESIAN_POINT ( 'NONE',  ( 21.05000000000000071, 1.115600667400684642E-11, -134.0000000000000284 ) ) ;
#228984=DIRECTION ( 'NONE',  ( -0.8660254037844653530, 0.000000000000000000, 0.4999999999999539257 ) ) ;
#228999=EDGE_CURVE ( 'NONE', #240710, #97170, #215221, .T. ) ;
#229000=EDGE_CURVE ( 'NONE', #54821, #243146, #110987, .T. ) ;
#229027=CARTESIAN_POINT ( 'NONE',  ( -18.50000000000000000, -1.362429037182155023, -141.8888812479212334 ) ) ;
#229053=AXIS2_PLACEMENT_3D ( 'NONE', #137270, #134692, #99417 ) ;
#229073=DIRECTION ( 'NONE',  ( 1.000000000000000000, 0.000000000000000000, 0.000000000000000000 ) ) ;
#229079=DIRECTION ( 'NONE',  ( 0.000000000000000000, -3.122502256758163408E-13, 1.000000000000000000 ) ) ;
#229099=VERTEX_POINT ( 'NONE', #244201 ) ;
#229129=DIRECTION ( 'NONE',  ( 0.000000000000000000, 0.6728971962616697722, 0.7397360091702875895 ) ) ;
#229137=AXIS2_PLACEMENT_3D ( 'NONE', #13171, #92687, #232232 ) ;
#229172=ORIENTED_EDGE ( 'NONE', *, *, #158672, .F. ) ;
#229176=AXIS2_PLACEMENT_3D ( 'NONE', #147608, #129331, #45941 ) ;
#229187=CARTESIAN_POINT ( 'NONE',  ( -20.64999999999999858, 1.115600667400684642E-11, -100.5000000000000284 ) ) ;
#229191=( BOUNDED_SURFACE ( )  B_SPLINE_SURFACE ( 3, 2, ( 
 ( #101177, #26856, #163779 ),
 ( #105029, #45103, #64662 ),
 ( #124647, #205448, #122083 ),
 ( #5953, #46368, #244579 ) ),
 .UNSPECIFIED., .F., .F., .F. ) 
 B_SPLINE_SURFACE_WITH_KNOTS ( ( 4, 4 ),
 ( 3, 3 ),
 ( 0.04058434257139457990, 0.04256401539001585660 ),
 ( 0.000000000000000000, 1.000000000000000000 ),
 .UNSPECIFIED. ) 
 GEOMETRIC_REPRESENTATION_ITEM ( )  RATIONAL_B_SPLINE_SURFACE ( (
 ( 1.000000000000000000, 0.7103081912008297749, 1.000000000000000000),
 ( 1.000000000000000000, 0.7104998333555392342, 1.000000000000000000),
 ( 1.000000000000000000, 0.7107238315755070035, 1.000000000000000000),
 ( 1.000000000000000000, 0.7110073749539291832, 1.000000000000000000) ) ) 
 REPRESENTATION_ITEM ( '' )  SURFACE ( )  );
#229211=EDGE_LOOP ( 'NONE', ( #162783, #49931, #189111, #79108, #13495, #74448, #208404, #97582 ) ) ;
#229216=EDGE_CURVE ( 'NONE', #193635, #53973, #201233, .T. ) ;
#229259=ORIENTED_EDGE ( 'NONE', *, *, #35793, .F. ) ;
#229269=DIRECTION ( 'NONE',  ( -0.000000000000000000, 0.1298341882520022694, 0.9915357197604853789 ) ) ;
#229297=CARTESIAN_POINT ( 'NONE',  ( 21.12400247839524070, 10.72148804404149836, -112.7500000000000284 ) ) ;
#229305=CYLINDRICAL_SURFACE ( 'NONE', #133815, 0.1000000000000028644 ) ;
#229320=DIRECTION ( 'NONE',  ( -0.000000000000000000, -0.000000000000000000, 1.000000000000000000 ) ) ;
#229345=AXIS2_PLACEMENT_3D ( 'NONE', #49536, #7853, #129074 ) ;
#229386=VECTOR ( 'NONE', #82235, 1000.000000000000000 ) ;
#229391=ORIENTED_EDGE ( 'NONE', *, *, #248772, .T. ) ;
#229399=CARTESIAN_POINT ( 'NONE',  ( 18.59999999999999787, -9.399999999988843058, -140.8820418481727188 ) ) ;
#229409=AXIS2_PLACEMENT_3D ( 'NONE', #211111, #170756, #50719 ) ;
#229417=CARTESIAN_POINT ( 'NONE',  ( -21.05000000000000071, 14.05000000001115623, -106.0136950707610310 ) ) ;
#229427=ORIENTED_EDGE ( 'NONE', *, *, #5792, .T. ) ;
#229474=ORIENTED_EDGE ( 'NONE', *, *, #193976, .F. ) ;
#229482=CARTESIAN_POINT ( 'NONE',  ( 20.94999999999999929, -11.29603075032412640, -130.9521008403361861 ) ) ;
#229504=CARTESIAN_POINT ( 'NONE',  ( -21.05000000000000071, 6.413759733821437159, -100.5856130608040360 ) ) ;
#229505=CARTESIAN_POINT ( 'NONE',  ( 21.14999999999999858, 1.115600667400684642E-11, -112.6500000000000341 ) ) ;
#229528=DIRECTION ( 'NONE',  ( 0.000000000000000000, -0.8660254037844411501, -0.4999999999999956701 ) ) ;
#229530=CARTESIAN_POINT ( 'NONE',  ( -22.59066674512252249, 11.75000000001115552, -100.4694958763693791 ) ) ;
#229642=CARTESIAN_POINT ( 'NONE',  ( 23.14999999999999858, 11.60000000001116227, -127.0717967697245427 ) ) ;
#229699=TOROIDAL_SURFACE ( 'NONE', #9115, 0.2000000000000000111, 0.1000000000000000056 ) ;
#229727=CARTESIAN_POINT ( 'NONE',  ( 18.46921299892753865, -9.509378177812608968, -107.4865787093704625 ) ) ;
#229733=ORIENTED_EDGE ( 'NONE', *, *, #13411, .T. ) ;
#229761=CARTESIAN_POINT ( 'NONE',  ( -18.59999999999999787, -9.399999999988851940, -140.8820418481727188 ) ) ;
#229772=DIRECTION ( 'NONE',  ( -1.000000000000000000, -1.836970198721029934E-16, 0.000000000000000000 ) ) ;
#229774=LINE ( 'NONE', #51106, #231417 ) ;
#229812=CYLINDRICAL_SURFACE ( 'NONE', #236179, 0.09999999999999939493 ) ;
#229825=EDGE_CURVE ( 'NONE', #126637, #126709, #54707, .T. ) ;
#229845=DIRECTION ( 'NONE',  ( -3.890533409366484652E-14, -0.1298341882520124002, -0.9915357197604841577 ) ) ;
#229853=EDGE_CURVE ( 'NONE', #153129, #215339, #40663, .T. ) ;
#229856=CIRCLE ( 'NONE', #250691, 12.97499999999998721 ) ;
#229861=ORIENTED_EDGE ( 'NONE', *, *, #246088, .T. ) ;
#229863=EDGE_CURVE ( 'NONE', #197589, #72909, #53068, .T. ) ;
#229901=FACE_OUTER_BOUND ( 'NONE', #125051, .T. ) ;
#229931=ORIENTED_EDGE ( 'NONE', *, *, #93294, .T. ) ;
#229941=VERTEX_POINT ( 'NONE', #173431 ) ;
#229986=ADVANCED_FACE ( 'NONE', ( #148044 ), #62419, .F. ) ;
#230037=DIRECTION ( 'NONE',  ( 2.827886303505249259E-16, -0.8660254037844411501, -0.4999999999999956701 ) ) ;
#230067=AXIS2_PLACEMENT_3D ( 'NONE', #36483, #73053, #95144 ) ;
#230129=FACE_OUTER_BOUND ( 'NONE', #56750, .T. ) ;
#230142=VECTOR ( 'NONE', #21994, 1000.000000000000000 ) ;
#230147=CARTESIAN_POINT ( 'NONE',  ( -21.05000000000000071, 1.115600667400684642E-11, -134.0000000000000284 ) ) ;
#230168=DIRECTION ( 'NONE',  ( 1.000000000000000000, 0.000000000000000000, 0.000000000000000000 ) ) ;
#230226=FACE_OUTER_BOUND ( 'NONE', #86767, .T. ) ;
#230245=DIRECTION ( 'NONE',  ( 0.000000000000000000, 0.000000000000000000, 1.000000000000000000 ) ) ;
#230283=EDGE_LOOP ( 'NONE', ( #106427, #168425, #115792, #59403 ) ) ;
#230339=AXIS2_PLACEMENT_3D ( 'NONE', #115021, #251957, #194588 ) ;
#230383=EDGE_CURVE ( 'NONE', #179995, #163256, #127732, .T. ) ;
#230401=CARTESIAN_POINT ( 'NONE',  ( -23.25000000000000000, -8.999999999988846255, -110.3939691226524786 ) ) ;
#230415=DIRECTION ( 'NONE',  ( -0.000000000000000000, 1.000000000000000000, -0.000000000000000000 ) ) ;
#230468=CARTESIAN_POINT ( 'NONE',  ( -18.50000000000000000, 11.65000000001115232, -121.8500000000000369 ) ) ;
#230473=EDGE_CURVE ( 'NONE', #18469, #130606, #23956, .T. ) ;
#230478=AXIS2_PLACEMENT_3D ( 'NONE', #133404, #115118, #13458 ) ;
#230492=CARTESIAN_POINT ( 'NONE',  ( -23.15000000000000213, 1.115648428625851357E-11, -130.1000000000000512 ) ) ;
#230493=CARTESIAN_POINT ( 'NONE',  ( 18.59999999999999076, 1.115600667400684642E-11, -134.0000000000000284 ) ) ;
#230517=ORIENTED_EDGE ( 'NONE', *, *, #233925, .T. ) ;
#230532=AXIS2_PLACEMENT_3D ( 'NONE', #99038, #39119, #238574 ) ;
#230548=CIRCLE ( 'NONE', #134822, 4.149999999999999467 ) ;
#230561=CARTESIAN_POINT ( 'NONE',  ( -18.43569575749026512, -9.519327731081288491, -107.4729763765593873 ) ) ;
#230583=CARTESIAN_POINT ( 'NONE',  ( 18.49999999999999289, -9.419078080838366063, -140.8299253502082991 ) ) ;
#230589=DIRECTION ( 'NONE',  ( 1.000000000000000000, -0.000000000000000000, 0.000000000000000000 ) ) ;
#230604=DIRECTION ( 'NONE',  ( 0.000000000000000000, 0.8660254037844385966, -0.5000000000000003331 ) ) ;
#230627=FACE_BOUND ( 'NONE', #151605, .T. ) ;
#230651=ORIENTED_EDGE ( 'NONE', *, *, #223541, .T. ) ;
#230693=VERTEX_POINT ( 'NONE', #134567 ) ;
#230694=ADVANCED_FACE ( 'NONE', ( #155482 ), #154206, .T. ) ;
#230705=AXIS2_PLACEMENT_3D ( 'NONE', #219120, #77052, #199602 ) ;
#230737=DIRECTION ( 'NONE',  ( 1.000000000000000000, -0.000000000000000000, -0.000000000000000000 ) ) ;
#230760=EDGE_CURVE ( 'NONE', #242360, #34846, #163159, .T. ) ;
#230779=ADVANCED_FACE ( 'NONE', ( #181443 ), #236042, .F. ) ;
#230801=CARTESIAN_POINT ( 'NONE',  ( 18.31325810956326805, -9.536388475995964953, -140.8684402063051948 ) ) ;
#230861=AXIS2_PLACEMENT_3D ( 'NONE', #105689, #108299, #170890 ) ;
#230901=VECTOR ( 'NONE', #151739, 1000.000000000000000 ) ;
#230949=CARTESIAN_POINT ( 'NONE',  ( 23.24999999999999289, 6.450000000011156587, -121.6500000000000341 ) ) ;
#230999=DIRECTION ( 'NONE',  ( -1.000000000000000000, 6.938893903907270030E-14, 0.000000000000000000 ) ) ;
#231004=DIRECTION ( 'NONE',  ( -1.000000000000000000, 0.000000000000000000, 0.000000000000000000 ) ) ;
#231024=ADVANCED_FACE ( 'NONE', ( #142224 ), #223045, .F. ) ;
#231026=CARTESIAN_POINT ( 'NONE',  ( 18.49999999999999289, 6.450000000011156587, -88.75000000000004263 ) ) ;
#231059=DIRECTION ( 'NONE',  ( -0.000000000000000000, 0.000000000000000000, 1.000000000000000000 ) ) ;
#231076=ORIENTED_EDGE ( 'NONE', *, *, #123192, .T. ) ;
#231080=ORIENTED_EDGE ( 'NONE', *, *, #224447, .F. ) ;
#231083=PLANE ( 'NONE',  #67499 ) ;
#231137=ORIENTED_EDGE ( 'NONE', *, *, #100327, .F. ) ;
#231165=ORIENTED_EDGE ( 'NONE', *, *, #186700, .F. ) ;
#231172=VERTEX_POINT ( 'NONE', #31309 ) ;
#231211=CARTESIAN_POINT ( 'NONE',  ( -21.29999999999995808, 1.115600667400684642E-11, -100.5000000000000284 ) ) ;
#231236=ORIENTED_EDGE ( 'NONE', *, *, #114734, .T. ) ;
#231241=VECTOR ( 'NONE', #124863, 1000.000000000000000 ) ;
#231259=VERTEX_POINT ( 'NONE', #168261 ) ;
#231292=CARTESIAN_POINT ( 'NONE',  ( 21.09610168723073187, 0.03358950690264430466, -94.12104428477526596 ) ) ;
#231295=AXIS2_PLACEMENT_3D ( 'NONE', #11801, #54740, #251664 ) ;
#231305=CIRCLE ( 'NONE', #206352, 0.1000000000000028644 ) ;
#231370=EDGE_LOOP ( 'NONE', ( #126207, #130552, #30997, #142691 ) ) ;
#231387=AXIS2_PLACEMENT_3D ( 'NONE', #227974, #46752, #29811 ) ;
#231396=ORIENTED_EDGE ( 'NONE', *, *, #110781, .T. ) ;
#231417=VECTOR ( 'NONE', #34179, 1000.000000000000000 ) ;
#231453=( BOUNDED_CURVE ( )  B_SPLINE_CURVE ( 3, ( #205483, #105066, #48983, #45137 ),
 .UNSPECIFIED., .F., .F. ) 
 B_SPLINE_CURVE_WITH_KNOTS ( ( 4, 4 ),
 ( 4.712388980384689674, 6.231880751915386263 ),
 .UNSPECIFIED. ) 
 CURVE ( )  GEOMETRIC_REPRESENTATION_ITEM ( )  RATIONAL_B_SPLINE_CURVE ( ( 1.000000000000000000, 0.8166740347213228279, 0.8166740347213228279, 1.000000000000000000 ) ) 
 REPRESENTATION_ITEM ( '' )  );
#231491=AXIS2_PLACEMENT_3D ( 'NONE', #72128, #135915, #134627 ) ;
#231492=CARTESIAN_POINT ( 'NONE',  ( 20.94999999999999574, 1.162701749949165642, -108.6000000000000227 ) ) ;
#231493=CARTESIAN_POINT ( 'NONE',  ( 20.94999999999999929, 1.115600667400684642E-11, -134.0000000000000284 ) ) ;
#231507=TOROIDAL_SURFACE ( 'NONE', #77351, 0.4000000000000003553, 0.1000000000000000056 ) ;
#231509=EDGE_CURVE ( 'NONE', #53442, #196016, #90643, .T. ) ;
#231510=ORIENTED_EDGE ( 'NONE', *, *, #9726, .F. ) ;
#231569=EDGE_LOOP ( 'NONE', ( #252865, #145706, #199874, #94190 ) ) ;
#231570=( GEOMETRIC_REPRESENTATION_CONTEXT ( 3 ) GLOBAL_UNCERTAINTY_ASSIGNED_CONTEXT ( ( #160080 ) ) GLOBAL_UNIT_ASSIGNED_CONTEXT ( ( #208057, #177910, #151940 ) ) REPRESENTATION_CONTEXT ( 'NONE', 'WORKASPACE' ) );
#231623=CARTESIAN_POINT ( 'NONE',  ( -20.94999999999999929, -0.2561057920810652089, -100.4651035583277405 ) ) ;
#231628=CIRCLE ( 'NONE', #6763, 0.09999999999999939493 ) ;
#231633=EDGE_CURVE ( 'NONE', #258105, #193670, #169817, .T. ) ;
#231636=ADVANCED_FACE ( 'NONE', ( #210878 ), #252556, .T. ) ;
#231637=DIRECTION ( 'NONE',  ( 1.000000000000000000, 0.000000000000000000, 0.000000000000000000 ) ) ;
#231646=FACE_OUTER_BOUND ( 'NONE', #185796, .T. ) ;
#231648=ADVANCED_FACE ( 'NONE', ( #158634 ), #115991, .T. ) ;
#231651=EDGE_LOOP ( 'NONE', ( #161960, #79308, #134521, #196222 ) ) ;
#231652=CARTESIAN_POINT ( 'NONE',  ( -18.59999999999999787, 11.65000000001115232, -88.75000000000004263 ) ) ;
#231657=CIRCLE ( 'NONE', #160920, 0.09999999999999939493 ) ;
#231664=VECTOR ( 'NONE', #250345, 1000.000000000000114 ) ;
#231696=AXIS2_PLACEMENT_3D ( 'NONE', #127695, #65134, #66432 ) ;
#231724=ORIENTED_EDGE ( 'NONE', *, *, #127447, .F. ) ;
#231734=CARTESIAN_POINT ( 'NONE',  ( 18.49999999999999645, 1.736257131608553550, -112.0686523290175245 ) ) ;
#231773=AXIS2_PLACEMENT_3D ( 'NONE', #91670, #171263, #152970 ) ;
#231784=STYLED_ITEM ( 'NONE', ( #75431 ), #189505 ) ;
#231788=DIRECTION ( 'NONE',  ( 0.000000000000000000, 0.000000000000000000, -1.000000000000000000 ) ) ;
#231842=AXIS2_PLACEMENT_3D ( 'NONE', #133310, #149034, #246818 ) ;
#231847=DIRECTION ( 'NONE',  ( 0.000000000000000000, 0.000000000000000000, 1.000000000000000000 ) ) ;
#231860=EDGE_CURVE ( 'NONE', #110815, #132129, #70217, .T. ) ;
#231893=DIRECTION ( 'NONE',  ( -1.000000000000000000, -2.952720810173289112E-16, 0.000000000000000000 ) ) ;
#231950=EDGE_LOOP ( 'NONE', ( #72141, #13922, #181017, #111681 ) ) ;
#231968=ORIENTED_EDGE ( 'NONE', *, *, #250852, .T. ) ;
#231975=VERTEX_POINT ( 'NONE', #254484 ) ;
#231996=VECTOR ( 'NONE', #23045, 1000.000000000000227 ) ;
#231999=ORIENTED_EDGE ( 'NONE', *, *, #8252, .F. ) ;
#232023=CARTESIAN_POINT ( 'NONE',  ( -20.94999999999999929, 1.835341550235567887, -112.0551512925630249 ) ) ;
#232024=DIRECTION ( 'NONE',  ( 1.000000000000000000, -0.000000000000000000, -0.000000000000000000 ) ) ;
#232065=FACE_OUTER_BOUND ( 'NONE', #197402, .T. ) ;
#232083=CARTESIAN_POINT ( 'NONE',  ( 18.60000000000000142, -9.480686695267809938, -140.9411151687578752 ) ) ;
#232102=DIRECTION ( 'NONE',  ( 0.000000000000000000, -0.1350103645451876666, -0.9908441862701600211 ) ) ;
#232111=FACE_OUTER_BOUND ( 'NONE', #155367, .T. ) ;
#232124=DIRECTION ( 'NONE',  ( 0.000000000000000000, 0.000000000000000000, 1.000000000000000000 ) ) ;
#232157=VERTEX_POINT ( 'NONE', #161863 ) ;
#232174=AXIS2_PLACEMENT_3D ( 'NONE', #224460, #83633, #223174 ) ;
#232181=EDGE_CURVE ( 'NONE', #76942, #64097, #61996, .T. ) ;
#232187=CIRCLE ( 'NONE', #94786, 0.09999999999999892308 ) ;
#232207=EDGE_CURVE ( 'NONE', #98538, #24198, #24605, .T. ) ;
#232232=DIRECTION ( 'NONE',  ( 0.000000000000000000, 1.734723475976997999E-14, -1.000000000000000000 ) ) ;
#232233=FACE_OUTER_BOUND ( 'NONE', #56938, .T. ) ;
#232252=ORIENTED_EDGE ( 'NONE', *, *, #162049, .T. ) ;
#232264=ADVANCED_FACE ( 'NONE', ( #88690 ), #168305, .F. ) ;
#232293=EDGE_CURVE ( 'NONE', #156135, #234219, #71743, .T. ) ;
#232321=CIRCLE ( 'NONE', #65698, 11.65000000000000036 ) ;
#232337=EDGE_CURVE ( 'NONE', #85468, #153726, #91219, .T. ) ;
#232339=AXIS2_PLACEMENT_3D ( 'NONE', #42825, #67511, #106617 ) ;
#232341=CIRCLE ( 'NONE', #178172, 0.1000000000000028644 ) ;
#232382=EDGE_CURVE ( 'NONE', #20260, #10689, #152581, .T. ) ;
#232387=DIRECTION ( 'NONE',  ( 1.000000000000000000, 0.000000000000000000, 0.000000000000000000 ) ) ;
#232389=DIRECTION ( 'NONE',  ( 1.000000000000000000, 0.000000000000000000, 0.000000000000000000 ) ) ;
#232446=ORIENTED_EDGE ( 'NONE', *, *, #229863, .T. ) ;
#232448=EDGE_CURVE ( 'NONE', #64218, #125538, #174655, .T. ) ;
#232479=DIRECTION ( 'NONE',  ( 1.000000000000000000, 0.000000000000000000, -0.000000000000000000 ) ) ;
#232510=DIRECTION ( 'NONE',  ( 0.000000000000000000, -1.000000000000000000, 0.000000000000000000 ) ) ;
#232519=CARTESIAN_POINT ( 'NONE',  ( 23.15000000000000213, -8.596261682231828516, -124.5498724828497501 ) ) ;
#232524=EDGE_LOOP ( 'NONE', ( #59242, #7489, #160095, #128075 ) ) ;
#232534=VECTOR ( 'NONE', #200901, 1000.000000000000000 ) ;
#232588=AXIS2_PLACEMENT_3D ( 'NONE', #11690, #220775, #185176 ) ;
#232595=DIRECTION ( 'NONE',  ( -1.000000000000000000, 0.000000000000000000, 0.000000000000000000 ) ) ;
#232618=EDGE_CURVE ( 'NONE', #188307, #154382, #124540, .T. ) ;
#232619=AXIS2_PLACEMENT_3D ( 'NONE', #36586, #170975, #136927 ) ;
#232635=AXIS2_PLACEMENT_3D ( 'NONE', #10473, #153883, #150003 ) ;
#232641=ORIENTED_EDGE ( 'NONE', *, *, #119823, .F. ) ;
#232642=CARTESIAN_POINT ( 'NONE',  ( -21.05000000000000071, -1.162701749926853712, -108.5000000000000426 ) ) ;
#232674=AXIS2_PLACEMENT_3D ( 'NONE', #96594, #256929, #78330 ) ;
#232679=CARTESIAN_POINT ( 'NONE',  ( -22.39999999999999858, -0.1008583690875579364, -88.75043287651064361 ) ) ;
#232692=CARTESIAN_POINT ( 'NONE',  ( 18.50000000000000000, -9.399999999988843058, -107.7972597596633193 ) ) ;
#232703=ADVANCED_FACE ( 'NONE', ( #178245 ), #236900, .F. ) ;
#232706=ADVANCED_FACE ( 'NONE', ( #135219 ), #156118, .F. ) ;
#232724=AXIS2_PLACEMENT_3D ( 'NONE', #75639, #255483, #177319 ) ;
#232738=DIRECTION ( 'NONE',  ( 0.000000000000000000, 1.000000000000000000, -6.308085367188393199E-16 ) ) ;
#232821=DIRECTION ( 'NONE',  ( 0.000000000000000000, -0.000000000000000000, 1.000000000000000000 ) ) ;
#232827=CARTESIAN_POINT ( 'NONE',  ( 18.59999999999999432, -1.835859311432484375, -145.5044391687985694 ) ) ;
#232872=ORIENTED_EDGE ( 'NONE', *, *, #172152, .F. ) ;
#232893=DIRECTION ( 'NONE',  ( 0.000000000000000000, 0.000000000000000000, -1.000000000000000000 ) ) ;
#232898=FACE_OUTER_BOUND ( 'NONE', #115838, .T. ) ;
#232899=CARTESIAN_POINT ( 'NONE',  ( 21.05000000000000071, 8.876614585098254295, -108.8850804788447135 ) ) ;
#232908=VERTEX_POINT ( 'NONE', #54098 ) ;
#232911=CARTESIAN_POINT ( 'NONE',  ( 21.14999999999999503, -11.64999999998883595, -103.4000000000000341 ) ) ;
#232920=TOROIDAL_SURFACE ( 'NONE', #20534, 0.2000000000000000111, 0.1000000000000000056 ) ;
#232950=ORIENTED_EDGE ( 'NONE', *, *, #172704, .F. ) ;
#232977=AXIS2_PLACEMENT_3D ( 'NONE', #137557, #95864, #21505 ) ;
#233001=DIRECTION ( 'NONE',  ( -1.000000000000000000, -0.000000000000000000, -0.000000000000000000 ) ) ;
#233010=ORIENTED_EDGE ( 'NONE', *, *, #108857, .T. ) ;
#233030=PLANE ( 'NONE',  #250067 ) ;
#233033=EDGE_CURVE ( 'NONE', #201736, #240390, #249800, .T. ) ;
#233034=DIRECTION ( 'NONE',  ( -1.000000000000000000, 0.000000000000000000, 0.000000000000000000 ) ) ;
#233058=VECTOR ( 'NONE', #76233, 1000.000000000000000 ) ;
#233130=CARTESIAN_POINT ( 'NONE',  ( 18.59999999999999076, 11.65000000001115943, -125.2500000000000284 ) ) ;
#233163=DIRECTION ( 'NONE',  ( 1.000000000000000000, 0.000000000000000000, 0.000000000000000000 ) ) ;
#233169=CARTESIAN_POINT ( 'NONE',  ( 20.95576188350343116, 10.60898054497455512, -108.1112337227543350 ) ) ;
#233172=EDGE_CURVE ( 'NONE', #110428, #37339, #195844, .T. ) ;
#233173=DIRECTION ( 'NONE',  ( 0.000000000000000000, 0.000000000000000000, 1.000000000000000000 ) ) ;
#233198=CIRCLE ( 'NONE', #120768, 0.09999999999998898659 ) ;
#233201=VERTEX_POINT ( 'NONE', #164769 ) ;
#233221=LINE ( 'NONE', #110679, #8208 ) ;
#233256=ADVANCED_FACE ( 'NONE', ( #181763 ), #3096, .T. ) ;
#233270=CARTESIAN_POINT ( 'NONE',  ( 20.85000000000000142, 1.115600667400684642E-11, -134.0000000000000284 ) ) ;
#233285=CARTESIAN_POINT ( 'NONE',  ( -20.64999999999999858, -8.730841121484170131, -124.4019252810157070 ) ) ;
#233314=FACE_OUTER_BOUND ( 'NONE', #44401, .T. ) ;
#233320=VERTEX_POINT ( 'NONE', #188186 ) ;
#233327=ORIENTED_EDGE ( 'NONE', *, *, #88027, .F. ) ;
#233330=B_SPLINE_CURVE_WITH_KNOTS ( 'NONE', 3,
 ( #14762, #176395, #18589, #255858, #73452, #133402, #117679, #177687, #257137, #212935, #16043, #78541, #218039, #55105, #193389, #158141, #237637, #233792, #175142 ),
 .UNSPECIFIED., .F., .F.,
 ( 4, 3, 3, 3, 3, 3, 4 ),
 ( 0.000000000000000000, 2.646747978908405501E-05, 5.271166642128941309E-05, 9.008788829885368374E-05, 0.0001426648776561097631, 0.0001897378458659760203, 0.0001917382627806482609 ),
 .UNSPECIFIED. ) ;
#233337=EDGE_LOOP ( 'NONE', ( #39576, #256514, #200602, #199319 ) ) ;
#233450=EDGE_LOOP ( 'NONE', ( #103317, #212121, #254144, #52152, #101067, #159507, #235098, #129374, #2137, #126813, #200061, #200843, #9434, #70421, #181959, #238791, #192588, #130013, #61347, #124305, #37306, #87377, #92435 ) ) ;
#233500=B_SPLINE_CURVE_WITH_KNOTS ( 'NONE', 3,
 ( #48811, #68390, #146609, #86626, #247004, #127072, #168814, #204031 ),
 .UNSPECIFIED., .F., .F.,
 ( 4, 2, 2, 4 ),
 ( 0.000000000000000000, 6.534141206311986901E-05, 0.0001306828241262397380, 0.0002613656482524943296 ),
 .UNSPECIFIED. ) ;
#233513=AXIS2_PLACEMENT_3D ( 'NONE', #57138, #137966, #97540 ) ;
#233529=CARTESIAN_POINT ( 'NONE',  ( -20.00857864376270001, 9.350000000011156942, -112.7500000000000284 ) ) ;
#233563=ORIENTED_EDGE ( 'NONE', *, *, #32961, .T. ) ;
#233569=DIRECTION ( 'NONE',  ( -0.7071067811865474617, -0.7071067811865474617, -0.000000000000000000 ) ) ;
#233572=ORIENTED_EDGE ( 'NONE', *, *, #22381, .T. ) ;
#233585=DIRECTION ( 'NONE',  ( -1.000000000000000000, -0.000000000000000000, -0.000000000000000000 ) ) ;
#233591=CARTESIAN_POINT ( 'NONE',  ( 18.52130828395272033, -9.481395502614633486, -107.5245067238836612 ) ) ;
#233594=ORIENTED_EDGE ( 'NONE', *, *, #13262, .T. ) ;
#233611=TOROIDAL_SURFACE ( 'NONE', #142014, 12.97499999999999787, 0.1000000000000000056 ) ;
#233616=EDGE_CURVE ( 'NONE', #159674, #234753, #222814, .T. ) ;
#233627=ORIENTED_EDGE ( 'NONE', *, *, #93148, .T. ) ;
#233661=CYLINDRICAL_SURFACE ( 'NONE', #102101, 0.09999999999999939493 ) ;
#233662=DIRECTION ( 'NONE',  ( 0.000000000000000000, 1.000000000000000000, 0.000000000000000000 ) ) ;
#233717=FACE_OUTER_BOUND ( 'NONE', #117542, .T. ) ;
#233732=ORIENTED_EDGE ( 'NONE', *, *, #63015, .T. ) ;
#233774=ORIENTED_EDGE ( 'NONE', *, *, #114615, .F. ) ;
#233777=ORIENTED_EDGE ( 'NONE', *, *, #42101, .F. ) ;
#233792=CARTESIAN_POINT ( 'NONE',  ( -18.50000000000000000, 10.29288807859935950, -139.4580020160122160 ) ) ;
#233810=CARTESIAN_POINT ( 'NONE',  ( -21.14999999999999858, 11.75000000001115552, -107.2838656629781866 ) ) ;
#233821=DIRECTION ( 'NONE',  ( 1.000000000000000000, -0.000000000000000000, -0.000000000000000000 ) ) ;
#233822=CARTESIAN_POINT ( 'NONE',  ( -23.25000000000000000, -1.736705739456431807, -145.5174225876237699 ) ) ;
#233826=CIRCLE ( 'NONE', #29834, 0.09999999999998898659 ) ;
#233833=DIRECTION ( 'NONE',  ( 0.000000000000000000, 0.6728971962616697722, 0.7397360091702875895 ) ) ;
#233844=EDGE_CURVE ( 'NONE', #253865, #114232, #212582, .T. ) ;
#233853=FACE_OUTER_BOUND ( 'NONE', #133240, .T. ) ;
#233857=LINE ( 'NONE', #117751, #124053 ) ;
#233862=CARTESIAN_POINT ( 'NONE',  ( 23.14999999999999858, 5.000000000011153745, -121.5947339810869465 ) ) ;
#233868=CARTESIAN_POINT ( 'NONE',  ( -23.15000000000000213, 1.925233644870967487, -121.2697564668739005 ) ) ;
#233876=CARTESIAN_POINT ( 'NONE',  ( -20.85000000000000142, -0.3238857010591806307, -133.9575895893140398 ) ) ;
#233919=ORIENTED_EDGE ( 'NONE', *, *, #93731, .T. ) ;
#233925=EDGE_CURVE ( 'NONE', #253865, #196016, #37989, .T. ) ;
#233955=EDGE_CURVE ( 'NONE', #104735, #175552, #222491, .T. ) ;
#233977=DIRECTION ( 'NONE',  ( 0.000000000000000000, 0.9908441862701596881, 0.1350103645451904977 ) ) ;
#234060=CARTESIAN_POINT ( 'NONE',  ( 21.05000000000000071, -0.09999999998884512298, -94.02295361821016684 ) ) ;
#234122=CIRCLE ( 'NONE', #121723, 0.3999999999999975797 ) ;
#234139=CARTESIAN_POINT ( 'NONE',  ( 18.59999999999999076, 6.450000000011156587, -121.6500000000000341 ) ) ;
#234146=LINE ( 'NONE', #215852, #149940 ) ;
#234179=CARTESIAN_POINT ( 'NONE',  ( 21.05000000000000071, 6.450000000011156587, -110.5170271704400591 ) ) ;
#234200=FACE_OUTER_BOUND ( 'NONE', #38721, .T. ) ;
#234219=VERTEX_POINT ( 'NONE', #158421 ) ;
#234264=AXIS2_PLACEMENT_3D ( 'NONE', #183544, #140544, #180977 ) ;
#234265=DIRECTION ( 'NONE',  ( -0.000000000000000000, 0.000000000000000000, 1.000000000000000000 ) ) ;
#234274=LINE ( 'NONE', #231734, #22112 ) ;
#234280=CARTESIAN_POINT ( 'NONE',  ( 20.94999999999999929, -8.999999999988842703, -124.1060308773475924 ) ) ;
#234287=ORIENTED_EDGE ( 'NONE', *, *, #99677, .F. ) ;
#234297=LINE ( 'NONE', #217288, #226637 ) ;
#234299=DIRECTION ( 'NONE',  ( 0.7071067811865475727, 0.7071067811865475727, -0.000000000000000000 ) ) ;
#234300=VECTOR ( 'NONE', #18386, 1000.000000000000000 ) ;
#234319=CIRCLE ( 'NONE', #71859, 0.09999999999998898659 ) ;
#234325=DIRECTION ( 'NONE',  ( 0.000000000000000000, -1.000000000000000000, 0.000000000000000000 ) ) ;
#234329=CARTESIAN_POINT ( 'NONE',  ( -20.54999999999999716, 2.000000000011154189, -113.7246219227621395 ) ) ;
#234331=ORIENTED_EDGE ( 'NONE', *, *, #192191, .F. ) ;
#234374=ORIENTED_EDGE ( 'NONE', *, *, #54909, .F. ) ;
#234377=DIRECTION ( 'NONE',  ( -1.000000000000000000, 0.000000000000000000, 0.000000000000000000 ) ) ;
#234388=PLANE ( 'NONE',  #130622 ) ;
#234391=ORIENTED_EDGE ( 'NONE', *, *, #9014, .T. ) ;
#234399=ORIENTED_EDGE ( 'NONE', *, *, #114055, .F. ) ;
#234407=DIRECTION ( 'NONE',  ( 0.000000000000000000, -1.000000000000000000, 0.000000000000000000 ) ) ;
#234413=CARTESIAN_POINT ( 'NONE',  ( 20.95539060131842746, 10.62386215766680131, -108.1537338136562312 ) ) ;
#234423=DIRECTION ( 'NONE',  ( 1.000000000000000000, -0.000000000000000000, -0.000000000000000000 ) ) ;
#234487=AXIS2_PLACEMENT_3D ( 'NONE', #115524, #77665, #257547 ) ;
#234509=AXIS2_PLACEMENT_3D ( 'NONE', #92117, #115530, #76389 ) ;
#234511=AXIS2_PLACEMENT_3D ( 'NONE', #177191, #36390, #156344 ) ;
#234544=FACE_BOUND ( 'NONE', #243286, .T. ) ;
#234550=AXIS2_PLACEMENT_3D ( 'NONE', #95247, #78242, #157837 ) ;
#234552=VERTEX_POINT ( 'NONE', #199508 ) ;
#234556=CARTESIAN_POINT ( 'NONE',  ( -18.59999999999999787, 9.150000000011157653, -121.6500000000000341 ) ) ;
#234563=DIRECTION ( 'NONE',  ( 0.000000000000000000, 0.000000000000000000, -1.000000000000000000 ) ) ;
#234565=DIRECTION ( 'NONE',  ( 0.000000000000000000, 0.000000000000000000, -1.000000000000000000 ) ) ;
#234572=VERTEX_POINT ( 'NONE', #8986 ) ;
#234597=ORIENTED_EDGE ( 'NONE', *, *, #179863, .T. ) ;
#234624=EDGE_CURVE ( 'NONE', #212285, #173670, #79819, .T. ) ;
#234629=DIRECTION ( 'NONE',  ( 0.000000000000000000, -1.000000000000000000, -0.000000000000000000 ) ) ;
#234648=CARTESIAN_POINT ( 'NONE',  ( -18.50000000000000355, -9.419203418015493767, -107.7477858104286952 ) ) ;
#234652=VERTEX_POINT ( 'NONE', #144631 ) ;
#234665=AXIS2_PLACEMENT_3D ( 'NONE', #149233, #48818, #90503 ) ;
#234733=DIRECTION ( 'NONE',  ( 0.000000000000000000, 0.000000000000000000, 1.000000000000000000 ) ) ;
#234748=DIRECTION ( 'NONE',  ( 1.000000000000000000, 0.000000000000000000, 0.000000000000000000 ) ) ;
#234753=VERTEX_POINT ( 'NONE', #38510 ) ;
#234754=ORIENTED_EDGE ( 'NONE', *, *, #69519, .T. ) ;
#234771=AXIS2_PLACEMENT_3D ( 'NONE', #55326, #133609, #150618 ) ;
#234793=EDGE_CURVE ( 'NONE', #104735, #131734, #71099, .T. ) ;
#234814=EDGE_CURVE ( 'NONE', #128969, #138064, #38340, .T. ) ;
#234832=CYLINDRICAL_SURFACE ( 'NONE', #136000, 0.09999999999998898659 ) ;
#234876=ADVANCED_FACE ( 'NONE', ( #78882 ), #200149, .T. ) ;
#234877=ORIENTED_EDGE ( 'NONE', *, *, #198020, .F. ) ;
#234890=ORIENTED_EDGE ( 'NONE', *, *, #170152, .T. ) ;
#234898=DIRECTION ( 'NONE',  ( 1.000000000000000000, 0.000000000000000000, -0.000000000000000000 ) ) ;
#234924=EDGE_LOOP ( 'NONE', ( #72969, #233010, #63846, #36424 ) ) ;
#234941=CARTESIAN_POINT ( 'NONE',  ( 20.85000000000000142, -11.64999999998883595, -134.0000000000000284 ) ) ;
#234960=CARTESIAN_POINT ( 'NONE',  ( -21.12757541349819590, 0.005161215820883788274, -94.02661942874847512 ) ) ;
#234981=DIRECTION ( 'NONE',  ( -0.000000000000000000, -1.000000000000000000, 0.000000000000000000 ) ) ;
#235011=VERTEX_POINT ( 'NONE', #166192 ) ;
#235092=DIRECTION ( 'NONE',  ( 0.000000000000000000, 0.000000000000000000, -1.000000000000000000 ) ) ;
#235098=ORIENTED_EDGE ( 'NONE', *, *, #92860, .F. ) ;
#235119=AXIS2_PLACEMENT_3D ( 'NONE', #101984, #62888, #223233 ) ;
#235135=DIRECTION ( 'NONE',  ( 0.000000000000000000, 0.000000000000000000, 1.000000000000000000 ) ) ;
#235161=AXIS2_PLACEMENT_3D ( 'NONE', #251190, #54280, #95969 ) ;
#235162=AXIS2_PLACEMENT_3D ( 'NONE', #175818, #58382, #57102 ) ;
#235163=ORIENTED_EDGE ( 'NONE', *, *, #115390, .T. ) ;
#235165=CARTESIAN_POINT ( 'NONE',  ( 20.85000000000000142, 11.65000000001115943, -134.0000000000000284 ) ) ;
#235188=EDGE_CURVE ( 'NONE', #215339, #204523, #75394, .T. ) ;
#235205=ORIENTED_EDGE ( 'NONE', *, *, #30844, .F. ) ;
#235220=AXIS2_PLACEMENT_3D ( 'NONE', #165808, #60253, #122824 ) ;
#235238=FACE_OUTER_BOUND ( 'NONE', #204513, .T. ) ;
#235239=ADVANCED_FACE ( 'NONE', ( #78598 ), #60319, .T. ) ;
#235244=CARTESIAN_POINT ( 'NONE',  ( -20.64999999999999858, 1.115600667400684642E-11, -134.0000000000000284 ) ) ;
#235260=ORIENTED_EDGE ( 'NONE', *, *, #92308, .F. ) ;
#235314=AXIS2_PLACEMENT_3D ( 'NONE', #34483, #108842, #93129 ) ;
#235342=ORIENTED_EDGE ( 'NONE', *, *, #133988, .T. ) ;
#235357=EDGE_CURVE ( 'NONE', #223382, #133593, #181579, .T. ) ;
#235383=SPHERICAL_SURFACE ( 'NONE', #232977, 0.1000000000000000056 ) ;
#235441=ADVANCED_FACE ( 'NONE', ( #126723 ), #207559, .T. ) ;
#235468=DIRECTION ( 'NONE',  ( -0.000000000000000000, 3.469446951953635015E-14, 1.000000000000000000 ) ) ;
#235483=CARTESIAN_POINT ( 'NONE',  ( -23.25000000000000000, 1.115600667400684642E-11, -134.0000000000000284 ) ) ;
#235499=AXIS2_PLACEMENT_3D ( 'NONE', #93107, #250892, #207951 ) ;
#235601=EDGE_CURVE ( 'NONE', #227912, #142813, #250508, .T. ) ;
#235608=DIRECTION ( 'NONE',  ( 0.000000000000000000, 1.897661533703519897E-16, -1.000000000000000000 ) ) ;
#235645=CIRCLE ( 'NONE', #23495, 0.1000000000000001860 ) ;
#235646=ORIENTED_EDGE ( 'NONE', *, *, #255971, .F. ) ;
#235660=CARTESIAN_POINT ( 'NONE',  ( 20.94999999999999574, 1.162701749949165642, -108.6000000000000227 ) ) ;
#235661=CIRCLE ( 'NONE', #169072, 0.09999999999999939493 ) ;
#235668=DIRECTION ( 'NONE',  ( 2.952720810173289112E-16, -1.000000000000000000, 0.000000000000000000 ) ) ;
#235669=DIRECTION ( 'NONE',  ( -0.000000000000000000, -0.000000000000000000, -1.000000000000000000 ) ) ;
#235670=FACE_OUTER_BOUND ( 'NONE', #147204, .T. ) ;
#235684=EDGE_CURVE ( 'NONE', #162687, #46758, #205172, .T. ) ;
#235700=CARTESIAN_POINT ( 'NONE',  ( -20.85000000000000142, 1.115600667400684642E-11, -134.0000000000000284 ) ) ;
#235745=DIRECTION ( 'NONE',  ( 1.000000000000000000, 0.000000000000000000, 0.000000000000000000 ) ) ;
#235788=DIRECTION ( 'NONE',  ( 1.000000000000000000, 0.000000000000000000, 0.000000000000000000 ) ) ;
#235794=DIRECTION ( 'NONE',  ( 0.000000000000000000, 0.000000000000000000, -1.000000000000000000 ) ) ;
#235819=CARTESIAN_POINT ( 'NONE',  ( -21.52071067811865746, 7.779289321892505882, -121.6500000000000341 ) ) ;
#235826=AXIS2_PLACEMENT_3D ( 'NONE', #11187, #51554, #111570 ) ;
#235827=AXIS2_PLACEMENT_3D ( 'NONE', #113029, #233001, #157318 ) ;
#235843=DIRECTION ( 'NONE',  ( 1.000000000000000000, 7.304098846218133681E-16, -4.217023435051677501E-16 ) ) ;
#235867=DIRECTION ( 'NONE',  ( -4.336808689942053235E-15, -0.8660254037844482555, -0.4999999999999836797 ) ) ;
#235874=VECTOR ( 'NONE', #64883, 1000.000000000000000 ) ;
#235900=CARTESIAN_POINT ( 'NONE',  ( 18.59999999999999076, 1.750000000011155743, -112.1695115579016857 ) ) ;
#235912=ORIENTED_EDGE ( 'NONE', *, *, #116822, .T. ) ;
#235928=ORIENTED_EDGE ( 'NONE', *, *, #49886, .F. ) ;
#235931=AXIS2_PLACEMENT_3D ( 'NONE', #66676, #9261, #225715 ) ;
#235955=AXIS2_PLACEMENT_3D ( 'NONE', #211914, #176642, #56633 ) ;
#235966=CIRCLE ( 'NONE', #123547, 11.64999999999999325 ) ;
#235985=EDGE_CURVE ( 'NONE', #58778, #213938, #80797, .T. ) ;
#236002=DIRECTION ( 'NONE',  ( 0.000000000000000000, -1.000000000000000000, 0.000000000000000000 ) ) ;
#236016=DIRECTION ( 'NONE',  ( 0.000000000000000000, 0.000000000000000000, 1.000000000000000000 ) ) ;
#236042=TOROIDAL_SURFACE ( 'NONE', #127907, 0.2000000000000000111, 0.1000000000000000056 ) ;
#236111=DIRECTION ( 'NONE',  ( 0.000000000000000000, 0.000000000000000000, -1.000000000000000000 ) ) ;
#236148=EDGE_LOOP ( 'NONE', ( #201293, #28956, #177750, #110730 ) ) ;
#236174=PLANE ( 'NONE',  #61812 ) ;
#236179=AXIS2_PLACEMENT_3D ( 'NONE', #151595, #152887, #172458 ) ;
#236192=ORIENTED_EDGE ( 'NONE', *, *, #194864, .F. ) ;
#236194=AXIS2_PLACEMENT_3D ( 'NONE', #89144, #124438, #47437 ) ;
#236202=ORIENTED_EDGE ( 'NONE', *, *, #23322, .T. ) ;
#236208=DIRECTION ( 'NONE',  ( -1.000000000000000000, 0.000000000000000000, 0.000000000000000000 ) ) ;
#236228=EDGE_LOOP ( 'NONE', ( #218806, #110268, #158580 ) ) ;
#236232=CARTESIAN_POINT ( 'NONE',  ( -23.25000000000000000, -9.599999999988847676, -110.3939691226524786 ) ) ;
#236237=DIRECTION ( 'NONE',  ( 1.000000000000000000, -0.000000000000000000, -0.000000000000000000 ) ) ;
#236241=DIRECTION ( 'NONE',  ( 1.000000000000000000, -0.000000000000000000, -0.000000000000000000 ) ) ;
#236244=VECTOR ( 'NONE', #44559, 1000.000000000000000 ) ;
#236262=FACE_BOUND ( 'NONE', #150064, .T. ) ;
#236279=AXIS2_PLACEMENT_3D ( 'NONE', #42542, #176962, #195241 ) ;
#236281=EDGE_LOOP ( 'NONE', ( #231968, #150250, #238809, #255959, #97376 ) ) ;
#236339=LINE ( 'NONE', #163236, #41508 ) ;
#236351=VECTOR ( 'NONE', #203958, 1000.000000000000000 ) ;
#236357=CARTESIAN_POINT ( 'NONE',  ( -23.25000000000000000, 1.115600667400684642E-11, -104.5500000000000256 ) ) ;
#236394=DIRECTION ( 'NONE',  ( 0.000000000000000000, 0.000000000000000000, -1.000000000000000000 ) ) ;
#236424=VERTEX_POINT ( 'NONE', #16444 ) ;
#236564=EDGE_LOOP ( 'NONE', ( #170220, #93956, #73789, #194305 ) ) ;
#236568=ORIENTED_EDGE ( 'NONE', *, *, #115834, .F. ) ;
#236592=LINE ( 'NONE', #193637, #3295 ) ;
#236594=ADVANCED_FACE ( 'NONE', ( #71934 ), #130880, .F. ) ;
#236613=CARTESIAN_POINT ( 'NONE',  ( -20.15000000000000568, 9.291421356248463326, -112.7500000000000284 ) ) ;
#236642=CARTESIAN_POINT ( 'NONE',  ( -22.60000000000080789, 0.04781698047652398198, -88.74997756884729938 ) ) ;
#236657=DIRECTION ( 'NONE',  ( -1.000000000000000000, -1.836970198721029934E-16, -3.186635328391151676E-31 ) ) ;
#236663=ORIENTED_EDGE ( 'NONE', *, *, #203900, .T. ) ;
#236666=CARTESIAN_POINT ( 'NONE',  ( 21.05000000000000071, -8.999999999988842703, -124.6060308773475924 ) ) ;
#236680=CARTESIAN_POINT ( 'NONE',  ( -20.64999999999999858, 1.115600667400684642E-11, -134.0000000000000284 ) ) ;
#236688=ORIENTED_EDGE ( 'NONE', *, *, #82280, .T. ) ;
#236700=CARTESIAN_POINT ( 'NONE',  ( 21.05000000000000071, 8.776282895303632259, -100.5000000000000284 ) ) ;
#236742=ORIENTED_EDGE ( 'NONE', *, *, #66022, .T. ) ;
#236771=CARTESIAN_POINT ( 'NONE',  ( 21.87500000000000355, 9.750000000011153745, -121.7500000000000426 ) ) ;
#236773=CARTESIAN_POINT ( 'NONE',  ( 18.54148534481893407, 10.32532329027886675, -139.5699343018359855 ) ) ;
#236794=DIRECTION ( 'NONE',  ( 0.000000000000000000, 0.000000000000000000, -1.000000000000000000 ) ) ;
#236815=CARTESIAN_POINT ( 'NONE',  ( -21.05000000000000071, -11.74999999998884448, -131.1000000000000227 ) ) ;
#236850=FACE_OUTER_BOUND ( 'NONE', #80312, .T. ) ;
#236860=CARTESIAN_POINT ( 'NONE',  ( -20.94999999999999929, 1.162701749949165642, -108.6000000000000227 ) ) ;
#236872=ORIENTED_EDGE ( 'NONE', *, *, #96712, .T. ) ;
#236884=AXIS2_PLACEMENT_3D ( 'NONE', #17427, #213054, #74875 ) ;
#236896=CYLINDRICAL_SURFACE ( 'NONE', #28373, 0.09999999999999804878 ) ;
#236898=LINE ( 'NONE', #118241, #65589 ) ;
#236900=CYLINDRICAL_SURFACE ( 'NONE', #12131, 0.1000000000000028644 ) ;
#236911=DIRECTION ( 'NONE',  ( 1.000000000000000000, -0.000000000000000000, -0.000000000000000000 ) ) ;
#236931=VERTEX_POINT ( 'NONE', #149892 ) ;
#236941=CIRCLE ( 'NONE', #178722, 0.09999999999999749367 ) ;
#236953=TOROIDAL_SURFACE ( 'NONE', #112063, 0.2000000000000000111, 0.1000000000000000056 ) ;
#236995=CYLINDRICAL_SURFACE ( 'NONE', #256920, 4.000000000000003553 ) ;
#237016=CARTESIAN_POINT ( 'NONE',  ( -21.55000000000000426, 7.750000000011159074, -121.7500000000000426 ) ) ;
#237021=FACE_OUTER_BOUND ( 'NONE', #152132, .T. ) ;
#237034=LINE ( 'NONE', #238303, #12468 ) ;
#237043=CYLINDRICAL_SURFACE ( 'NONE', #169462, 11.75000000000001066 ) ;
#237067=DIRECTION ( 'NONE',  ( 0.000000000000000000, 0.000000000000000000, 1.000000000000000000 ) ) ;
#237072=EDGE_LOOP ( 'NONE', ( #81252, #190716, #18027, #42002, #2142 ) ) ;
#237086=DIRECTION ( 'NONE',  ( 1.000000000000000000, 0.000000000000000000, -0.000000000000000000 ) ) ;
#237087=ORIENTED_EDGE ( 'NONE', *, *, #61700, .T. ) ;
#237090=ADVANCED_FACE ( 'NONE', ( #135426 ), #168894, .T. ) ;
#237118=CARTESIAN_POINT ( 'NONE',  ( -20.05000000000000426, 9.250000000011157297, -112.8500000000000369 ) ) ;
#237120=DIRECTION ( 'NONE',  ( 1.000000000000000000, 0.000000000000000000, 0.000000000000000000 ) ) ;
#237129=CARTESIAN_POINT ( 'NONE',  ( -21.14999999999999858, 1.115600667400684642E-11, -100.5000000000000284 ) ) ;
#237153=CARTESIAN_POINT ( 'NONE',  ( 18.59999999999999787, -1.851028230129704522, -112.1539132694225316 ) ) ;
#237162=DIRECTION ( 'NONE',  ( -6.938893903907222856E-15, 1.000000000000000000, 0.000000000000000000 ) ) ;
#237167=DIRECTION ( 'NONE',  ( 0.000000000000000000, -1.000000000000000000, 0.000000000000000000 ) ) ;
#237171=ORIENTED_EDGE ( 'NONE', *, *, #167549, .F. ) ;
#237172=DIRECTION ( 'NONE',  ( 0.000000000000000000, 0.4999999999999949485, -0.8660254037844415942 ) ) ;
#237207=DIRECTION ( 'NONE',  ( 0.000000000000000000, 0.000000000000000000, 1.000000000000000000 ) ) ;
#237211=CARTESIAN_POINT ( 'NONE',  ( -23.15000000000000213, 1.115600667400684642E-11, -134.0000000000000284 ) ) ;
#237226=ORIENTED_EDGE ( 'NONE', *, *, #81045, .T. ) ;
#237249=FACE_OUTER_BOUND ( 'NONE', #183741, .T. ) ;
#237253=CIRCLE ( 'NONE', #54067, 11.75000000000000000 ) ;
#237276=CARTESIAN_POINT ( 'NONE',  ( -21.05000000000000071, 5.850000000011156942, -123.8675027757221159 ) ) ;
#237318=AXIS2_PLACEMENT_3D ( 'NONE', #190215, #191520, #192779 ) ;
#237330=ORIENTED_EDGE ( 'NONE', *, *, #145437, .F. ) ;
#237384=AXIS2_PLACEMENT_3D ( 'NONE', #15060, #94569, #192401 ) ;
#237392=VECTOR ( 'NONE', #158040, 1000.000000000000000 ) ;
#237402=EDGE_CURVE ( 'NONE', #74961, #256383, #186116, .T. ) ;
#237424=DIRECTION ( 'NONE',  ( 0.000000000000000000, 0.000000000000000000, -1.000000000000000000 ) ) ;
#237460=VERTEX_POINT ( 'NONE', #171720 ) ;
#237465=CARTESIAN_POINT ( 'NONE',  ( 18.59999999999999076, 10.25000000001115552, -125.2500000000000284 ) ) ;
#237471=CARTESIAN_POINT ( 'NONE',  ( 21.05000000000000071, 5.400000000011154988, -112.9052660189131245 ) ) ;
#237472=EDGE_CURVE ( 'NONE', #49667, #20965, #235661, .T. ) ;
#237478=ORIENTED_EDGE ( 'NONE', *, *, #174246, .T. ) ;
#237486=CARTESIAN_POINT ( 'NONE',  ( -21.05000000000000071, 1.115600667400684642E-11, -122.2000000000000313 ) ) ;
#237516=CARTESIAN_POINT ( 'NONE',  ( -21.05000000000000071, -1.162701749926853712, -108.5000000000000426 ) ) ;
#237566=EDGE_CURVE ( 'NONE', #241330, #46619, #77697, .T. ) ;
#237580=LINE ( 'NONE', #35552, #182507 ) ;
#237587=DIRECTION ( 'NONE',  ( 0.000000000000000000, 1.000000000000000000, 0.000000000000000000 ) ) ;
#237605=VERTEX_POINT ( 'NONE', #121984 ) ;
#237622=CARTESIAN_POINT ( 'NONE',  ( -20.94999999999999929, 11.60000000001115517, -127.0717967697245143 ) ) ;
#237628=DIRECTION ( 'NONE',  ( 0.000000000000000000, 0.000000000000000000, 1.000000000000000000 ) ) ;
#237637=CARTESIAN_POINT ( 'NONE',  ( -18.50000324121759121, 10.29307482169070198, -139.4586421466940749 ) ) ;
#237655=FACE_OUTER_BOUND ( 'NONE', #8715, .T. ) ;
#237667=CARTESIAN_POINT ( 'NONE',  ( 21.05000000000000071, 5.000000000011153745, -121.5947339810869465 ) ) ;
#237674=B_SPLINE_CURVE_WITH_KNOTS ( 'NONE', 3,
 ( #129717, #89294, #168888, #248384, #189695, #51431, #205381, #209248 ),
 .UNSPECIFIED., .F., .F.,
 ( 4, 2, 2, 4 ),
 ( 0.000000000000000000, 0.0001094981963948460927, 0.0002189963927896921853, 0.0004379927855793843707 ),
 .UNSPECIFIED. ) ;
#237722=VERTEX_POINT ( 'NONE', #47560 ) ;
#237744=EDGE_LOOP ( 'NONE', ( #79628, #7856, #161915, #142355 ) ) ;
#237771=AXIS2_PLACEMENT_3D ( 'NONE', #1000, #63571, #41477 ) ;
#237784=DIRECTION ( 'NONE',  ( 0.000000000000000000, -9.769962616701387022E-15, 1.000000000000000000 ) ) ;
#237825=AXIS2_PLACEMENT_3D ( 'NONE', #149110, #49988, #70871 ) ;
#237872=ADVANCED_FACE ( 'NONE', ( #129253 ), #107109, .F. ) ;
#237889=CARTESIAN_POINT ( 'NONE',  ( -18.50000000000000000, 9.250000000011157297, -121.6500000000000341 ) ) ;
#237895=CARTESIAN_POINT ( 'NONE',  ( 18.59999999999999076, 10.20857864377385127, -125.1500000000000341 ) ) ;
#237899=ORIENTED_EDGE ( 'NONE', *, *, #198648, .F. ) ;
#237921=EDGE_CURVE ( 'NONE', #104735, #221499, #210726, .T. ) ;
#237975=AXIS2_PLACEMENT_3D ( 'NONE', #217392, #98705, #59584 ) ;
#238001=LINE ( 'NONE', #59335, #95430 ) ;
#238064=VERTEX_POINT ( 'NONE', #254843 ) ;
#238069=DIRECTION ( 'NONE',  ( -1.000000000000000000, 0.000000000000000000, 0.000000000000000000 ) ) ;
#238115=AXIS2_PLACEMENT_3D ( 'NONE', #137864, #255205, #2204 ) ;
#238130=CARTESIAN_POINT ( 'NONE',  ( 19.87657994471988232, 11.75000000001116263, -125.2657881246251037 ) ) ;
#238176=EDGE_LOOP ( 'NONE', ( #32633, #141934, #217562 ) ) ;
#238196=DIRECTION ( 'NONE',  ( -0.000000000000000000, -0.7397360091702755991, -0.6728971962616832059 ) ) ;
#238215=EDGE_CURVE ( 'NONE', #143179, #62956, #163510, .T. ) ;
#238234=AXIS2_PLACEMENT_3D ( 'NONE', #163861, #102559, #222520 ) ;
#238237=VECTOR ( 'NONE', #138109, 1000.000000000000000 ) ;
#238279=ORIENTED_EDGE ( 'NONE', *, *, #213436, .F. ) ;
#238281=DIRECTION ( 'NONE',  ( 1.000000000000000000, -7.304098846218134667E-16, -4.217023435051626718E-16 ) ) ;
#238288=ORIENTED_EDGE ( 'NONE', *, *, #14823, .F. ) ;
#238289=AXIS2_PLACEMENT_3D ( 'NONE', #106815, #186384, #222913 ) ;
#238292=AXIS2_PLACEMENT_3D ( 'NONE', #39032, #58555, #178557 ) ;
#238303=CARTESIAN_POINT ( 'NONE',  ( -23.15000000000000213, 2.500000000011154633, -120.7753780772379457 ) ) ;
#238313=DIRECTION ( 'NONE',  ( -0.000000000000000000, 0.000000000000000000, 1.000000000000000000 ) ) ;
#238357=ORIENTED_EDGE ( 'NONE', *, *, #97431, .F. ) ;
#238362=DIRECTION ( 'NONE',  ( 0.000000000000000000, -0.8700118002898359348, 0.4930308989875165082 ) ) ;
#238368=ADVANCED_FACE ( 'NONE', ( #12163 ), #186950, .F. ) ;
#238371=ORIENTED_EDGE ( 'NONE', *, *, #13341, .T. ) ;
#238393=LINE ( 'NONE', #237118, #12743 ) ;
#238403=EDGE_CURVE ( 'NONE', #46937, #121101, #56160, .T. ) ;
#238422=DIRECTION ( 'NONE',  ( -1.000000000000000000, -0.000000000000000000, -0.000000000000000000 ) ) ;
#238428=VERTEX_POINT ( 'NONE', #194658 ) ;
#238459=VERTEX_POINT ( 'NONE', #261 ) ;
#238462=FACE_OUTER_BOUND ( 'NONE', #80636, .T. ) ;
#238477=CARTESIAN_POINT ( 'NONE',  ( -20.94999999999999929, -1.835341550213255957, -112.0551512925630249 ) ) ;
#238478=CARTESIAN_POINT ( 'NONE',  ( 18.57071067811864040, 10.17928932189250091, -121.8500000000000369 ) ) ;
#238479=DIRECTION ( 'NONE',  ( 0.000000000000000000, -1.000000000000000000, -0.000000000000000000 ) ) ;
#238505=CARTESIAN_POINT ( 'NONE',  ( -21.05000000000000071, -11.64999999998884306, -131.0000000000000284 ) ) ;
#238539=CARTESIAN_POINT ( 'NONE',  ( -21.95218792049438861, 0.09902843981107177507, -93.29849243875335674 ) ) ;
#238573=ORIENTED_EDGE ( 'NONE', *, *, #180316, .F. ) ;
#238574=DIRECTION ( 'NONE',  ( 0.000000000000000000, -1.000000000000000000, 0.000000000000000000 ) ) ;
#238583=CARTESIAN_POINT ( 'NONE',  ( -18.59999999999999787, -1.736257131586239844, -112.0686523290175245 ) ) ;
#238607=ORIENTED_EDGE ( 'NONE', *, *, #254801, .F. ) ;
#238620=ORIENTED_EDGE ( 'NONE', *, *, #21573, .T. ) ;
#238636=ORIENTED_EDGE ( 'NONE', *, *, #41371, .T. ) ;
#238665=EDGE_CURVE ( 'NONE', #55613, #107956, #105766, .T. ) ;
#238670=ORIENTED_EDGE ( 'NONE', *, *, #250205, .T. ) ;
#238678=CARTESIAN_POINT ( 'NONE',  ( -20.99142135623731065, 11.60000000001115161, -127.0717967697245570 ) ) ;
#238719=LINE ( 'NONE', #60069, #141678 ) ;
#238774=EDGE_CURVE ( 'NONE', #74786, #17092, #223729, .T. ) ;
#238775=VECTOR ( 'NONE', #48228, 1000.000000000000000 ) ;
#238779=VECTOR ( 'NONE', #184843, 1000.000000000000114 ) ;
#238785=ORIENTED_EDGE ( 'NONE', *, *, #237472, .T. ) ;
#238791=ORIENTED_EDGE ( 'NONE', *, *, #121370, .F. ) ;
#238809=ORIENTED_EDGE ( 'NONE', *, *, #171520, .F. ) ;
#238829=SPHERICAL_SURFACE ( 'NONE', #223307, 0.1000000000000000056 ) ;
#238832=DIRECTION ( 'NONE',  ( 1.000000000000000000, 7.304098846218133681E-16, -4.607487905232622991E-31 ) ) ;
#238857=FACE_OUTER_BOUND ( 'NONE', #125939, .T. ) ;
#238864=DIRECTION ( 'NONE',  ( 1.000000000000000000, -0.000000000000000000, -0.000000000000000000 ) ) ;
#238871=ORIENTED_EDGE ( 'NONE', *, *, #194495, .T. ) ;
#238874=CIRCLE ( 'NONE', #92929, 0.09999999999999939493 ) ;
#238884=EDGE_CURVE ( 'NONE', #34079, #194066, #153962, .T. ) ;
#238899=FACE_OUTER_BOUND ( 'NONE', #211184, .T. ) ;
#238913=CYLINDRICAL_SURFACE ( 'NONE', #222439, 0.09999999999999939493 ) ;
#238922=AXIS2_PLACEMENT_3D ( 'NONE', #223841, #166487, #45221 ) ;
#238924=DIRECTION ( 'NONE',  ( 0.000000000000000000, 0.000000000000000000, 1.000000000000000000 ) ) ;
#238944=AXIS2_PLACEMENT_3D ( 'NONE', #92341, #96179, #115762 ) ;
#238954=VERTEX_POINT ( 'NONE', #219006 ) ;
#238955=CIRCLE ( 'NONE', #109932, 0.1000000000000020595 ) ;
#238980=EDGE_CURVE ( 'NONE', #189217, #197646, #183748, .T. ) ;
#239012=EDGE_CURVE ( 'NONE', #120723, #208327, #123996, .T. ) ;
#239014=VERTEX_POINT ( 'NONE', #164191 ) ;
#239028=DIRECTION ( 'NONE',  ( 1.000000000000000000, 0.000000000000000000, 0.000000000000000000 ) ) ;
#239049=VERTEX_POINT ( 'NONE', #224141 ) ;
#239056=DIRECTION ( 'NONE',  ( 0.000000000000000000, -1.000000000000000000, 0.000000000000000000 ) ) ;
#239097=CARTESIAN_POINT ( 'NONE',  ( -20.94999999999999929, -1.849153571964891274, -145.6059666197970728 ) ) ;
#239100=CIRCLE ( 'NONE', #93335, 0.5000000000000004441 ) ;
#239101=DIRECTION ( 'NONE',  ( 0.000000000000000000, 0.000000000000000000, -1.000000000000000000 ) ) ;
#239145=CARTESIAN_POINT ( 'NONE',  ( 21.05000000000000426, 0.09843750001147434647, -94.20076908990776587 ) ) ;
#239146=CIRCLE ( 'NONE', #101736, 11.74999999999999645 ) ;
#239164=EDGE_CURVE ( 'NONE', #64377, #196043, #52724, .T. ) ;
#239167=DIRECTION ( 'NONE',  ( -1.000000000000000000, 0.000000000000000000, 0.000000000000000000 ) ) ;
#239200=CARTESIAN_POINT ( 'NONE',  ( 23.15000000000000213, -11.64999999998883595, -130.9000000000000341 ) ) ;
#239203=DIRECTION ( 'NONE',  ( 0.000000000000000000, 0.000000000000000000, -1.000000000000000000 ) ) ;
#239241=VECTOR ( 'NONE', #33684, 1000.000000000000227 ) ;
#239256=VERTEX_POINT ( 'NONE', #57032 ) ;
#239261=CARTESIAN_POINT ( 'NONE',  ( 22.59066674512249762, 11.75000000001115552, -100.4694958763694217 ) ) ;
#239262=EDGE_CURVE ( 'NONE', #223255, #156135, #69829, .T. ) ;
#239268=EDGE_CURVE ( 'NONE', #110564, #221229, #248890, .T. ) ;
#239270=PLANE ( 'NONE',  #43573 ) ;
#239274=EDGE_LOOP ( 'NONE', ( #188629, #178249, #187962, #104055 ) ) ;
#239319=ADVANCED_FACE ( 'NONE', ( #100007 ), #103866, .F. ) ;
#239347=DIRECTION ( 'NONE',  ( 0.000000000000000000, 0.000000000000000000, -1.000000000000000000 ) ) ;
#239384=DIRECTION ( 'NONE',  ( -0.000000000000000000, 0.8660254037844411501, 0.4999999999999956701 ) ) ;
#239392=CARTESIAN_POINT ( 'NONE',  ( 21.14999999999999858, -0.09999999998884338825, -88.85042919245522341 ) ) ;
#239413=EDGE_CURVE ( 'NONE', #239014, #8107, #224110, .T. ) ;
#239434=DIRECTION ( 'NONE',  ( 0.000000000000000000, -1.000000000000000000, 0.000000000000000000 ) ) ;
#239438=CARTESIAN_POINT ( 'NONE',  ( 19.96984138294323685, 11.75000000001116263, -125.2245720712022461 ) ) ;
#239440=DIRECTION ( 'NONE',  ( -1.000000000000000000, -0.000000000000000000, -0.000000000000000000 ) ) ;
#239481=DIRECTION ( 'NONE',  ( -0.000000000000000000, 1.000000000000000000, 1.734723475976807292E-15 ) ) ;
#239490=ORIENTED_EDGE ( 'NONE', *, *, #80191, .F. ) ;
#239492=DIRECTION ( 'NONE',  ( 0.000000000000000000, 0.1575844902526835067, 0.9875055080513738259 ) ) ;
#239498=CARTESIAN_POINT ( 'NONE',  ( -21.05000000000000071, 1.115653327213047955E-11, -96.20000000000007390 ) ) ;
#239546=EDGE_CURVE ( 'NONE', #177351, #90545, #61621, .T. ) ;
#239569=LINE ( 'NONE', #197860, #252089 ) ;
#239589=DIRECTION ( 'NONE',  ( 0.000000000000000000, 6.938893903907222067E-15, -1.000000000000000000 ) ) ;
#239598=ADVANCED_FACE ( 'NONE', ( #253353 ), #165702, .T. ) ;
#239640=DIRECTION ( 'NONE',  ( -0.000000000000000000, 0.000000000000000000, 1.000000000000000000 ) ) ;
#239657=VERTEX_POINT ( 'NONE', #233810 ) ;
#239674=CARTESIAN_POINT ( 'NONE',  ( -18.58744394320938298, -9.566385154537240254, -140.8228480538762994 ) ) ;
#239701=EDGE_LOOP ( 'NONE', ( #134306, #146507, #237330, #102261, #87965, #210099, #244864, #155860, #202171, #189102, #88969, #207773 ) ) ;
#239723=VERTEX_POINT ( 'NONE', #43307 ) ;
#239728=ORIENTED_EDGE ( 'NONE', *, *, #79784, .T. ) ;
#239738=ORIENTED_EDGE ( 'NONE', *, *, #96503, .T. ) ;
#239748=DIRECTION ( 'NONE',  ( 1.000000000000000000, 0.000000000000000000, 0.000000000000000000 ) ) ;
#239794=DIRECTION ( 'NONE',  ( 0.000000000000000000, 0.000000000000000000, -1.000000000000000000 ) ) ;
#239810=VECTOR ( 'NONE', #47245, 1000.000000000000000 ) ;
#239826=FACE_OUTER_BOUND ( 'NONE', #35724, .T. ) ;
#239852=DIRECTION ( 'NONE',  ( -0.000000000000000000, 0.000000000000000000, -1.000000000000000000 ) ) ;
#239870=EDGE_CURVE ( 'NONE', #176862, #173164, #215896, .T. ) ;
#239879=CARTESIAN_POINT ( 'NONE',  ( 18.56308993302939925, 10.38069115533503961, -125.2392226389383012 ) ) ;
#239913=VECTOR ( 'NONE', #178020, 1000.000000000000000 ) ;
#239925=CARTESIAN_POINT ( 'NONE',  ( 18.59999999999999432, 1.261786168576181755, -108.5864989635455089 ) ) ;
#239937=LINE ( 'NONE', #24760, #176535 ) ;
#239952=VERTEX_POINT ( 'NONE', #138209 ) ;
#240024=ADVANCED_FACE ( 'NONE', ( #195672 ), #56108, .T. ) ;
#240033=CARTESIAN_POINT ( 'NONE',  ( -20.07928932188135107, 9.220710678129810489, -121.6500000000000341 ) ) ;
#240041=TOROIDAL_SURFACE ( 'NONE', #6803, 0.2000000000000000111, 0.1000000000000000056 ) ;
#240045=CARTESIAN_POINT ( 'NONE',  ( 23.14999999999999503, 6.550000000011156231, -112.8500000000000369 ) ) ;
#240056=CARTESIAN_POINT ( 'NONE',  ( 18.46947024752531874, -9.509297157144976254, -107.4866894486978879 ) ) ;
#240059=VERTEX_POINT ( 'NONE', #75709 ) ;
#240078=FACE_OUTER_BOUND ( 'NONE', #138046, .T. ) ;
#240090=ORIENTED_EDGE ( 'NONE', *, *, #28810, .T. ) ;
#240102=VERTEX_POINT ( 'NONE', #114820 ) ;
#240112=DIRECTION ( 'NONE',  ( 1.000000000000000000, 0.000000000000000000, 0.000000000000000000 ) ) ;
#240123=ORIENTED_EDGE ( 'NONE', *, *, #96442, .F. ) ;
#240124=CARTESIAN_POINT ( 'NONE',  ( -20.00857864376270001, 9.150000000011157653, -121.6500000000000341 ) ) ;
#240148=CARTESIAN_POINT ( 'NONE',  ( 23.14999999999999858, 4.813084112160684214, -122.0584822434762060 ) ) ;
#240160=AXIS2_PLACEMENT_3D ( 'NONE', #171668, #73847, #95926 ) ;
#240198=FACE_OUTER_BOUND ( 'NONE', #218023, .T. ) ;
#240206=DIRECTION ( 'NONE',  ( 0.000000000000000000, 0.000000000000000000, -1.000000000000000000 ) ) ;
#240299=CIRCLE ( 'NONE', #256798, 11.64999999999999325 ) ;
#240336=VECTOR ( 'NONE', #221805, 1000.000000000000000 ) ;
#240337=EDGE_CURVE ( 'NONE', #92883, #224679, #127668, .T. ) ;
#240339=CIRCLE ( 'NONE', #227849, 11.80000000000000249 ) ;
#240375=FACE_OUTER_BOUND ( 'NONE', #30820, .T. ) ;
#240390=VERTEX_POINT ( 'NONE', #173256 ) ;
#240392=CARTESIAN_POINT ( 'NONE',  ( 21.05000000000000071, 10.42338541492406279, -107.9920519238701218 ) ) ;
#240430=FACE_OUTER_BOUND ( 'NONE', #85713, .T. ) ;
#240438=ORIENTED_EDGE ( 'NONE', *, *, #160687, .F. ) ;
#240444=CARTESIAN_POINT ( 'NONE',  ( -18.59999999999999787, -1.687074390080403941, -87.68542703345838163 ) ) ;
#240505=ADVANCED_FACE ( 'NONE', ( #2242 ), #160079, .T. ) ;
#240524=CARTESIAN_POINT ( 'NONE',  ( 20.95520789717937404, 10.57693059939611224, -108.0802329738748853 ) ) ;
#240548=CYLINDRICAL_SURFACE ( 'NONE', #18920, 2.000000000000001776 ) ;
#240560=CARTESIAN_POINT ( 'NONE',  ( -21.70464131381649509, 7.095358018979010417, -100.5000000000000284 ) ) ;
#240590=DIRECTION ( 'NONE',  ( -0.000000000000000000, 1.000000000000000000, 0.000000000000000000 ) ) ;
#240591=DIRECTION ( 'NONE',  ( 0.000000000000000000, 0.000000000000000000, -1.000000000000000000 ) ) ;
#240593=CARTESIAN_POINT ( 'NONE',  ( -20.85000000000000142, 6.846123162363745074, -137.7377262668498759 ) ) ;
#240622=AXIS2_PLACEMENT_3D ( 'NONE', #89953, #209927, #52099 ) ;
#240644=EDGE_CURVE ( 'NONE', #236424, #211247, #244709, .T. ) ;
#240689=ORIENTED_EDGE ( 'NONE', *, *, #169192, .F. ) ;
#240699=ORIENTED_EDGE ( 'NONE', *, *, #246469, .T. ) ;
#240705=VECTOR ( 'NONE', #1835, 1000.000000000000000 ) ;
#240710=VERTEX_POINT ( 'NONE', #106466 ) ;
#240729=CARTESIAN_POINT ( 'NONE',  ( 20.97217846901852312, 8.875441724720827708, -109.0012276839372447 ) ) ;
#240732=EDGE_CURVE ( 'NONE', #187769, #66771, #153219, .T. ) ;
#240747=DIRECTION ( 'NONE',  ( 0.000000000000000000, 0.000000000000000000, 1.000000000000000000 ) ) ;
#240785=DIRECTION ( 'NONE',  ( 0.000000000000000000, 0.000000000000000000, -1.000000000000000000 ) ) ;
#240806=DIRECTION ( 'NONE',  ( 1.000000000000000000, 0.000000000000000000, 0.000000000000000000 ) ) ;
#240835=EDGE_CURVE ( 'NONE', #121457, #189217, #251121, .T. ) ;
#240845=EDGE_CURVE ( 'NONE', #20729, #59138, #203060, .T. ) ;
#240848=CARTESIAN_POINT ( 'NONE',  ( -22.50000000000000000, 7.790779598384560245, -100.4000000000000341 ) ) ;
#240851=EDGE_CURVE ( 'NONE', #240710, #9426, #123977, .T. ) ;
#240883=FACE_OUTER_BOUND ( 'NONE', #96992, .T. ) ;
#240955=CARTESIAN_POINT ( 'NONE',  ( -18.50000000000000000, -9.399999999988850163, -140.8820418481727188 ) ) ;
#240967=CARTESIAN_POINT ( 'NONE',  ( -23.15000000000000213, 1.115600667400684642E-11, -130.0000000000000284 ) ) ;
#240999=AXIS2_PLACEMENT_3D ( 'NONE', #123336, #184578, #226249 ) ;
#241006=ADVANCED_FACE ( 'NONE', ( #84009 ), #11250, .T. ) ;
#241024=ORIENTED_EDGE ( 'NONE', *, *, #231509, .T. ) ;
#241028=VERTEX_POINT ( 'NONE', #89194 ) ;
#241029=FACE_OUTER_BOUND ( 'NONE', #15888, .T. ) ;
#241088=DIRECTION ( 'NONE',  ( 0.000000000000000000, -1.000000000000000000, 6.308085367188393199E-16 ) ) ;
#241114=CYLINDRICAL_SURFACE ( 'NONE', #111353, 0.09999999999999939493 ) ;
#241139=LINE ( 'NONE', #138140, #218679 ) ;
#241144=VERTEX_POINT ( 'NONE', #153077 ) ;
#241152=B_SPLINE_CURVE_WITH_KNOTS ( 'NONE', 3,
 ( #77154, #38060, #216672, #175033, #74637, #115001, #154178, #155459, #73342, #18474, #15936, #55001, #97980, #212832, #197096, #234960, #135833, #215378, #117569 ),
 .UNSPECIFIED., .F., .F.,
 ( 4, 3, 3, 3, 3, 3, 4 ),
 ( 0.000000000000000000, 1.655171619026035414E-05, 2.773500582848695921E-05, 5.941817267378285075E-05, 0.0001114174635873568916, 0.0001914169455916313886, 0.0002627181070750597572 ),
 .UNSPECIFIED. ) ;
#241165=CARTESIAN_POINT ( 'NONE',  ( 18.49999999999999289, 10.49142135624846617, -125.2500000000000426 ) ) ;
#241209=CARTESIAN_POINT ( 'NONE',  ( -21.56666275994539816, 1.115600667400684642E-11, -93.54263159310670517 ) ) ;
#241223=FACE_OUTER_BOUND ( 'NONE', #224278, .T. ) ;
#241224=LINE ( 'NONE', #100383, #55861 ) ;
#241230=ORIENTED_EDGE ( 'NONE', *, *, #208411, .T. ) ;
#241235=AXIS2_PLACEMENT_3D ( 'NONE', #68560, #108949, #73713 ) ;
#241243=CARTESIAN_POINT ( 'NONE',  ( -18.59999999999999787, 1.340746217944851715, -90.22713749457885513 ) ) ;
#241248=AXIS2_PLACEMENT_3D ( 'NONE', #139713, #200997, #43209 ) ;
#241254=CARTESIAN_POINT ( 'NONE',  ( -22.50000000000094147, 0.1000000000110504439, -88.85042919245520920 ) ) ;
#241256=EDGE_LOOP ( 'NONE', ( #77067, #10215, #36264, #113068 ) ) ;
#241275=EDGE_CURVE ( 'NONE', #163726, #25563, #104267, .T. ) ;
#241290=CARTESIAN_POINT ( 'NONE',  ( 18.49999999999999645, 1.115600667400684642E-11, -100.5000000000000284 ) ) ;
#241308=CIRCLE ( 'NONE', #120517, 0.1000000000000028644 ) ;
#241319=CARTESIAN_POINT ( 'NONE',  ( -20.94999999999999929, -1.135018845899022466, -141.7169768834323520 ) ) ;
#241330=VERTEX_POINT ( 'NONE', #45606 ) ;
#241347=CARTESIAN_POINT ( 'NONE',  ( 18.41789779300684060, -9.499999999988844479, -107.5320696663599307 ) ) ;
#241353=CARTESIAN_POINT ( 'NONE',  ( -20.64999999999999858, 7.150000000011155876, -112.8500000000000369 ) ) ;
#241391=CARTESIAN_POINT ( 'NONE',  ( 21.05000000000000071, -8.999999999988842703, -124.5060308773475839 ) ) ;
#241469=CARTESIAN_POINT ( 'NONE',  ( -20.94999999999999929, 1.115600667400684642E-11, -100.5000000000000284 ) ) ;
#241495=ORIENTED_EDGE ( 'NONE', *, *, #139344, .F. ) ;
#241505=DIRECTION ( 'NONE',  ( 0.000000000000000000, 0.008583690987128059571, -0.9999631594459056361 ) ) ;
#241509=CARTESIAN_POINT ( 'NONE',  ( -23.25000000000000000, 1.115626384983466744E-11, -131.9000000000000341 ) ) ;
#241552=EDGE_LOOP ( 'NONE', ( #238785, #198028, #87644, #171528 ) ) ;
#241555=ORIENTED_EDGE ( 'NONE', *, *, #31823, .F. ) ;
#241595=ORIENTED_EDGE ( 'NONE', *, *, #38795, .T. ) ;
#241596=CARTESIAN_POINT ( 'NONE',  ( 22.49999999999999645, 0.1000000000111554016, -88.85042919245522341 ) ) ;
#241621=DIRECTION ( 'NONE',  ( -1.000000000000000000, -2.952720810173289112E-16, 0.000000000000000000 ) ) ;
#241650=CARTESIAN_POINT ( 'NONE',  ( -20.94560253601877164, 11.75000000001115197, -127.0100835125151093 ) ) ;
#241725=LINE ( 'NONE', #177916, #75637 ) ;
#241730=CARTESIAN_POINT ( 'NONE',  ( -21.14999999999999858, 11.65000000001115232, -100.5000000000000284 ) ) ;
#241759=DIRECTION ( 'NONE',  ( 1.000000000000000000, 0.000000000000000000, 0.000000000000000000 ) ) ;
#241806=ORIENTED_EDGE ( 'NONE', *, *, #108045, .T. ) ;
#241869=DIRECTION ( 'NONE',  ( 1.000000000000000000, 0.000000000000000000, -0.000000000000000000 ) ) ;
#241886=DIRECTION ( 'NONE',  ( 0.000000000000000000, 1.000000000000000000, 0.000000000000000000 ) ) ;
#241905=DIRECTION ( 'NONE',  ( -0.000000000000000000, 0.000000000000000000, 1.000000000000000000 ) ) ;
#241932=VERTEX_POINT ( 'NONE', #34319 ) ;
#241947=CIRCLE ( 'NONE', #46142, 0.09999999999999911737 ) ;
#241950=VERTEX_POINT ( 'NONE', #38159 ) ;
#241956=CARTESIAN_POINT ( 'NONE',  ( 21.05000000000036309, 10.60832956796502025, -108.0916850132954607 ) ) ;
#241968=ADVANCED_FACE ( 'NONE', ( #155558 ), #149660, .T. ) ;
#241981=ORIENTED_EDGE ( 'NONE', *, *, #125705, .T. ) ;
#241990=FACE_OUTER_BOUND ( 'NONE', #154983, .T. ) ;
#242004=CARTESIAN_POINT ( 'NONE',  ( -23.15000000000000213, 11.65000000001115588, -88.75000000000004263 ) ) ;
#242007=VERTEX_POINT ( 'NONE', #39463 ) ;
#242009=ORIENTED_EDGE ( 'NONE', *, *, #151039, .F. ) ;
#242041=DIRECTION ( 'NONE',  ( 0.000000000000000000, -1.734723475976757554E-14, 1.000000000000000000 ) ) ;
#242051=CARTESIAN_POINT ( 'NONE',  ( -23.15000000000000213, -8.596261682231830292, -124.5498724828497501 ) ) ;
#242060=DIRECTION ( 'NONE',  ( 0.000000000000000000, 0.000000000000000000, 1.000000000000000000 ) ) ;
#242072=DIRECTION ( 'NONE',  ( 0.000000000000000000, -0.8660254037844411501, -0.4999999999999956146 ) ) ;
#242095=EDGE_CURVE ( 'NONE', #238428, #48720, #236339, .T. ) ;
#242187=AXIS2_PLACEMENT_3D ( 'NONE', #240444, #222128, #138728 ) ;
#242192=ORIENTED_EDGE ( 'NONE', *, *, #140996, .F. ) ;
#242245=FACE_OUTER_BOUND ( 'NONE', #246123, .T. ) ;
#242281=ORIENTED_EDGE ( 'NONE', *, *, #153106, .T. ) ;
#242319=DIRECTION ( 'NONE',  ( -0.000000000000000000, -0.8660254037844459241, -0.4999999999999873990 ) ) ;
#242322=DIRECTION ( 'NONE',  ( 7.304098846218134667E-16, -1.000000000000000000, 0.000000000000000000 ) ) ;
#242327=DIRECTION ( 'NONE',  ( 0.000000000000000000, 0.6728971962616697722, 0.7397360091702875895 ) ) ;
#242342=CARTESIAN_POINT ( 'NONE',  ( -23.15000000000000213, 1.115600667400684642E-11, -134.0000000000000284 ) ) ;
#242352=ORIENTED_EDGE ( 'NONE', *, *, #163545, .T. ) ;
#242360=VERTEX_POINT ( 'NONE', #169689 ) ;
#242387=CARTESIAN_POINT ( 'NONE',  ( 22.48970261584622321, 11.65000000001115588, -100.4446305117826199 ) ) ;
#242420=FACE_OUTER_BOUND ( 'NONE', #37388, .T. ) ;
#242432=ORIENTED_EDGE ( 'NONE', *, *, #142084, .F. ) ;
#242433=DIRECTION ( 'NONE',  ( 0.000000000000000000, -1.000000000000000000, 0.000000000000000000 ) ) ;
#242466=TOROIDAL_SURFACE ( 'NONE', #104884, 0.2000000000000000111, 0.1000000000000000056 ) ;
#242479=ADVANCED_FACE ( 'NONE', ( #254293 ), #245686, .F. ) ;
#242480=CARTESIAN_POINT ( 'NONE',  ( 20.94999999999999574, 1.849084418638171856, -112.1560105214471577 ) ) ;
#242494=VERTEX_POINT ( 'NONE', #140786 ) ;
#242506=DIRECTION ( 'NONE',  ( 0.000000000000000000, 0.000000000000000000, -1.000000000000000000 ) ) ;
#242508=AXIS2_PLACEMENT_3D ( 'NONE', #41252, #141597, #42494 ) ;
#242517=ORIENTED_EDGE ( 'NONE', *, *, #25139, .F. ) ;
#242529=LINE ( 'NONE', #172025, #70 ) ;
#242541=FACE_OUTER_BOUND ( 'NONE', #79840, .T. ) ;
#242542=ORIENTED_EDGE ( 'NONE', *, *, #254801, .T. ) ;
#242555=VERTEX_POINT ( 'NONE', #222877 ) ;
#242562=ORIENTED_EDGE ( 'NONE', *, *, #139344, .T. ) ;
#242627=SPHERICAL_SURFACE ( 'NONE', #103746, 0.1000000000000000056 ) ;
#242630=DIRECTION ( 'NONE',  ( 0.000000000000000000, -0.9915357197604971473, 0.1298341882519111479 ) ) ;
#242632=DIRECTION ( 'NONE',  ( 0.000000000000000000, 0.000000000000000000, -1.000000000000000000 ) ) ;
#242694=ORIENTED_EDGE ( 'NONE', *, *, #95376, .T. ) ;
#242714=VECTOR ( 'NONE', #232738, 1000.000000000000000 ) ;
#242729=FACE_OUTER_BOUND ( 'NONE', #68988, .T. ) ;
#242760=EDGE_CURVE ( 'NONE', #198122, #23723, #87454, .T. ) ;
#242789=CARTESIAN_POINT ( 'NONE',  ( -21.05000000000000071, -11.39257802169451672, -103.5739495798319751 ) ) ;
#242843=AXIS2_PLACEMENT_3D ( 'NONE', #148256, #227787, #49154 ) ;
#242888=AXIS2_PLACEMENT_3D ( 'NONE', #8740, #149558, #229079 ) ;
#242927=DIRECTION ( 'NONE',  ( 2.952720810173289112E-16, -1.000000000000000000, 0.000000000000000000 ) ) ;
#242928=CARTESIAN_POINT ( 'NONE',  ( -20.87155475150660777, 11.75000000001115197, -127.0955865291576714 ) ) ;
#242939=AXIS2_PLACEMENT_3D ( 'NONE', #171666, #148208, #67392 ) ;
#242980=LINE ( 'NONE', #186893, #10096 ) ;
#242984=EDGE_LOOP ( 'NONE', ( #133241, #196621, #185248, #224669 ) ) ;
#243031=ORIENTED_EDGE ( 'NONE', *, *, #30866, .F. ) ;
#243082=DIRECTION ( 'NONE',  ( 6.484947573744954877E-15, 0.9274965247785529332, -0.3738317757009255171 ) ) ;
#243095=CARTESIAN_POINT ( 'NONE',  ( -21.05000000000000071, 6.299230910103437608, -100.4015624999997414 ) ) ;
#243097=ORIENTED_EDGE ( 'NONE', *, *, #158867, .T. ) ;
#243107=ADVANCED_FACE ( 'NONE', ( #212014 ), #225166, .F. ) ;
#243111=AXIS2_PLACEMENT_3D ( 'NONE', #223700, #45083, #124626 ) ;
#243126=CYLINDRICAL_SURFACE ( 'NONE', #244216, 0.09999999999999939493 ) ;
#243132=DIRECTION ( 'NONE',  ( 0.000000000000000000, 0.9908441862701600211, -0.1350103645451876666 ) ) ;
#243135=CARTESIAN_POINT ( 'NONE',  ( 21.13461538461538325, 10.61458296203669249, -112.8500000000000369 ) ) ;
#243146=VERTEX_POINT ( 'NONE', #209420 ) ;
#243158=ORIENTED_EDGE ( 'NONE', *, *, #254971, .F. ) ;
#243168=EDGE_LOOP ( 'NONE', ( #215990, #24714, #165943, #95539 ) ) ;
#243174=AXIS2_PLACEMENT_3D ( 'NONE', #4529, #10650, #121933 ) ;
#243176=CARTESIAN_POINT ( 'NONE',  ( -21.78635804494510708, 7.035661485164336426, -100.4009949344923456 ) ) ;
#243195=DIRECTION ( 'NONE',  ( 0.000000000000000000, 0.000000000000000000, 1.000000000000000000 ) ) ;
#243223=EDGE_CURVE ( 'NONE', #182849, #119449, #150384, .T. ) ;
#243232=CARTESIAN_POINT ( 'NONE',  ( 21.05000000000000071, 10.62872031401550288, -108.1649135690876449 ) ) ;
#243236=CARTESIAN_POINT ( 'NONE',  ( -20.94999999999999929, -11.48912529306490349, -103.5000000000000426 ) ) ;
#243243=CYLINDRICAL_SURFACE ( 'NONE', #122820, 4.000000000000003553 ) ;
#243247=EDGE_LOOP ( 'NONE', ( #28445, #47611, #154910, #3159 ) ) ;
#243261=CARTESIAN_POINT ( 'NONE',  ( 20.04142135391667168, 11.75000000001116263, -125.2025068656295588 ) ) ;
#243272=CARTESIAN_POINT ( 'NONE',  ( 20.52683494730037239, 8.980530818312608687, -109.0052527225372359 ) ) ;
#243286=EDGE_LOOP ( 'NONE', ( #194160, #191065 ) ) ;
#243325=VERTEX_POINT ( 'NONE', #98421 ) ;
#243354=EDGE_CURVE ( 'NONE', #23723, #120532, #133606, .T. ) ;
#243360=CARTESIAN_POINT ( 'NONE',  ( -21.05000000000000071, 1.115600667400684642E-11, -134.0000000000000284 ) ) ;
#243362=VERTEX_POINT ( 'NONE', #1915 ) ;
#243456=AXIS2_PLACEMENT_3D ( 'NONE', #197909, #104871, #20585 ) ;
#243518=AXIS2_PLACEMENT_3D ( 'NONE', #119625, #199149, #20531 ) ;
#243547=DIRECTION ( 'NONE',  ( 1.000000000000000000, 0.000000000000000000, 0.000000000000000000 ) ) ;
#243559=DIRECTION ( 'NONE',  ( 1.000000000000000000, 0.000000000000000000, 0.000000000000000000 ) ) ;
#243566=( BOUNDED_CURVE ( )  B_SPLINE_CURVE ( 3, ( #5014, #84529, #183693, #207106 ),
 .UNSPECIFIED., .F., .F. ) 
 B_SPLINE_CURVE_WITH_KNOTS ( ( 4, 4 ),
 ( 3.141592653589791784, 4.712388980384688786 ),
 .UNSPECIFIED. ) 
 CURVE ( )  GEOMETRIC_REPRESENTATION_ITEM ( )  RATIONAL_B_SPLINE_CURVE ( ( 1.000000000000000000, 0.8047378541243649375, 0.8047378541243649375, 1.000000000000000000 ) ) 
 REPRESENTATION_ITEM ( '' )  );
#243581=ORIENTED_EDGE ( 'NONE', *, *, #15436, .F. ) ;
#243602=AXIS2_PLACEMENT_3D ( 'NONE', #27614, #31463, #107108 ) ;
#243609=ORIENTED_EDGE ( 'NONE', *, *, #184834, .T. ) ;
#243626=CARTESIAN_POINT ( 'NONE',  ( -20.85000000000000142, -1.164121893230052995, -141.9148480855716343 ) ) ;
#243644=CARTESIAN_POINT ( 'NONE',  ( -23.15000000000000213, 11.75000000001115552, -112.7500000000000284 ) ) ;
#243648=ORIENTED_EDGE ( 'NONE', *, *, #73860, .F. ) ;
#243650=EDGE_CURVE ( 'NONE', #132129, #44449, #56133, .T. ) ;
#243652=ORIENTED_EDGE ( 'NONE', *, *, #91435, .F. ) ;
#243654=CARTESIAN_POINT ( 'NONE',  ( 21.30000000000002558, 1.115650265596050101E-11, -104.5500000000000256 ) ) ;
#243655=DIRECTION ( 'NONE',  ( 0.000000000000000000, 0.000000000000000000, 1.000000000000000000 ) ) ;
#243704=CARTESIAN_POINT ( 'NONE',  ( -20.94999999999999929, 1.115600667400684642E-11, -134.0000000000000284 ) ) ;
#243759=B_SPLINE_CURVE_WITH_KNOTS ( 'NONE', 3,
 ( #31825, #168787, #111334, #248272, #231292, #210445, #190899, #147897 ),
 .UNSPECIFIED., .F., .F.,
 ( 4, 2, 2, 4 ),
 ( 0.000000000000000000, 0.0001306511400391185051, 0.0001959767100586981136, 0.0002613022800782777220 ),
 .UNSPECIFIED. ) ;
#243790=DIRECTION ( 'NONE',  ( -0.000000000000000000, -0.000000000000000000, -1.000000000000000000 ) ) ;
#243821=VERTEX_POINT ( 'NONE', #149830 ) ;
#243842=ORIENTED_EDGE ( 'NONE', *, *, #69742, .F. ) ;
#243856=CARTESIAN_POINT ( 'NONE',  ( 20.94999999999999929, 1.115600667400684642E-11, -134.0000000000000284 ) ) ;
#243900=ORIENTED_EDGE ( 'NONE', *, *, #57051, .F. ) ;
#243906=CARTESIAN_POINT ( 'NONE',  ( -21.05000000000000426, 11.63687328911556662, -107.3217592133250520 ) ) ;
#243932=DIRECTION ( 'NONE',  ( -1.000000000000000000, 0.000000000000000000, 0.000000000000000000 ) ) ;
#243952=PLANE ( 'NONE',  #14747 ) ;
#243975=EDGE_CURVE ( 'NONE', #146245, #16782, #71644, .T. ) ;
#243981=CARTESIAN_POINT ( 'NONE',  ( 21.05000000000000071, 6.540656951712400691, -100.6000000000000369 ) ) ;
#244010=DIRECTION ( 'NONE',  ( -0.000000000000000000, 0.8660254037844383745, -0.5000000000000003331 ) ) ;
#244055=CARTESIAN_POINT ( 'NONE',  ( -23.25000000000000000, -9.599999999988845900, -124.1060308773475924 ) ) ;
#244080=ORIENTED_EDGE ( 'NONE', *, *, #32032, .F. ) ;
#244097=ADVANCED_FACE ( 'NONE', ( #184765 ), #171616, .T. ) ;
#244105=CARTESIAN_POINT ( 'NONE',  ( 23.14999999999999503, 11.65000000001116298, -126.9851942293460922 ) ) ;
#244110=ORIENTED_EDGE ( 'NONE', *, *, #19680, .T. ) ;
#244113=CARTESIAN_POINT ( 'NONE',  ( -23.25000000000000000, -0.1008583690875562017, -88.75043287651064361 ) ) ;
#244137=ORIENTED_EDGE ( 'NONE', *, *, #223023, .T. ) ;
#244201=CARTESIAN_POINT ( 'NONE',  ( -18.59999999999999787, 11.75000000001115552, -134.0000000000000284 ) ) ;
#244216=AXIS2_PLACEMENT_3D ( 'NONE', #164885, #238313, #235745 ) ;
#244266=ORIENTED_EDGE ( 'NONE', *, *, #16713, .F. ) ;
#244277=ORIENTED_EDGE ( 'NONE', *, *, #92879, .T. ) ;
#244289=DIRECTION ( 'NONE',  ( 0.000000000000000000, 0.000000000000000000, -1.000000000000000000 ) ) ;
#244294=DIRECTION ( 'NONE',  ( 0.7071067811865474617, 0.7071067811865474617, -0.000000000000000000 ) ) ;
#244308=LINE ( 'NONE', #46113, #165906 ) ;
#244375=CARTESIAN_POINT ( 'NONE',  ( -21.05000000000000071, -1.835341550213255957, -112.0551512925630107 ) ) ;
#244380=CARTESIAN_POINT ( 'NONE',  ( 22.49544290803769897, 11.74987023786852802, -100.4346880407425573 ) ) ;
#244444=ADVANCED_FACE ( 'NONE', ( #34709 ), #18961, .T. ) ;
#244462=CARTESIAN_POINT ( 'NONE',  ( 23.14999999999999858, 5.950000000011160139, -123.6942976949652149 ) ) ;
#244483=LINE ( 'NONE', #86667, #195315 ) ;
#244490=ORIENTED_EDGE ( 'NONE', *, *, #82356, .T. ) ;
#244491=DIRECTION ( 'NONE',  ( -1.000000000000000000, 0.000000000000000000, 0.000000000000000000 ) ) ;
#244504=ORIENTED_EDGE ( 'NONE', *, *, #107906, .F. ) ;
#244511=CARTESIAN_POINT ( 'NONE',  ( 20.85000000000000142, 1.115600667400684642E-11, -134.0000000000000284 ) ) ;
#244512=CYLINDRICAL_SURFACE ( 'NONE', #151521, 0.5000000000000004441 ) ;
#244523=CIRCLE ( 'NONE', #198736, 0.5000000000000004441 ) ;
#244531=ORIENTED_EDGE ( 'NONE', *, *, #251254, .T. ) ;
#244550=ORIENTED_EDGE ( 'NONE', *, *, #189576, .T. ) ;
#244554=B_SPLINE_CURVE_WITH_KNOTS ( 'NONE', 3,
 ( #220043, #21850, #101323, #2257, #161368, #225150, #124802, #89500, #169095, #145624 ),
 .UNSPECIFIED., .F., .F.,
 ( 4, 3, 3, 4 ),
 ( 0.000000000000000000, 3.394313611811197040E-05, 6.779740500700327799E-05, 0.0001049857339142765996 ),
 .UNSPECIFIED. ) ;
#244563=CARTESIAN_POINT ( 'NONE',  ( 18.59999999999999432, 1.162701749949165642, -108.6000000000000227 ) ) ;
#244579=CARTESIAN_POINT ( 'NONE',  ( -21.07094088545303379, 6.320167221927637691, -100.4011062974478250 ) ) ;
#244589=CARTESIAN_POINT ( 'NONE',  ( -23.15000000000000213, -9.499999999988846255, -124.1060308773475924 ) ) ;
#244590=CARTESIAN_POINT ( 'NONE',  ( 20.94999999999999929, -11.64999999998883595, -134.0000000000000284 ) ) ;
#244645=DIRECTION ( 'NONE',  ( 1.000000000000000000, 0.000000000000000000, 0.000000000000000000 ) ) ;
#244648=AXIS2_PLACEMENT_3D ( 'NONE', #250996, #114064, #249741 ) ;
#244661=DIRECTION ( 'NONE',  ( 0.000000000000000000, -1.000000000000000000, 0.000000000000000000 ) ) ;
#244709=LINE ( 'NONE', #9966, #194898 ) ;
#244769=VECTOR ( 'NONE', #73605, 1000.000000000000000 ) ;
#244785=CARTESIAN_POINT ( 'NONE',  ( -18.31331870001081086, -9.536294719169568168, -140.8685786909853732 ) ) ;
#244824=CIRCLE ( 'NONE', #132424, 0.09999999999999939493 ) ;
#244828=DIRECTION ( 'NONE',  ( -0.000000000000000000, -0.000000000000000000, -1.000000000000000000 ) ) ;
#244831=CARTESIAN_POINT ( 'NONE',  ( -23.15000000000000213, -11.64999999998884483, -130.9000000000000341 ) ) ;
#244864=ORIENTED_EDGE ( 'NONE', *, *, #78544, .T. ) ;
#244865=CARTESIAN_POINT ( 'NONE',  ( -21.55000000000000426, 7.750000000011155521, -112.8500000000000369 ) ) ;
#244913=EDGE_CURVE ( 'NONE', #154121, #234753, #162050, .T. ) ;
#244922=CARTESIAN_POINT ( 'NONE',  ( -23.15000000000000213, 1.115600667400684642E-11, -134.0000000000000284 ) ) ;
#244939=ORIENTED_EDGE ( 'NONE', *, *, #57315, .T. ) ;
#244961=AXIS2_PLACEMENT_3D ( 'NONE', #196920, #198205, #14466 ) ;
#245007=DIRECTION ( 'NONE',  ( -1.000000000000000000, -0.000000000000000000, -0.000000000000000000 ) ) ;
#245014=CIRCLE ( 'NONE', #36951, 0.1000000000000000472 ) ;
#245015=FACE_OUTER_BOUND ( 'NONE', #171012, .T. ) ;
#245026=VECTOR ( 'NONE', #90527, 1000.000000000000000 ) ;
#245030=AXIS2_PLACEMENT_3D ( 'NONE', #155066, #232024, #234565 ) ;
#245050=CARTESIAN_POINT ( 'NONE',  ( 23.24999999999999289, 6.650000000011155876, -112.6500000000000341 ) ) ;
#245055=VERTEX_POINT ( 'NONE', #109746 ) ;
#245071=ORIENTED_EDGE ( 'NONE', *, *, #87278, .F. ) ;
#245076=CIRCLE ( 'NONE', #207672, 0.09999999999998898659 ) ;
#245090=ORIENTED_EDGE ( 'NONE', *, *, #113747, .F. ) ;
#245108=DIRECTION ( 'NONE',  ( 0.000000000000000000, -0.9999631594459056361, -0.008583690987124413183 ) ) ;
#245121=ORIENTED_EDGE ( 'NONE', *, *, #159742, .F. ) ;
#245126=CYLINDRICAL_SURFACE ( 'NONE', #253490, 0.09999999999998898659 ) ;
#245139=AXIS2_PLACEMENT_3D ( 'NONE', #54798, #74415, #217715 ) ;
#245141=LINE ( 'NONE', #48214, #116563 ) ;
#245159=AXIS2_PLACEMENT_3D ( 'NONE', #203614, #161943, #182787 ) ;
#245170=ORIENTED_EDGE ( 'NONE', *, *, #147757, .F. ) ;
#245173=EDGE_LOOP ( 'NONE', ( #111207, #123334, #194055, #219205 ) ) ;
#245179=ORIENTED_EDGE ( 'NONE', *, *, #128700, .T. ) ;
#245218=CARTESIAN_POINT ( 'NONE',  ( -21.05000000000000071, -11.48912529306489994, -130.9000000000000341 ) ) ;
#245231=EDGE_CURVE ( 'NONE', #159306, #146245, #209162, .T. ) ;
#245237=CARTESIAN_POINT ( 'NONE',  ( 20.94999999999999574, -1.162701749926853712, -108.6000000000000227 ) ) ;
#245242=DIRECTION ( 'NONE',  ( 1.000000000000000000, 0.000000000000000000, 0.000000000000000000 ) ) ;
#245275=ORIENTED_EDGE ( 'NONE', *, *, #166379, .T. ) ;
#245297=CARTESIAN_POINT ( 'NONE',  ( 20.94999999999999929, 5.000000000011153745, -121.5947339810869465 ) ) ;
#245301=DIRECTION ( 'NONE',  ( -1.000000000000000000, -1.836970198721029934E-16, 0.000000000000000000 ) ) ;
#245307=DIRECTION ( 'NONE',  ( 1.000000000000000000, -0.000000000000000000, -0.000000000000000000 ) ) ;
#245354=EDGE_CURVE ( 'NONE', #109044, #239723, #127604, .T. ) ;
#245404=LINE ( 'NONE', #203702, #94675 ) ;
#245405=LINE ( 'NONE', #62902, #134833 ) ;
#245410=CARTESIAN_POINT ( 'NONE',  ( 18.59999999999999787, -11.74999999998883737, -121.8500000000000369 ) ) ;
#245428=EDGE_CURVE ( 'NONE', #101037, #124696, #196547, .T. ) ;
#245447=EDGE_CURVE ( 'NONE', #123284, #169627, #247618, .T. ) ;
#245489=CARTESIAN_POINT ( 'NONE',  ( 23.15000000000000213, -9.599999999988845900, -110.3939691226524786 ) ) ;
#245498=ORIENTED_EDGE ( 'NONE', *, *, #240337, .T. ) ;
#245510=EDGE_CURVE ( 'NONE', #239049, #140362, #105547, .T. ) ;
#245523=DIRECTION ( 'NONE',  ( 0.000000000000000000, -0.1298341882520022694, -0.9915357197604853789 ) ) ;
#245561=EDGE_CURVE ( 'NONE', #253135, #196436, #68166, .T. ) ;
#245564=CARTESIAN_POINT ( 'NONE',  ( -21.05000000000000071, 1.162701749949165642, -108.4000000000000341 ) ) ;
#245598=EDGE_LOOP ( 'NONE', ( #154420, #38870, #139421, #176177, #180923 ) ) ;
#245604=B_SPLINE_CURVE_WITH_KNOTS ( 'NONE', 3,
 ( #243135, #84010, #226115, #106175, #63198, #86607 ),
 .UNSPECIFIED., .F., .F.,
 ( 4, 2, 4 ),
 ( 0.000000000000000000, 0.0001497467027049297528, 0.0002994934054098595056 ),
 .UNSPECIFIED. ) ;
#245621=ADVANCED_FACE ( 'NONE', ( #156762 ), #52474, .T. ) ;
#245632=ADVANCED_FACE ( 'NONE', ( #233717 ), #59758, .F. ) ;
#245656=ORIENTED_EDGE ( 'NONE', *, *, #190127, .T. ) ;
#245666=ORIENTED_EDGE ( 'NONE', *, *, #39354, .T. ) ;
#245686=TOROIDAL_SURFACE ( 'NONE', #4233, 0.4000000000000015210, 0.1000000000000000056 ) ;
#245711=VERTEX_POINT ( 'NONE', #163170 ) ;
#245714=CARTESIAN_POINT ( 'NONE',  ( -20.64999999999999858, -8.999999999988844479, -124.6060308773475924 ) ) ;
#245719=CARTESIAN_POINT ( 'NONE',  ( 18.52928932188133970, 10.27928932189250411, -125.2500000000000284 ) ) ;
#245734=CARTESIAN_POINT ( 'NONE',  ( -23.15000000000000213, 4.350000000011156054, -112.6500000000000483 ) ) ;
#245768=VERTEX_POINT ( 'NONE', #88727 ) ;
#245770=CARTESIAN_POINT ( 'NONE',  ( -20.94999999999999929, -11.74999999998884448, -130.9000000000000341 ) ) ;
#245775=CARTESIAN_POINT ( 'NONE',  ( -21.05000000000000071, 11.65000000001115232, -100.6000000000000369 ) ) ;
#245802=AXIS2_PLACEMENT_3D ( 'NONE', #196443, #239440, #161185 ) ;
#245814=FACE_OUTER_BOUND ( 'NONE', #224415, .T. ) ;
#245837=VERTEX_POINT ( 'NONE', #109586 ) ;
#245865=DIRECTION ( 'NONE',  ( 0.000000000000000000, 0.000000000000000000, -1.000000000000000000 ) ) ;
#245883=CARTESIAN_POINT ( 'NONE',  ( -23.25000000000000000, -0.09999999998884338825, -88.85042919245522341 ) ) ;
#245884=( NAMED_UNIT ( * ) SI_UNIT ( $, .STERADIAN. ) SOLID_ANGLE_UNIT ( ) );
#245888=VERTEX_POINT ( 'NONE', #35233 ) ;
#245896=CARTESIAN_POINT ( 'NONE',  ( 23.24999999999999289, 4.150000000011154988, -100.5000000000000284 ) ) ;
#245917=ORIENTED_EDGE ( 'NONE', *, *, #44466, .T. ) ;
#245944=DIRECTION ( 'NONE',  ( 1.000000000000000000, -0.000000000000000000, -0.000000000000000000 ) ) ;
#246018=CARTESIAN_POINT ( 'NONE',  ( -21.05000000000000071, -0.09999999998884338825, -93.95934304829879125 ) ) ;
#246021=DIRECTION ( 'NONE',  ( 0.000000000000000000, 0.000000000000000000, -1.000000000000000000 ) ) ;
#246056=DIRECTION ( 'NONE',  ( 1.000000000000000000, 0.000000000000000000, -0.000000000000000000 ) ) ;
#246083=VECTOR ( 'NONE', #173147, 1000.000000000000000 ) ;
#246088=EDGE_CURVE ( 'NONE', #5875, #104969, #78835, .T. ) ;
#246123=EDGE_LOOP ( 'NONE', ( #159818, #194942, #13591, #196993, #61183 ) ) ;
#246134=DIRECTION ( 'NONE',  ( 1.000000000000000000, -0.000000000000000000, -0.000000000000000000 ) ) ;
#246136=ORIENTED_EDGE ( 'NONE', *, *, #185297, .T. ) ;
#246152=ORIENTED_EDGE ( 'NONE', *, *, #55907, .F. ) ;
#246176=CARTESIAN_POINT ( 'NONE',  ( -23.25000000000000000, 6.933893972137497030, -137.7856458343736108 ) ) ;
#246181=DIRECTION ( 'NONE',  ( 1.000000000000000000, 3.265361837132813093E-16, -0.000000000000000000 ) ) ;
#246242=AXIS2_PLACEMENT_3D ( 'NONE', #49456, #212397, #92418 ) ;
#246284=ADVANCED_FACE ( 'NONE', ( #24654 ), #127574, .T. ) ;
#246288=FACE_OUTER_BOUND ( 'NONE', #126615, .T. ) ;
#246299=DIRECTION ( 'NONE',  ( 0.000000000000000000, 1.776356839400246520E-15, -1.000000000000000000 ) ) ;
#246313=EDGE_CURVE ( 'NONE', #245711, #55613, #45724, .T. ) ;
#246339=CARTESIAN_POINT ( 'NONE',  ( -18.59999999999999787, 1.115600667400684642E-11, -134.0000000000000284 ) ) ;
#246369=DIRECTION ( 'NONE',  ( 0.000000000000000000, 1.000000000000000000, -0.000000000000000000 ) ) ;
#246420=VERTEX_POINT ( 'NONE', #195270 ) ;
#246429=EDGE_LOOP ( 'NONE', ( #241806, #30282, #42195 ) ) ;
#246434=AXIS2_PLACEMENT_3D ( 'NONE', #256191, #37232, #228037 ) ;
#246469=EDGE_CURVE ( 'NONE', #58778, #150130, #224774, .T. ) ;
#246471=DIRECTION ( 'NONE',  ( 0.000000000000000000, -0.4930308989874653269, -0.8700118002898649117 ) ) ;
#246478=EDGE_CURVE ( 'NONE', #179371, #92785, #141393, .T. ) ;
#246483=CARTESIAN_POINT ( 'NONE',  ( 21.08832698747859169, 8.775364393428372267, -112.7287174664641753 ) ) ;
#246494=AXIS2_PLACEMENT_3D ( 'NONE', #61192, #164154, #140726 ) ;
#246547=CARTESIAN_POINT ( 'NONE',  ( -21.05000000000000426, -0.09999999998884340213, -94.02293297887531764 ) ) ;
#246559=CIRCLE ( 'NONE', #75880, 0.09999999999998898659 ) ;
#246560=EDGE_CURVE ( 'NONE', #249313, #102466, #104150, .T. ) ;
#246574=ORIENTED_EDGE ( 'NONE', *, *, #85505, .T. ) ;
#246600=FACE_OUTER_BOUND ( 'NONE', #17007, .T. ) ;
#246609=EDGE_CURVE ( 'NONE', #172291, #111426, #8331, .T. ) ;
#246634=VERTEX_POINT ( 'NONE', #106385 ) ;
#246635=EDGE_LOOP ( 'NONE', ( #224799, #236202, #256345, #17590 ) ) ;
#246653=VECTOR ( 'NONE', #102884, 1000.000000000000000 ) ;
#246671=LINE ( 'NONE', #206274, #32069 ) ;
#246676=CARTESIAN_POINT ( 'NONE',  ( -20.54999999999999716, -8.999999999988844479, -124.1060308773475924 ) ) ;
#246726=CIRCLE ( 'NONE', #26182, 0.09999999999999693856 ) ;
#246740=EDGE_LOOP ( 'NONE', ( #151552, #21576, #11185, #130009, #169235 ) ) ;
#246777=CARTESIAN_POINT ( 'NONE',  ( 20.94999999999999574, 1.162701749949165642, -108.5000000000000426 ) ) ;
#246818=DIRECTION ( 'NONE',  ( 0.000000000000000000, 0.000000000000000000, -1.000000000000000000 ) ) ;
#246834=ORIENTED_EDGE ( 'NONE', *, *, #7961, .F. ) ;
#246927=CARTESIAN_POINT ( 'NONE',  ( -21.14999999999999858, 6.257814610487270279, -100.4022097086912311 ) ) ;
#247004=CARTESIAN_POINT ( 'NONE',  ( -21.10257677756356642, 6.398381742543891804, -100.4750492504320931 ) ) ;
#247006=ORIENTED_EDGE ( 'NONE', *, *, #18431, .T. ) ;
#247017=CARTESIAN_POINT ( 'NONE',  ( -18.59999999999999787, 11.65000000001115232, -121.8500000000000369 ) ) ;
#247027=ORIENTED_EDGE ( 'NONE', *, *, #192194, .F. ) ;
#247029=VECTOR ( 'NONE', #198433, 1000.000000000000000 ) ;
#247064=VERTEX_POINT ( 'NONE', #147480 ) ;
#247126=CARTESIAN_POINT ( 'NONE',  ( 20.97565083910961548, 10.47461740128996510, -108.0779431765885903 ) ) ;
#247130=DIRECTION ( 'NONE',  ( 1.000000000000000000, 0.000000000000000000, 0.000000000000000000 ) ) ;
#247149=CIRCLE ( 'NONE', #209573, 0.6000000000000033085 ) ;
#247168=VERTEX_POINT ( 'NONE', #156507 ) ;
#247174=DIRECTION ( 'NONE',  ( 0.000000000000000000, -1.000000000000000000, 0.000000000000000000 ) ) ;
#247208=CYLINDRICAL_SURFACE ( 'NONE', #58886, 4.049999999999998046 ) ;
#247213=DIRECTION ( 'NONE',  ( 0.000000000000000000, 1.000000000000000000, 0.000000000000000000 ) ) ;
#247219=AXIS2_PLACEMENT_3D ( 'NONE', #129309, #228425, #230999 ) ;
#247234=CARTESIAN_POINT ( 'NONE',  ( -21.44999999999999929, 7.150000000011155876, -112.8500000000000369 ) ) ;
#247252=DIRECTION ( 'NONE',  ( 0.000000000000000000, 1.000000000000000000, 2.891205793294679805E-16 ) ) ;
#247291=EDGE_LOOP ( 'NONE', ( #103323, #62669, #200342, #108926 ) ) ;
#247300=CARTESIAN_POINT ( 'NONE',  ( 23.14999999999999858, -3.999999999988843147, -134.0000000000000284 ) ) ;
#247339=VERTEX_POINT ( 'NONE', #24686 ) ;
#247418=EDGE_LOOP ( 'NONE', ( #166743, #84688, #66533, #206373 ) ) ;
#247431=CARTESIAN_POINT ( 'NONE',  ( -21.45000000000000284, 7.708578643773852157, -112.8500000000000369 ) ) ;
#247450=DIRECTION ( 'NONE',  ( 1.000000000000000000, -0.000000000000000000, -0.000000000000000000 ) ) ;
#247466=CIRCLE ( 'NONE', #135008, 0.09999999999999344136 ) ;
#247467=ORIENTED_EDGE ( 'NONE', *, *, #84327, .T. ) ;
#247528=EDGE_CURVE ( 'NONE', #11869, #5875, #142127, .T. ) ;
#247544=ORIENTED_EDGE ( 'NONE', *, *, #225427, .F. ) ;
#247549=CARTESIAN_POINT ( 'NONE',  ( -18.46902351632712680, -9.509470118669714367, -107.4864539342573408 ) ) ;
#247564=CARTESIAN_POINT ( 'NONE',  ( 21.09793522318394920, 10.72462451022393282, -112.7392908709769586 ) ) ;
#247567=DIRECTION ( 'NONE',  ( -1.000000000000000000, 0.000000000000000000, 0.000000000000000000 ) ) ;
#247598=AXIS2_PLACEMENT_3D ( 'NONE', #117520, #36733, #176233 ) ;
#247609=CARTESIAN_POINT ( 'NONE',  ( -18.59999999999999787, 7.120270961708750512, -137.6595630418393625 ) ) ;
#247615=ORIENTED_EDGE ( 'NONE', *, *, #25510, .F. ) ;
#247618=CIRCLE ( 'NONE', #163850, 12.87500000000000000 ) ;
#247626=CARTESIAN_POINT ( 'NONE',  ( 20.94999999999999574, -1.249999999988843369, -108.5000000000000426 ) ) ;
#247652=AXIS2_PLACEMENT_3D ( 'NONE', #227781, #103963, #49142 ) ;
#247678=AXIS2_PLACEMENT_3D ( 'NONE', #55307, #192299, #214410 ) ;
#247720=ORIENTED_EDGE ( 'NONE', *, *, #148616, .F. ) ;
#247768=CARTESIAN_POINT ( 'NONE',  ( -21.05000000000000071, 11.65000000001115588, -107.2838656629781724 ) ) ;
#247771=CARTESIAN_POINT ( 'NONE',  ( 18.46163235739460262, -9.480150806907179373, -140.6576105398774814 ) ) ;
#247787=ADVANCED_FACE ( 'NONE', ( #137855 ), #117032, .T. ) ;
#247794=CARTESIAN_POINT ( 'NONE',  ( -22.49544290803751423, 11.74987023786864171, -100.4346880407423015 ) ) ;
#247802=ORIENTED_EDGE ( 'NONE', *, *, #238774, .F. ) ;
#247803=CYLINDRICAL_SURFACE ( 'NONE', #47349, 0.09999999999999939493 ) ;
#247807=ADVANCED_FACE ( 'NONE', ( #219973 ), #197838, .F. ) ;
#247815=DIRECTION ( 'NONE',  ( 0.000000000000000000, 0.000000000000000000, -1.000000000000000000 ) ) ;
#247865=VECTOR ( 'NONE', #115820, 1000.000000000000114 ) ;
#247881=ADVANCED_FACE ( 'NONE', ( #102560 ), #256471, .T. ) ;
#247915=DIRECTION ( 'NONE',  ( 1.000000000000000000, 1.836970198721029934E-16, 0.000000000000000000 ) ) ;
#247921=CIRCLE ( 'NONE', #181311, 7.899999999999990585 ) ;
#247931=EDGE_CURVE ( 'NONE', #26411, #124703, #4751, .T. ) ;
#247936=CARTESIAN_POINT ( 'NONE',  ( 20.85000000000000142, 1.115600667400684642E-11, -134.0000000000000284 ) ) ;
#247979=DIRECTION ( 'NONE',  ( -1.000000000000000000, -0.000000000000000000, -0.000000000000000000 ) ) ;
#247991=ORIENTED_EDGE ( 'NONE', *, *, #232382, .F. ) ;
#248007=SPHERICAL_SURFACE ( 'NONE', #205826, 0.1000000000000000056 ) ;
#248018=CIRCLE ( 'NONE', #181416, 0.1000000000000028644 ) ;
#248028=TOROIDAL_SURFACE ( 'NONE', #68993, 0.2000000000000000111, 0.1000000000000000056 ) ;
#248051=ORIENTED_EDGE ( 'NONE', *, *, #139843, .F. ) ;
#248057=ORIENTED_EDGE ( 'NONE', *, *, #111925, .F. ) ;
#248070=ORIENTED_EDGE ( 'NONE', *, *, #245447, .T. ) ;
#248079=CIRCLE ( 'NONE', #31638, 11.80000000000000426 ) ;
#248085=ORIENTED_EDGE ( 'NONE', *, *, #168100, .T. ) ;
#248092=ADVANCED_FACE ( 'NONE', ( #129849 ), #117378, .T. ) ;
#248098=DIRECTION ( 'NONE',  ( 0.000000000000000000, 0.000000000000000000, -1.000000000000000000 ) ) ;
#248101=LINE ( 'NONE', #16897, #83017 ) ;
#248103=EDGE_CURVE ( 'NONE', #208162, #70123, #67469, .T. ) ;
#248148=DIRECTION ( 'NONE',  ( -2.940209281316621016E-16, 1.000000000000000000, 0.000000000000000000 ) ) ;
#248150=ADVANCED_FACE ( 'NONE', ( #35921 ), #95850, .T. ) ;
#248179=ADVANCED_FACE ( 'NONE', ( #219658 ), #204838, .F. ) ;
#248215=CIRCLE ( 'NONE', #52562, 0.1000000000000053069 ) ;
#248272=CARTESIAN_POINT ( 'NONE',  ( 21.10257677756356642, 0.02495074957913656979, -94.10161825746727970 ) ) ;
#248305=CIRCLE ( 'NONE', #90074, 0.1000000000000028644 ) ;
#248313=VERTEX_POINT ( 'NONE', #123148 ) ;
#248324=VECTOR ( 'NONE', #5685, 1000.000000000000000 ) ;
#248358=ORIENTED_EDGE ( 'NONE', *, *, #163596, .T. ) ;
#248364=DIRECTION ( 'NONE',  ( 0.000000000000000000, 0.000000000000000000, -1.000000000000000000 ) ) ;
#248384=CARTESIAN_POINT ( 'NONE',  ( -18.52328366898031931, -9.642321089030097880, -140.7148193375701055 ) ) ;
#248389=CARTESIAN_POINT ( 'NONE',  ( 18.39999999999999858, -9.499999999988842703, -107.5320693966997112 ) ) ;
#248417=DIRECTION ( 'NONE',  ( -1.000000000000000000, 0.000000000000000000, 0.000000000000000000 ) ) ;
#248428=DIRECTION ( 'NONE',  ( 0.000000000000000000, 0.000000000000000000, -1.000000000000000000 ) ) ;
#248469=DIRECTION ( 'NONE',  ( -1.000000000000000000, 0.000000000000000000, 0.000000000000000000 ) ) ;
#248476=ADVANCED_FACE ( 'NONE', ( #216790 ), #81120, .F. ) ;
#248532=EDGE_LOOP ( 'NONE', ( #53581, #220297, #123714, #7546 ) ) ;
#248552=ORIENTED_EDGE ( 'NONE', *, *, #126182, .F. ) ;
#248592=ORIENTED_EDGE ( 'NONE', *, *, #131018, .T. ) ;
#248620=DIRECTION ( 'NONE',  ( 1.000000000000000000, 0.000000000000000000, 0.000000000000000000 ) ) ;
#248622=CARTESIAN_POINT ( 'NONE',  ( 21.05000000000000071, 8.815201804578325806, -108.9205374966854123 ) ) ;
#248647=CARTESIAN_POINT ( 'NONE',  ( 18.49999999999999289, 10.29270135741298731, -139.4573618871519614 ) ) ;
#248672=DIRECTION ( 'NONE',  ( 0.000000000000000000, 0.000000000000000000, -1.000000000000000000 ) ) ;
#248681=CARTESIAN_POINT ( 'NONE',  ( -20.94999999999999929, 1.115649653272650466E-11, -138.0000000000000284 ) ) ;
#248717=EDGE_LOOP ( 'NONE', ( #194328, #151250, #75525, #91596 ) ) ;
#248730=CARTESIAN_POINT ( 'NONE',  ( 21.14999999999999503, 1.115600667400684642E-11, -94.25000000000002842 ) ) ;
#248748=ORIENTED_EDGE ( 'NONE', *, *, #3682, .F. ) ;
#248772=EDGE_CURVE ( 'NONE', #111426, #237722, #100394, .T. ) ;
#248856=CARTESIAN_POINT ( 'NONE',  ( 18.41416235934318024, -9.499999999988844479, -140.6001893912220737 ) ) ;
#248863=CARTESIAN_POINT ( 'NONE',  ( -21.05000000000000071, 1.162701749949165642, -108.6000000000000227 ) ) ;
#248883=ORIENTED_EDGE ( 'NONE', *, *, #58526, .T. ) ;
#248885=ADVANCED_FACE ( 'NONE', ( #237021 ), #83035, .T. ) ;
#248889=DIRECTION ( 'NONE',  ( 2.952720810173289112E-16, -1.000000000000000000, 0.000000000000000000 ) ) ;
#248890=CIRCLE ( 'NONE', #165508, 0.1000000000000028644 ) ;
#248921=AXIS2_PLACEMENT_3D ( 'NONE', #182101, #199090, #158710 ) ;
#248966=CARTESIAN_POINT ( 'NONE',  ( 20.94999999999999929, 1.835341550235569663, -112.0551512925630249 ) ) ;
#249001=EDGE_CURVE ( 'NONE', #241144, #157934, #195032, .T. ) ;
#249013=ORIENTED_EDGE ( 'NONE', *, *, #34555, .F. ) ;
#249036=ORIENTED_EDGE ( 'NONE', *, *, #141799, .F. ) ;
#249078=CARTESIAN_POINT ( 'NONE',  ( 18.49362639424878552, -9.442604367877253324, -140.7644409335108264 ) ) ;
#249083=DIRECTION ( 'NONE',  ( 0.000000000000000000, 0.000000000000000000, -1.000000000000000000 ) ) ;
#249084=DIRECTION ( 'NONE',  ( -0.7071067811865475727, -0.7071067811865475727, 0.000000000000000000 ) ) ;
#249096=CARTESIAN_POINT ( 'NONE',  ( 21.98333005346336932, 1.115600667400684642E-11, -93.12592467094336257 ) ) ;
#249122=FACE_OUTER_BOUND ( 'NONE', #216302, .T. ) ;
#249123=EDGE_CURVE ( 'NONE', #91963, #49667, #12113, .T. ) ;
#249149=CARTESIAN_POINT ( 'NONE',  ( -21.05000000000000071, 0.03363273534480401561, -94.24118280531854452 ) ) ;
#249153=DIRECTION ( 'NONE',  ( 0.000000000000000000, 0.000000000000000000, -1.000000000000000000 ) ) ;
#249161=CARTESIAN_POINT ( 'NONE',  ( -20.94999999999999929, -1.835341550213257733, -112.0551512925630249 ) ) ;
#249171=CYLINDRICAL_SURFACE ( 'NONE', #136806, 0.09999999999999939493 ) ;
#249211=DIRECTION ( 'NONE',  ( 0.000000000000000000, 0.000000000000000000, -1.000000000000000000 ) ) ;
#249234=AXIS2_PLACEMENT_3D ( 'NONE', #26291, #105785, #206204 ) ;
#249238=EDGE_CURVE ( 'NONE', #257642, #238954, #208933, .T. ) ;
#249240=AXIS2_PLACEMENT_3D ( 'NONE', #235483, #116835, #94693 ) ;
#249275=CARTESIAN_POINT ( 'NONE',  ( 21.13461538461538325, 10.61458296203669249, -112.8500000000000369 ) ) ;
#249305=ORIENTED_EDGE ( 'NONE', *, *, #189576, .F. ) ;
#249313=VERTEX_POINT ( 'NONE', #165126 ) ;
#249334=VERTEX_POINT ( 'NONE', #105107 ) ;
#249341=CARTESIAN_POINT ( 'NONE',  ( -20.94999999999999929, 1.115600667400684642E-11, -100.5000000000000284 ) ) ;
#249437=VECTOR ( 'NONE', #193300, 1000.000000000000000 ) ;
#249441=EDGE_CURVE ( 'NONE', #71456, #241932, #104842, .T. ) ;
#249470=AXIS2_PLACEMENT_3D ( 'NONE', #23487, #5133, #125131 ) ;
#249494=DIRECTION ( 'NONE',  ( 0.000000000000000000, -1.000000000000000000, 0.000000000000000000 ) ) ;
#249532=EDGE_CURVE ( 'NONE', #116896, #83495, #61076, .T. ) ;
#249546=CARTESIAN_POINT ( 'NONE',  ( 18.59999999999999076, 11.65000000001115943, -125.3500000000000512 ) ) ;
#249553=CIRCLE ( 'NONE', #133030, 0.1000000000000000472 ) ;
#249557=VECTOR ( 'NONE', #238864, 1000.000000000000000 ) ;
#249630=DIRECTION ( 'NONE',  ( 0.000000000000000000, 0.000000000000000000, -1.000000000000000000 ) ) ;
#249644=ORIENTED_EDGE ( 'NONE', *, *, #163545, .F. ) ;
#249651=FACE_OUTER_BOUND ( 'NONE', #182913, .T. ) ;
#249657=ORIENTED_EDGE ( 'NONE', *, *, #153169, .F. ) ;
#249663=ORIENTED_EDGE ( 'NONE', *, *, #69175, .T. ) ;
#249687=DIRECTION ( 'NONE',  ( 1.000000000000000000, -0.000000000000000000, -0.000000000000000000 ) ) ;
#249715=CIRCLE ( 'NONE', #8115, 0.1000000000000028644 ) ;
#249727=DIRECTION ( 'NONE',  ( 1.000000000000000000, 0.000000000000000000, 0.000000000000000000 ) ) ;
#249741=DIRECTION ( 'NONE',  ( 0.000000000000000000, 0.000000000000000000, -1.000000000000000000 ) ) ;
#249746=CARTESIAN_POINT ( 'NONE',  ( -20.93302460841142931, 10.31565961587945424, -139.5364194119178478 ) ) ;
#249762=ORIENTED_EDGE ( 'NONE', *, *, #4826, .T. ) ;
#249764=CARTESIAN_POINT ( 'NONE',  ( -20.64999999999999858, 2.400000000011155432, -113.7246219227621395 ) ) ;
#249779=ADVANCED_FACE ( 'NONE', ( #111274 ), #92984, .F. ) ;
#249800=CIRCLE ( 'NONE', #178917, 0.09999999999999971412 ) ;
#249824=ORIENTED_EDGE ( 'NONE', *, *, #107633, .F. ) ;
#249852=DIRECTION ( 'NONE',  ( 1.000000000000000000, 0.000000000000000000, 0.000000000000000000 ) ) ;
#249880=LINE ( 'NONE', #71265, #20883 ) ;
#249881=CARTESIAN_POINT ( 'NONE',  ( 20.04142135623730070, 11.65000000001115943, -121.8500000000000369 ) ) ;
#249898=DIRECTION ( 'NONE',  ( 0.000000000000000000, 0.000000000000000000, -1.000000000000000000 ) ) ;
#249905=DIRECTION ( 'NONE',  ( 0.000000000000000000, -1.000000000000000000, 0.000000000000000000 ) ) ;
#249920=ADVANCED_FACE ( 'NONE', ( #175148 ), #76029, .T. ) ;
#249923=ORIENTED_EDGE ( 'NONE', *, *, #154257, .T. ) ;
#249925=ORIENTED_EDGE ( 'NONE', *, *, #249238, .T. ) ;
#249933=ADVANCED_FACE ( 'NONE', ( #60270 ), #139797, .T. ) ;
#249959=DIRECTION ( 'NONE',  ( 0.000000000000000000, 0.000000000000000000, -1.000000000000000000 ) ) ;
#249972=DIRECTION ( 'NONE',  ( -0.000000000000000000, 0.000000000000000000, 1.000000000000000000 ) ) ;
#249974=CARTESIAN_POINT ( 'NONE',  ( 22.48508240969612615, 0.04627641452807085970, -88.84998926842646938 ) ) ;
#249994=CIRCLE ( 'NONE', #96035, 7.899999999999990585 ) ;
#250007=DIRECTION ( 'NONE',  ( 0.000000000000000000, 0.000000000000000000, -1.000000000000000000 ) ) ;
#250054=DIRECTION ( 'NONE',  ( 0.000000000000000000, -1.000000000000000000, 0.000000000000000000 ) ) ;
#250067=AXIS2_PLACEMENT_3D ( 'NONE', #213433, #16541, #37391 ) ;
#250106=DIRECTION ( 'NONE',  ( -0.000000000000000000, -0.4791956752371546724, -0.8777080977375153470 ) ) ;
#250112=EDGE_LOOP ( 'NONE', ( #235163, #119322, #88103, #79033 ) ) ;
#250121=EDGE_LOOP ( 'NONE', ( #249036, #38935, #258011, #6916 ) ) ;
#250138=CARTESIAN_POINT ( 'NONE',  ( 20.95512840106819752, 10.62384869378447583, -112.7024792207986650 ) ) ;
#250144=CARTESIAN_POINT ( 'NONE',  ( 21.05000000000000071, 1.115600667400684642E-11, -100.5000000000000284 ) ) ;
#250169=FACE_OUTER_BOUND ( 'NONE', #243168, .T. ) ;
#250205=EDGE_CURVE ( 'NONE', #135831, #134210, #47107, .T. ) ;
#250212=EDGE_CURVE ( 'NONE', #54914, #37949, #147906, .T. ) ;
#250269=ORIENTED_EDGE ( 'NONE', *, *, #116265, .F. ) ;
#250281=FACE_OUTER_BOUND ( 'NONE', #250875, .T. ) ;
#250329=CARTESIAN_POINT ( 'NONE',  ( 21.05000000000000071, 1.115600667400684642E-11, -134.0000000000000284 ) ) ;
#250332=VECTOR ( 'NONE', #52204, 1000.000000000000000 ) ;
#250336=EDGE_LOOP ( 'NONE', ( #222666, #181307, #94082, #234374 ) ) ;
#250344=CARTESIAN_POINT ( 'NONE',  ( -18.59999999999999787, 7.021664781911246322, -137.8335654018973457 ) ) ;
#250345=DIRECTION ( 'NONE',  ( -0.000000000000000000, 0.8660254037844383745, -0.5000000000000003331 ) ) ;
#250368=VERTEX_POINT ( 'NONE', #156540 ) ;
#250463=EDGE_LOOP ( 'NONE', ( #120648, #129909, #180742, #234890 ) ) ;
#250470=CARTESIAN_POINT ( 'NONE',  ( 20.04142135623730070, 11.75000000001115907, -88.75000000000004263 ) ) ;
#250492=AXIS2_PLACEMENT_3D ( 'NONE', #24670, #100295, #101568 ) ;
#250503=EDGE_CURVE ( 'NONE', #173650, #67578, #68981, .T. ) ;
#250508=LINE ( 'NONE', #215247, #226002 ) ;
#250575=DIRECTION ( 'NONE',  ( 0.000000000000000000, 0.9908441862701596881, -0.1350103645451904977 ) ) ;
#250577=VERTEX_POINT ( 'NONE', #54520 ) ;
#250578=ADVANCED_FACE ( 'NONE', ( #212337 ), #136609, .T. ) ;
#250583=AXIS2_PLACEMENT_3D ( 'NONE', #129581, #72188, #112589 ) ;
#250594=LINE ( 'NONE', #30286, #239810 ) ;
#250645=LINE ( 'NONE', #91592, #194574 ) ;
#250656=CIRCLE ( 'NONE', #96698, 0.09999999999999939493 ) ;
#250663=AXIS2_PLACEMENT_3D ( 'NONE', #235660, #58297, #34944 ) ;
#250685=DIRECTION ( 'NONE',  ( 1.000000000000000000, 0.000000000000000000, 0.000000000000000000 ) ) ;
#250688=CIRCLE ( 'NONE', #88158, 0.09999999999999363565 ) ;
#250691=AXIS2_PLACEMENT_3D ( 'NONE', #173181, #74062, #153617 ) ;
#250697=DIRECTION ( 'NONE',  ( 1.000000000000000000, 0.000000000000000000, 0.000000000000000000 ) ) ;
#250705=CIRCLE ( 'NONE', #59137, 0.09999999999998898659 ) ;
#250712=DIRECTION ( 'NONE',  ( 0.000000000000000000, -0.5000000000000275335, -0.8660254037844228314 ) ) ;
#250762=APPLICATION_CONTEXT ( 'automotive_design' ) ;
#250770=ORIENTED_EDGE ( 'NONE', *, *, #62317, .T. ) ;
#250791=ORIENTED_EDGE ( 'NONE', *, *, #138619, .T. ) ;
#250811=CIRCLE ( 'NONE', #163337, 1.900000000000012790 ) ;
#250813=EDGE_CURVE ( 'NONE', #177002, #249313, #42655, .T. ) ;
#250818=DIRECTION ( 'NONE',  ( 0.000000000000000000, 0.1568667991644863147, -0.9876197685951252359 ) ) ;
#250820=CARTESIAN_POINT ( 'NONE',  ( -20.85000000000000142, -1.835859311432479268, -145.5044391687985694 ) ) ;
#250824=CARTESIAN_POINT ( 'NONE',  ( 23.24999999999999645, 1.115600667400684642E-11, -134.0000000000000284 ) ) ;
#250826=CARTESIAN_POINT ( 'NONE',  ( -18.59999999999999787, -1.164121893230052995, -141.9148480855716343 ) ) ;
#250828=PLANE ( 'NONE',  #212549 ) ;
#250843=AXIS2_PLACEMENT_3D ( 'NONE', #130253, #12916, #94980 ) ;
#250848=ORIENTED_EDGE ( 'NONE', *, *, #29377, .F. ) ;
#250852=EDGE_CURVE ( 'NONE', #115014, #151151, #63926, .T. ) ;
#250875=EDGE_LOOP ( 'NONE', ( #145796, #120087, #188059, #162745 ) ) ;
#250892=DIRECTION ( 'NONE',  ( 0.000000000000000000, 0.2605042016806672911, -0.9654727137038716656 ) ) ;
#250905=DIRECTION ( 'NONE',  ( 2.659396599871503635E-15, 0.6132151058540549204, -0.7899159663865520375 ) ) ;
#250923=DIRECTION ( 'NONE',  ( 0.000000000000000000, 0.000000000000000000, -1.000000000000000000 ) ) ;
#250933=CARTESIAN_POINT ( 'NONE',  ( 18.47654891039378100, -9.465274948371153130, -107.6259759051946787 ) ) ;
#250958=CARTESIAN_POINT ( 'NONE',  ( 22.01447462590973458, 0.09903700007069084210, -93.23619979877013009 ) ) ;
#250962=EDGE_CURVE ( 'NONE', #162338, #58778, #168023, .T. ) ;
#250966=CARTESIAN_POINT ( 'NONE',  ( -22.39999999999999858, 11.75000000001115552, -100.5000000000000284 ) ) ;
#250974=CARTESIAN_POINT ( 'NONE',  ( 20.22516295850462598, 9.899364295460458152, -108.4100657120914235 ) ) ;
#250990=CIRCLE ( 'NONE', #9401, 0.09999999999999939493 ) ;
#250996=CARTESIAN_POINT ( 'NONE',  ( 21.05000000000000071, 5.000000000011153745, -121.5947339810869465 ) ) ;
#251004=DIRECTION ( 'NONE',  ( 1.000000000000000000, 3.265361837132813093E-16, -0.000000000000000000 ) ) ;
#251005=CARTESIAN_POINT ( 'NONE',  ( 20.85000000000000142, 11.75000000001115907, -127.2161343370219413 ) ) ;
#251022=ORIENTED_EDGE ( 'NONE', *, *, #215972, .F. ) ;
#251023=CIRCLE ( 'NONE', #55369, 0.1000000000000028644 ) ;
#251064=EDGE_CURVE ( 'NONE', #254860, #150422, #91533, .T. ) ;
#251075=CARTESIAN_POINT ( 'NONE',  ( -18.50000000000000000, 7.021664781911246322, -137.6335654018973287 ) ) ;
#251117=ORIENTED_EDGE ( 'NONE', *, *, #73456, .T. ) ;
#251121=LINE ( 'NONE', #236700, #57308 ) ;
#251143=CIRCLE ( 'NONE', #255202, 0.1000000000000002554 ) ;
#251145=FACE_OUTER_BOUND ( 'NONE', #246429, .T. ) ;
#251146=TOROIDAL_SURFACE ( 'NONE', #38798, 0.2000000000000000111, 0.1000000000000000056 ) ;
#251147=AXIS2_PLACEMENT_3D ( 'NONE', #168501, #247979, #218448 ) ;
#251158=EDGE_LOOP ( 'NONE', ( #41647, #34227, #68134, #62119, #34822, #170642, #181415, #143942, #15446, #228030, #139826, #40906, #666, #254921 ) ) ;
#251189=DIRECTION ( 'NONE',  ( 0.000000000000000000, 0.000000000000000000, -1.000000000000000000 ) ) ;
#251190=CARTESIAN_POINT ( 'NONE',  ( 23.14999999999999503, 11.65000000001116298, -126.9851942293460922 ) ) ;
#251217=FACE_OUTER_BOUND ( 'NONE', #246635, .T. ) ;
#251254=EDGE_CURVE ( 'NONE', #241330, #208598, #64102, .T. ) ;
#251272=ORIENTED_EDGE ( 'NONE', *, *, #87254, .T. ) ;
#251289=DIRECTION ( 'NONE',  ( -1.000000000000000000, -2.952720810173289112E-16, 0.000000000000000000 ) ) ;
#251292=DIRECTION ( 'NONE',  ( -0.7071067811865388020, 0.7071067811865561215, 0.000000000000000000 ) ) ;
#251325=ORIENTED_EDGE ( 'NONE', *, *, #179863, .F. ) ;
#251331=VECTOR ( 'NONE', #247450, 1000.000000000000000 ) ;
#251346=ORIENTED_EDGE ( 'NONE', *, *, #223156, .F. ) ;
#251349=DIRECTION ( 'NONE',  ( 0.000000000000000000, 0.5000000000000078826, -0.8660254037844340447 ) ) ;
#251358=DIRECTION ( 'NONE',  ( 0.000000000000000000, 0.000000000000000000, 1.000000000000000000 ) ) ;
#251410=ORIENTED_EDGE ( 'NONE', *, *, #62305, .T. ) ;
#251415=FACE_OUTER_BOUND ( 'NONE', #196387, .T. ) ;
#251416=CIRCLE ( 'NONE', #5682, 0.09999999999999824307 ) ;
#251425=FACE_OUTER_BOUND ( 'NONE', #169941, .T. ) ;
#251457=DIRECTION ( 'NONE',  ( 0.000000000000000000, 0.000000000000000000, -1.000000000000000000 ) ) ;
#251484=CONICAL_SURFACE ( 'NONE', #230861, 4.299999999999956302, 0.7853981633974466137 ) ;
#251489=CARTESIAN_POINT ( 'NONE',  ( -18.59999999999999787, 1.736257131608553550, -112.0686523290175245 ) ) ;
#251558=VECTOR ( 'NONE', #191206, 999.9999999999998863 ) ;
#251571=VERTEX_POINT ( 'NONE', #162987 ) ;
#251586=LINE ( 'NONE', #49539, #165379 ) ;
#251596=CARTESIAN_POINT ( 'NONE',  ( 21.05000000000000071, 10.72371710471867701, -108.1649135690876449 ) ) ;
#251600=AXIS2_PLACEMENT_3D ( 'NONE', #214492, #158416, #35889 ) ;
#251602=CARTESIAN_POINT ( 'NONE',  ( 21.14999999999999858, -11.74999999998884448, -112.7500000000000284 ) ) ;
#251628=CARTESIAN_POINT ( 'NONE',  ( 18.37172112093886511, -9.570961652231645189, -140.8167344534842300 ) ) ;
#251630=DIRECTION ( 'NONE',  ( 4.408576920032447355E-17, -0.1350103645451876666, 0.9908441862701600211 ) ) ;
#251639=CIRCLE ( 'NONE', #76840, 0.09999999999999939493 ) ;
#251664=DIRECTION ( 'NONE',  ( 0.000000000000000000, 0.000000000000000000, -1.000000000000000000 ) ) ;
#251720=ORIENTED_EDGE ( 'NONE', *, *, #184609, .F. ) ;
#251735=DIRECTION ( 'NONE',  ( -1.000000000000000000, 0.000000000000000000, 0.000000000000000000 ) ) ;
#251813=DIRECTION ( 'NONE',  ( 1.000000000000000000, -0.000000000000000000, -0.000000000000000000 ) ) ;
#251824=CARTESIAN_POINT ( 'NONE',  ( 21.14999999999999503, -11.74999999998883560, -103.4000000000000341 ) ) ;
#251826=ADVANCED_FACE ( 'NONE', ( #98782 ), #55810, .F. ) ;
#251843=ADVANCED_FACE ( 'NONE', ( #97505 ), #6190, .T. ) ;
#251847=TOROIDAL_SURFACE ( 'NONE', #39518, 12.97499999999999609, 0.1000000000000000056 ) ;
#251854=LINE ( 'NONE', #216585, #234300 ) ;
#251860=ORIENTED_EDGE ( 'NONE', *, *, #258058, .F. ) ;
#251867=VECTOR ( 'NONE', #229320, 1000.000000000000000 ) ;
#251947=CIRCLE ( 'NONE', #106180, 0.09999999999998898659 ) ;
#251957=DIRECTION ( 'NONE',  ( 1.000000000000000000, -0.000000000000000000, 0.000000000000000000 ) ) ;
#252030=ADVANCED_FACE ( 'NONE', ( #201765 ), #110250, .T. ) ;
#252044=CARTESIAN_POINT ( 'NONE',  ( 23.14999999999999858, 1.115600667400684642E-11, -134.0000000000000284 ) ) ;
#252054=CARTESIAN_POINT ( 'NONE',  ( 21.14999999999999858, 11.75000000001116263, -112.6500000000000341 ) ) ;
#252081=AXIS2_PLACEMENT_3D ( 'NONE', #180667, #4569, #46267 ) ;
#252086=FACE_OUTER_BOUND ( 'NONE', #129388, .T. ) ;
#252089=VECTOR ( 'NONE', #60914, 1000.000000000000000 ) ;
#252137=DIRECTION ( 'NONE',  ( 1.000000000000000000, 0.000000000000000000, 0.000000000000000000 ) ) ;
#252154=ADVANCED_FACE ( 'NONE', ( #32151 ), #102208, .T. ) ;
#252202=CIRCLE ( 'NONE', #18971, 2.100000000000002309 ) ;
#252203=ADVANCED_FACE ( 'NONE', ( #15138 ), #217155, .F. ) ;
#252212=CYLINDRICAL_SURFACE ( 'NONE', #64197, 0.5000000000000004441 ) ;
#252224=CARTESIAN_POINT ( 'NONE',  ( 21.00000000000000000, 9.750000000011153745, -121.7500000000000426 ) ) ;
#252247=DIRECTION ( 'NONE',  ( 0.000000000000000000, 1.000000000000000000, 0.000000000000000000 ) ) ;
#252259=EDGE_CURVE ( 'NONE', #49667, #124745, #64640, .T. ) ;
#252261=CARTESIAN_POINT ( 'NONE',  ( 20.21567752745019320, 10.19811410124265905, -108.3826203476516810 ) ) ;
#252273=EDGE_CURVE ( 'NONE', #37616, #162687, #210421, .T. ) ;
#252274=DIRECTION ( 'NONE',  ( 0.000000000000000000, 0.000000000000000000, -1.000000000000000000 ) ) ;
#252414=CARTESIAN_POINT ( 'NONE',  ( 18.59999999999997655, 1.115600667400684642E-11, -134.0000000000000284 ) ) ;
#252446=ORIENTED_EDGE ( 'NONE', *, *, #155622, .F. ) ;
#252452=ORIENTED_EDGE ( 'NONE', *, *, #147786, .T. ) ;
#252457=LINE ( 'NONE', #12608, #59117 ) ;
#252518=DIRECTION ( 'NONE',  ( 1.000000000000000000, -0.000000000000000000, -0.000000000000000000 ) ) ;
#252554=DIRECTION ( 'NONE',  ( 0.000000000000000000, 0.000000000000000000, 1.000000000000000000 ) ) ;
#252556=CYLINDRICAL_SURFACE ( 'NONE', #3528, 11.74999999999999645 ) ;
#252569=EDGE_LOOP ( 'NONE', ( #125827, #214329, #110950, #204574 ) ) ;
#252571=DIRECTION ( 'NONE',  ( 0.000000000000000000, 8.881784197000696176E-16, -1.000000000000000000 ) ) ;
#252610=EDGE_LOOP ( 'NONE', ( #247544, #54205, #107962, #8505 ) ) ;
#252630=CARTESIAN_POINT ( 'NONE',  ( -18.59999999999999787, 11.65000000001115232, -107.5148057706540357 ) ) ;
#252689=DIRECTION ( 'NONE',  ( 0.000000000000000000, -1.000000000000000000, 0.000000000000000000 ) ) ;
#252690=DIRECTION ( 'NONE',  ( 0.000000000000000000, 1.000000000000000000, 0.000000000000000000 ) ) ;
#252716=ORIENTED_EDGE ( 'NONE', *, *, #18776, .T. ) ;
#252775=ORIENTED_EDGE ( 'NONE', *, *, #143760, .F. ) ;
#252838=CARTESIAN_POINT ( 'NONE',  ( 21.14999999999999858, 10.71339244341104013, -112.7500000000000284 ) ) ;
#252865=ORIENTED_EDGE ( 'NONE', *, *, #39955, .T. ) ;
#252887=CIRCLE ( 'NONE', #207120, 0.1999999999999987899 ) ;
#252896=LINE ( 'NONE', #57245, #71829 ) ;
#252923=VERTEX_POINT ( 'NONE', #174794 ) ;
#252926=CARTESIAN_POINT ( 'NONE',  ( -22.49072729836729678, 0.05648193274477467801, -88.84999175084509204 ) ) ;
#252962=DIRECTION ( 'NONE',  ( 0.000000000000000000, 0.1350103645451876666, -0.9908441862701600211 ) ) ;
#252996=ORIENTED_EDGE ( 'NONE', *, *, #165966, .F. ) ;
#253019=EDGE_CURVE ( 'NONE', #39812, #247339, #7480, .T. ) ;
#253025=VERTEX_POINT ( 'NONE', #222664 ) ;
#253062=CARTESIAN_POINT ( 'NONE',  ( 21.11345278033283179, 8.882122073382040739, -112.7460221707548698 ) ) ;
#253084=VERTEX_POINT ( 'NONE', #53021 ) ;
#253104=ORIENTED_EDGE ( 'NONE', *, *, #90291, .F. ) ;
#253130=CARTESIAN_POINT ( 'NONE',  ( 18.60000000000000853, -9.364236010355611484, -107.6802544007246354 ) ) ;
#253135=VERTEX_POINT ( 'NONE', #78977 ) ;
#253172=ORIENTED_EDGE ( 'NONE', *, *, #21198, .T. ) ;
#253190=ORIENTED_EDGE ( 'NONE', *, *, #192194, .T. ) ;
#253202=DIRECTION ( 'NONE',  ( 0.000000000000000000, -0.000000000000000000, 1.000000000000000000 ) ) ;
#253209=AXIS2_PLACEMENT_3D ( 'NONE', #166080, #104748, #26550 ) ;
#253242=DIRECTION ( 'NONE',  ( 0.000000000000000000, 1.000000000000000000, 0.000000000000000000 ) ) ;
#253255=ORIENTED_EDGE ( 'NONE', *, *, #42198, .F. ) ;
#253290=FACE_OUTER_BOUND ( 'NONE', #184214, .T. ) ;
#253293=VECTOR ( 'NONE', #179600, 1000.000000000000000 ) ;
#253301=VERTEX_POINT ( 'NONE', #202807 ) ;
#253335=DIRECTION ( 'NONE',  ( 1.000000000000000000, 0.000000000000000000, 0.000000000000000000 ) ) ;
#253353=FACE_OUTER_BOUND ( 'NONE', #224779, .T. ) ;
#253365=LINE ( 'NONE', #35643, #102360 ) ;
#253382=CARTESIAN_POINT ( 'NONE',  ( 23.14999999999999858, 5.000000000011153745, -121.5947339810869465 ) ) ;
#253389=ADVANCED_FACE ( 'NONE', ( #210524 ), #153157, .F. ) ;
#253423=DIRECTION ( 'NONE',  ( -1.000000000000000000, 0.000000000000000000, 0.000000000000000000 ) ) ;
#253427=ADVANCED_FACE ( 'NONE', ( #174009 ), #213078, .F. ) ;
#253444=ORIENTED_EDGE ( 'NONE', *, *, #94095, .T. ) ;
#253457=( BOUNDED_SURFACE ( )  B_SPLINE_SURFACE ( 3, 2, ( 
 ( #11785, #30063, #89996 ),
 ( #110852, #65305, #167017 ),
 ( #88695, #247794, #229530 ),
 ( #67872, #48311, #50851 ) ),
 .UNSPECIFIED., .F., .F., .F. ) 
 B_SPLINE_SURFACE_WITH_KNOTS ( ( 4, 4 ),
 ( 3, 3 ),
 ( 0.0006461284895274040097, 0.0007503702773986315041 ),
 ( 0.000000000000000000, 1.000000000000000000 ),
 .UNSPECIFIED. ) 
 GEOMETRIC_REPRESENTATION_ITEM ( )  RATIONAL_B_SPLINE_SURFACE ( (
 ( 1.000000000000000000, 0.7071067811865475727, 1.000000000000000000),
 ( 1.000000000000000000, 0.7076476444649029141, 1.000000000000000000),
 ( 1.000000000000000000, 0.7075727925191180878, 1.000000000000000000),
 ( 1.000000000000000000, 0.7071067811865719976, 1.000000000000000000) ) ) 
 REPRESENTATION_ITEM ( '' )  SURFACE ( )  );
#253475=CIRCLE ( 'NONE', #41130, 0.1000000000000028644 ) ;
#253490=AXIS2_PLACEMENT_3D ( 'NONE', #106881, #135092, #213350 ) ;
#253571=ORIENTED_EDGE ( 'NONE', *, *, #200496, .T. ) ;
#253581=ORIENTED_EDGE ( 'NONE', *, *, #185636, .F. ) ;
#253612=LINE ( 'NONE', #112838, #7907 ) ;
#253637=DIRECTION ( 'NONE',  ( 0.000000000000000000, -8.673617379883787770E-15, 1.000000000000000000 ) ) ;
#253654=CARTESIAN_POINT ( 'NONE',  ( -21.13435531349828267, 6.493721063603252297, -100.5000000000000284 ) ) ;
#253659=EDGE_CURVE ( 'NONE', #74892, #110439, #117831, .T. ) ;
#253679=CARTESIAN_POINT ( 'NONE',  ( 23.24999999999999645, 1.115600667400684642E-11, -100.5000000000000284 ) ) ;
#253683=VERTEX_POINT ( 'NONE', #62993 ) ;
#253689=AXIS2_PLACEMENT_3D ( 'NONE', #68960, #252689, #226712 ) ;
#253715=AXIS2_PLACEMENT_3D ( 'NONE', #208673, #7903, #144804 ) ;
#253721=DIRECTION ( 'NONE',  ( 0.000000000000000000, -0.9908441862701596881, 0.1350103645451904977 ) ) ;
#253736=ADVANCED_FACE ( 'NONE', ( #44730 ), #87678, .T. ) ;
#253746=CARTESIAN_POINT ( 'NONE',  ( 20.94999999999999574, 6.400000000011158541, -110.4304246300616086 ) ) ;
#253756=EDGE_LOOP ( 'NONE', ( #211801, #188732, #67306, #148632, #80570, #114797, #238279, #59998, #120021, #62368, #126372, #258056, #199285, #55071, #138388, #53122 ) ) ;
#253757=CARTESIAN_POINT ( 'NONE',  ( 18.59999999999999076, 11.65000000001115943, -125.3500000000000512 ) ) ;
#253765=CARTESIAN_POINT ( 'NONE',  ( 18.55121869061587958, 10.32747123227773400, -139.5774032850249569 ) ) ;
#253775=EDGE_LOOP ( 'NONE', ( #70295, #89775, #46332, #51456 ) ) ;
#253795=EDGE_CURVE ( 'NONE', #45115, #146870, #223022, .T. ) ;
#253797=DIRECTION ( 'NONE',  ( -1.000000000000000000, 0.000000000000000000, 0.000000000000000000 ) ) ;
#253804=DIRECTION ( 'NONE',  ( 0.000000000000000000, 0.000000000000000000, -1.000000000000000000 ) ) ;
#253810=FACE_OUTER_BOUND ( 'NONE', #87658, .T. ) ;
#253812=LINE ( 'NONE', #152192, #71752 ) ;
#253834=DIRECTION ( 'NONE',  ( 0.000000000000000000, 0.000000000000000000, -1.000000000000000000 ) ) ;
#253856=CYLINDRICAL_SURFACE ( 'NONE', #76693, 0.09999999999999892308 ) ;
#253865=VERTEX_POINT ( 'NONE', #49849 ) ;
#253867=EDGE_CURVE ( 'NONE', #151223, #185811, #229774, .T. ) ;
#253879=CIRCLE ( 'NONE', #199754, 11.70000000000000284 ) ;
#253881=ORIENTED_EDGE ( 'NONE', *, *, #173785, .F. ) ;
#253946=DIRECTION ( 'NONE',  ( 0.000000000000000000, 0.000000000000000000, -1.000000000000000000 ) ) ;
#253972=CARTESIAN_POINT ( 'NONE',  ( 20.95132126680579887, 10.48994987015794322, -108.0703245384345621 ) ) ;
#254030=CARTESIAN_POINT ( 'NONE',  ( 21.05000000000000071, -11.74999999998883560, -103.4000000000000341 ) ) ;
#254051=CYLINDRICAL_SURFACE ( 'NONE', #170603, 0.09999999999999939493 ) ;
#254074=ORIENTED_EDGE ( 'NONE', *, *, #36632, .F. ) ;
#254097=FACE_OUTER_BOUND ( 'NONE', #122336, .T. ) ;
#254105=DIRECTION ( 'NONE',  ( 1.000000000000000000, 0.000000000000000000, 0.000000000000000000 ) ) ;
#254144=ORIENTED_EDGE ( 'NONE', *, *, #128146, .T. ) ;
#254176=EDGE_CURVE ( 'NONE', #129441, #169534, #23343, .T. ) ;
#254205=DIRECTION ( 'NONE',  ( 1.000000000000000000, 0.000000000000000000, 0.000000000000000000 ) ) ;
#254226=ORIENTED_EDGE ( 'NONE', *, *, #7197, .F. ) ;
#254237=CARTESIAN_POINT ( 'NONE',  ( 22.49999999999999645, 11.64976291804307884, -100.4111900236131021 ) ) ;
#254293=FACE_OUTER_BOUND ( 'NONE', #236281, .T. ) ;
#254304=CIRCLE ( 'NONE', #196068, 0.2000000000000057288 ) ;
#254318=CARTESIAN_POINT ( 'NONE',  ( -23.15000000000000213, -11.64999999998884483, -130.9000000000000341 ) ) ;
#254324=VERTEX_POINT ( 'NONE', #159894 ) ;
#254344=AXIS2_PLACEMENT_3D ( 'NONE', #115106, #237628, #257130 ) ;
#254352=LINE ( 'NONE', #245719, #50382 ) ;
#254361=CARTESIAN_POINT ( 'NONE',  ( -18.59999999999999787, -1.149570369564537842, -141.8159124845019790 ) ) ;
#254374=LINE ( 'NONE', #94034, #10121 ) ;
#254460=DIRECTION ( 'NONE',  ( 0.000000000000000000, 0.000000000000000000, -1.000000000000000000 ) ) ;
#254473=CIRCLE ( 'NONE', #21304, 12.87499999999999822 ) ;
#254484=CARTESIAN_POINT ( 'NONE',  ( -20.64999999999999858, 2.500000000011154633, -120.7753780772379315 ) ) ;
#254526=ADVANCED_FACE ( 'NONE', ( #170198 ), #94450, .T. ) ;
#254534=DIRECTION ( 'NONE',  ( -1.000000000000000000, 0.000000000000000000, 0.000000000000000000 ) ) ;
#254548=AXIS2_PLACEMENT_3D ( 'NONE', #239200, #37167, #241759 ) ;
#254582=DIRECTION ( 'NONE',  ( 0.000000000000000000, 1.000000000000000000, 0.000000000000000000 ) ) ;
#254584=ADVANCED_FACE ( 'NONE', ( #150588 ), #129731, .F. ) ;
#254601=DIRECTION ( 'NONE',  ( -1.000000000000000000, 0.000000000000000000, 0.000000000000000000 ) ) ;
#254619=DIRECTION ( 'NONE',  ( 1.000000000000000000, 0.000000000000000000, -0.000000000000000000 ) ) ;
#254631=LINE ( 'NONE', #19919, #82 ) ;
#254645=DIRECTION ( 'NONE',  ( 0.000000000000000000, -0.9876197685951252359, -0.1568667991644863424 ) ) ;
#254655=FACE_OUTER_BOUND ( 'NONE', #529, .T. ) ;
#254670=VECTOR ( 'NONE', #92713, 1000.000000000000000 ) ;
#254671=AXIS2_PLACEMENT_3D ( 'NONE', #167720, #204239, #24352 ) ;
#254690=CARTESIAN_POINT ( 'NONE',  ( 21.05000000000000071, 6.650000000011155876, -110.5170271704400591 ) ) ;
#254701=ORIENTED_EDGE ( 'NONE', *, *, #142671, .T. ) ;
#254707=ADVANCED_FACE ( 'NONE', ( #61750 ), #141292, .T. ) ;
#254712=ORIENTED_EDGE ( 'NONE', *, *, #92875, .F. ) ;
#254785=DIRECTION ( 'NONE',  ( 0.000000000000000000, 0.000000000000000000, -1.000000000000000000 ) ) ;
#254801=EDGE_CURVE ( 'NONE', #216892, #185811, #111155, .T. ) ;
#254829=VECTOR ( 'NONE', #246134, 1000.000000000000000 ) ;
#254831=DIRECTION ( 'NONE',  ( 0.000000000000000000, 0.000000000000000000, -1.000000000000000000 ) ) ;
#254843=CARTESIAN_POINT ( 'NONE',  ( -18.50000000000000000, -1.164121893230052995, -141.7148480855716457 ) ) ;
#254850=EDGE_CURVE ( 'NONE', #160408, #177524, #250645, .T. ) ;
#254860=VERTEX_POINT ( 'NONE', #208964 ) ;
#254862=DIRECTION ( 'NONE',  ( 0.000000000000000000, 0.000000000000000000, 1.000000000000000000 ) ) ;
#254870=ORIENTED_EDGE ( 'NONE', *, *, #253867, .F. ) ;
#254891=CARTESIAN_POINT ( 'NONE',  ( -20.85000000000000142, 7.021664781911246322, -137.7335654018973514 ) ) ;
#254902=CARTESIAN_POINT ( 'NONE',  ( -21.05000000000000071, -1.835341550213257733, -112.0551512925630249 ) ) ;
#254911=CARTESIAN_POINT ( 'NONE',  ( 20.95512820512820440, 10.62384868372303615, -121.7500000000000426 ) ) ;
#254921=ORIENTED_EDGE ( 'NONE', *, *, #163530, .T. ) ;
#254965=ORIENTED_EDGE ( 'NONE', *, *, #245354, .T. ) ;
#254971=EDGE_CURVE ( 'NONE', #245888, #224306, #211119, .T. ) ;
#255003=ORIENTED_EDGE ( 'NONE', *, *, #116010, .T. ) ;
#255006=CARTESIAN_POINT ( 'NONE',  ( -18.50000000000000000, 1.340746217944851715, -90.22713749457885513 ) ) ;
#255037=AXIS2_PLACEMENT_3D ( 'NONE', #250820, #134716, #192165 ) ;
#255048=VERTEX_POINT ( 'NONE', #236232 ) ;
#255054=ADVANCED_FACE ( 'NONE', ( #198393 ), #38061, .F. ) ;
#255064=ORIENTED_EDGE ( 'NONE', *, *, #255216, .F. ) ;
#255087=VECTOR ( 'NONE', #153291, 1000.000000000000000 ) ;
#255138=CARTESIAN_POINT ( 'NONE',  ( -20.85000000000000142, 1.115600667400684642E-11, -134.0000000000000284 ) ) ;
#255150=SPHERICAL_SURFACE ( 'NONE', #103031, 0.1000000000000000056 ) ;
#255159=VERTEX_POINT ( 'NONE', #84828 ) ;
#255202=AXIS2_PLACEMENT_3D ( 'NONE', #205756, #246181, #46673 ) ;
#255205=DIRECTION ( 'NONE',  ( 0.000000000000000000, -1.000000000000000000, -0.000000000000000000 ) ) ;
#255216=EDGE_CURVE ( 'NONE', #126709, #163726, #112010, .T. ) ;
#255218=DIRECTION ( 'NONE',  ( 1.000000000000000000, 0.000000000000000000, -0.000000000000000000 ) ) ;
#255340=AXIS2_PLACEMENT_3D ( 'NONE', #36318, #237067, #53300 ) ;
#255358=LINE ( 'NONE', #156353, #184772 ) ;
#255372=ORIENTED_EDGE ( 'NONE', *, *, #35662, .T. ) ;
#255410=ADVANCED_FACE ( 'NONE', ( #213800 ), #255440, .T. ) ;
#255412=DIRECTION ( 'NONE',  ( 0.000000000000000000, 0.000000000000000000, -1.000000000000000000 ) ) ;
#255439=CARTESIAN_POINT ( 'NONE',  ( -21.05000000000000071, 5.900000000011162093, -123.7809002353436654 ) ) ;
#255440=CYLINDRICAL_SURFACE ( 'NONE', #238292, 0.09999999999998898659 ) ;
#255441=EDGE_CURVE ( 'NONE', #2430, #16782, #195153, .T. ) ;
#255456=AXIS2_PLACEMENT_3D ( 'NONE', #190712, #86407, #225913 ) ;
#255459=ORIENTED_EDGE ( 'NONE', *, *, #17679, .F. ) ;
#255472=LINE ( 'NONE', #73081, #87468 ) ;
#255483=DIRECTION ( 'NONE',  ( -1.000000000000000000, 0.000000000000000000, 0.000000000000000000 ) ) ;
#255485=CARTESIAN_POINT ( 'NONE',  ( -22.14074124539699895, 0.09905289585522827900, -93.10992214895625807 ) ) ;
#255543=EDGE_CURVE ( 'NONE', #26647, #88045, #200888, .T. ) ;
#255563=AXIS2_PLACEMENT_3D ( 'NONE', #194897, #174074, #56606 ) ;
#255603=EDGE_CURVE ( 'NONE', #149981, #185072, #121799, .T. ) ;
#255619=ORIENTED_EDGE ( 'NONE', *, *, #143676, .T. ) ;
#255638=AXIS2_PLACEMENT_3D ( 'NONE', #178863, #217920, #127510 ) ;
#255654=ORIENTED_EDGE ( 'NONE', *, *, #146766, .F. ) ;
#255666=ORIENTED_EDGE ( 'NONE', *, *, #78423, .F. ) ;
#255700=VERTEX_POINT ( 'NONE', #53128 ) ;
#255718=ADVANCED_FACE ( 'NONE', ( #148389 ), #38578, .T. ) ;
#255726=EDGE_CURVE ( 'NONE', #39812, #36453, #171703, .T. ) ;
#255751=ORIENTED_EDGE ( 'NONE', *, *, #99099, .F. ) ;
#255858=CARTESIAN_POINT ( 'NONE',  ( -18.57399277249657032, 10.33112638556969465, -139.5901228926975080 ) ) ;
#255883=ORIENTED_EDGE ( 'NONE', *, *, #81399, .F. ) ;
#255889=CYLINDRICAL_SURFACE ( 'NONE', #26501, 0.09999999999998898659 ) ;
#255899=CARTESIAN_POINT ( 'NONE',  ( 22.16821283564876666, 7.558973340791918183, -100.5000000000000284 ) ) ;
#255943=AXIS2_PLACEMENT_3D ( 'NONE', #157273, #94696, #38584 ) ;
#255959=ORIENTED_EDGE ( 'NONE', *, *, #34130, .F. ) ;
#255971=EDGE_CURVE ( 'NONE', #144465, #167927, #80364, .T. ) ;
#255983=DIRECTION ( 'NONE',  ( 0.000000000000000000, 0.000000000000000000, -1.000000000000000000 ) ) ;
#256028=LINE ( 'NONE', #159565, #190303 ) ;
#256031=EDGE_CURVE ( 'NONE', #99810, #50561, #184488, .T. ) ;
#256034=ORIENTED_EDGE ( 'NONE', *, *, #93278, .T. ) ;
#256035=B_SPLINE_CURVE_WITH_KNOTS ( 'NONE', 3,
 ( #240392, #61747, #46027, #141286, #121742, #181701 ),
 .UNSPECIFIED., .F., .F.,
 ( 4, 2, 4 ),
 ( 0.000000000000000000, 0.0002113392456166019308, 0.0004226784912332038615 ),
 .UNSPECIFIED. ) ;
#256038=DIRECTION ( 'NONE',  ( 0.000000000000000000, 1.776356839400277286E-15, -1.000000000000000000 ) ) ;
#256055=EDGE_LOOP ( 'NONE', ( #24800, #174889, #139065, #95287 ) ) ;
#256071=CYLINDRICAL_SURFACE ( 'NONE', #43076, 11.80000000000000426 ) ;
#256103=LINE ( 'NONE', #237889, #145338 ) ;
#256159=AXIS2_PLACEMENT_3D ( 'NONE', #150958, #148393, #149697 ) ;
#256191=CARTESIAN_POINT ( 'NONE',  ( 18.59999999999999076, 6.450000000011156587, -110.5170271704400591 ) ) ;
#256226=EDGE_CURVE ( 'NONE', #255048, #50561, #117618, .T. ) ;
#256227=CYLINDRICAL_SURFACE ( 'NONE', #197055, 0.09999999999998898659 ) ;
#256289=ORIENTED_EDGE ( 'NONE', *, *, #243354, .T. ) ;
#256295=CYLINDRICAL_SURFACE ( 'NONE', #23089, 4.049999999999998046 ) ;
#256334=VERTEX_POINT ( 'NONE', #235819 ) ;
#256336=TOROIDAL_SURFACE ( 'NONE', #52386, 0.6000000000000013101, 0.1000000000000000056 ) ;
#256345=ORIENTED_EDGE ( 'NONE', *, *, #122991, .F. ) ;
#256383=VERTEX_POINT ( 'NONE', #134149 ) ;
#256386=DIRECTION ( 'NONE',  ( 0.000000000000000000, -1.000000000000000000, 0.000000000000000000 ) ) ;
#256411=ORIENTED_EDGE ( 'NONE', *, *, #173785, .T. ) ;
#256426=CARTESIAN_POINT ( 'NONE',  ( 20.85000000000000142, -1.835859311432481045, -145.5044391687985694 ) ) ;
#256471=SPHERICAL_SURFACE ( 'NONE', #175647, 0.1000000000000000056 ) ;
#256474=AXIS2_PLACEMENT_3D ( 'NONE', #164986, #226205, #205378 ) ;
#256494=AXIS2_PLACEMENT_3D ( 'NONE', #19714, #61391, #200900 ) ;
#256500=ORIENTED_EDGE ( 'NONE', *, *, #76820, .F. ) ;
#256514=ORIENTED_EDGE ( 'NONE', *, *, #192865, .F. ) ;
#256518=VERTEX_POINT ( 'NONE', #240967 ) ;
#256541=DIRECTION ( 'NONE',  ( 0.000000000000000000, 0.000000000000000000, 1.000000000000000000 ) ) ;
#256589=DIRECTION ( 'NONE',  ( -1.000000000000000000, -0.000000000000000000, -0.000000000000000000 ) ) ;
#256604=DIRECTION ( 'NONE',  ( 0.000000000000000000, 0.1568667991644863147, 0.9876197685951252359 ) ) ;
#256656=ORIENTED_EDGE ( 'NONE', *, *, #93731, .F. ) ;
#256672=AXIS2_PLACEMENT_3D ( 'NONE', #196467, #96075, #240747 ) ;
#256694=ADVANCED_FACE ( 'NONE', ( #234544, #254097 ), #157624, .T. ) ;
#256698=ORIENTED_EDGE ( 'NONE', *, *, #103185, .T. ) ;
#256699=ORIENTED_EDGE ( 'NONE', *, *, #112993, .F. ) ;
#256734=DIRECTION ( 'NONE',  ( -1.000000000000000000, 0.000000000000000000, 0.000000000000000000 ) ) ;
#256759=AXIS2_PLACEMENT_3D ( 'NONE', #152921, #154220, #226647 ) ;
#256773=DIRECTION ( 'NONE',  ( 0.000000000000000000, -0.9908441862701596881, 0.1350103645451904977 ) ) ;
#256798=AXIS2_PLACEMENT_3D ( 'NONE', #195907, #156790, #217988 ) ;
#256802=EDGE_CURVE ( 'NONE', #95681, #124743, #122337, .T. ) ;
#256803=FACE_OUTER_BOUND ( 'NONE', #124998, .T. ) ;
#256826=VERTEX_POINT ( 'NONE', #58452 ) ;
#256873=EDGE_CURVE ( 'NONE', #124743, #256334, #62334, .T. ) ;
#256890=AXIS2_PLACEMENT_3D ( 'NONE', #244462, #21583, #80218 ) ;
#256893=VECTOR ( 'NONE', #203217, 1000.000000000000114 ) ;
#256920=AXIS2_PLACEMENT_3D ( 'NONE', #137867, #216128, #120922 ) ;
#256929=DIRECTION ( 'NONE',  ( -1.000000000000000000, 0.000000000000000000, 0.000000000000000000 ) ) ;
#256935=CIRCLE ( 'NONE', #256759, 0.09999999999999949207 ) ;
#256940=ORIENTED_EDGE ( 'NONE', *, *, #127575, .T. ) ;
#256967=CARTESIAN_POINT ( 'NONE',  ( -20.64999999999999858, 4.350000000011156054, -121.7500000000000426 ) ) ;
#257005=ORIENTED_EDGE ( 'NONE', *, *, #150699, .F. ) ;
#257023=AXIS2_PLACEMENT_3D ( 'NONE', #110929, #127933, #52222 ) ;
#257028=ORIENTED_EDGE ( 'NONE', *, *, #160425, .T. ) ;
#257042=DIRECTION ( 'NONE',  ( 0.000000000000000000, 0.000000000000000000, -1.000000000000000000 ) ) ;
#257043=ORIENTED_EDGE ( 'NONE', *, *, #92860, .T. ) ;
#257047=CARTESIAN_POINT ( 'NONE',  ( 21.14999999999999858, 11.65000000001115943, -100.6000000000000369 ) ) ;
#257059=DIRECTION ( 'NONE',  ( -1.000000000000000000, -2.952720810173289112E-16, 0.000000000000000000 ) ) ;
#257074=CIRCLE ( 'NONE', #256494, 12.87499999999999822 ) ;
#257108=VERTEX_POINT ( 'NONE', #157298 ) ;
#257128=DIRECTION ( 'NONE',  ( 0.000000000000000000, 0.000000000000000000, -1.000000000000000000 ) ) ;
#257130=DIRECTION ( 'NONE',  ( 1.000000000000000000, 0.000000000000000000, 0.000000000000000000 ) ) ;
#257137=CARTESIAN_POINT ( 'NONE',  ( -18.53317502108577131, 10.32263460347359540, -139.5605957968672328 ) ) ;
#257140=ORIENTED_EDGE ( 'NONE', *, *, #16983, .T. ) ;
#257168=ADVANCED_FACE ( 'NONE', ( #251217 ), #201616, .T. ) ;
#257173=DIRECTION ( 'NONE',  ( 1.000000000000000000, -7.304098846218135653E-16, -2.111765289898286048E-31 ) ) ;
#257187=AXIS2_PLACEMENT_3D ( 'NONE', #191202, #92062, #18941 ) ;
#257204=AXIS2_PLACEMENT_3D ( 'NONE', #62981, #163378, #107242 ) ;
#257243=DIRECTION ( 'NONE',  ( 0.000000000000000000, 0.1350103645451876666, -0.9908441862701600211 ) ) ;
#257268=VERTEX_POINT ( 'NONE', #122002 ) ;
#257280=ORIENTED_EDGE ( 'NONE', *, *, #127451, .F. ) ;
#257288=ORIENTED_EDGE ( 'NONE', *, *, #2174, .T. ) ;
#257315=DIRECTION ( 'NONE',  ( 0.000000000000000000, 0.000000000000000000, 1.000000000000000000 ) ) ;
#257353=EDGE_CURVE ( 'NONE', #34960, #172291, #97725, .T. ) ;
#257366=AXIS2_PLACEMENT_3D ( 'NONE', #166961, #226890, #7867 ) ;
#257371=VECTOR ( 'NONE', #192200, 1000.000000000000114 ) ;
#257383=ADVANCED_FACE ( 'NONE', ( #223643 ), #124578, .F. ) ;
#257484=VERTEX_POINT ( 'NONE', #199648 ) ;
#257494=EDGE_CURVE ( 'NONE', #243821, #109956, #80987, .T. ) ;
#257529=CIRCLE ( 'NONE', #220193, 0.09999999999999939493 ) ;
#257547=DIRECTION ( 'NONE',  ( -1.000000000000000000, 0.000000000000000000, 0.000000000000000000 ) ) ;
#257569=CARTESIAN_POINT ( 'NONE',  ( 21.05000000000000071, 6.477552182504600964, -100.5999999652995882 ) ) ;
#257614=LINE ( 'NONE', #79009, #96634 ) ;
#257618=VERTEX_POINT ( 'NONE', #185195 ) ;
#257642=VERTEX_POINT ( 'NONE', #100488 ) ;
#257647=ORIENTED_EDGE ( 'NONE', *, *, #198379, .T. ) ;
#257667=FACE_OUTER_BOUND ( 'NONE', #52756, .T. ) ;
#257673=CIRCLE ( 'NONE', #207691, 3.899999999999987033 ) ;
#257699=CYLINDRICAL_SURFACE ( 'NONE', #10444, 0.5000000000000004441 ) ;
#257703=EDGE_CURVE ( 'NONE', #64997, #175552, #222827, .T. ) ;
#257722=CARTESIAN_POINT ( 'NONE',  ( -20.94999999999999929, 1.115600667400684642E-11, -134.0000000000000284 ) ) ;
#257750=CIRCLE ( 'NONE', #3726, 11.70000000000000284 ) ;
#257776=CARTESIAN_POINT ( 'NONE',  ( -20.54999999999999716, 2.000000000011154189, -113.7246219227621395 ) ) ;
#257783=DIRECTION ( 'NONE',  ( 0.000000000000000000, 0.000000000000000000, -1.000000000000000000 ) ) ;
#257824=ORIENTED_EDGE ( 'NONE', *, *, #25510, .T. ) ;
#257829=DIRECTION ( 'NONE',  ( 1.000000000000000000, -0.000000000000000000, -0.000000000000000000 ) ) ;
#257836=CARTESIAN_POINT ( 'NONE',  ( -21.05000000000000071, -11.48912529306489994, -130.9000000000000341 ) ) ;
#257843=DIRECTION ( 'NONE',  ( 0.000000000000000000, 1.265107689135680095E-16, -1.000000000000000000 ) ) ;
#257852=ORIENTED_EDGE ( 'NONE', *, *, #216949, .T. ) ;
#257914=DIRECTION ( 'NONE',  ( 1.000000000000000000, 7.304098846218134667E-16, 0.000000000000000000 ) ) ;
#257931=CARTESIAN_POINT ( 'NONE',  ( -21.05000000000000071, -11.64999999998884306, -131.1000000000000227 ) ) ;
#257968=DIRECTION ( 'NONE',  ( 1.000000000000000000, 0.000000000000000000, 0.000000000000000000 ) ) ;
#257981=DIRECTION ( 'NONE',  ( 0.000000000000000000, -0.9893560106964500722, 0.1455152366551550613 ) ) ;
#257987=ORIENTED_EDGE ( 'NONE', *, *, #179077, .F. ) ;
#257990=CARTESIAN_POINT ( 'NONE',  ( -18.50000000000000000, 9.250000000011157297, -121.7500000000000426 ) ) ;
#258011=ORIENTED_EDGE ( 'NONE', *, *, #116126, .F. ) ;
#258016=ORIENTED_EDGE ( 'NONE', *, *, #203726, .F. ) ;
#258054=VECTOR ( 'NONE', #210022, 1000.000000000000000 ) ;
#258056=ORIENTED_EDGE ( 'NONE', *, *, #123303, .T. ) ;
#258057=EDGE_CURVE ( 'NONE', #20141, #205, #19647, .T. ) ;
#258058=EDGE_CURVE ( 'NONE', #90910, #155920, #160705, .T. ) ;
#258066=LINE ( 'NONE', #19515, #72991 ) ;
#258092=CARTESIAN_POINT ( 'NONE',  ( 21.05000000000000071, 5.850000000011156942, -123.8675027757221159 ) ) ;
#258105=VERTEX_POINT ( 'NONE', #148325 ) ;
ENDSEC;
END-ISO-10303-21;
